ISO-10303-21;
HEADER;
FILE_DESCRIPTION (('STEP AP214'),
    '1' );
FILE_NAME ('Drip Tip - Airflow Cap.step',
    '2026-10-05T22:38:29',
    ( '' ),
    ( '' ),
    'SwSTEP 2.0',
    'SolidWorks 2020',
    '' );
FILE_SCHEMA (( 'AUTOMOTIVE_DESIGN' ));
ENDSEC;

DATA;
#20=CARTESIAN_POINT ( 'NONE',  ( 29.60000000000000142, 0.000000000000000000, 9.250000000000000000 ) ) ;
#32=VECTOR ( 'NONE', #8697, 999.9999999999998863 ) ;
#35=B_SPLINE_SURFACE_WITH_KNOTS ( 'NONE', 3, 3, ( 
 ( #2869, #65803, #50776, #34359 ),
 ( #29812, #34009, #40284, #7079 ),
 ( #23854, #61601, #66495, #55327 ),
 ( #7424, #28419, #39247, #8122 ),
 ( #61263, #39944, #28771, #60570 ),
 ( #24197, #50084, #1494, #45534 ),
 ( #13032, #2527, #23505, #44847 ),
 ( #22810, #49733, #13718, #17578 ),
 ( #55678, #56015, #66844, #65457 ),
 ( #50423, #38906, #18957, #35048 ),
 ( #1842, #60228, #7777, #56363 ),
 ( #23160, #12678, #66153, #18271 ) ),
 .UNSPECIFIED., .F., .F., .F.,
 ( 4, 1, 1, 1, 1, 1, 1, 1, 1, 4 ),
 ( 4, 4 ),
 ( 0.01095778183512000070, 0.05000000000000000278, 0.1000000000000000056, 0.1499999999999999944, 0.2000000000000000111, 0.2500000000000000000, 0.2999999999999999889, 0.3499999999999999778, 0.4000000000000000222, 0.4461465442842999507 ),
 ( -0.2706701497076000051, 1.270791666117000007 ),
 .UNSPECIFIED. ) ;
#42=CARTESIAN_POINT ( 'NONE',  ( 18.35676500243362952, -3.328522075972216498, -12.07468831868077963 ) ) ;
#47=CARTESIAN_POINT ( 'NONE',  ( 15.36937411412500154, -8.827864207275998965, -7.821779713377999599 ) ) ;
#50=ORIENTED_EDGE ( 'NONE', *, *, #56829, .T. ) ;
#68=CARTESIAN_POINT ( 'NONE',  ( 24.30000000000000071, 8.810505093353000916, -8.810505093353000916 ) ) ;
#72=CARTESIAN_POINT ( 'NONE',  ( 23.84129431493439455, 9.640979322668712825, -9.399448990175832463 ) ) ;
#75=EDGE_CURVE ( 'NONE', #48923, #52150, #18017, .T. ) ;
#76=CARTESIAN_POINT ( 'NONE',  ( 24.22109577643600176, 12.94658526084000094, -3.131939672619000081 ) ) ;
#78=B_SPLINE_CURVE_WITH_KNOTS ( 'NONE', 3,
 ( #47462, #68766, #250, #37651 ),
 .UNSPECIFIED., .F., .F.,
 ( 4, 4 ),
 ( 0.000000000000000000, 1.000000000000000000 ),
 .UNSPECIFIED. ) ;
#83=FACE_OUTER_BOUND ( 'NONE', #29738, .T. ) ;
#87=CARTESIAN_POINT ( 'NONE',  ( 23.84019513318622074, 3.320741495842120639, -13.05081507454588241 ) ) ;
#89=CARTESIAN_POINT ( 'NONE',  ( 14.46666666323366890, -9.471992681081616183, -8.194936219980965220 ) ) ;
#92=CARTESIAN_POINT ( 'NONE',  ( 13.73959992722299894, 11.36892293904000084, 2.362143082378000081 ) ) ;
#105=CARTESIAN_POINT ( 'NONE',  ( 12.83944380997200163, 12.16696032571000075, -3.135189167188999537 ) ) ;
#106=CARTESIAN_POINT ( 'NONE',  ( 18.29845715546600005, 11.81398323980999976, -3.695357857504999899 ) ) ;
#107=B_SPLINE_CURVE_WITH_KNOTS ( 'NONE', 3,
 ( #46552, #47923, #10170, #41640 ),
 .UNSPECIFIED., .F., .F.,
 ( 4, 4 ),
 ( 0.000000000000000000, 1.000000000000000000 ),
 .UNSPECIFIED. ) ;
#110=AXIS2_PLACEMENT_3D ( 'NONE', #3453, #51019, #35292 ) ;
#112=CARTESIAN_POINT ( 'NONE',  ( 18.47645006436894022, 11.77746884181073384, -4.263736182725015311 ) ) ;
#116=AXIS2_PLACEMENT_3D ( 'NONE', #14745, #2874, #57380 ) ;
#122=B_SPLINE_CURVE_WITH_KNOTS ( 'NONE', 3,
 ( #66091, #18210, #1783, #39886 ),
 .UNSPECIFIED., .F., .F.,
 ( 4, 4 ),
 ( 0.000000000000000000, 1.000000000000000000 ),
 .UNSPECIFIED. ) ;
#128=DIRECTION ( 'NONE',  ( -0.3310054520069888873, 0.000000000000000000, -0.9436288416224086761 ) ) ;
#131=CIRCLE ( 'NONE', #66002, 11.65000000000000036 ) ;
#134=EDGE_CURVE ( 'NONE', #63154, #64134, #61396, .T. ) ;
#139=CARTESIAN_POINT ( 'NONE',  ( 16.13763077846600069, -3.625006537420000008, -11.03132468648999875 ) ) ;
#140=CARTESIAN_POINT ( 'NONE',  ( 13.64331666222400052, -12.23490852752999913, -2.418322770048999981 ) ) ;
#144=CARTESIAN_POINT ( 'NONE',  ( 15.39999999998900293, -9.471998555523999386, -8.194929586088999685 ) ) ;
#149=CARTESIAN_POINT ( 'NONE',  ( 24.44496487975900223, 3.224879802562000464, -12.03535984693000138 ) ) ;
#152=EDGE_LOOP ( 'NONE', ( #38398, #58380, #48495, #62252 ) ) ;
#177=CARTESIAN_POINT ( 'NONE',  ( 25.19966795687700056, 11.70907786114999993, -2.905888020798000237 ) ) ;
#189=CARTESIAN_POINT ( 'NONE',  ( 16.04647714749799903, 3.814092932148000159, 11.87318743920999964 ) ) ;
#193=CARTESIAN_POINT ( 'NONE',  ( 13.63045347340496072, -12.32568024774126414, -2.226002549929300134 ) ) ;
#196=DIRECTION ( 'NONE',  ( 0.000000000000000000, -0.7577476854548028662, 0.6525476574074028369 ) ) ;
#197=CARTESIAN_POINT ( 'NONE',  ( 25.60000000000000142, 2.258942858049999725, 12.29419282279000036 ) ) ;
#213=CARTESIAN_POINT ( 'NONE',  ( 13.99999999379500082, -8.815218614167999789, -7.616697584347000394 ) ) ;
#239=ORIENTED_EDGE ( 'NONE', *, *, #67496, .F. ) ;
#242=B_SPLINE_CURVE_WITH_KNOTS ( 'NONE', 3,
 ( #55856, #2711, #2367, #19824 ),
 .UNSPECIFIED., .F., .F.,
 ( 4, 4 ),
 ( 0.000000000000000000, 1.000000000000000000 ),
 .UNSPECIFIED. ) ;
#244=CARTESIAN_POINT ( 'NONE',  ( 11.79999999771000141, -12.39026187696000036, -1.832249219479999969 ) ) ;
#245=ORIENTED_EDGE ( 'NONE', *, *, #68293, .F. ) ;
#247=CARTESIAN_POINT ( 'NONE',  ( 11.26443347348000046, 11.78677031080999882, 1.538950076482000107 ) ) ;
#250=CARTESIAN_POINT ( 'NONE',  ( 18.36662463489987474, -2.877217017167624125, 12.05304703251516507 ) ) ;
#252=VERTEX_POINT ( 'NONE', #5244 ) ;
#253=CARTESIAN_POINT ( 'NONE',  ( 15.71007343403957002, -8.769519461636603452, -7.669310999670508444 ) ) ;
#258=ORIENTED_EDGE ( 'NONE', *, *, #890, .F. ) ;
#264=CARTESIAN_POINT ( 'NONE',  ( 27.09999999999999787, 0.000000000000000000, 0.000000000000000000 ) ) ;
#269=CARTESIAN_POINT ( 'NONE',  ( 23.56666365135700403, -9.069641144872004901, 7.556701426719000025 ) ) ;
#272=ADVANCED_FACE ( 'NONE', ( #33201 ), #34811, .F. ) ;
#274=CARTESIAN_POINT ( 'NONE',  ( 18.22725926606490532, 3.461153921112412934, 12.03746648326613133 ) ) ;
#279=CONICAL_SURFACE ( 'NONE', #19241, 5.886037960926999268, 0.3217505543965463732 ) ;
#280=CARTESIAN_POINT ( 'NONE',  ( 11.44730853405000204, -12.38161968051000095, -1.492087993499999987 ) ) ;
#284=CARTESIAN_POINT ( 'NONE',  ( 24.30000000000000071, 2.548720605937000006, 12.21654710926000220 ) ) ;
#285=CARTESIAN_POINT ( 'NONE',  ( 24.02043810212400032, -12.55433174484000070, 3.484779853151999784 ) ) ;
#292=CARTESIAN_POINT ( 'NONE',  ( 11.29999334531184552, -11.74553346643965490, -1.558194258341520699 ) ) ;
#306=CARTESIAN_POINT ( 'NONE',  ( 24.72544608131600086, 8.702416312035001766, -9.187185040898000921 ) ) ;
#330=CARTESIAN_POINT ( 'NONE',  ( 24.15421034170099901, 3.593683958043000004, 12.72347868493999989 ) ) ;
#331=ORIENTED_EDGE ( 'NONE', *, *, #21053, .T. ) ;
#332=DIRECTION ( 'NONE',  ( 1.000000000000000000, 0.000000000000000000, 0.000000000000000000 ) ) ;
#352=B_SPLINE_CURVE_WITH_KNOTS ( 'NONE', 3,
 ( #56236, #18494, #65060, #55897 ),
 .UNSPECIFIED., .F., .F.,
 ( 4, 4 ),
 ( 0.000000000000000000, 0.5000000026798849806 ),
 .UNSPECIFIED. ) ;
#358=CONICAL_SURFACE ( 'NONE', #32750, 12.71246950475999959, 0.8960553845711767273 ) ;
#363=CARTESIAN_POINT ( 'NONE',  ( 23.56665676678100141, -0.02078841289292433087, 13.98987519048835360 ) ) ;
#386=EDGE_CURVE ( 'NONE', #57373, #55782, #131, .T. ) ;
#387=CARTESIAN_POINT ( 'NONE',  ( 17.60000000085000238, 12.11987927271999865, -3.159802730921999814 ) ) ;
#394=DIRECTION ( 'NONE',  ( 0.000000000000000000, -0.7071067811865475727, -0.7071067811865475727 ) ) ;
#401=ADVANCED_FACE ( 'NONE', ( #48505 ), #41881, .F. ) ;
#406=FACE_OUTER_BOUND ( 'NONE', #31055, .T. ) ;
#409=LINE ( 'NONE', #47627, #4203 ) ;
#418=DIRECTION ( 'NONE',  ( -1.000000000000000000, 0.000000000000000000, 0.000000000000000000 ) ) ;
#431=CARTESIAN_POINT ( 'NONE',  ( 18.35295676019000055, -2.690485605734000085, 11.48482900035000043 ) ) ;
#434=CARTESIAN_POINT ( 'NONE',  ( 29.60000000000000142, 0.000000000000000000, 0.000000000000000000 ) ) ;
#437=CARTESIAN_POINT ( 'NONE',  ( 13.64504292973000332, 11.45087266113000091, 2.419799131125000002 ) ) ;
#445=CARTESIAN_POINT ( 'NONE',  ( 16.86666666157666583, 3.216308280197299752, 11.40341444503674850 ) ) ;
#451=CARTESIAN_POINT ( 'NONE',  ( 12.21268235885900033, 11.62758720635999765, -4.758865308234000224 ) ) ;
#452=CARTESIAN_POINT ( 'NONE',  ( 18.19608105989800251, 11.86124369401000145, -3.532130569927999897 ) ) ;
#457=CARTESIAN_POINT ( 'NONE',  ( 17.98628609634500108, -3.388648274289000284, 11.90503202562999974 ) ) ;
#463=DIRECTION ( 'NONE',  ( -0.9486832980505238710, 8.389526310658208895E-10, -0.3162277660168079652 ) ) ;
#471=CARTESIAN_POINT ( 'NONE',  ( 23.60000000000000142, -9.305479840184000651, 8.315530346521999405 ) ) ;
#477=AXIS2_PLACEMENT_3D ( 'NONE', #56146, #39734, #50561 ) ;
#480=CARTESIAN_POINT ( 'NONE',  ( 11.35394314717303388, -3.574441963229890717, 11.79291588350140252 ) ) ;
#491=CARTESIAN_POINT ( 'NONE',  ( 11.49999672494999992, 5.885481364898664580, -10.12743717035875157 ) ) ;
#492=EDGE_LOOP ( 'NONE', ( #43852, #65890, #15231, #61686 ) ) ;
#495=DIRECTION ( 'NONE',  ( 0.000000000000000000, -1.000000000000000000, 0.000000000000000000 ) ) ;
#498=ORIENTED_EDGE ( 'NONE', *, *, #46740, .T. ) ;
#499=CARTESIAN_POINT ( 'NONE',  ( 25.08881866225100410, -11.66016336090999950, -3.018804192941999975 ) ) ;
#512=CARTESIAN_POINT ( 'NONE',  ( 15.35917414208899956, 8.811049802147000065, 7.563839685023999948 ) ) ;
#520=CARTESIAN_POINT ( 'NONE',  ( 24.48565841892600048, 12.12924569191000046, -3.164390090946999745 ) ) ;
#521=B_SPLINE_CURVE_WITH_KNOTS ( 'NONE', 3,
 ( #66809, #55639, #22770, #44121, #29079, #18920 ),
 .UNSPECIFIED., .F., .F.,
 ( 4, 2, 4 ),
 ( 0.000000000000000000, 0.5000000000000000000, 1.000000000000000000 ),
 .UNSPECIFIED. ) ;
#522=CARTESIAN_POINT ( 'NONE',  ( 25.46372676430900128, 8.354609436172999892, -8.148458316574000548 ) ) ;
#528=CARTESIAN_POINT ( 'NONE',  ( 23.56664309646999911, -10.37807348783000094, 9.381504613656002078 ) ) ;
#535=CARTESIAN_POINT ( 'NONE',  ( 16.39944283128300029, 3.410739012457999930, 11.89826262991000050 ) ) ;
#537=CARTESIAN_POINT ( 'NONE',  ( 24.16219604515211117, 12.44497281315807413, 3.348778968579924520 ) ) ;
#545=CARTESIAN_POINT ( 'NONE',  ( 18.38566024598074833, -11.99831085744367165, 3.595680291927078276 ) ) ;
#548=CARTESIAN_POINT ( 'NONE',  ( 25.25778303248700141, 2.569631777580000165, 11.37091703377000051 ) ) ;
#551=B_SPLINE_CURVE_WITH_KNOTS ( 'NONE', 3,
 ( #46391, #63486, #3386, #19819 ),
 .UNSPECIFIED., .F., .F.,
 ( 4, 4 ),
 ( 0.000000000000000000, 1.000000000000000000 ),
 .UNSPECIFIED. ) ;
#557=CARTESIAN_POINT ( 'NONE',  ( 15.89994436294300151, 8.847904542234999781, 8.580301953175000662 ) ) ;
#565=CARTESIAN_POINT ( 'NONE',  ( 24.60999195316300003, -8.752663949940000521, -9.057796881813999335 ) ) ;
#566=PRODUCT_DEFINITION_FORMATION_WITH_SPECIFIED_SOURCE ( 'ANY', '', #18770, .NOT_KNOWN. ) ;
#570=CARTESIAN_POINT ( 'NONE',  ( 17.97872601847819851, -3.578425380680470447, 12.00298730842247252 ) ) ;
#575=CYLINDRICAL_SURFACE ( 'NONE', #60048, 0.5000000000000004441 ) ;
#593=CARTESIAN_POINT ( 'NONE',  ( 15.99022209853100129, -3.654801648850000362, -11.82543339652000114 ) ) ;
#594=CARTESIAN_POINT ( 'NONE',  ( 11.71278712779700015, 11.72302084951000190, 1.966028253584000129 ) ) ;
#595=ORIENTED_EDGE ( 'NONE', *, *, #47317, .T. ) ;
#599=ORIENTED_EDGE ( 'NONE', *, *, #49645, .F. ) ;
#602=CARTESIAN_POINT ( 'NONE',  ( 24.32158614469118518, -12.72716443521392016, 3.095238905934254880 ) ) ;
#608=ORIENTED_EDGE ( 'NONE', *, *, #1012, .T. ) ;
#610=CARTESIAN_POINT ( 'NONE',  ( 15.39165415090800337, -9.395515400280999074, -8.199438574490999443 ) ) ;
#617=FACE_OUTER_BOUND ( 'NONE', #1285, .T. ) ;
#619=CARTESIAN_POINT ( 'NONE',  ( 24.30001697352500045, -3.271769158411000245, -12.21048181092999840 ) ) ;
#628=CARTESIAN_POINT ( 'NONE',  ( 11.48828127163000268, -12.23964378314000001, -1.839251152677999990 ) ) ;
#636=CARTESIAN_POINT ( 'NONE',  ( 23.86822025922500146, -13.28639123634000008, 3.449149526223000084 ) ) ;
#643=CARTESIAN_POINT ( 'NONE',  ( 17.60000001994400165, -11.53041320601000130, 4.891397783926000109 ) ) ;
#647=FACE_OUTER_BOUND ( 'NONE', #28213, .T. ) ;
#648=CARTESIAN_POINT ( 'NONE',  ( 23.52034043602500191, -10.38860555204000136, 9.575296714885999094 ) ) ;
#656=( GEOMETRIC_REPRESENTATION_CONTEXT ( 3 ) GLOBAL_UNCERTAINTY_ASSIGNED_CONTEXT ( ( #63933 ) ) GLOBAL_UNIT_ASSIGNED_CONTEXT ( ( #8267, #61410, #19098 ) ) REPRESENTATION_CONTEXT ( 'NONE', 'WORKASPACE' ) );
#670=ORIENTED_EDGE ( 'NONE', *, *, #63025, .T. ) ;
#672=CARTESIAN_POINT ( 'NONE',  ( 12.38412398422500083, -11.44428158143999852, 4.450268217599000486 ) ) ;
#692=CARTESIAN_POINT ( 'NONE',  ( 23.72390849569146454, 9.881471858020274723, 9.454770968183350277 ) ) ;
#693=ORIENTED_EDGE ( 'NONE', *, *, #12418, .T. ) ;
#700=CARTESIAN_POINT ( 'NONE',  ( 13.64731601457200050, 9.647116713587001513, 7.903424745186999445 ) ) ;
#709=CARTESIAN_POINT ( 'NONE',  ( 23.60205915885299888, -11.53346724329999873, 4.150849519444998137 ) ) ;
#711=CARTESIAN_POINT ( 'NONE',  ( 11.84785375340600133, 12.11644693747000012, 2.030267990277999868 ) ) ;
#724=AXIS2_PLACEMENT_3D ( 'NONE', #29766, #40575, #8080 ) ;
#730=CARTESIAN_POINT ( 'NONE',  ( 18.15060209888356724, -3.510419631047395850, -12.02305644365783976 ) ) ;
#732=CARTESIAN_POINT ( 'NONE',  ( 12.21312755196900390, 11.61418968116140249, -4.689146002353034248 ) ) ;
#742=CARTESIAN_POINT ( 'NONE',  ( 12.25964841771344638, -11.59985379594602861, 4.724415456180611983 ) ) ;
#749=CARTESIAN_POINT ( 'NONE',  ( 12.10000000004390586, 11.04996331189681946, -3.691231723793510167 ) ) ;
#752=CARTESIAN_POINT ( 'NONE',  ( 18.23980063401625173, -2.972525811573661692, 11.47315805793748389 ) ) ;
#759=CARTESIAN_POINT ( 'NONE',  ( 15.52628979459879588, 9.187490316955907232, 8.213190486479970076 ) ) ;
#761=AXIS2_PLACEMENT_3D ( 'NONE', #40490, #29334, #65681 ) ;
#762=DIRECTION ( 'NONE',  ( -1.000000000000000000, 0.000000000000000000, 0.000000000000000000 ) ) ;
#764=CARTESIAN_POINT ( 'NONE',  ( 24.14075320594848861, 9.153203792121958671, -9.127249519516993814 ) ) ;
#769=ORIENTED_EDGE ( 'NONE', *, *, #2828, .T. ) ;
#776=CARTESIAN_POINT ( 'NONE',  ( 24.01910276523975796, 3.345607443898567457, -12.71185236705795418 ) ) ;
#784=ORIENTED_EDGE ( 'NONE', *, *, #40961, .T. ) ;
#789=CARTESIAN_POINT ( 'NONE',  ( 15.90018573812399971, 8.493548356068000516, 8.263529029821000904 ) ) ;
#792=CARTESIAN_POINT ( 'NONE',  ( 25.09889915318881393, -8.522830760771270775, 8.212608576531337690 ) ) ;
#796=CARTESIAN_POINT ( 'NONE',  ( 23.56666365135700403, -8.673757318230000735, -7.881093921673004488 ) ) ;
#800=CARTESIAN_POINT ( 'NONE',  ( 18.10540495109299997, 12.00990144118000025, -3.349639255392000248 ) ) ;
#809=ORIENTED_EDGE ( 'NONE', *, *, #32463, .T. ) ;
#810=CARTESIAN_POINT ( 'NONE',  ( 30.60000000000000142, 0.000000000000000000, 0.000000000000000000 ) ) ;
#816=DIRECTION ( 'NONE',  ( -1.000000000000000000, 0.000000000000000000, 0.000000000000000000 ) ) ;
#828=AXIS2_PLACEMENT_3D ( 'NONE', #21507, #9987, #48429 ) ;
#831=CARTESIAN_POINT ( 'NONE',  ( 23.56665657345700282, -13.31365812469000076, 4.296923216748999685 ) ) ;
#834=B_SPLINE_CURVE_WITH_KNOTS ( 'NONE', 3,
 ( #1682, #43648, #12175, #38390, #60071, #63918 ),
 .UNSPECIFIED., .F., .F.,
 ( 4, 1, 1, 4 ),
 ( 0.000000000000000000, 0.1550125193758622177, 0.7488612380771151322, 1.000000000000000000 ),
 .UNSPECIFIED. ) ;
#837=CARTESIAN_POINT ( 'NONE',  ( 24.44496483130000186, -3.224879855413000040, 12.03535978074999946 ) ) ;
#839=CARTESIAN_POINT ( 'NONE',  ( 23.59999999999999787, 11.54195020457962606, 7.798376075308690147 ) ) ;
#855=VERTEX_POINT ( 'NONE', #54700 ) ;
#860=CARTESIAN_POINT ( 'NONE',  ( 23.60000648363190123, -13.25016151468667225, 4.189794345519016971 ) ) ;
#868=EDGE_CURVE ( 'NONE', #40899, #66838, #6329, .T. ) ;
#871=CARTESIAN_POINT ( 'NONE',  ( 25.41802413019000184, 11.20519658595999957, -3.227494277392999766 ) ) ;
#882=B_SPLINE_CURVE_WITH_KNOTS ( 'NONE', 3,
 ( #55892, #6952, #65330, #54503, #12550, #23382, #29330, #18142, #17089, #17449, #39119, #1712, #11847, #33185, #6603, #65678, #27945, #28284, #60099, #12205, #17800, #33533, #60442, #54852, #49604, #23031, #55197, #7299, #28640, #49951, #2064 ),
 .UNSPECIFIED., .F., .F.,
 ( 4, 2, 2, 1, 1, 2, 2, 2, 1, 2, 2, 2, 2, 2, 2, 2, 4 ),
 ( 0.000000000000000000, 0.06250000000000358047, 0.09375000000000592582, 0.1093750000000056066, 0.1171875000000048711, 0.1210937500000059258, 0.1250000000000069666, 0.1875000000000131839, 0.2187500000000159872, 0.2343750000000168199, 0.2500000000000176525, 0.3750000000000245359, 0.4375000000000285882, 0.4687500000000288658, 0.5000000000000291989, 0.7500000000000146549, 1.000000000000000000 ),
 .UNSPECIFIED. ) ;
#883=CARTESIAN_POINT ( 'NONE',  ( 24.81123823827553565, 11.68013870454559289, -3.194582531880967746 ) ) ;
#887=ORIENTED_EDGE ( 'NONE', *, *, #47584, .T. ) ;
#890=EDGE_CURVE ( 'NONE', #26237, #27264, #13051, .T. ) ;
#891=CARTESIAN_POINT ( 'NONE',  ( 18.47604564451473053, -11.77695503131875121, 4.265147058870558894 ) ) ;
#909=CARTESIAN_POINT ( 'NONE',  ( 12.09999922233642522, -11.66744139996562701, 3.971920075675145156 ) ) ;
#917=CARTESIAN_POINT ( 'NONE',  ( 24.15346678657299861, 9.222906534045000271, 9.474494998088001552 ) ) ;
#919=FACE_OUTER_BOUND ( 'NONE', #48407, .T. ) ;
#921=DIRECTION ( 'NONE',  ( -1.000000000000000000, 0.000000000000000000, 0.000000000000000000 ) ) ;
#923=CONICAL_SURFACE ( 'NONE', #42201, 11.34994642770999818, 0.7853934433894341760 ) ;
#924=CARTESIAN_POINT ( 'NONE',  ( 13.49980696792483137, -10.68794281923488931, -6.218617845733625416 ) ) ;
#927=ORIENTED_EDGE ( 'NONE', *, *, #61621, .F. ) ;
#933=CARTESIAN_POINT ( 'NONE',  ( 15.80279819343546599, -8.703657694420874336, -8.043987028914523663 ) ) ;
#955=EDGE_CURVE ( 'NONE', #66838, #16567, #68868, .T. ) ;
#963=ORIENTED_EDGE ( 'NONE', *, *, #30747, .T. ) ;
#973=ORIENTED_EDGE ( 'NONE', *, *, #67687, .F. ) ;
#976=CARTESIAN_POINT ( 'NONE',  ( 11.75750014570500035, -12.43407951582999971, -1.799970604841000021 ) ) ;
#988=CARTESIAN_POINT ( 'NONE',  ( 23.60000000000000142, 9.305479840184000651, -8.315530346521999405 ) ) ;
#991=AXIS2_PLACEMENT_3D ( 'NONE', #2694, #50934, #24364 ) ;
#994=CARTESIAN_POINT ( 'NONE',  ( 24.22107886057200332, -9.185649942997999418, -9.646111962386999750 ) ) ;
#997=ORIENTED_EDGE ( 'NONE', *, *, #11789, .F. ) ;
#1009=B_SPLINE_CURVE_WITH_KNOTS ( 'NONE', 3,
 ( #13795, #60995, #55062, #45270 ),
 .UNSPECIFIED., .F., .F.,
 ( 4, 4 ),
 ( 0.000000000000000000, 1.000000000000000000 ),
 .UNSPECIFIED. ) ;
#1012=EDGE_CURVE ( 'NONE', #60415, #6697, #5473, .T. ) ;
#1021=CARTESIAN_POINT ( 'NONE',  ( 12.00339635128600158, -11.70009917314000170, 4.315816162729000816 ) ) ;
#1032=B_SPLINE_CURVE_WITH_KNOTS ( 'NONE', 3,
 ( #42511, #68372, #21179, #4744 ),
 .UNSPECIFIED., .F., .F.,
 ( 4, 4 ),
 ( 0.000000000000000000, 1.000000000000000000 ),
 .UNSPECIFIED. ) ;
#1033=B_SPLINE_SURFACE_WITH_KNOTS ( 'NONE', 3, 3, ( 
 ( #27951, #38781, #17456, #33888 ),
 ( #10223, #42043, #25962, #54858 ),
 ( #17096, #52877, #23037, #44386 ),
 ( #20716, #60108, #58121, #4976 ),
 ( #38428, #49262, #12212, #10564 ),
 ( #43684, #47291, #63349, #28291 ),
 ( #59752, #31555, #33541, #39125 ),
 ( #6960, #47976, #26659, #49611 ),
 ( #21061, #65686, #1718, #76 ),
 ( #1372, #60450, #17809, #11854 ),
 ( #58458, #22690, #22347, #37141 ),
 ( #26309, #33193, #53216, #68594 ) ),
 .UNSPECIFIED., .F., .F., .F.,
 ( 4, 1, 1, 1, 1, 1, 1, 1, 1, 4 ),
 ( 4, 4 ),
 ( 0.5515699153562999557, 0.5999999999999999778, 0.6500000000000000222, 0.6999999999999999556, 0.7500000000000000000, 0.8000000000000000444, 0.8499999999999999778, 0.9000000000000000222, 0.9499999999999999556, 0.9893635532735000071 ),
 ( -0.2706691663378000268, 1.270787837442000079 ),
 .UNSPECIFIED. ) ;
#1038=EDGE_LOOP ( 'NONE', ( #13976, #62077, #33921, #6620 ) ) ;
#1044=CARTESIAN_POINT ( 'NONE',  ( 23.71153137169101299, 9.910002971162056085, 9.457066138817401324 ) ) ;
#1045=ORIENTED_EDGE ( 'NONE', *, *, #54865, .F. ) ;
#1048=CARTESIAN_POINT ( 'NONE',  ( 23.56666365135700403, 2.009474831861002286, -11.63289034805000277 ) ) ;
#1051=CARTESIAN_POINT ( 'NONE',  ( 12.79999999202000005, 11.41069016990000051, -4.623987642516999230 ) ) ;
#1062=EDGE_CURVE ( 'NONE', #36031, #28388, #27149, .T. ) ;
#1089=CARTESIAN_POINT ( 'NONE',  ( 23.97709314544701442, -9.403781800835757210, -9.292205342148244895 ) ) ;
#1090=CARTESIAN_POINT ( 'NONE',  ( 12.68562097720242576, -12.11848650044661291, 3.165127050490176064 ) ) ;
#1094=B_SPLINE_CURVE_WITH_KNOTS ( 'NONE', 3,
 ( #11339, #860, #32680, #22177, #53993, #43517, #64815, #16925, #59583, #11684, #6438, #29526, #66895, #39303, #23909, #60282, #38965, #40334, #13436, #50143, #29171, #7139, #45590, #45246, #66552, #18670, #13086, #28477, #2581, #1548, #49793, #65861 ),
 .UNSPECIFIED., .F., .F.,
 ( 4, 2, 2, 2, 2, 2, 2, 2, 1, 2, 2, 2, 1, 1, 1, 2, 2, 4 ),
 ( 0.000000000000000000, 0.2499999999999824030, 0.3749999999999745759, 0.4374999999999704681, 0.4687499999999693578, 0.4999999999999682476, 0.6249999999999634737, 0.6874999999999632516, 0.7187499999999620304, 0.7343749999999621414, 0.7499999999999622524, 0.8124999999999668043, 0.8437499999999708011, 0.8593749999999727995, 0.8671874999999756861, 0.8710937499999781286, 0.8749999999999804601, 1.000000000000000000 ),
 .UNSPECIFIED. ) ;
#1097=CARTESIAN_POINT ( 'NONE',  ( 24.63805276219900264, 3.694107246557000401, -12.29549514572999946 ) ) ;
#1101=CARTESIAN_POINT ( 'NONE',  ( 18.17745566902672394, -10.88889238843039209, 4.142628063310672459 ) ) ;
#1102=CARTESIAN_POINT ( 'NONE',  ( 21.05000072320150295, 1.558041382508999773E-13, -6.372680161347999694E-14 ) ) ;
#1104=CARTESIAN_POINT ( 'NONE',  ( 18.50003594170800270, -2.686563649653999963, 11.33603604535000109 ) ) ;
#1109=LINE ( 'NONE', #53890, #62457 ) ;
#1113=CARTESIAN_POINT ( 'NONE',  ( 24.60320129348500018, 12.45517092796000114, 2.982541609212000289 ) ) ;
#1123=CARTESIAN_POINT ( 'NONE',  ( 24.30000000000000071, -3.224868684338999980, 12.03537377768999939 ) ) ;
#1124=CARTESIAN_POINT ( 'NONE',  ( 18.24051303026600124, -3.055556278716000218, 11.39470302754000031 ) ) ;
#1127=CARTESIAN_POINT ( 'NONE',  ( 13.99999999231800096, 8.833253877201999060, 7.896562762484000686 ) ) ;
#1137=CARTESIAN_POINT ( 'NONE',  ( 21.00000000000000000, 0.000000000000000000, 0.000000000000000000 ) ) ;
#1146=CARTESIAN_POINT ( 'NONE',  ( 23.59999172348799945, -10.30759808834999980, 9.317726582648999667 ) ) ;
#1148=VERTEX_POINT ( 'NONE', #12661 ) ;
#1168=AXIS2_PLACEMENT_3D ( 'NONE', #5018, #52227, #25660 ) ;
#1176=CARTESIAN_POINT ( 'NONE',  ( 11.53943995709000170, 3.847421095330999741, -11.95976051375000004 ) ) ;
#1177=EDGE_CURVE ( 'NONE', #35879, #44670, #28401, .T. ) ;
#1190=CARTESIAN_POINT ( 'NONE',  ( 25.27036502875199986, -8.566977734595999650, 7.889724197193000776 ) ) ;
#1202=DIRECTION ( 'NONE',  ( -5.239392413525232509E-16, -0.6482718649732923666, -0.7614089499631913061 ) ) ;
#1204=ORIENTED_EDGE ( 'NONE', *, *, #33666, .T. ) ;
#1208=DIRECTION ( 'NONE',  ( 0.000000000000000000, -0.1862490057674050514, -0.9825025739664263735 ) ) ;
#1211=CARTESIAN_POINT ( 'NONE',  ( 16.39999999347100257, -3.345256695718999751, -11.86066175541999890 ) ) ;
#1223=AXIS2_PLACEMENT_3D ( 'NONE', #19547, #14309, #13625 ) ;
#1225=CARTESIAN_POINT ( 'NONE',  ( 16.29309513285500088, 3.300500509464999954, 11.83372189959999865 ) ) ;
#1234=CARTESIAN_POINT ( 'NONE',  ( 17.65734784985741967, -11.53038622195815144, 4.891402515914990090 ) ) ;
#1236=CARTESIAN_POINT ( 'NONE',  ( 16.39999999485600313, -3.595156957901000094, -11.99794989424000136 ) ) ;
#1242=CARTESIAN_POINT ( 'NONE',  ( 24.30000000000000071, 8.756202924575998026, -7.455126447192999883 ) ) ;
#1245=CARTESIAN_POINT ( 'NONE',  ( 24.30001696810800027, 12.21047201856000086, 3.271805692349999628 ) ) ;
#1248=DIRECTION ( 'NONE',  ( -1.000000000000000000, 0.000000000000000000, 0.000000000000000000 ) ) ;
#1252=FACE_OUTER_BOUND ( 'NONE', #59376, .T. ) ;
#1259=CARTESIAN_POINT ( 'NONE',  ( 17.74638838757299553, 10.78680295286436852, -4.401676307962380186 ) ) ;
#1262=CARTESIAN_POINT ( 'NONE',  ( 44.24148000000000280, -11.77655473258999841, 4.190794510628000680 ) ) ;
#1263=FACE_OUTER_BOUND ( 'NONE', #6963, .T. ) ;
#1285=EDGE_LOOP ( 'NONE', ( #36999, #35644, #17389, #40139 ) ) ;
#1288=CARTESIAN_POINT ( 'NONE',  ( 24.81126097005384779, -8.606648885476735344, -8.517984218207937275 ) ) ;
#1290=EDGE_LOOP ( 'NONE', ( #30271, #11363, #2119, #42884 ) ) ;
#1291=CARTESIAN_POINT ( 'NONE',  ( 16.09586749610213374, -8.411110950737080927, -8.060864562931225663 ) ) ;
#1306=DIRECTION ( 'NONE',  ( -1.000000000000000000, 0.000000000000000000, 0.000000000000000000 ) ) ;
#1310=ORIENTED_EDGE ( 'NONE', *, *, #68127, .T. ) ;
#1312=ORIENTED_EDGE ( 'NONE', *, *, #52096, .F. ) ;
#1313=CARTESIAN_POINT ( 'NONE',  ( 11.53681706333000179, -12.46890164658000089, -1.535189833763999978 ) ) ;
#1326=CARTESIAN_POINT ( 'NONE',  ( 18.49055856039300139, 2.949841519493000330, -11.23086453091999992 ) ) ;
#1329=VECTOR ( 'NONE', #54963, 1000.000000000000000 ) ;
#1330=CARTESIAN_POINT ( 'NONE',  ( 24.22093573973900149, -8.982850686176998778, -8.867479996275999810 ) ) ;
#1331=CARTESIAN_POINT ( 'NONE',  ( 23.64072730899000163, -10.12004117118999957, 9.384740691128001799 ) ) ;
#1333=ORIENTED_EDGE ( 'NONE', *, *, #47460, .F. ) ;
#1337=ADVANCED_FACE ( 'NONE', ( #40605 ), #57360, .F. ) ;
#1342=ORIENTED_EDGE ( 'NONE', *, *, #57044, .F. ) ;
#1343=CARTESIAN_POINT ( 'NONE',  ( 24.85114803437500086, 3.384270252302000070, -11.84837700269999949 ) ) ;
#1348=ORIENTED_EDGE ( 'NONE', *, *, #39585, .T. ) ;
#1350=B_SPLINE_CURVE_WITH_KNOTS ( 'NONE', 3,
 ( #42513, #41819, #30998, #32375, #5450, #42175 ),
 .UNSPECIFIED., .F., .F.,
 ( 4, 2, 4 ),
 ( 0.000000000000000000, 0.5000000000000000000, 1.000000000000000000 ),
 .UNSPECIFIED. ) ;
#1358=CARTESIAN_POINT ( 'NONE',  ( 12.83176788310500172, -11.93188535256000016, 3.261584788209999974 ) ) ;
#1365=CARTESIAN_POINT ( 'NONE',  ( 24.72672761098415961, -11.76480477972923389, -3.190859381812851669 ) ) ;
#1367=EDGE_CURVE ( 'NONE', #27101, #12493, #24548, .T. ) ;
#1368=CARTESIAN_POINT ( 'NONE',  ( 17.60000000532009423, 11.20144845259485678, -4.552734317499857575 ) ) ;
#1372=CARTESIAN_POINT ( 'NONE',  ( 24.13719010493599981, 12.33331563296999889, -3.394048515820999867 ) ) ;
#1377=AXIS2_PLACEMENT_3D ( 'NONE', #9487, #68209, #20329 ) ;
#1379=VERTEX_POINT ( 'NONE', #56694 ) ;
#1383=DIRECTION ( 'NONE',  ( 0.000000000000000000, 0.6664713972124013397, -0.7455306007789014311 ) ) ;
#1386=CARTESIAN_POINT ( 'NONE',  ( 23.89320776801300283, 3.288740538445000805, -12.20874841465999516 ) ) ;
#1388=CARTESIAN_POINT ( 'NONE',  ( 18.48305742508500416, -12.00075408335000127, 3.715624526910999759 ) ) ;
#1399=CARTESIAN_POINT ( 'NONE',  ( 11.31944011432000075, 12.15765269271000015, 1.759220518310000037 ) ) ;
#1403=ADVANCED_FACE ( 'NONE', ( #48865 ), #37022, .F. ) ;
#1425=CARTESIAN_POINT ( 'NONE',  ( 12.22262912535705937, 10.88886164601108675, -4.142707164787215568 ) ) ;
#1426=CARTESIAN_POINT ( 'NONE',  ( 24.77780280611190378, 11.71374231672910504, 3.192708380903468868 ) ) ;
#1428=CARTESIAN_POINT ( 'NONE',  ( 23.59999193302000364, -13.22318594659000013, 4.267778254689999606 ) ) ;
#1435=CARTESIAN_POINT ( 'NONE',  ( 11.80000000000000071, -49.70447530208000586, -8.683202977359000485 ) ) ;
#1439=CARTESIAN_POINT ( 'NONE',  ( 24.22079749817700289, 3.188112890658000076, -12.21338637798000093 ) ) ;
#1440=CARTESIAN_POINT ( 'NONE',  ( 12.99403162610500040, -12.11619719077999946, -2.031914795679000019 ) ) ;
#1445=CARTESIAN_POINT ( 'NONE',  ( 18.22968849645625511, -3.214251582956586528, -11.19784508593207484 ) ) ;
#1453=CARTESIAN_POINT ( 'NONE',  ( 11.72005178064354780, -3.595543782890631146, 11.99782022136165871 ) ) ;
#1456=CARTESIAN_POINT ( 'NONE',  ( 24.46275371508600216, 12.39843049379000028, 3.098824767661999768 ) ) ;
#1469=CARTESIAN_POINT ( 'NONE',  ( 24.30001694670299983, 8.938702829764999080, 8.938676122491999720 ) ) ;
#1471=CARTESIAN_POINT ( 'NONE',  ( 11.31919037786000182, 3.456300244116000453, -11.37193521011000108 ) ) ;
#1494=CARTESIAN_POINT ( 'NONE',  ( 23.85158989719599987, -3.519737302176999982, -13.16814931014999956 ) ) ;
#1500=DIRECTION ( 'NONE',  ( -1.000000000000000000, 0.000000000000000000, 0.000000000000000000 ) ) ;
#1511=ORIENTED_EDGE ( 'NONE', *, *, #59478, .F. ) ;
#1512=CONICAL_SURFACE ( 'NONE', #11528, 11.34994642770999818, 0.7853934433896081480 ) ;
#1524=EDGE_CURVE ( 'NONE', #48385, #63935, #65393, .T. ) ;
#1526=AXIS2_PLACEMENT_3D ( 'NONE', #10852, #31849, #11534 ) ;
#1527=CARTESIAN_POINT ( 'NONE',  ( 25.59994555223599733, 8.527741194213000142, 7.260611644044000279 ) ) ;
#1531=CARTESIAN_POINT ( 'NONE',  ( 24.87547543774200065, -8.587518678078000178, 8.379277945963000462 ) ) ;
#1536=CARTESIAN_POINT ( 'NONE',  ( 13.87289819560299975, -8.829573912736998764, -7.542332231507000273 ) ) ;
#1548=CARTESIAN_POINT ( 'NONE',  ( 24.17206752463402708, -12.42860866793109231, 3.341570834813612390 ) ) ;
#1551=DIRECTION ( 'NONE',  ( -1.000000000000000000, 0.000000000000000000, 0.000000000000000000 ) ) ;
#1563=CARTESIAN_POINT ( 'NONE',  ( 23.50387503050299998, 3.769846058462999530E-06, -14.00000000000000000 ) ) ;
#1564=CARTESIAN_POINT ( 'NONE',  ( 15.99022209853100129, 3.654801648850000362, 11.82543339652000114 ) ) ;
#1565=CARTESIAN_POINT ( 'NONE',  ( 23.60205915885299888, 2.489696159930001595, 12.09604418630999945 ) ) ;
#1572=ORIENTED_EDGE ( 'NONE', *, *, #63116, .F. ) ;
#1573=CARTESIAN_POINT ( 'NONE',  ( 17.79999999998900151, -3.595165934733000057, -11.99793354950999991 ) ) ;
#1575=CARTESIAN_POINT ( 'NONE',  ( 17.90362871669234579, -11.55108254360806264, 4.842339049571677378 ) ) ;
#1578=CARTESIAN_POINT ( 'NONE',  ( 24.87547783684399860, 2.962907585147000145, 11.62664596340999879 ) ) ;
#1580=TOROIDAL_SURFACE ( 'NONE', #38402, 6.000000000000000000, 1.000000000000000000 ) ;
#1586=AXIS2_PLACEMENT_3D ( 'NONE', #15876, #57487, #64105 ) ;
#1590=EDGE_CURVE ( 'NONE', #12209, #11759, #18729, .T. ) ;
#1607=CARTESIAN_POINT ( 'NONE',  ( 23.56665676678199972, -7.629452625224000015E-13, 2.908784324518000003E-13 ) ) ;
#1608=VECTOR ( 'NONE', #56881, 1000.000000000000000 ) ;
#1611=EDGE_CURVE ( 'NONE', #23725, #4046, #18063, .T. ) ;
#1617=EDGE_CURVE ( 'NONE', #31379, #59008, #56247, .T. ) ;
#1618=CARTESIAN_POINT ( 'NONE',  ( 23.79452366329859458, -13.02995649425213465, -3.714610742098415130 ) ) ;
#1620=ORIENTED_EDGE ( 'NONE', *, *, #65212, .F. ) ;
#1623=CARTESIAN_POINT ( 'NONE',  ( 23.56664676942400050, 2.935522432666999748, 13.67843419499999946 ) ) ;
#1628=CARTESIAN_POINT ( 'NONE',  ( 16.43164332880499856, -3.528999066054999467, -11.96046905204000055 ) ) ;
#1633=CIRCLE ( 'NONE', #34034, 5.000000000000000000 ) ;
#1635=EDGE_LOOP ( 'NONE', ( #49943, #30620, #39046, #66215, #5952, #10313 ) ) ;
#1637=CARTESIAN_POINT ( 'NONE',  ( 25.49996575949806044, -2.042068214647287938, -11.11386275109044774 ) ) ;
#1641=VERTEX_POINT ( 'NONE', #10250 ) ;
#1652=CARTESIAN_POINT ( 'NONE',  ( 25.59997125372800042, -2.856414944279999979, 11.13959160109000024 ) ) ;
#1656=EDGE_CURVE ( 'NONE', #4626, #15819, #9908, .T. ) ;
#1657=ORIENTED_EDGE ( 'NONE', *, *, #17610, .F. ) ;
#1659=ORIENTED_EDGE ( 'NONE', *, *, #37399, .T. ) ;
#1661=CARTESIAN_POINT ( 'NONE',  ( 11.80877518040099972, -12.11591042788000117, -2.033719807695000270 ) ) ;
#1667=CARTESIAN_POINT ( 'NONE',  ( 24.51038902278400045, 12.36384862481999924, 3.075095933055000064 ) ) ;
#1669=ORIENTED_EDGE ( 'NONE', *, *, #30622, .T. ) ;
#1673=CARTESIAN_POINT ( 'NONE',  ( 18.50003594167399967, -2.686563651857999613, -11.33603604486000016 ) ) ;
#1674=EDGE_CURVE ( 'NONE', #28639, #10089, #68734, .T. ) ;
#1680=CARTESIAN_POINT ( 'NONE',  ( 24.38582845604300076, -8.886027874258999759, -8.989742048622000326 ) ) ;
#1681=CARTESIAN_POINT ( 'NONE',  ( 23.73390405283800320, -9.844988621918998817, 9.786411380388001291 ) ) ;
#1682=CARTESIAN_POINT ( 'NONE',  ( 24.53429011008099891, 3.614318944477000084, -12.31267538233000103 ) ) ;
#1687=CARTESIAN_POINT ( 'NONE',  ( 23.56666365135700403, -2.920993777334001340, 11.72568747145000145 ) ) ;
#1702=EDGE_LOOP ( 'NONE', ( #43272, #25436, #49295, #17211 ) ) ;
#1703=CARTESIAN_POINT ( 'NONE',  ( 24.36809152945900081, 12.06003563633000120, -3.271087558346000179 ) ) ;
#1704=CARTESIAN_POINT ( 'NONE',  ( 12.13343030045100157, -11.60886806805999960, 4.031065632098000506 ) ) ;
#1708=CARTESIAN_POINT ( 'NONE',  ( 24.60115016793161757, 12.20856116708383965, 3.061105478265555568 ) ) ;
#1712=CARTESIAN_POINT ( 'NONE',  ( 24.11212158815197526, -9.194244891325380920, 9.158718484554565720 ) ) ;
#1714=ORIENTED_EDGE ( 'NONE', *, *, #11784, .T. ) ;
#1716=VERTEX_POINT ( 'NONE', #14133 ) ;
#1718=CARTESIAN_POINT ( 'NONE',  ( 24.15441789255899963, 12.81544408666000123, -3.249376310703999682 ) ) ;
#1725=DIRECTION ( 'NONE',  ( -0.000000000000000000, 0.4815106998111243208, 0.8764402124317445253 ) ) ;
#1726=ORIENTED_EDGE ( 'NONE', *, *, #31675, .F. ) ;
#1732=CARTESIAN_POINT ( 'NONE',  ( 18.35381692023100086, -11.68079677495000013, 4.101394359672999812 ) ) ;
#1742=CARTESIAN_POINT ( 'NONE',  ( 23.60205915885299888, -11.56239291744999065, 3.974820703413998846 ) ) ;
#1745=CARTESIAN_POINT ( 'NONE',  ( 23.74333388532700084, -3.207902546252999976, 13.21027681470999937 ) ) ;
#1755=CARTESIAN_POINT ( 'NONE',  ( 24.60320129348500018, -3.644628662557000354, -12.27776523668999786 ) ) ;
#1758=CIRCLE ( 'NONE', #38577, 6.772075922005999615 ) ;
#1760=EDGE_CURVE ( 'NONE', #63538, #8271, #19600, .T. ) ;
#1762=ORIENTED_EDGE ( 'NONE', *, *, #66570, .T. ) ;
#1779=CARTESIAN_POINT ( 'NONE',  ( 24.30001682246400208, -8.938702682732001747, -8.938676171235998780 ) ) ;
#1781=CARTESIAN_POINT ( 'NONE',  ( 12.79999998712400178, -11.53033693765999779, 4.891431908114999949 ) ) ;
#1783=CARTESIAN_POINT ( 'NONE',  ( 16.86666666253433533, 3.351256455363717190, 11.15757949424526352 ) ) ;
#1787=CARTESIAN_POINT ( 'NONE',  ( 13.73682146000800053, -12.29517900649999973, -2.580790095973999776 ) ) ;
#1800=ADVANCED_FACE ( 'NONE', ( #14738 ), #53780, .T. ) ;
#1803=CARTESIAN_POINT ( 'NONE',  ( 11.29998658800000122, 3.824194713071000340, -11.71675648045999907 ) ) ;
#1804=CARTESIAN_POINT ( 'NONE',  ( 12.48079089692552479, -10.80976533111302729, 4.345114765590690986 ) ) ;
#1806=ORIENTED_EDGE ( 'NONE', *, *, #5814, .T. ) ;
#1823=EDGE_CURVE ( 'NONE', #15006, #18158, #54635, .T. ) ;
#1828=EDGE_LOOP ( 'NONE', ( #1310, #33184, #16721, #22187 ) ) ;
#1831=CARTESIAN_POINT ( 'NONE',  ( 25.02478208083906708, -8.536665412330339819, 8.299458527514417483 ) ) ;
#1836=B_SPLINE_CURVE_WITH_KNOTS ( 'NONE', 3,
 ( #53669, #27444, #27801, #5761 ),
 .UNSPECIFIED., .F., .F.,
 ( 4, 4 ),
 ( 0.000000000000000000, 1.000000000000000000 ),
 .UNSPECIFIED. ) ;
#1837=CARTESIAN_POINT ( 'NONE',  ( 23.89320776801300283, -8.283889223751996767, -7.778387372934005839 ) ) ;
#1841=CARTESIAN_POINT ( 'NONE',  ( 17.60677072361600182, 12.04986663410999981, -3.196654394853999825 ) ) ;
#1842=CARTESIAN_POINT ( 'NONE',  ( 23.61707933771300105, -2.917569334758999933, -13.53508108455999981 ) ) ;
#1844=B_SPLINE_CURVE_WITH_KNOTS ( 'NONE', 3,
 ( #61692, #56452, #8558, #29905, #16201, #31264 ),
 .UNSPECIFIED., .F., .F.,
 ( 4, 2, 4 ),
 ( 0.000000000000000000, 0.5000000000000000000, 1.000000000000000000 ),
 .UNSPECIFIED. ) ;
#1850=CARTESIAN_POINT ( 'NONE',  ( 23.66004879239100234, 3.393653897912999984, 13.50507458845999942 ) ) ;
#1863=CIRCLE ( 'NONE', #3003, 1.500000000000001332 ) ;
#1871=VERTEX_POINT ( 'NONE', #31504 ) ;
#1872=B_SPLINE_CURVE_WITH_KNOTS ( 'NONE', 3,
 ( #57319, #67460, #19585, #62227 ),
 .UNSPECIFIED., .F., .F.,
 ( 4, 4 ),
 ( 0.000000000000000000, 1.000000000000000000 ),
 .UNSPECIFIED. ) ;
#1878=CARTESIAN_POINT ( 'NONE',  ( 24.46225079000999969, -3.515716880278999756, 12.28737560831000053 ) ) ;
#1884=CARTESIAN_POINT ( 'NONE',  ( 24.56666016946500264, -8.743959839545999202, 8.863853254959998651 ) ) ;
#1886=ORIENTED_EDGE ( 'NONE', *, *, #26542, .T. ) ;
#1889=CARTESIAN_POINT ( 'NONE',  ( 21.00000012402669824, 12.42499880353999941, 0.000000000000000000 ) ) ;
#1890=CARTESIAN_POINT ( 'NONE',  ( 25.25797159228700295, -8.562781201510999196, -7.910473564811001168 ) ) ;
#1891=CARTESIAN_POINT ( 'NONE',  ( 13.00000000001300116, -11.52577654661000039, -1.696746661728000038 ) ) ;
#1893=CARTESIAN_POINT ( 'NONE',  ( 13.26944243593800010, 12.10482456369999937, 2.110592202804000284 ) ) ;
#1895=CARTESIAN_POINT ( 'NONE',  ( 23.56666365135700403, 9.069641144917994779, 7.556701426681005529 ) ) ;
#1898=CARTESIAN_POINT ( 'NONE',  ( 24.67921430886200085, -8.727631620858000261, -9.158313288899000426 ) ) ;
#1899=CARTESIAN_POINT ( 'NONE',  ( 24.99831752671624585, 8.543272426953288701, -8.328706555083702057 ) ) ;
#1906=EDGE_LOOP ( 'NONE', ( #68804, #41397, #34788, #67548, #39477, #23973, #37921, #1572, #51184, #50832 ) ) ;
#1908=DIRECTION ( 'NONE',  ( 1.000000000000000000, 0.000000000000000000, 0.000000000000000000 ) ) ;
#1910=VERTEX_POINT ( 'NONE', #11537 ) ;
#1911=CIRCLE ( 'NONE', #8592, 14.00000000000000000 ) ;
#1915=ORIENTED_EDGE ( 'NONE', *, *, #46236, .F. ) ;
#1919=CARTESIAN_POINT ( 'NONE',  ( 24.53429015151300163, -3.614318902553999902, -12.31267542782000035 ) ) ;
#1920=CARTESIAN_POINT ( 'NONE',  ( 24.35365242081699932, 1.906711579079999552, 11.36048031428999572 ) ) ;
#1930=CARTESIAN_POINT ( 'NONE',  ( 17.33333333161133538, -3.595161661652010565, -11.99793472338498646 ) ) ;
#1931=CARTESIAN_POINT ( 'NONE',  ( 24.37846962615400059, 3.167532807711999965, 12.03742776834999972 ) ) ;
#1942=CARTESIAN_POINT ( 'NONE',  ( 23.66004879239100234, 3.393652551760000247, -13.50507492672999987 ) ) ;
#1948=LINE ( 'NONE', #66253, #10161 ) ;
#1957=B_SPLINE_CURVE_WITH_KNOTS ( 'NONE', 3,
 ( #15570, #36898, #45511, #49442 ),
 .UNSPECIFIED., .F., .F.,
 ( 4, 4 ),
 ( 0.000000000000000000, 1.000000000000000000 ),
 .UNSPECIFIED. ) ;
#1961=CARTESIAN_POINT ( 'NONE',  ( 18.29995268966800026, -2.861739928647000220, -11.98821236628000086 ) ) ;
#1968=DIRECTION ( 'NONE',  ( 0.000000000000000000, -0.9466492601157000530, 0.3222656952305000266 ) ) ;
#1974=EDGE_CURVE ( 'NONE', #63863, #13607, #32628, .T. ) ;
#1981=ORIENTED_EDGE ( 'NONE', *, *, #34379, .F. ) ;
#1983=CARTESIAN_POINT ( 'NONE',  ( 24.30001680106099826, 12.21047197645999915, -3.271805488357999891 ) ) ;
#1985=ORIENTED_EDGE ( 'NONE', *, *, #955, .T. ) ;
#1991=ORIENTED_EDGE ( 'NONE', *, *, #5864, .T. ) ;
#1993=CARTESIAN_POINT ( 'NONE',  ( 24.22085262432600317, -12.94683699972000035, -3.132093620313999960 ) ) ;
#1996=ORIENTED_EDGE ( 'NONE', *, *, #50585, .F. ) ;
#2001=CARTESIAN_POINT ( 'NONE',  ( 24.34832162669904321, 8.810502600456597833, 8.810502600456597833 ) ) ;
#2007=B_SPLINE_CURVE_WITH_KNOTS ( 'NONE', 3,
 ( #39401, #49889, #44661, #18079 ),
 .UNSPECIFIED., .F., .F.,
 ( 4, 4 ),
 ( 0.000000000000000000, 1.000000000000000000 ),
 .UNSPECIFIED. ) ;
#2027=AXIS2_PLACEMENT_3D ( 'NONE', #65321, #17437, #66358 ) ;
#2032=CARTESIAN_POINT ( 'NONE',  ( 23.74223885472600060, -9.839017400655999168, 9.383841620339000045 ) ) ;
#2039=CARTESIAN_POINT ( 'NONE',  ( 15.90000000000314451, -3.738168175168965046, -11.41174933108808176 ) ) ;
#2042=CARTESIAN_POINT ( 'NONE',  ( 24.78226642313899930, 3.612166370762999623, -12.07973911291999869 ) ) ;
#2043=CARTESIAN_POINT ( 'NONE',  ( 17.76385332268500150, 3.526697956045000026, 11.96114712952999959 ) ) ;
#2047=ORIENTED_EDGE ( 'NONE', *, *, #59211, .T. ) ;
#2050=CARTESIAN_POINT ( 'NONE',  ( 25.27001783331474627, 3.169702853053691260, -11.48327890507672144 ) ) ;
#2057=EDGE_CURVE ( 'NONE', #28231, #31293, #31531, .T. ) ;
#2064=CARTESIAN_POINT ( 'NONE',  ( 23.59999172348799945, -10.30759808834999980, 9.317726582648999667 ) ) ;
#2067=DIRECTION ( 'NONE',  ( 2.801582883299285241E-16, -0.3352635608502960163, 0.9421243786071880066 ) ) ;
#2072=CARTESIAN_POINT ( 'NONE',  ( 24.30000000000000071, 8.756202924575998026, 7.455126447192999883 ) ) ;
#2087=CARTESIAN_POINT ( 'NONE',  ( 13.99999999379500082, 8.815218614167999789, 7.616697584347000394 ) ) ;
#2089=CARTESIAN_POINT ( 'NONE',  ( 17.57251690949600231, -11.38899788448000017, 4.574196188622000392 ) ) ;
#2100=CARTESIAN_POINT ( 'NONE',  ( 23.89320776801300283, -10.75689324691000337, 4.023240149132002230 ) ) ;
#2104=CARTESIAN_POINT ( 'NONE',  ( 18.53493609108600282, 3.035043098171999798, -12.19104765307000093 ) ) ;
#2119=ORIENTED_EDGE ( 'NONE', *, *, #25190, .F. ) ;
#2120=CARTESIAN_POINT ( 'NONE',  ( 25.41800012423099986, 8.397683232140998655, 8.090286078321000218 ) ) ;
#2129=CARTESIAN_POINT ( 'NONE',  ( 24.12728729028544450, -9.172538159014450798, -9.141953683885004622 ) ) ;
#2136=CARTESIAN_POINT ( 'NONE',  ( 24.44496356232399847, -3.224881240379999792, -12.03535804424000055 ) ) ;
#2137=ORIENTED_EDGE ( 'NONE', *, *, #3463, .T. ) ;
#2143=CARTESIAN_POINT ( 'NONE',  ( 18.30003129334700063, -2.732683817159999862, 11.53064095410000078 ) ) ;
#2149=DIRECTION ( 'NONE',  ( 0.000000000000000000, -0.9466492601157001641, 0.3222656952305000266 ) ) ;
#2158=VERTEX_POINT ( 'NONE', #53344 ) ;
#2160=ORIENTED_EDGE ( 'NONE', *, *, #46879, .T. ) ;
#2164=ORIENTED_EDGE ( 'NONE', *, *, #36441, .F. ) ;
#2166=CARTESIAN_POINT ( 'NONE',  ( 24.97036958156635578, -2.963721569976427439, -11.58470578805197526 ) ) ;
#2170=CARTESIAN_POINT ( 'NONE',  ( 24.39664890157733268, -12.09373467336017960, 3.240506439202065270 ) ) ;
#2171=DIRECTION ( 'NONE',  ( 1.000000000000000000, 0.000000000000000000, 0.000000000000000000 ) ) ;
#2186=CARTESIAN_POINT ( 'NONE',  ( 23.60205915885299888, -9.230633470673003771, -8.204162215335996322 ) ) ;
#2197=CARTESIAN_POINT ( 'NONE',  ( 17.76910169249500271, -3.411882384414000047, 11.89794055422999897 ) ) ;
#2198=CARTESIAN_POINT ( 'NONE',  ( 25.59994555223600088, 10.09686240769173793, 5.033199831112243672 ) ) ;
#2200=DIRECTION ( 'NONE',  ( 0.000000000000000000, -1.000000000000000000, 0.000000000000000000 ) ) ;
#2208=CARTESIAN_POINT ( 'NONE',  ( 15.48018231457700189, -8.819832297131000587, -7.692419064155999742 ) ) ;
#2210=DIRECTION ( 'NONE',  ( 0.000000000000000000, 2.692747180787898834E-07, -0.9999999999999638067 ) ) ;
#2211=ORIENTED_EDGE ( 'NONE', *, *, #64933, .T. ) ;
#2220=EDGE_CURVE ( 'NONE', #22693, #7406, #5340, .T. ) ;
#2221=EDGE_CURVE ( 'NONE', #8563, #48552, #29298, .T. ) ;
#2235=CARTESIAN_POINT ( 'NONE',  ( 24.85106292538000261, -8.568916185850000033, -8.855133745165000292 ) ) ;
#2239=CARTESIAN_POINT ( 'NONE',  ( 13.36350100824700071, 12.09092425779999935, 2.196870506499999820 ) ) ;
#2240=ORIENTED_EDGE ( 'NONE', *, *, #41188, .T. ) ;
#2248=CARTESIAN_POINT ( 'NONE',  ( 13.73886390325583484, -9.223149073484993465, -8.172668166918892751 ) ) ;
#2252=ORIENTED_EDGE ( 'NONE', *, *, #59755, .T. ) ;
#2262=CARTESIAN_POINT ( 'NONE',  ( 20.75138802851920161, 5.760487483753345295, -0.05108123232907756106 ) ) ;
#2272=CARTESIAN_POINT ( 'NONE',  ( 24.95408850090100117, 3.532265432305000008, 11.87004585020000036 ) ) ;
#2274=CARTESIAN_POINT ( 'NONE',  ( 25.34046477980565726, -8.480592698500919013, 7.990868443695373635 ) ) ;
#2276=EDGE_CURVE ( 'NONE', #59370, #20699, #35967, .T. ) ;
#2278=EDGE_LOOP ( 'NONE', ( #10024, #47177, #239, #5015 ) ) ;
#2286=LINE ( 'NONE', #22909, #50725 ) ;
#2288=ORIENTED_EDGE ( 'NONE', *, *, #68127, .F. ) ;
#2298=EDGE_CURVE ( 'NONE', #1148, #1871, #54939, .T. ) ;
#2299=CARTESIAN_POINT ( 'NONE',  ( 25.29987667925500361, 10.83443035398000021, 3.855530949778000149 ) ) ;
#2302=PLANE ( 'NONE',  #6545 ) ;
#2308=CARTESIAN_POINT ( 'NONE',  ( 24.11240964069585146, -12.52839750956255571, -3.382904902698306682 ) ) ;
#2309=CARTESIAN_POINT ( 'NONE',  ( 24.36809152945900081, 3.197172894633000251, -12.07984101077999917 ) ) ;
#2313=CYLINDRICAL_SURFACE ( 'NONE', #26337, 1.000000000000000444 ) ;
#2322=CARTESIAN_POINT ( 'NONE',  ( 16.20679720086500097, 3.450734216086000394, 11.08786462205999968 ) ) ;
#2326=DIRECTION ( 'NONE',  ( 0.000000000000000000, -1.000000000000000000, -4.343197676503993465E-12 ) ) ;
#2330=CARTESIAN_POINT ( 'NONE',  ( 18.19991693152162426, -3.160411602603943049, 11.91446363486502413 ) ) ;
#2332=CARTESIAN_POINT ( 'NONE',  ( 24.67921580188599862, 3.567514645466999923, -12.13750897870000145 ) ) ;
#2333=CARTESIAN_POINT ( 'NONE',  ( 24.56914242134000048, -12.57279260814000033, -2.966897477730999544 ) ) ;
#2335=CONICAL_SURFACE ( 'NONE', #44768, 12.47499939740000130, 0.7853981102588313279 ) ;
#2336=DIRECTION ( 'NONE',  ( 0.000000000000000000, -0.2437104726400046162, 0.9698480321811173699 ) ) ;
#2343=CARTESIAN_POINT ( 'NONE',  ( 24.44496488009700030, 8.810487470433001178, 8.810507756548000557 ) ) ;
#2349=DIRECTION ( 'NONE',  ( 0.000000000000000000, 0.2588190451024934835, 0.9659258262890757507 ) ) ;
#2354=DIRECTION ( 'NONE',  ( 1.000000000000000000, 0.000000000000000000, 0.000000000000000000 ) ) ;
#2359=CARTESIAN_POINT ( 'NONE',  ( 15.90000000000000036, 0.000000000000000000, 0.000000000000000000 ) ) ;
#2367=CARTESIAN_POINT ( 'NONE',  ( 25.39409677104811891, -11.19592564009993474, -3.259886264983261839 ) ) ;
#2370=CARTESIAN_POINT ( 'NONE',  ( 24.25375554908000097, 3.234179890672000290, 12.21792844062999883 ) ) ;
#2371=VECTOR ( 'NONE', #50412, 1000.000000000000114 ) ;
#2377=CARTESIAN_POINT ( 'NONE',  ( 23.66004879239100234, 3.393653897912999984, 13.50507458845999942 ) ) ;
#2383=CARTESIAN_POINT ( 'NONE',  ( 16.32027728221806484, 3.351613101376117232, 11.15747237328652730 ) ) ;
#2391=CARTESIAN_POINT ( 'NONE',  ( 11.44792571093000255, -3.801678398496999733, 11.87711516161999903 ) ) ;
#2397=ORIENTED_EDGE ( 'NONE', *, *, #34906, .F. ) ;
#2400=ORIENTED_EDGE ( 'NONE', *, *, #29004, .T. ) ;
#2406=EDGE_CURVE ( 'NONE', #38892, #23870, #46951, .T. ) ;
#2416=CARTESIAN_POINT ( 'NONE',  ( 24.13791493634210994, 9.157217056292619617, 9.130314356011920651 ) ) ;
#2417=EDGE_LOOP ( 'NONE', ( #49117, #33023, #2657, #42134 ) ) ;
#2422=CARTESIAN_POINT ( 'NONE',  ( 18.01908732848200145, -11.78185846591000008, 3.459210216787000025 ) ) ;
#2433=CARTESIAN_POINT ( 'NONE',  ( 23.99192513437000329, -3.573328852826999746, 12.95691943739999985 ) ) ;
#2436=CARTESIAN_POINT ( 'NONE',  ( 18.48724299199999876, 3.206939682244000167, -12.14698705996000072 ) ) ;
#2442=EDGE_CURVE ( 'NONE', #19263, #35108, #66140, .T. ) ;
#2457=EDGE_CURVE ( 'NONE', #40201, #63789, #28641, .T. ) ;
#2458=CARTESIAN_POINT ( 'NONE',  ( 13.50000000000000178, 11.75776087185409402, 2.440894935389088527 ) ) ;
#2460=CARTESIAN_POINT ( 'NONE',  ( 24.92848013445852828, 11.55907645929356775, 3.214033862752819992 ) ) ;
#2463=ORIENTED_EDGE ( 'NONE', *, *, #6826, .F. ) ;
#2467=CARTESIAN_POINT ( 'NONE',  ( 20.75138802851920161, -5.760713961201000544, 0.000000000000000000 ) ) ;
#2469=CARTESIAN_POINT ( 'NONE',  ( 24.60999195273300089, -12.22061417745999989, 3.051130890667999918 ) ) ;
#2474=ORIENTED_EDGE ( 'NONE', *, *, #38115, .F. ) ;
#2481=ORIENTED_EDGE ( 'NONE', *, *, #29770, .T. ) ;
#2482=CARTESIAN_POINT ( 'NONE',  ( 17.60000000085000238, 12.11987927271999865, -3.159802730921999814 ) ) ;
#2491=CARTESIAN_POINT ( 'NONE',  ( 24.50549018585800098, 12.34681877080999968, 3.084981659446000002 ) ) ;
#2494=VERTEX_POINT ( 'NONE', #37694 ) ;
#2499=CARTESIAN_POINT ( 'NONE',  ( 25.26127586260790281, -2.660441985988178715, -11.37584977663462205 ) ) ;
#2503=B_SPLINE_CURVE_WITH_KNOTS ( 'NONE', 3,
 ( #58616, #12108, #11748, #54406 ),
 .UNSPECIFIED., .F., .F.,
 ( 4, 4 ),
 ( 0.000000000000000000, 1.000000000000000000 ),
 .UNSPECIFIED. ) ;
#2511=VERTEX_POINT ( 'NONE', #988 ) ;
#2526=CARTESIAN_POINT ( 'NONE',  ( 13.50018479229300006, -11.60142623882999935, -2.415183939829000259 ) ) ;
#2527=CARTESIAN_POINT ( 'NONE',  ( 23.73943898212699821, -3.322335461309999793, -13.28161925880999839 ) ) ;
#2542=CARTESIAN_POINT ( 'NONE',  ( 23.59299099590867499, -13.38589721419561407, 4.028864339703104314 ) ) ;
#2543=VERTEX_POINT ( 'NONE', #33149 ) ;
#2545=CARTESIAN_POINT ( 'NONE',  ( 18.29999330150736014, -11.02846243710336616, 3.754394858745019103 ) ) ;
#2549=CARTESIAN_POINT ( 'NONE',  ( 23.56666365135700403, 11.07911597677999360, -4.076188921367005058 ) ) ;
#2551=VERTEX_POINT ( 'NONE', #11127 ) ;
#2553=AXIS2_PLACEMENT_3D ( 'NONE', #7891, #67894, #51816 ) ;
#2556=PRODUCT_DEFINITION_SHAPE ( 'NONE', 'NONE',  #35119 ) ;
#2563=CARTESIAN_POINT ( 'NONE',  ( 25.47111570701200023, 11.11941859758999840, 3.299547261379999874 ) ) ;
#2569=CARTESIAN_POINT ( 'NONE',  ( 25.20464492906199894, -8.548379336130999206, -7.995593105742999640 ) ) ;
#2570=CARTESIAN_POINT ( 'NONE',  ( 13.09269116698435909, -11.52576810756808356, -1.696811579065486741 ) ) ;
#2571=CARTESIAN_POINT ( 'NONE',  ( 23.59999445750599989, -13.22316420035999940, -4.267800004853000040 ) ) ;
#2579=CARTESIAN_POINT ( 'NONE',  ( 24.74120093721589342, 3.111623860952520193, 11.77170576849003147 ) ) ;
#2581=CARTESIAN_POINT ( 'NONE',  ( 24.13791496213264409, -12.48569266960873136, 3.365225404910305418 ) ) ;
#2591=CARTESIAN_POINT ( 'NONE',  ( 25.39991778581708814, 10.74016754877895430, 3.821986718425039786 ) ) ;
#2614=ORIENTED_EDGE ( 'NONE', *, *, #19176, .T. ) ;
#2619=CARTESIAN_POINT ( 'NONE',  ( 23.51521487668100008, 10.46906073003999893, -9.496281516038997950 ) ) ;
#2621=CARTESIAN_POINT ( 'NONE',  ( 18.26242637978999994, -2.744390477411999818, -11.56740641610000075 ) ) ;
#2631=B_SPLINE_CURVE_WITH_KNOTS ( 'NONE', 3,
 ( #3979, #24641, #39692, #14155 ),
 .UNSPECIFIED., .F., .F.,
 ( 4, 4 ),
 ( 0.000000000000000000, 1.000000000000000000 ),
 .UNSPECIFIED. ) ;
#2642=CARTESIAN_POINT ( 'NONE',  ( 18.23777342769881926, -3.105166803968429257, -11.92942855515249967 ) ) ;
#2648=CARTESIAN_POINT ( 'NONE',  ( 24.41456973790700147, 3.182129207855000086, -12.02370739584000070 ) ) ;
#2657=ORIENTED_EDGE ( 'NONE', *, *, #16478, .F. ) ;
#2659=DIRECTION ( 'NONE',  ( 0.000000000000000000, 0.8765967884314782577, -0.4812255921203881792 ) ) ;
#2665=EDGE_CURVE ( 'NONE', #30301, #35342, #42003, .T. ) ;
#2674=CARTESIAN_POINT ( 'NONE',  ( 23.74313545907000389, -13.04470672865000047, -3.827358778968999786 ) ) ;
#2675=FACE_OUTER_BOUND ( 'NONE', #19705, .T. ) ;
#2676=SURFACE_STYLE_USAGE ( .BOTH. , #55825 ) ;
#2685=CARTESIAN_POINT ( 'NONE',  ( 24.34833239419533513, 3.256146798601845749, 12.15210528928062494 ) ) ;
#2694=CARTESIAN_POINT ( 'NONE',  ( 23.58333425412700279, 1.475264355121999897E-12, 7.429612480791998923E-13 ) ) ;
#2699=CARTESIAN_POINT ( 'NONE',  ( 13.00000000009400303, -11.69118001589999878, -1.923222888683999932 ) ) ;
#2711=CARTESIAN_POINT ( 'NONE',  ( 25.34046054230887179, -11.16058825301069746, -3.348982524390977655 ) ) ;
#2714=DIRECTION ( 'NONE',  ( 0.000000000000000000, 0.000000000000000000, -1.000000000000000000 ) ) ;
#2715=DIRECTION ( 'NONE',  ( 0.000000000000000000, 0.000000000000000000, 1.000000000000000000 ) ) ;
#2717=ORIENTED_EDGE ( 'NONE', *, *, #10477, .F. ) ;
#2733=CARTESIAN_POINT ( 'NONE',  ( 17.60000000024299993, 11.86189249994999884, -3.298671769835999967 ) ) ;
#2744=ORIENTED_EDGE ( 'NONE', *, *, #13110, .T. ) ;
#2746=ORIENTED_EDGE ( 'NONE', *, *, #66997, .F. ) ;
#2747=EDGE_CURVE ( 'NONE', #34308, #25967, #67870, .T. ) ;
#2748=EDGE_CURVE ( 'NONE', #44042, #28231, #31973, .T. ) ;
#2751=CARTESIAN_POINT ( 'NONE',  ( 23.58334011193800350, 0.000000000000000000, -3.819167204710999951E-13 ) ) ;
#2756=VERTEX_POINT ( 'NONE', #22990 ) ;
#2758=CONICAL_SURFACE ( 'NONE', #6086, 12.71246950475999959, 0.8960553845711767273 ) ;
#2768=CARTESIAN_POINT ( 'NONE',  ( 18.35500032369700207, -2.879010252073999521, -12.03969535450000095 ) ) ;
#2769=CARTESIAN_POINT ( 'NONE',  ( 24.46729256497600247, -8.826997888156999039, 8.952499470947000049 ) ) ;
#2778=EDGE_CURVE ( 'NONE', #26398, #63101, #12858, .T. ) ;
#2779=CARTESIAN_POINT ( 'NONE',  ( 23.64145649527500126, -3.069298110642999955, 13.45466198155999926 ) ) ;
#2789=CONICAL_SURFACE ( 'NONE', #21735, 13.94999929345000211, 0.7853981072369679017 ) ;
#2805=ORIENTED_EDGE ( 'NONE', *, *, #68468, .T. ) ;
#2808=CARTESIAN_POINT ( 'NONE',  ( 12.79999999824001122, 12.03389405692475300, -3.206111686008664918 ) ) ;
#2827=EDGE_CURVE ( 'NONE', #12746, #20439, #6973, .T. ) ;
#2828=EDGE_CURVE ( 'NONE', #56347, #4626, #55851, .T. ) ;
#2829=CARTESIAN_POINT ( 'NONE',  ( 18.50001572531400029, -1.956586047027013553, 12.40985500578818090 ) ) ;
#2831=CARTESIAN_POINT ( 'NONE',  ( 11.79999999684100054, 3.345264396959000130, -11.86064773189999855 ) ) ;
#2832=EDGE_CURVE ( 'NONE', #60315, #18158, #48686, .T. ) ;
#2843=CARTESIAN_POINT ( 'NONE',  ( 24.67921321731900264, -3.567517257907000250, -12.13750614118000115 ) ) ;
#2849=CARTESIAN_POINT ( 'NONE',  ( 11.35562122949000141, 3.716778816705999855, -11.19591510979999960 ) ) ;
#2853=DIRECTION ( 'NONE',  ( 1.000000000000000000, 0.000000000000000000, 0.000000000000000000 ) ) ;
#2865=ORIENTED_EDGE ( 'NONE', *, *, #21607, .T. ) ;
#2869=CARTESIAN_POINT ( 'NONE',  ( 24.25865791894600321, -3.167027296516999879, -12.13989236613999978 ) ) ;
#2870=CARTESIAN_POINT ( 'NONE',  ( 23.59999443371599881, 2.915558930973999985, 13.58549620949000136 ) ) ;
#2874=DIRECTION ( 'NONE',  ( 1.000000000000000000, 0.000000000000000000, 0.000000000000000000 ) ) ;
#2875=CARTESIAN_POINT ( 'NONE',  ( 24.67921580255100267, 8.727633792449999817, 9.158312800479000870 ) ) ;
#2876=CARTESIAN_POINT ( 'NONE',  ( 25.55282635881618347, 11.13089659500204753, -3.116549873335771714 ) ) ;
#2887=CARTESIAN_POINT ( 'NONE',  ( 23.56665657345700282, -13.31365812469000076, 4.296923216748999685 ) ) ;
#2895=CARTESIAN_POINT ( 'NONE',  ( 23.89320776801300283, 8.283889223723997830, -7.778387373039001851 ) ) ;
#2901=CIRCLE ( 'NONE', #48672, 13.98989063586000370 ) ;
#2907=CARTESIAN_POINT ( 'NONE',  ( 24.48513962453899850, -12.12976302882999846, -3.164527203478999962 ) ) ;
#2908=ADVANCED_FACE ( 'NONE', ( #9657 ), #54785, .F. ) ;
#2911=CARTESIAN_POINT ( 'NONE',  ( 13.99956681845000084, -8.827069132150999309, -7.822720559936999329 ) ) ;
#2912=CARTESIAN_POINT ( 'NONE',  ( 21.72233714749290101, 4.999803429358669504, -0.04433585200820212152 ) ) ;
#2913=CARTESIAN_POINT ( 'NONE',  ( 25.37646317443000044, -8.494765284640999781, -7.922174285211998956 ) ) ;
#2914=CARTESIAN_POINT ( 'NONE',  ( 23.60000000000000497, -10.96673476284452775, -8.588459421149421402 ) ) ;
#2922=CONICAL_SURFACE ( 'NONE', #52019, 13.94999929345000211, 0.7853981072369679017 ) ;
#2932=ORIENTED_EDGE ( 'NONE', *, *, #1367, .F. ) ;
#2933=ADVANCED_FACE ( 'NONE', ( #31003 ), #4409, .T. ) ;
#2940=CARTESIAN_POINT ( 'NONE',  ( 23.89320776801300283, 3.226867021103002831, 11.46303308828999867 ) ) ;
#2944=CARTESIAN_POINT ( 'NONE',  ( 24.37808886069849379, 3.385972254890575961, -12.24452376059983827 ) ) ;
#2948=CONICAL_SURFACE ( 'NONE', #63219, 11.74991359182999950, 0.7853990805437361944 ) ;
#2952=AXIS2_PLACEMENT_3D ( 'NONE', #21154, #64468, #1208 ) ;
#2954=ORIENTED_EDGE ( 'NONE', *, *, #53131, .T. ) ;
#2958=ADVANCED_FACE ( 'NONE', ( #38297 ), #52907, .T. ) ;
#2963=CARTESIAN_POINT ( 'NONE',  ( 23.58699436501100166, 10.27243565008999937, -9.419031392528999902 ) ) ;
#2964=CARTESIAN_POINT ( 'NONE',  ( 17.96012107570599881, -3.168891391480999520, -11.45723209283999999 ) ) ;
#2980=DIRECTION ( 'NONE',  ( 0.000000000000000000, 0.7071067811865475727, -0.7071067811865475727 ) ) ;
#2986=CARTESIAN_POINT ( 'NONE',  ( 16.09997386696500143, 7.697446472043785626, 8.794756076490960695 ) ) ;
#2987=CARTESIAN_POINT ( 'NONE',  ( 24.55996189763800075, 3.658601031398000192, -12.32999353876000015 ) ) ;
#2989=ORIENTED_EDGE ( 'NONE', *, *, #56853, .T. ) ;
#2991=EDGE_CURVE ( 'NONE', #64727, #56117, #39528, .T. ) ;
#2992=EDGE_CURVE ( 'NONE', #5259, #36190, #47323, .T. ) ;
#2998=AXIS2_PLACEMENT_3D ( 'NONE', #30155, #14412, #14748 ) ;
#3000=EDGE_LOOP ( 'NONE', ( #68141, #29600, #65568, #23670, #1333 ) ) ;
#3001=CARTESIAN_POINT ( 'NONE',  ( 16.03350391962053578, -3.653603504000225932, -11.13263026093549790 ) ) ;
#3003=AXIS2_PLACEMENT_3D ( 'NONE', #26242, #5251, #11516 ) ;
#3007=CARTESIAN_POINT ( 'NONE',  ( 23.73952317692686975, -9.827649483940422925, -9.725500440716153605 ) ) ;
#3011=CARTESIAN_POINT ( 'NONE',  ( 24.66807826193639031, 3.571100427759083651, 12.15100773348912178 ) ) ;
#3012=ORIENTED_EDGE ( 'NONE', *, *, #50136, .F. ) ;
#3021=CARTESIAN_POINT ( 'NONE',  ( 23.60000336012799593, 13.25014977213286471, -4.189788727593960260 ) ) ;
#3025=CARTESIAN_POINT ( 'NONE',  ( 24.14062753054661314, -3.327835720320030166, -12.49067376861903433 ) ) ;
#3029=ORIENTED_EDGE ( 'NONE', *, *, #2832, .F. ) ;
#3037=CARTESIAN_POINT ( 'NONE',  ( 24.30000000000000071, -8.756202924575998026, -7.455126447192999883 ) ) ;
#3038=CARTESIAN_POINT ( 'NONE',  ( 23.58461259684199973, 13.39492983452999830, 4.041214499598000387 ) ) ;
#3042=CARTESIAN_POINT ( 'NONE',  ( 24.39664835772133600, -8.853227849050998799, -8.853227849050998799 ) ) ;
#3048=CARTESIAN_POINT ( 'NONE',  ( 24.30000000000000071, -2.524919604596999712, 12.12772056298999956 ) ) ;
#3054=CARTESIAN_POINT ( 'NONE',  ( 23.61277708754100146, 10.15828648011000190, 9.482376091975998733 ) ) ;
#3061=AXIS2_PLACEMENT_3D ( 'NONE', #55633, #23467, #64713 ) ;
#3073=CARTESIAN_POINT ( 'NONE',  ( 11.72754826524499983, -3.413272067235999963, 11.89753034518999897 ) ) ;
#3081=EDGE_LOOP ( 'NONE', ( #7939, #42566, #1511, #24982 ) ) ;
#3090=FACE_OUTER_BOUND ( 'NONE', #60427, .T. ) ;
#3098=AXIS2_PLACEMENT_3D ( 'NONE', #5641, #36435, #58447 ) ;
#3108=CARTESIAN_POINT ( 'NONE',  ( 18.35168611684299833, -2.962034070680999776, -12.02052262816000017 ) ) ;
#3109=CARTESIAN_POINT ( 'NONE',  ( 24.40777907856499951, -8.879621479695998687, 9.005112135669000040 ) ) ;
#3119=CARTESIAN_POINT ( 'NONE',  ( 12.10000000004390408, -11.04996331180911717, 3.691231724050993979 ) ) ;
#3121=CARTESIAN_POINT ( 'NONE',  ( 24.23279320724300234, -3.402312112046000259, 12.43077114457000043 ) ) ;
#3127=CARTESIAN_POINT ( 'NONE',  ( 24.67921321731900264, -3.567517257907000250, -12.13750614118000115 ) ) ;
#3128=ORIENTED_EDGE ( 'NONE', *, *, #16611, .F. ) ;
#3145=CARTESIAN_POINT ( 'NONE',  ( 24.30000000000000071, -2.204728229456999866, 11.99913219504999873 ) ) ;
#3152=CARTESIAN_POINT ( 'NONE',  ( 12.09999922233642344, 11.66744139996707119, -3.971920075670921424 ) ) ;
#3154=CARTESIAN_POINT ( 'NONE',  ( 11.42397234076999979, 3.432581932914000156, -11.79497283202000091 ) ) ;
#3161=CARTESIAN_POINT ( 'NONE',  ( 18.49993212792200126, -2.908182645667999999, -12.18276646858999968 ) ) ;
#3163=ORIENTED_EDGE ( 'NONE', *, *, #38453, .T. ) ;
#3182=CARTESIAN_POINT ( 'NONE',  ( 11.40010796094000334, -6.616929226765999876E-14, -1.143529715363999905E-14 ) ) ;
#3185=ORIENTED_EDGE ( 'NONE', *, *, #62808, .T. ) ;
#3187=DIRECTION ( 'NONE',  ( -1.000000000000000000, 0.000000000000000000, 0.000000000000000000 ) ) ;
#3201=DIRECTION ( 'NONE',  ( 0.000000000000000000, 1.000000000000000000, 0.000000000000000000 ) ) ;
#3205=CARTESIAN_POINT ( 'NONE',  ( 24.71768044457226665, 8.650200248279249493, 8.600992414847871359 ) ) ;
#3214=DIRECTION ( 'NONE',  ( -1.000000000000000000, 0.000000000000000000, 0.000000000000000000 ) ) ;
#3226=DIRECTION ( 'NONE',  ( 0.000000000000000000, -0.2588190451024934835, -0.9659258262890757507 ) ) ;
#3228=EDGE_CURVE ( 'NONE', #2494, #12730, #63524, .T. ) ;
#3233=CARTESIAN_POINT ( 'NONE',  ( 15.72922381500400313, -8.763625284509998892, -7.896085856502000233 ) ) ;
#3244=CARTESIAN_POINT ( 'NONE',  ( 23.56666365135700403, 8.694246338465996260, -8.392498551259993889 ) ) ;
#3256=CARTESIAN_POINT ( 'NONE',  ( 24.77999265559800079, -12.27030725872999817, -2.912406685646000248 ) ) ;
#3261=CARTESIAN_POINT ( 'NONE',  ( 23.60000000000000497, -12.52449491606653709, -6.096403221384886884 ) ) ;
#3263=ORIENTED_EDGE ( 'NONE', *, *, #15874, .F. ) ;
#3268=CARTESIAN_POINT ( 'NONE',  ( 24.73253374366442969, 3.116078331550232505, 11.77909370293319036 ) ) ;
#3273=CARTESIAN_POINT ( 'NONE',  ( 13.63315305048521964, -12.20113081363247076, -2.519319003639654220 ) ) ;
#3287=CARTESIAN_POINT ( 'NONE',  ( 24.60320129348500018, -12.45517092796000114, -2.982541609212000289 ) ) ;
#3289=ORIENTED_EDGE ( 'NONE', *, *, #33539, .T. ) ;
#3302=EDGE_CURVE ( 'NONE', #35662, #64677, #11035, .T. ) ;
#3303=ADVANCED_FACE ( 'NONE', ( #35813 ), #53629, .F. ) ;
#3305=CARTESIAN_POINT ( 'NONE',  ( 24.08742125846098503, 3.338819417450129112, 12.58660453514891309 ) ) ;
#3306=CARTESIAN_POINT ( 'NONE',  ( 23.62017846084600237, 10.21547452202000095, -9.339924903530999245 ) ) ;
#3307=CARTESIAN_POINT ( 'NONE',  ( 17.76937411412500367, -3.251867979506000150, -11.33740618442000070 ) ) ;
#3313=CARTESIAN_POINT ( 'NONE',  ( 24.35365242081700288, -10.90899669677000006, -3.315896191878997978 ) ) ;
#3317=CARTESIAN_POINT ( 'NONE',  ( 21.60000000000000142, -12.52500000000000036, 0.000000000000000000 ) ) ;
#3319=EDGE_CURVE ( 'NONE', #37580, #53410, #13840, .T. ) ;
#3324=B_SPLINE_SURFACE_WITH_KNOTS ( 'NONE', 3, 3, ( 
 ( #31250, #5353, #53595, #20750 ),
 ( #37511, #37857, #52910, #26692 ),
 ( #15508, #47326, #53247, #68629 ),
 ( #5691, #5007, #9911, #26343 ),
 ( #59182, #10595, #47669, #68981 ),
 ( #10943, #48346, #42421, #21095 ),
 ( #27033, #16531, #63728, #52559 ),
 ( #15840, #64068, #37172, #58491 ),
 ( #48700, #42760, #31937, #48007 ),
 ( #58835, #21770, #106, #11282 ),
 ( #32621, #64407, #452, #21423 ),
 ( #43105, #800, #22117, #25995 ),
 ( #53932, #43462, #6035, #27373 ),
 ( #15159, #36479, #4655, #60227 ),
 ( #12330, #1841, #13031, #65801 ),
 ( #11976, #17928, #54980, #11623 ) ),
 .UNSPECIFIED., .F., .F., .F.,
 ( 4, 1, 1, 1, 1, 1, 1, 1, 1, 1, 1, 1, 1, 4 ),
 ( 4, 4 ),
 ( 0.01677647950063999860, 0.07692307692307999434, 0.1538461538461999845, 0.2307692307692000011, 0.3076923076922999933, 0.3846153846154000133, 0.4615384615385000333, 0.5384615384614999112, 0.6153846153845999867, 0.6923076923076999512, 0.7692307692308000266, 0.8461538461537999600, 0.9230769230769000355, 0.9705716827899999455 ),
 ( -0.1835260008786999963, 1.183623993927000129 ),
 .UNSPECIFIED. ) ;
#3330=FACE_OUTER_BOUND ( 'NONE', #63610, .T. ) ;
#3332=CARTESIAN_POINT ( 'NONE',  ( 18.06247470437139313, -3.164801830692922202, -11.41978211458705594 ) ) ;
#3342=ORIENTED_EDGE ( 'NONE', *, *, #53039, .F. ) ;
#3343=FACE_BOUND ( 'NONE', #40249, .T. ) ;
#3363=CARTESIAN_POINT ( 'NONE',  ( 23.59999172237900211, -2.915589696762999949, -13.58550518520000061 ) ) ;
#3377=CARTESIAN_POINT ( 'NONE',  ( 23.66465205395200044, 13.24762218775999933, 3.909563642290999397 ) ) ;
#3382=ADVANCED_FACE ( 'NONE', ( #21782 ), #32300, .T. ) ;
#3383=CARTESIAN_POINT ( 'NONE',  ( 15.58628609634500073, 9.247881098673000011, 8.227358011109998870 ) ) ;
#3386=CARTESIAN_POINT ( 'NONE',  ( 13.56663763856171734, 9.565814837444753138, 7.877123307579370071 ) ) ;
#3388=CARTESIAN_POINT ( 'NONE',  ( 24.37899130486400168, -12.00803297839000017, 3.275428646162999780 ) ) ;
#3391=CARTESIAN_POINT ( 'NONE',  ( 24.41555930013399944, 3.181808913646000381, 12.02251225967000003 ) ) ;
#3392=DIRECTION ( 'NONE',  ( 1.000000000000000000, 0.000000000000000000, 0.000000000000000000 ) ) ;
#3393=CARTESIAN_POINT ( 'NONE',  ( 25.29989727901499919, -2.078227429405999693, -11.31065739696999906 ) ) ;
#3396=DIRECTION ( 'NONE',  ( -1.000000000000000000, 0.000000000000000000, 0.000000000000000000 ) ) ;
#3402=CARTESIAN_POINT ( 'NONE',  ( 17.77415039705200073, 3.297056071606000227, 11.83473721697999892 ) ) ;
#3414=CARTESIAN_POINT ( 'NONE',  ( 11.35641146476999985, -3.755935701663000170, 11.79446980948000068 ) ) ;
#3437=ORIENTED_EDGE ( 'NONE', *, *, #43227, .T. ) ;
#3442=CARTESIAN_POINT ( 'NONE',  ( 18.53936233968600078, -2.923364741758000207, -12.21823820824000073 ) ) ;
#3443=CARTESIAN_POINT ( 'NONE',  ( 24.26733150070300127, -8.951944080097000267, 8.897842723392001218 ) ) ;
#3453=CARTESIAN_POINT ( 'NONE',  ( 15.20000000000000107, -11.99088163391999906, 3.229229350024999778 ) ) ;
#3457=PLANE ( 'NONE',  #41636 ) ;
#3459=CARTESIAN_POINT ( 'NONE',  ( 25.59997821859199973, 2.856411258734000036, -11.13959759756999901 ) ) ;
#3461=AXIS2_PLACEMENT_3D ( 'NONE', #63406, #62717, #36854 ) ;
#3463=EDGE_CURVE ( 'NONE', #7451, #11759, #19904, .T. ) ;
#3467=B_SPLINE_CURVE_WITH_KNOTS ( 'NONE', 3,
 ( #7363, #50023, #51052, #8406, #29056, #66434 ),
 .UNSPECIFIED., .F., .F.,
 ( 4, 2, 4 ),
 ( 0.000000000000000000, 0.5000000000000000000, 1.000000000000000000 ),
 .UNSPECIFIED. ) ;
#3468=CARTESIAN_POINT ( 'NONE',  ( 23.63877154019659343, -10.04588656656894408, -9.676553435357190480 ) ) ;
#3491=CARTESIAN_POINT ( 'NONE',  ( 13.78326532032400031, -9.295717737520000412, -8.172239456948000580 ) ) ;
#3493=CARTESIAN_POINT ( 'NONE',  ( 25.50731327284336558, -8.309743679583657894, 8.116427603517399447 ) ) ;
#3494=CARTESIAN_POINT ( 'NONE',  ( 11.49978667957999967, -12.43119799159999950, -1.530013559959999991 ) ) ;
#3500=CARTESIAN_POINT ( 'NONE',  ( 13.50018479229300006, -11.60142623882999935, -2.415183939829000259 ) ) ;
#3511=CARTESIAN_POINT ( 'NONE',  ( 23.84019000122944831, -3.320739317830645021, 13.05082518065574426 ) ) ;
#3521=CARTESIAN_POINT ( 'NONE',  ( 24.57710018668033669, -3.191964740936587663, -11.91258045713028224 ) ) ;
#3532=CARTESIAN_POINT ( 'NONE',  ( 25.50737144172638438, 11.18383546498688297, 3.138211644118512833 ) ) ;
#3543=ORIENTED_EDGE ( 'NONE', *, *, #65361, .F. ) ;
#3545=CARTESIAN_POINT ( 'NONE',  ( 25.44994642811700203, 0.000000000000000000, 2.140509991476999645E-13 ) ) ;
#3548=DIRECTION ( 'NONE',  ( -1.000000000000000000, 0.000000000000000000, 0.000000000000000000 ) ) ;
#3549=ADVANCED_FACE ( 'NONE', ( #45201 ), #8157, .T. ) ;
#3561=DIRECTION ( 'NONE',  ( 0.000000000000000000, 0.7577476854548028662, -0.6525476574074028369 ) ) ;
#3564=CARTESIAN_POINT ( 'NONE',  ( 16.04382898362900178, -8.457859886528000359, -8.090718092504999959 ) ) ;
#3574=CARTESIAN_POINT ( 'NONE',  ( 24.35365242081699932, 10.79182034089001796, -4.028979492054000744 ) ) ;
#3595=CIRCLE ( 'NONE', #19280, 0.9999999999999993339 ) ;
#3611=CARTESIAN_POINT ( 'NONE',  ( 21.60000012424471194, 13.89999856298999958, 0.000000000000000000 ) ) ;
#3620=CARTESIAN_POINT ( 'NONE',  ( 17.79999999998900151, -3.595165934733000057, 11.99793354950999991 ) ) ;
#3621=B_SPLINE_CURVE_WITH_KNOTS ( 'NONE', 3,
 ( #19156, #55540, #18480, #39804 ),
 .UNSPECIFIED., .F., .F.,
 ( 4, 4 ),
 ( 0.000000000000000000, 1.000000000000000000 ),
 .UNSPECIFIED. ) ;
#3623=CARTESIAN_POINT ( 'NONE',  ( 13.50007192468514106, -9.074936576711701619, -7.617865797329282707 ) ) ;
#3629=EDGE_CURVE ( 'NONE', #15208, #67674, #35195, .T. ) ;
#3633=EDGE_LOOP ( 'NONE', ( #18086, #32343, #38437, #61367, #66252, #67432, #51642, #5520, #4334, #36983, #15639, #15704, #18460, #55837, #60774 ) ) ;
#3634=ORIENTED_EDGE ( 'NONE', *, *, #890, .T. ) ;
#3638=CARTESIAN_POINT ( 'NONE',  ( 24.11240984803955456, 3.334517130192976353, 12.54136258879263544 ) ) ;
#3639=CARTESIAN_POINT ( 'NONE',  ( 23.85292159917500143, 9.641972580453998631, -9.631818861864001491 ) ) ;
#3640=CARTESIAN_POINT ( 'NONE',  ( 18.16715644869600155, -3.024463723863999753, -11.49930835314999911 ) ) ;
#3645=AXIS2_PLACEMENT_3D ( 'NONE', #3145, #44779, #24476 ) ;
#3662=CARTESIAN_POINT ( 'NONE',  ( 16.09997386696500143, 8.350085070477001992, 8.123950967096998710 ) ) ;
#3669=CARTESIAN_POINT ( 'NONE',  ( 13.25609597789999938, -11.48890257311000163, -1.688129671228999928 ) ) ;
#3676=CARTESIAN_POINT ( 'NONE',  ( 15.95266668291200141, 3.685671355860000276, 11.20570641515999988 ) ) ;
#3680=CARTESIAN_POINT ( 'NONE',  ( 23.58602290021012493, 10.21078611479860854, 9.552280232028873996 ) ) ;
#3681=ADVANCED_FACE ( 'NONE', ( #9152 ), #55156, .F. ) ;
#3684=CARTESIAN_POINT ( 'NONE',  ( 18.29995268966800026, -2.861739928647000220, -11.98821236628000086 ) ) ;
#3697=CARTESIAN_POINT ( 'NONE',  ( 24.01908949132420545, 12.68161222272001609, -3.458556830167235585 ) ) ;
#3707=EDGE_CURVE ( 'NONE', #65107, #43577, #17735, .T. ) ;
#3708=AXIS2_PLACEMENT_3D ( 'NONE', #39749, #7581, #28930 ) ;
#3713=LINE ( 'NONE', #67343, #35066 ) ;
#3716=ORIENTED_EDGE ( 'NONE', *, *, #29201, .F. ) ;
#3719=CARTESIAN_POINT ( 'NONE',  ( 16.04495723965300158, 8.927588545536998765, 8.707532029612000457 ) ) ;
#3725=CARTESIAN_POINT ( 'NONE',  ( 24.63781072324900023, -11.77741428486000075, 3.228729438162000420 ) ) ;
#3727=B_SPLINE_CURVE_WITH_KNOTS ( 'NONE', 3,
 ( #56755, #9876, #3933, #15475 ),
 .UNSPECIFIED., .F., .F.,
 ( 4, 4 ),
 ( 0.000000000000000000, 1.000000000000000000 ),
 .UNSPECIFIED. ) ;
#3730=DIRECTION ( 'NONE',  ( 0.000000000000000000, 0.7071067811865475727, 0.7071067811865475727 ) ) ;
#3733=CARTESIAN_POINT ( 'NONE',  ( 23.73689480596400259, 9.842602752810000410, 9.652213948273999478 ) ) ;
#3734=ORIENTED_EDGE ( 'NONE', *, *, #1611, .T. ) ;
#3745=CARTESIAN_POINT ( 'NONE',  ( 11.79999999550100220, 3.351258778187000242, -11.15757272551999968 ) ) ;
#3748=CARTESIAN_POINT ( 'NONE',  ( 15.40000000001299973, 8.815237407733999220, 7.616696375847999967 ) ) ;
#3751=CARTESIAN_POINT ( 'NONE',  ( 11.60578299225600141, -3.447612089971000326, 11.88742905964999963 ) ) ;
#3759=ORIENTED_EDGE ( 'NONE', *, *, #23060, .T. ) ;
#3763=LINE ( 'NONE', #37313, #50964 ) ;
#3772=ORIENTED_EDGE ( 'NONE', *, *, #2221, .F. ) ;
#3776=CARTESIAN_POINT ( 'NONE',  ( 15.89994436294300151, -8.847904542234999781, -8.580301953175000662 ) ) ;
#3782=CARTESIAN_POINT ( 'NONE',  ( 17.61613042390700201, -12.05009377076000021, 3.195812565461000343 ) ) ;
#3783=FACE_OUTER_BOUND ( 'NONE', #40083, .T. ) ;
#3793=CARTESIAN_POINT ( 'NONE',  ( 23.60001133530950668, -1.983597864821140026E-14, -13.89477126879791058 ) ) ;
#3798=CARTESIAN_POINT ( 'NONE',  ( 17.79290994143500271, 3.413161104324000217, -11.89755508104000015 ) ) ;
#3807=CARTESIAN_POINT ( 'NONE',  ( 24.87965768662300192, 8.586235434208999706, 8.375234271308000800 ) ) ;
#3809=CIRCLE ( 'NONE', #30631, 10.75000000000000000 ) ;
#3813=ADVANCED_FACE ( 'NONE', ( #24205 ), #40976, .T. ) ;
#3814=VERTEX_POINT ( 'NONE', #45548 ) ;
#3822=ORIENTED_EDGE ( 'NONE', *, *, #9776, .T. ) ;
#3824=CARTESIAN_POINT ( 'NONE',  ( 12.18965064077888627, 11.77436608085541536, -3.633175706307454345 ) ) ;
#3828=CARTESIAN_POINT ( 'NONE',  ( 15.89979320884932967, 7.372865056442157616, 9.926947018133178702 ) ) ;
#3832=CARTESIAN_POINT ( 'NONE',  ( 24.81129275592842021, -11.68008348722340273, 3.194587719868046349 ) ) ;
#3852=CARTESIAN_POINT ( 'NONE',  ( 24.14474107922869806, -3.678932646489693870, -12.80134524014008690 ) ) ;
#3854=CARTESIAN_POINT ( 'NONE',  ( 24.37847033660100138, -3.167532588666000404, -12.03742754479999988 ) ) ;
#3862=CARTESIAN_POINT ( 'NONE',  ( 23.58888753768338375, 10.33110938381009980, -9.338951014280834073 ) ) ;
#3872=CARTESIAN_POINT ( 'NONE',  ( 18.49993212792200126, 2.908182645667999999, 12.18276646858999968 ) ) ;
#3875=ORIENTED_EDGE ( 'NONE', *, *, #52731, .T. ) ;
#3876=EDGE_CURVE ( 'NONE', #7451, #8271, #61935, .T. ) ;
#3880=CARTESIAN_POINT ( 'NONE',  ( 23.59999468372399889, -2.915558691838999739, 13.58549495651999983 ) ) ;
#3881=EDGE_CURVE ( 'NONE', #48209, #5914, #7697, .T. ) ;
#3885=ORIENTED_EDGE ( 'NONE', *, *, #23279, .T. ) ;
#3906=CARTESIAN_POINT ( 'NONE',  ( 23.57471769411892737, -13.35750757171955527, 4.149007248513409074 ) ) ;
#3908=CARTESIAN_POINT ( 'NONE',  ( 18.30000000000000071, -7.694584455362999620, 1.879999999999999893 ) ) ;
#3909=AXIS2_PLACEMENT_3D ( 'NONE', #14813, #62691, #29884 ) ;
#3916=CARTESIAN_POINT ( 'NONE',  ( 23.61813871572700307, 2.884258943580999990, -13.53885632044999987 ) ) ;
#3929=VECTOR ( 'NONE', #14484, 1000.000000000000227 ) ;
#3933=CARTESIAN_POINT ( 'NONE',  ( 24.34832118755700137, -8.810502277406902394, 8.810502277406998317 ) ) ;
#3938=ORIENTED_EDGE ( 'NONE', *, *, #63566, .F. ) ;
#3939=ADVANCED_FACE ( 'NONE', ( #34546 ), #59289, .T. ) ;
#3946=CARTESIAN_POINT ( 'NONE',  ( 13.86901036581968860, 9.187486520156699754, 8.213234632844541139 ) ) ;
#3951=CARTESIAN_POINT ( 'NONE',  ( 25.29987261392200182, 8.756202924575998026, -7.455126447192999883 ) ) ;
#3952=( BOUNDED_SURFACE ( )  B_SPLINE_SURFACE ( 3, 3, ( 
 ( #65004, #2100, #59089, #709 ),
 ( #28672, #33564, #43710, #1742 ),
 ( #16772, #32871, #17832, #54184 ),
 ( #54883, #17123, #6282, #66056 ) ),
 .UNSPECIFIED., .F., .F., .T. ) 
 B_SPLINE_SURFACE_WITH_KNOTS ( ( 4, 4 ),
 ( 4, 4 ),
 ( 0.000000000000000000, 1.000000000000000000 ),
 ( 0.000000000000000000, 1.000000000000000000 ),
 .UNSPECIFIED. ) 
 GEOMETRIC_REPRESENTATION_ITEM ( )  RATIONAL_B_SPLINE_SURFACE ( (
 ( 1.512182578520000042, 1.160176301760999840, 1.160176301760999840, 1.512182578520000042),
 ( 1.111288591041000196, 0.8526025270081000196, 0.8526025270081000196, 1.111288591041000196),
 ( 1.111288591041000196, 0.8526025270081000196, 0.8526025270081000196, 1.111288591041000196),
 ( 1.512182578520000042, 1.160176301760999840, 1.160176301760999840, 1.512182578520000042) ) ) 
 REPRESENTATION_ITEM ( '' )  SURFACE ( )  );
#3960=CIRCLE ( 'NONE', #63140, 1.000000000000000222 ) ;
#3961=CARTESIAN_POINT ( 'NONE',  ( 12.79999999202000005, 11.41069016990000051, -4.623987642516999230 ) ) ;
#3972=ORIENTED_EDGE ( 'NONE', *, *, #6609, .F. ) ;
#3975=CARTESIAN_POINT ( 'NONE',  ( 21.00000012402669824, 1.558133232118999877E-13, -6.372680161347999694E-14 ) ) ;
#3977=CARTESIAN_POINT ( 'NONE',  ( 25.25776035775700024, 8.562683428954001030, -7.910855114518000164 ) ) ;
#3978=CARTESIAN_POINT ( 'NONE',  ( 23.58549012003300049, 10.19447453086000088, -9.580977173348999898 ) ) ;
#3979=CARTESIAN_POINT ( 'NONE',  ( 11.50001496185000249, 12.52500000000000036, 0.000000000000000000 ) ) ;
#3995=CARTESIAN_POINT ( 'NONE',  ( 13.60249209530700121, 8.943624754334001281, 7.827978252961999672 ) ) ;
#4000=CARTESIAN_POINT ( 'NONE',  ( 18.50003594170800270, 2.686563649653999963, -11.33603604535000109 ) ) ;
#4001=CARTESIAN_POINT ( 'NONE',  ( 18.50003594167399967, -2.686563651857999613, -11.33603604486000016 ) ) ;
#4005=DIRECTION ( 'NONE',  ( 0.000000000000000000, 0.7455306007789014311, 0.6664713972124013397 ) ) ;
#4007=ORIENTED_EDGE ( 'NONE', *, *, #18487, .T. ) ;
#4015=ORIENTED_EDGE ( 'NONE', *, *, #62507, .F. ) ;
#4021=CARTESIAN_POINT ( 'NONE',  ( 16.13959992722299930, 8.325816698831998153, 8.094004264449001340 ) ) ;
#4026=DIRECTION ( 'NONE',  ( -1.000000000000000000, 0.000000000000000000, 0.000000000000000000 ) ) ;
#4042=CARTESIAN_POINT ( 'NONE',  ( 11.50001258332000020, 11.56502147876000031, 1.404302031979000054 ) ) ;
#4046=VERTEX_POINT ( 'NONE', #20085 ) ;
#4056=CARTESIAN_POINT ( 'NONE',  ( 15.89994436294300151, -8.847904542234999781, -8.580301953175000662 ) ) ;
#4063=CARTESIAN_POINT ( 'NONE',  ( 15.95309301929700219, 8.865091978629999758, 8.639514276306002216 ) ) ;
#4064=CARTESIAN_POINT ( 'NONE',  ( 18.29983863915590447, 1.925365965127968426, -12.21183828433472307 ) ) ;
#4066=CARTESIAN_POINT ( 'NONE',  ( 23.56666365135700403, -2.920993777382001166, -11.72568747150000412 ) ) ;
#4071=EDGE_CURVE ( 'NONE', #59692, #48385, #36506, .T. ) ;
#4076=ORIENTED_EDGE ( 'NONE', *, *, #57743, .T. ) ;
#4083=AXIS2_PLACEMENT_3D ( 'NONE', #52972, #46702, #5069 ) ;
#4085=AXIS2_PLACEMENT_3D ( 'NONE', #36814, #15140, #63010 ) ;
#4096=CARTESIAN_POINT ( 'NONE',  ( 11.44731512799000228, -3.899625435828999898, 11.84583327264999930 ) ) ;
#4097=CARTESIAN_POINT ( 'NONE',  ( 15.83979990366733048, 8.664995957719213493, 8.086229679809639137 ) ) ;
#4124=CARTESIAN_POINT ( 'NONE',  ( 18.26122879894100137, -2.828234032943000020, -11.95647652451000020 ) ) ;
#4125=CARTESIAN_POINT ( 'NONE',  ( 23.66004879239100234, -13.39256464007999980, -3.813546745462999876 ) ) ;
#4127=ADVANCED_FACE ( 'NONE', ( #46666 ), #62627, .T. ) ;
#4141=CARTESIAN_POINT ( 'NONE',  ( 18.23043922992600230, 3.518658233831999826, -12.06062508533999988 ) ) ;
#4146=EDGE_LOOP ( 'NONE', ( #22610, #46769, #68896, #11093 ) ) ;
#4158=AXIS2_PLACEMENT_3D ( 'NONE', #8165, #60009, #18995 ) ;
#4160=VERTEX_POINT ( 'NONE', #42103 ) ;
#4165=DIRECTION ( 'NONE',  ( 0.000000000000000000, 1.000000000000000000, 0.000000000000000000 ) ) ;
#4176=ORIENTED_EDGE ( 'NONE', *, *, #2665, .F. ) ;
#4180=CARTESIAN_POINT ( 'NONE',  ( 24.65661251414474009, -11.83370281768760002, 3.192273988792572403 ) ) ;
#4186=CARTESIAN_POINT ( 'NONE',  ( 24.63002439619599926, 0.000000000000000000, 0.000000000000000000 ) ) ;
#4189=FACE_OUTER_BOUND ( 'NONE', #4146, .T. ) ;
#4191=ORIENTED_EDGE ( 'NONE', *, *, #67942, .T. ) ;
#4198=CARTESIAN_POINT ( 'NONE',  ( 24.13557959378723794, -3.329020217945502846, 12.49973103956492082 ) ) ;
#4200=CARTESIAN_POINT ( 'NONE',  ( 24.30000000000000071, 12.03537377768999939, -3.224868684338999980 ) ) ;
#4203=VECTOR ( 'NONE', #68937, 1000.000000000000227 ) ;
#4204=CARTESIAN_POINT ( 'NONE',  ( 24.63626627244600087, -12.49727471743999985, -2.949030056809999856 ) ) ;
#4207=CARTESIAN_POINT ( 'NONE',  ( 15.44552286930127494, -9.471974105402734878, -8.194957690431824204 ) ) ;
#4222=ORIENTED_EDGE ( 'NONE', *, *, #60750, .F. ) ;
#4223=DIRECTION ( 'NONE',  ( 0.000000000000000000, -0.9659258262890756397, 0.2588190451024934280 ) ) ;
#4234=CARTESIAN_POINT ( 'NONE',  ( 24.44916829770000177, 8.894890565782000991, 9.199951775352998240 ) ) ;
#4235=CARTESIAN_POINT ( 'NONE',  ( 24.30000000000000071, 50.50083396221999976, 14.25635100356000073 ) ) ;
#4239=CARTESIAN_POINT ( 'NONE',  ( 24.34832116925733203, -12.03536991270508061, -3.224867648718668267 ) ) ;
#4251=CARTESIAN_POINT ( 'NONE',  ( 18.30000103245939158, -11.66744832144745203, 3.971921730545766138 ) ) ;
#4253=CARTESIAN_POINT ( 'NONE',  ( 11.30000000000000071, -12.07633875558669345, -1.479860865542806714 ) ) ;
#4261=CIRCLE ( 'NONE', #48889, 12.52500000000000036 ) ;
#4262=CARTESIAN_POINT ( 'NONE',  ( 11.36663360327350070, 3.844887449686455572, -11.78015558627826920 ) ) ;
#4265=CARTESIAN_POINT ( 'NONE',  ( 23.64080852780499953, 3.067619660802999970, -13.45636821867999977 ) ) ;
#4282=CARTESIAN_POINT ( 'NONE',  ( 13.64750315638899991, -9.067203425066999500, -7.400836607049000371 ) ) ;
#4287=ORIENTED_EDGE ( 'NONE', *, *, #55091, .F. ) ;
#4290=ORIENTED_EDGE ( 'NONE', *, *, #48322, .T. ) ;
#4294=VECTOR ( 'NONE', #38728, 1000.000000000000000 ) ;
#4299=CARTESIAN_POINT ( 'NONE',  ( 21.70000133425200062, 0.000000000000000000, 0.000000000000000000 ) ) ;
#4306=ORIENTED_EDGE ( 'NONE', *, *, #2748, .F. ) ;
#4312=ORIENTED_EDGE ( 'NONE', *, *, #36299, .F. ) ;
#4319=CARTESIAN_POINT ( 'NONE',  ( 17.75917414208900169, 3.376094807733999836, 11.11072694497999969 ) ) ;
#4322=VERTEX_POINT ( 'NONE', #5029 ) ;
#4326=CARTESIAN_POINT ( 'NONE',  ( 23.81723299462928622, 3.309383924426469559, 13.09646026573576272 ) ) ;
#4334=ORIENTED_EDGE ( 'NONE', *, *, #47404, .T. ) ;
#4336=B_SPLINE_CURVE_WITH_KNOTS ( 'NONE', 3,
 ( #5777, #1234, #6468, #11366, #48436, #17664, #1575, #32704, #32029, #12067, #22893, #891, #49120, #22204, #64841, #545, #53342, #16272, #44244, #26781, #65190, #37597, #17309, #58930, #11032, #21858 ),
 .UNSPECIFIED., .F., .F.,
 ( 4, 2, 2, 2, 2, 2, 2, 2, 2, 2, 2, 2, 4 ),
 ( 0.000000000000000000, 0.06250000000000215106, 0.09375000000000133227, 0.1250000000000005274, 0.2500000000000011102, 0.3750000000000016653, 0.5000000000000022204, 0.6250000000000028866, 0.7500000000000033307, 0.8125000000000039968, 0.8437500000000027756, 0.8750000000000014433, 1.000000000000000000 ),
 .UNSPECIFIED. ) ;
#4344=DIRECTION ( 'NONE',  ( 0.000000000000000000, 1.000000000000000000, 0.000000000000000000 ) ) ;
#4351=ORIENTED_EDGE ( 'NONE', *, *, #17205, .F. ) ;
#4361=CARTESIAN_POINT ( 'NONE',  ( 13.73712493497300180, -11.35980872612999804, -2.405726353896999736 ) ) ;
#4362=DIRECTION ( 'NONE',  ( -0.000000000000000000, 0.9624505444715651947, 0.2714570858282905341 ) ) ;
#4364=ORIENTED_EDGE ( 'NONE', *, *, #51382, .F. ) ;
#4369=DIRECTION ( 'NONE',  ( 1.000000000000000000, 0.000000000000000000, 0.000000000000000000 ) ) ;
#4371=CARTESIAN_POINT ( 'NONE',  ( 23.61227780979461954, 10.11764914276287541, 9.630145176663825524 ) ) ;
#4375=FACE_OUTER_BOUND ( 'NONE', #16806, .T. ) ;
#4379=CARTESIAN_POINT ( 'NONE',  ( 12.62563329236251519, 11.41733447966572434, -4.609296053777672597 ) ) ;
#4385=CARTESIAN_POINT ( 'NONE',  ( 23.57382309776751583, -10.27665349734288291, 9.488812925140930332 ) ) ;
#4386=CARTESIAN_POINT ( 'NONE',  ( 24.17201630339561902, 12.42869476374950821, -3.341605307461719576 ) ) ;
#4388=DIRECTION ( 'NONE',  ( 0.000000000000000000, -0.9999606858717338120, 0.008867170401640298016 ) ) ;
#4391=CARTESIAN_POINT ( 'NONE',  ( 11.53159663546301417, 3.486713160384601107, -11.11613240504657796 ) ) ;
#4395=ORIENTED_EDGE ( 'NONE', *, *, #15057, .T. ) ;
#4406=CARTESIAN_POINT ( 'NONE',  ( 24.30000000000000071, 8.810505093353000916, -8.810505093353000916 ) ) ;
#4409=PLANE ( 'NONE',  #33782 ) ;
#4416=EDGE_CURVE ( 'NONE', #12823, #40899, #65123, .T. ) ;
#4417=CARTESIAN_POINT ( 'NONE',  ( 14.93333333127366735, -8.815235367372471487, -7.616700428521845367 ) ) ;
#4421=DIRECTION ( 'NONE',  ( 0.000000000000000000, 0.6482718649732923666, -0.7614089499631913061 ) ) ;
#4426=LINE ( 'NONE', #19140, #27824 ) ;
#4436=CARTESIAN_POINT ( 'NONE',  ( 24.57937622057101379, 8.815984698512634665, -9.246564900184520042 ) ) ;
#4438=ORIENTED_EDGE ( 'NONE', *, *, #8103, .F. ) ;
#4448=CARTESIAN_POINT ( 'NONE',  ( 16.39999999308669842, -3.302282894619416265, -11.70823727156336425 ) ) ;
#4458=CIRCLE ( 'NONE', #17911, 0.6999999999999992895 ) ;
#4466=EDGE_CURVE ( 'NONE', #36754, #29376, #5078, .T. ) ;
#4467=CARTESIAN_POINT ( 'NONE',  ( 23.63971702668698072, -13.40694874527435410, -3.855832365366145265 ) ) ;
#4474=ORIENTED_EDGE ( 'NONE', *, *, #29547, .F. ) ;
#4482=CARTESIAN_POINT ( 'NONE',  ( 24.57010863793600208, -12.57173122536999976, 2.966538848022999719 ) ) ;
#4484=B_SPLINE_CURVE_WITH_KNOTS ( 'NONE', 3,
 ( #60677, #22231, #49147, #60335, #12441, #19749 ),
 .UNSPECIFIED., .F., .F.,
 ( 4, 2, 4 ),
 ( 0.000000000000000000, 0.5000000000000000000, 1.000000000000000000 ),
 .UNSPECIFIED. ) ;
#4495=CIRCLE ( 'NONE', #68128, 11.50000000000000533 ) ;
#4516=CARTESIAN_POINT ( 'NONE',  ( 17.79999999998900151, 3.595165934733000057, -11.99793354950999991 ) ) ;
#4530=CARTESIAN_POINT ( 'NONE',  ( 24.22025250524800200, 3.188360109827999889, 12.21446149360000000 ) ) ;
#4538=CARTESIAN_POINT ( 'NONE',  ( 24.30001680216799897, -3.271769318036999774, 12.21048166890999909 ) ) ;
#4541=B_SPLINE_CURVE_WITH_KNOTS ( 'NONE', 3,
 ( #4001, #25338, #32915, #6326, #26031, #33613, #47706, #17529, #1445, #59472, #21129, #33958, #49683, #17168 ),
 .UNSPECIFIED., .F., .F.,
 ( 4, 2, 2, 2, 2, 2, 4 ),
 ( 0.000000000000000000, 0.1249999999999998890, 0.2499999999999997780, 0.4999999999999995559, 0.6249999999999994449, 0.7499999999999993339, 1.000000000000000000 ),
 .UNSPECIFIED. ) ;
#4542=CARTESIAN_POINT ( 'NONE',  ( 24.34833250136633609, -8.895958538877664523, 8.895958538877664523 ) ) ;
#4558=B_SPLINE_CURVE_WITH_KNOTS ( 'NONE', 3,
 ( #26656, #37820, #20713, #36798 ),
 .UNSPECIFIED., .F., .F.,
 ( 4, 4 ),
 ( 0.000000000000000000, 1.000000000000000000 ),
 .UNSPECIFIED. ) ;
#4563=EDGE_CURVE ( 'NONE', #15006, #27711, #23564, .T. ) ;
#4566=CARTESIAN_POINT ( 'NONE',  ( 24.71426445414105544, -3.125270931515957695, 11.79471460629179624 ) ) ;
#4578=ADVANCED_FACE ( 'NONE', ( #46239 ), #11782, .F. ) ;
#4593=CARTESIAN_POINT ( 'NONE',  ( 15.46873602477000276, -8.828190495471000432, -7.821444125541998638 ) ) ;
#4599=CARTESIAN_POINT ( 'NONE',  ( 24.30000000000000071, 9.517611874540000017, -8.103398312166000039 ) ) ;
#4608=CARTESIAN_POINT ( 'NONE',  ( 24.30001683570900184, 3.271769286791000209, 12.21048169671000139 ) ) ;
#4615=DIRECTION ( 'NONE',  ( -1.000000000000000000, 0.000000000000000000, 0.000000000000000000 ) ) ;
#4621=CARTESIAN_POINT ( 'NONE',  ( 23.85399064179406281, 3.593187972531236341, -13.20264717798629306 ) ) ;
#4625=CARTESIAN_POINT ( 'NONE',  ( 25.59997239626699894, -8.218962899087999929, 8.043524294852000267 ) ) ;
#4626=VERTEX_POINT ( 'NONE', #32450 ) ;
#4630=CARTESIAN_POINT ( 'NONE',  ( 18.40015514469800095, -2.331468351713000075E-14, -1.065814103639999827E-13 ) ) ;
#4632=ORIENTED_EDGE ( 'NONE', *, *, #15141, .F. ) ;
#4641=CARTESIAN_POINT ( 'NONE',  ( 13.91137892731300063, 9.265832517555999459, 8.206449300197000696 ) ) ;
#4650=TOROIDAL_SURFACE ( 'NONE', #22519, 8.250000000000000000, 1.000000000000000000 ) ;
#4654=CARTESIAN_POINT ( 'NONE',  ( 12.79413755118400253, 11.93226572510000061, -3.260039893805000144 ) ) ;
#4655=CARTESIAN_POINT ( 'NONE',  ( 17.70600070946500182, 11.93155574656999995, -3.263109129670000108 ) ) ;
#4660=CARTESIAN_POINT ( 'NONE',  ( 17.95534550153200115, -3.277905616156999713, 11.84067279748999901 ) ) ;
#4681=CARTESIAN_POINT ( 'NONE',  ( 15.86018463513499910, -3.716003765078999876, -11.29289727949000088 ) ) ;
#4693=CARTESIAN_POINT ( 'NONE',  ( 23.60000000000000142, 11.77655473258999841, 4.190794510628000680 ) ) ;
#4700=CARTESIAN_POINT ( 'NONE',  ( 12.99421883851900184, -11.64667883987999986, -1.861676925984000031 ) ) ;
#4706=ORIENTED_EDGE ( 'NONE', *, *, #66046, .F. ) ;
#4710=CARTESIAN_POINT ( 'NONE',  ( 16.00429364930199938, 8.559608311085998622, 7.983357056237001537 ) ) ;
#4712=CARTESIAN_POINT ( 'NONE',  ( 23.66004879239100234, 9.998911746292000302, 9.691526727427998367 ) ) ;
#4714=DIRECTION ( 'NONE',  ( 0.000000000000000000, 0.000000000000000000, 1.000000000000000000 ) ) ;
#4716=VERTEX_POINT ( 'NONE', #41764 ) ;
#4719=EDGE_CURVE ( 'NONE', #28231, #64377, #34325, .T. ) ;
#4720=CARTESIAN_POINT ( 'NONE',  ( 25.37646601934299895, 11.10818569620999874, -3.395594564468000343 ) ) ;
#4722=CARTESIAN_POINT ( 'NONE',  ( 12.45594992591494155, 11.44468663792899754, -4.547234112432383846 ) ) ;
#4731=LINE ( 'NONE', #57887, #28798 ) ;
#4744=CARTESIAN_POINT ( 'NONE',  ( 25.60000000000000142, -10.55163788719000095, -3.754896668835000284 ) ) ;
#4750=CARTESIAN_POINT ( 'NONE',  ( 12.68949153424100196, -11.39033517652999983, 4.571431300619999583 ) ) ;
#4752=FACE_OUTER_BOUND ( 'NONE', #4871, .T. ) ;
#4753=CARTESIAN_POINT ( 'NONE',  ( 15.77677363193000204, 9.321312496448001639, 8.284802892401000207 ) ) ;
#4759=CARTESIAN_POINT ( 'NONE',  ( 21.00000000000000000, -11.79499999999999993, 0.000000000000000000 ) ) ;
#4764=ORIENTED_EDGE ( 'NONE', *, *, #13690, .T. ) ;
#4771=CARTESIAN_POINT ( 'NONE',  ( 18.04816728597000264, 3.610133590554000182, 12.03375048192000207 ) ) ;
#4775=EDGE_LOOP ( 'NONE', ( #973, #997, #21904, #47816 ) ) ;
#4776=ADVANCED_FACE ( 'NONE', ( #10631 ), #14853, .F. ) ;
#4783=CARTESIAN_POINT ( 'NONE',  ( 11.53681523859000002, -3.897571790034000117, 11.94316735528000173 ) ) ;
#4790=CARTESIAN_POINT ( 'NONE',  ( 11.53937873044000106, 11.52961813267000046, 1.376592384073999975 ) ) ;
#4793=CARTESIAN_POINT ( 'NONE',  ( 20.75138802851920161, 5.760713961201000544, 0.000000000000000000 ) ) ;
#4808=EDGE_CURVE ( 'NONE', #8116, #2756, #12270, .T. ) ;
#4815=CARTESIAN_POINT ( 'NONE',  ( 24.35365242081699932, -8.948887819865001703, 8.923422014301001681 ) ) ;
#4816=DIRECTION ( 'NONE',  ( 0.000000000000000000, 0.000000000000000000, -1.000000000000000000 ) ) ;
#4827=EDGE_CURVE ( 'NONE', #52918, #8614, #63138, .T. ) ;
#4828=DIRECTION ( 'NONE',  ( -0.7070974425254246132, 0.000000000000000000, -0.7071161197243376328 ) ) ;
#4830=CARTESIAN_POINT ( 'NONE',  ( 23.83547933438500266, -13.04069008200000113, 3.622007013137000353 ) ) ;
#4831=CARTESIAN_POINT ( 'NONE',  ( 16.39999999485600313, 3.595156957901000094, 11.99794989424000136 ) ) ;
#4848=ORIENTED_EDGE ( 'NONE', *, *, #55092, .T. ) ;
#4858=PLANE ( 'NONE',  #51220 ) ;
#4861=CARTESIAN_POINT ( 'NONE',  ( 13.94794651623100101, -9.527030574842997979, -8.190375113092999371 ) ) ;
#4862=DIRECTION ( 'NONE',  ( -1.000000000000000000, 0.000000000000000000, 0.000000000000000000 ) ) ;
#4864=ORIENTED_EDGE ( 'NONE', *, *, #48779, .T. ) ;
#4869=CARTESIAN_POINT ( 'NONE',  ( 24.87155164401192664, -11.61820474743187681, 3.203191883057006084 ) ) ;
#4871=EDGE_LOOP ( 'NONE', ( #24194, #30693, #7713, #10149, #45409, #9140 ) ) ;
#4876=DIRECTION ( 'NONE',  ( 0.000000000000000000, 0.9659258262890756397, -0.2588190451024934280 ) ) ;
#4882=CARTESIAN_POINT ( 'NONE',  ( 11.72001955157836406, 12.39031618367868148, 1.831854259322070133 ) ) ;
#4884=ORIENTED_EDGE ( 'NONE', *, *, #19257, .F. ) ;
#4886=CARTESIAN_POINT ( 'NONE',  ( 23.76527432394305706, -3.280151047146071974, 13.20034468938107608 ) ) ;
#4890=CARTESIAN_POINT ( 'NONE',  ( 24.30001697071400457, -8.938702858184001343, 8.938676113071998941 ) ) ;
#4895=ORIENTED_EDGE ( 'NONE', *, *, #26187, .T. ) ;
#4897=CARTESIAN_POINT ( 'NONE',  ( 13.12628980020838654, -12.15998242465562029, -2.000325904698448287 ) ) ;
#4912=CARTESIAN_POINT ( 'NONE',  ( 24.81123736889670184, -3.073480331628497542, 11.71258898044826324 ) ) ;
#4916=EDGE_CURVE ( 'NONE', #52535, #31379, #56470, .T. ) ;
#4919=CARTESIAN_POINT ( 'NONE',  ( 11.29998578400000042, -3.824193979571000046, 11.71675423233000046 ) ) ;
#4923=CARTESIAN_POINT ( 'NONE',  ( 21.72233714749290101, 0.000000000000000000, 0.000000000000000000 ) ) ;
#4935=DIRECTION ( 'NONE',  ( 1.000000000000000000, 0.000000000000000000, 0.000000000000000000 ) ) ;
#4937=CARTESIAN_POINT ( 'NONE',  ( 12.68583900965842481, 11.53041019655173294, -4.891346001956314637 ) ) ;
#4945=ORIENTED_EDGE ( 'NONE', *, *, #21994, .T. ) ;
#4953=DIRECTION ( 'NONE',  ( 0.000000000000000000, -0.9979497300302145879, 0.06400262754467088422 ) ) ;
#4956=CARTESIAN_POINT ( 'NONE',  ( 23.74236379950000142, 3.207225084832999951, -13.21247651630999975 ) ) ;
#4959=ADVANCED_FACE ( 'NONE', ( #32654 ), #9482, .F. ) ;
#4963=CARTESIAN_POINT ( 'NONE',  ( 24.67921311619700120, 3.567517360056999820, 12.13750603036999998 ) ) ;
#4973=CARTESIAN_POINT ( 'NONE',  ( 11.50001544675000353, -5.131800296024274566, 11.50030236634318115 ) ) ;
#4976=CARTESIAN_POINT ( 'NONE',  ( 23.55780499550100160, 13.49844004384999963, -4.021617545008000505 ) ) ;
#4986=CARTESIAN_POINT ( 'NONE',  ( 17.88015371777900242, -3.314513509857999640, 11.22393657228000130 ) ) ;
#4990=CARTESIAN_POINT ( 'NONE',  ( 12.09999922233642344, 11.66744139996707119, -3.971920075670921424 ) ) ;
#4996=EDGE_LOOP ( 'NONE', ( #6712, #64741 ) ) ;
#4999=EDGE_CURVE ( 'NONE', #17060, #5259, #51834, .T. ) ;
#5004=DIRECTION ( 'NONE',  ( 1.000000000000000000, 0.000000000000000000, 0.000000000000000000 ) ) ;
#5005=ORIENTED_EDGE ( 'NONE', *, *, #67862, .T. ) ;
#5006=CARTESIAN_POINT ( 'NONE',  ( 12.83176788310500172, 11.93188535256000016, -3.261584788209999974 ) ) ;
#5007=CARTESIAN_POINT ( 'NONE',  ( 17.93554207161599834, 11.52135921566999954, -4.763665720747999544 ) ) ;
#5010=CARTESIAN_POINT ( 'NONE',  ( 12.71442162208122539, -11.86191914805648118, 3.298674357357659126 ) ) ;
#5012=CARTESIAN_POINT ( 'NONE',  ( 18.14341877109137968, 11.59808500082729843, -4.729434285192278153 ) ) ;
#5014=VERTEX_POINT ( 'NONE', #7809 ) ;
#5015=ORIENTED_EDGE ( 'NONE', *, *, #11738, .F. ) ;
#5018=CARTESIAN_POINT ( 'NONE',  ( 18.90826270587400160, 11.15000000000000036, 4.842816425653999965E-11 ) ) ;
#5029=CARTESIAN_POINT ( 'NONE',  ( 25.29995422340600086, 2.596935224161999844, 11.35301931920000129 ) ) ;
#5035=CARTESIAN_POINT ( 'NONE',  ( 15.40000000005200143, -9.187454762873001002, -8.213177997099000649 ) ) ;
#5043=ORIENTED_EDGE ( 'NONE', *, *, #44330, .F. ) ;
#5055=CARTESIAN_POINT ( 'NONE',  ( 18.90826270587400160, 0.000000000000000000, 0.000000000000000000 ) ) ;
#5058=ORIENTED_EDGE ( 'NONE', *, *, #51471, .T. ) ;
#5066=ORIENTED_EDGE ( 'NONE', *, *, #57541, .F. ) ;
#5067=CARTESIAN_POINT ( 'NONE',  ( 23.58987130287489364, 10.19425842954025008, 9.567338712638951748 ) ) ;
#5069=DIRECTION ( 'NONE',  ( 0.000000000000000000, 0.2098314828218890149, -0.9777375664342490280 ) ) ;
#5071=EDGE_LOOP ( 'NONE', ( #57404, #46277, #23931, #54854 ) ) ;
#5076=ORIENTED_EDGE ( 'NONE', *, *, #37399, .F. ) ;
#5078=B_SPLINE_CURVE_WITH_KNOTS ( 'NONE', 3,
 ( #53957, #6060, #45559, #44532 ),
 .UNSPECIFIED., .F., .F.,
 ( 4, 4 ),
 ( 0.000000000000000000, 1.000000000000000000 ),
 .UNSPECIFIED. ) ;
#5079=ORIENTED_EDGE ( 'NONE', *, *, #46740, .F. ) ;
#5084=B_SPLINE_CURVE_WITH_KNOTS ( 'NONE', 3,
 ( #32160, #53812, #26911, #37054, #31812, #52785 ),
 .UNSPECIFIED., .F., .F.,
 ( 4, 2, 4 ),
 ( 0.000000000000000000, 0.5000000000000000000, 1.000000000000000000 ),
 .UNSPECIFIED. ) ;
#5085=CYLINDRICAL_SURFACE ( 'NONE', #16290, 1.000000000000000666 ) ;
#5086=CARTESIAN_POINT ( 'NONE',  ( 24.01967379662025692, 12.68055978488803781, 3.458368538996728248 ) ) ;
#5093=MECHANICAL_DESIGN_GEOMETRIC_PRESENTATION_REPRESENTATION('',(#8453),#656);
#5099=AXIS2_PLACEMENT_3D ( 'NONE', #57391, #58093, #68565 ) ;
#5101=ORIENTED_EDGE ( 'NONE', *, *, #37255, .T. ) ;
#5104=DIRECTION ( 'NONE',  ( 0.000000000000000000, -0.9999606858717338120, 0.008867170401640298016 ) ) ;
#5108=CARTESIAN_POINT ( 'NONE',  ( 12.10004069261316495, -11.60802777289428533, 4.146429405019953940 ) ) ;
#5115=CARTESIAN_POINT ( 'NONE',  ( 12.80000000000000071, 10.78295181803999903, -4.410266442048000002 ) ) ;
#5120=ADVANCED_FACE ( 'NONE', ( #8842 ), #46256, .T. ) ;
#5123=VERTEX_POINT ( 'NONE', #29503 ) ;
#5124=CARTESIAN_POINT ( 'NONE',  ( 18.06944243593800081, 3.222040310929999762, 11.85748006108999952 ) ) ;
#5129=CARTESIAN_POINT ( 'NONE',  ( 25.26997868831114147, -8.359964803326231930, 8.486741637760111701 ) ) ;
#5131=CARTESIAN_POINT ( 'NONE',  ( 15.90018573812399971, -8.493548356068000516, -8.263529029821000904 ) ) ;
#5132=CARTESIAN_POINT ( 'NONE',  ( 13.99999999379500082, -8.815218614167999789, -7.616697584347000394 ) ) ;
#5141=CARTESIAN_POINT ( 'NONE',  ( 11.80738107398800274, 11.64644714240999868, 1.863397721619000080 ) ) ;
#5142=ORIENTED_EDGE ( 'NONE', *, *, #25704, .T. ) ;
#5145=CARTESIAN_POINT ( 'NONE',  ( 24.65660926167039690, -8.681443375485125458, -8.652152413449039514 ) ) ;
#5159=B_SPLINE_CURVE_WITH_KNOTS ( 'NONE', 3,
 ( #43061, #1453, #5992, #16147, #59830, #33275 ),
 .UNSPECIFIED., .F., .F.,
 ( 4, 2, 4 ),
 ( 0.000000000000000000, 0.5000000000000000000, 1.000000000000000000 ),
 .UNSPECIFIED. ) ;
#5166=CARTESIAN_POINT ( 'NONE',  ( 17.80000000001300009, 3.351264566333000072, 11.15757590352999884 ) ) ;
#5171=CARTESIAN_POINT ( 'NONE',  ( 13.69997185827399733, -10.91304490500501423, -4.183762365652779813 ) ) ;
#5174=VERTEX_POINT ( 'NONE', #29846 ) ;
#5185=ORIENTED_EDGE ( 'NONE', *, *, #52574, .T. ) ;
#5197=ORIENTED_EDGE ( 'NONE', *, *, #55257, .F. ) ;
#5204=CARTESIAN_POINT ( 'NONE',  ( 24.56046482271400322, 8.848342285916999117, -9.332993724188000328 ) ) ;
#5210=CARTESIAN_POINT ( 'NONE',  ( 13.70005190196300227, 9.005348107749998832, 7.391036106496999381 ) ) ;
#5230=DIRECTION ( 'NONE',  ( 0.000000000000000000, 0.5000000000000168754, 0.8660254037844288266 ) ) ;
#5236=B_SPLINE_CURVE_WITH_KNOTS ( 'NONE', 3,
 ( #48986, #22059, #7025, #43407 ),
 .UNSPECIFIED., .F., .F.,
 ( 4, 4 ),
 ( 0.000000000000000000, 1.000000000000000000 ),
 .UNSPECIFIED. ) ;
#5240=CARTESIAN_POINT ( 'NONE',  ( 24.44496350777200178, -12.03536639536000052, -3.224849854974999985 ) ) ;
#5242=CARTESIAN_POINT ( 'NONE',  ( 24.44496264144000364, 8.810483598181999554, -8.810508341310001157 ) ) ;
#5243=ORIENTED_EDGE ( 'NONE', *, *, #10951, .T. ) ;
#5244=CARTESIAN_POINT ( 'NONE',  ( 12.79999998712400178, -11.53033693765999779, 4.891431908114999949 ) ) ;
#5251=DIRECTION ( 'NONE',  ( -1.951617227613594778E-27, 1.000000000000000000, -3.745441456982000038E-14 ) ) ;
#5259=VERTEX_POINT ( 'NONE', #13750 ) ;
#5283=CARTESIAN_POINT ( 'NONE',  ( 12.79999999914999975, 12.11987927271999865, -3.159802730921999814 ) ) ;
#5287=CARTESIAN_POINT ( 'NONE',  ( 15.39421883851900219, -8.828753284254000633, -7.820747050108999510 ) ) ;
#5291=AXIS2_PLACEMENT_3D ( 'NONE', #29843, #35755, #40646 ) ;
#5299=DIRECTION ( 'NONE',  ( -0.9999999999848602217, 4.443944958194825790E-06, -3.245118987008870144E-06 ) ) ;
#5308=DIRECTION ( 'NONE',  ( 0.9999999999995219380, 9.778750636281211500E-07, -5.518305718317118909E-11 ) ) ;
#5310=CIRCLE ( 'NONE', #45515, 0.6999999999999992895 ) ;
#5315=CARTESIAN_POINT ( 'NONE',  ( 24.30001694670299983, 8.938702829764999080, 8.938676122491999720 ) ) ;
#5316=CARTESIAN_POINT ( 'NONE',  ( 24.00946830465457538, 9.351498316855998638, -9.262241387363053136 ) ) ;
#5322=ORIENTED_EDGE ( 'NONE', *, *, #50357, .T. ) ;
#5325=ORIENTED_EDGE ( 'NONE', *, *, #3881, .T. ) ;
#5328=CARTESIAN_POINT ( 'NONE',  ( 18.26001707275200303, -2.811958703674000137, 11.55267125806999928 ) ) ;
#5329=CARTESIAN_POINT ( 'NONE',  ( 15.39999999998900293, -9.471998555523999386, -8.194929586088999685 ) ) ;
#5340=B_SPLINE_CURVE_WITH_KNOTS ( 'NONE', 3,
 ( #63817, #59265, #32032, #11034, #43543, #31335 ),
 .UNSPECIFIED., .F., .F.,
 ( 4, 1, 1, 4 ),
 ( 0.000000000000000000, 0.2305484662529838635, 0.8346924768898069669, 1.000000000000000000 ),
 .UNSPECIFIED. ) ;
#5351=ORIENTED_EDGE ( 'NONE', *, *, #32542, .F. ) ;
#5352=CARTESIAN_POINT ( 'NONE',  ( 12.11132301796900101, 11.62873132690000055, -4.501748577889000735 ) ) ;
#5353=CARTESIAN_POINT ( 'NONE',  ( 17.56428496274500262, 11.49803451072999927, -4.818043541624000170 ) ) ;
#5358=CARTESIAN_POINT ( 'NONE',  ( 17.79408754209099897, -3.298114924730999764, 11.83441383768999877 ) ) ;
#5360=B_SPLINE_CURVE_WITH_KNOTS ( 'NONE', 3,
 ( #28210, #16328, #10739, #58988, #602, #64557 ),
 .UNSPECIFIED., .F., .F.,
 ( 4, 2, 4 ),
 ( 0.000000000000000000, 0.5000000000000000000, 1.000000000000000000 ),
 .UNSPECIFIED. ) ;
#5368=DIRECTION ( 'NONE',  ( 0.000000000000000000, 0.7146936510990797853, 0.6994376205771799526 ) ) ;
#5382=CARTESIAN_POINT ( 'NONE',  ( 16.04649313145500145, -3.595593625533999749, -11.13765277391999931 ) ) ;
#5383=CARTESIAN_POINT ( 'NONE',  ( 12.95870478550200211, -12.43384127863000010, -1.801469962976000039 ) ) ;
#5394=CYLINDRICAL_SURFACE ( 'NONE', #23070, 14.00000000000000000 ) ;
#5404=CARTESIAN_POINT ( 'NONE',  ( 11.49999672495000169, -11.64999999999999858, 1.217117305822866591 ) ) ;
#5407=EDGE_LOOP ( 'NONE', ( #4632, #53145, #11568, #53828, #57100, #64828 ) ) ;
#5416=CARTESIAN_POINT ( 'NONE',  ( 23.59999172237900211, -2.915589696762999949, -13.58550518520000061 ) ) ;
#5420=ORIENTED_EDGE ( 'NONE', *, *, #26187, .F. ) ;
#5422=CARTESIAN_POINT ( 'NONE',  ( 25.58980493882700458, 11.09071452174999806, -3.239363653489999884 ) ) ;
#5426=CARTESIAN_POINT ( 'NONE',  ( 11.30000000000000071, -3.781170318299324595, 11.56421629219343394 ) ) ;
#5435=CARTESIAN_POINT ( 'NONE',  ( 23.85847163005615812, 12.93463607130301618, 3.627669834457176279 ) ) ;
#5440=CARTESIAN_POINT ( 'NONE',  ( 13.55676532395741063, -12.34669046015853766, -2.106274408588768132 ) ) ;
#5444=CARTESIAN_POINT ( 'NONE',  ( 13.12628980020843450, 12.15998242465557233, 2.000325904699570057 ) ) ;
#5450=CARTESIAN_POINT ( 'NONE',  ( 13.70003001321900449, -10.31266399190331384, -7.179884396236143829 ) ) ;
#5459=FACE_OUTER_BOUND ( 'NONE', #36713, .T. ) ;
#5466=CARTESIAN_POINT ( 'NONE',  ( 24.57010313871199969, 8.854968118029999502, 9.404173716609999900 ) ) ;
#5470=CARTESIAN_POINT ( 'NONE',  ( 24.63329087101742942, 8.756202933458791193, -7.455126436760659558 ) ) ;
#5472=EDGE_LOOP ( 'NONE', ( #45140, #11863, #11674, #4351 ) ) ;
#5473=B_SPLINE_CURVE_WITH_KNOTS ( 'NONE', 3,
 ( #37161, #21082, #32950, #789 ),
 .UNSPECIFIED., .F., .F.,
 ( 4, 4 ),
 ( 0.000000000000000000, 1.000000000000000000 ),
 .UNSPECIFIED. ) ;
#5475=CARTESIAN_POINT ( 'NONE',  ( 27.09999999999999787, 0.000000000000000000, -9.250000000000000000 ) ) ;
#5481=EDGE_CURVE ( 'NONE', #29214, #15051, #32336, .T. ) ;
#5493=CARTESIAN_POINT ( 'NONE',  ( 24.95274028248806886, 2.977348869105516105, -11.59849451147599808 ) ) ;
#5494=CARTESIAN_POINT ( 'NONE',  ( 24.71427135204747216, -8.651883463778640149, -8.603915179283948333 ) ) ;
#5500=CARTESIAN_POINT ( 'NONE',  ( 11.79999999471800010, 3.216299622513999701, -11.40340969442000052 ) ) ;
#5506=CARTESIAN_POINT ( 'NONE',  ( 15.66944243593800046, -9.081775842407999733, -8.276637282895999093 ) ) ;
#5508=ORIENTED_EDGE ( 'NONE', *, *, #40499, .T. ) ;
#5511=CARTESIAN_POINT ( 'NONE',  ( 23.89320776801300283, -8.313844348326997036, 8.526065359053994541 ) ) ;
#5512=DIRECTION ( 'NONE',  ( 0.000000000000000000, 0.9999606858717338120, -0.008867170401640424651 ) ) ;
#5517=ADVANCED_FACE ( 'NONE', ( #21476 ), #63778, .F. ) ;
#5520=ORIENTED_EDGE ( 'NONE', *, *, #57561, .F. ) ;
#5527=CARTESIAN_POINT ( 'NONE',  ( 23.58475003573600048, -13.39488253062000211, 4.040730013063999593 ) ) ;
#5533=EDGE_CURVE ( 'NONE', #60622, #60101, #35090, .T. ) ;
#5535=CARTESIAN_POINT ( 'NONE',  ( 17.85726930274100255, 3.190143309604999811, -11.45065656613999927 ) ) ;
#5543=FACE_OUTER_BOUND ( 'NONE', #36453, .T. ) ;
#5548=B_SPLINE_CURVE_WITH_KNOTS ( 'NONE', 3,
 ( #60115, #54868, #48589, #28298, #22697, #1044, #692, #6968, #43352, #21324, #63963, #64652, #38086, #43694, #17105, #6622, #16075, #27961, #37406, #58728, #18506, #28655, #61492, #56248, #12566, #40504, #24087, #8354, #2416, #61829, #56591, #33896 ),
 .UNSPECIFIED., .F., .F.,
 ( 4, 2, 2, 2, 2, 2, 2, 2, 1, 2, 2, 2, 1, 1, 1, 2, 2, 4 ),
 ( 0.000000000000000000, 0.2500000000000310862, 0.3750000000000450751, 0.4375000000000534017, 0.4687500000000560663, 0.5000000000000587308, 0.6250000000000562883, 0.6875000000000531797, 0.7187500000000527356, 0.7343750000000519584, 0.7500000000000512923, 0.8125000000000498490, 0.8437500000000496270, 0.8593750000000495159, 0.8671875000000479616, 0.8710937500000468514, 0.8750000000000456302, 1.000000000000000000 ),
 .UNSPECIFIED. ) ;
#5549=ORIENTED_EDGE ( 'NONE', *, *, #42841, .T. ) ;
#5550=CARTESIAN_POINT ( 'NONE',  ( 16.03314433152361218, -8.943717616153330496, -8.673217039016838825 ) ) ;
#5555=ORIENTED_EDGE ( 'NONE', *, *, #62176, .T. ) ;
#5569=VERTEX_POINT ( 'NONE', #59226 ) ;
#5587=DIRECTION ( 'NONE',  ( 0.000000000000000000, -0.5000000000000168754, -0.8660254037844288266 ) ) ;
#5602=DIRECTION ( 'NONE',  ( 0.000000000000000000, 0.000000000000000000, -1.000000000000000000 ) ) ;
#5605=CARTESIAN_POINT ( 'NONE',  ( 24.25374608244500152, 8.963954835242001096, 8.909854536156000648 ) ) ;
#5607=CARTESIAN_POINT ( 'NONE',  ( 13.70009528508592211, -8.955766972928978831, -7.451364690503297084 ) ) ;
#5608=ADVANCED_FACE ( 'NONE', ( #55029 ), #2789, .T. ) ;
#5613=EDGE_CURVE ( 'NONE', #6251, #67640, #57468, .T. ) ;
#5617=B_SPLINE_CURVE_WITH_KNOTS ( 'NONE', 3,
 ( #60049, #7251, #33834, #56181 ),
 .UNSPECIFIED., .F., .F.,
 ( 4, 4 ),
 ( 0.000000000000000000, 1.000000000000000000 ),
 .UNSPECIFIED. ) ;
#5627=CARTESIAN_POINT ( 'NONE',  ( 12.73341336140044611, 10.78295181804158354, -4.410266442043442758 ) ) ;
#5629=FACE_OUTER_BOUND ( 'NONE', #56136, .T. ) ;
#5633=FACE_OUTER_BOUND ( 'NONE', #9412, .T. ) ;
#5639=FACE_OUTER_BOUND ( 'NONE', #26848, .T. ) ;
#5641=CARTESIAN_POINT ( 'NONE',  ( 27.09999999999999787, 0.000000000000000000, 0.000000000000000000 ) ) ;
#5642=CARTESIAN_POINT ( 'NONE',  ( 18.15531827657417097, -3.266808065250859983, 11.18265383028970206 ) ) ;
#5653=CARTESIAN_POINT ( 'NONE',  ( 24.30001685126999789, 8.938702716825000394, -8.938676159935001309 ) ) ;
#5666=CARTESIAN_POINT ( 'NONE',  ( 23.91427437024694669, 3.339324960032359346, -12.90828973773218635 ) ) ;
#5672=CARTESIAN_POINT ( 'NONE',  ( 13.16012107570600342, 11.71981102724999957, 1.988987020038000209 ) ) ;
#5684=CARTESIAN_POINT ( 'NONE',  ( 24.83136307050961022, -8.598812902131761859, 8.498673240716678734 ) ) ;
#5690=CARTESIAN_POINT ( 'NONE',  ( 12.03709034744600181, 11.69601057336999972, -4.586677359659000253 ) ) ;
#5691=CARTESIAN_POINT ( 'NONE',  ( 17.97171023854900085, 11.57811841779999895, -4.879106015068000346 ) ) ;
#5695=EDGE_CURVE ( 'NONE', #53272, #13468, #54864, .T. ) ;
#5696=CARTESIAN_POINT ( 'NONE',  ( 12.09997738314682891, -11.69706276465794126, 3.884924152325089697 ) ) ;
#5705=CARTESIAN_POINT ( 'NONE',  ( 23.60000000000000142, -2.548720605937000006, 12.21654710926000220 ) ) ;
#5706=DIRECTION ( 'NONE',  ( -1.000000000000000000, 0.000000000000000000, 0.000000000000000000 ) ) ;
#5719=CARTESIAN_POINT ( 'NONE',  ( 16.27289819560299833, -3.403267206945999934, -11.10251878130000058 ) ) ;
#5726=EDGE_CURVE ( 'NONE', #34183, #66927, #26512, .T. ) ;
#5731=CARTESIAN_POINT ( 'NONE',  ( 24.98214528072500329, -8.515982190356998771, 8.483938328266001250 ) ) ;
#5734=CARTESIAN_POINT ( 'NONE',  ( 25.29577264028900174, -11.38513750862999885, -3.114196631034000351 ) ) ;
#5738=CARTESIAN_POINT ( 'NONE',  ( 25.59994555223600088, -1.356777910713382829, -11.13814279612294911 ) ) ;
#5739=CARTESIAN_POINT ( 'NONE',  ( 11.30000000000000071, 0.000000000000000000, 0.000000000000000000 ) ) ;
#5747=CARTESIAN_POINT ( 'NONE',  ( 15.39421883851900219, 8.828753284254000633, 7.820747050108999510 ) ) ;
#5761=CARTESIAN_POINT ( 'NONE',  ( 11.50029455687000102, 11.65000000000000036, 0.000000000000000000 ) ) ;
#5769=CARTESIAN_POINT ( 'NONE',  ( 16.13854985688900001, 3.352851047014000052, 11.81842075147999971 ) ) ;
#5772=ORIENTED_EDGE ( 'NONE', *, *, #2406, .T. ) ;
#5773=CARTESIAN_POINT ( 'NONE',  ( 13.68260097612285264, -12.30227370000369369, -2.353106563162954856 ) ) ;
#5777=CARTESIAN_POINT ( 'NONE',  ( 17.60000001994400165, -11.53041320601000130, 4.891397783926000109 ) ) ;
#5794=CONICAL_SURFACE ( 'NONE', #31512, 11.34994642770999818, 0.7853934433896081480 ) ;
#5796=CARTESIAN_POINT ( 'NONE',  ( 17.68520301169487752, 11.41062399034242425, -4.624005385410825397 ) ) ;
#5805=DIRECTION ( 'NONE',  ( -3.667724557042155543E-10, -0.9466472399347399813, 0.3222716294121134584 ) ) ;
#5807=AXIS2_PLACEMENT_3D ( 'NONE', #43470, #38208, #52919 ) ;
#5814=EDGE_CURVE ( 'NONE', #46546, #57489, #13881, .T. ) ;
#5815=CARTESIAN_POINT ( 'NONE',  ( 23.59999172237900211, -2.915589696762999949, -13.58550518520000061 ) ) ;
#5818=CARTESIAN_POINT ( 'NONE',  ( 15.83979990366733048, -8.664995957719217046, -8.086229679809637361 ) ) ;
#5827=ORIENTED_EDGE ( 'NONE', *, *, #55658, .F. ) ;
#5828=CARTESIAN_POINT ( 'NONE',  ( 16.20650642310300071, -3.719849042574000286, -12.00042637259999978 ) ) ;
#5829=CARTESIAN_POINT ( 'NONE',  ( 11.83156678923300120, 11.57054462408999917, 1.756438942007999993 ) ) ;
#5834=B_SPLINE_CURVE_WITH_KNOTS ( 'NONE', 3,
 ( #29587, #65582, #60687, #23975 ),
 .UNSPECIFIED., .F., .F.,
 ( 4, 4 ),
 ( 0.000000000000000000, 1.000000000000000000 ),
 .UNSPECIFIED. ) ;
#5836=CARTESIAN_POINT ( 'NONE',  ( 13.50003721581400029, 9.159934378815998812, 7.517910889891000537 ) ) ;
#5842=EDGE_CURVE ( 'NONE', #18715, #59008, #18422, .T. ) ;
#5850=CARTESIAN_POINT ( 'NONE',  ( 25.46372676430900128, 8.354609436172999892, -8.148458316574000548 ) ) ;
#5854=CARTESIAN_POINT ( 'NONE',  ( 13.69997185827400088, -11.21472423003502072, -3.290649947225299243 ) ) ;
#5860=CARTESIAN_POINT ( 'NONE',  ( 11.40162633574000139, -12.25609765133000018, -1.727435033673999865 ) ) ;
#5864=EDGE_CURVE ( 'NONE', #50878, #22693, #46442, .T. ) ;
#5865=CARTESIAN_POINT ( 'NONE',  ( 24.30001696810800027, 12.21047201856000086, 3.271805692349999628 ) ) ;
#5868=VERTEX_POINT ( 'NONE', #47211 ) ;
#5870=CARTESIAN_POINT ( 'NONE',  ( 18.44382898362900036, 2.795331802377000407, 11.36579223931000016 ) ) ;
#5874=CARTESIAN_POINT ( 'NONE',  ( 18.26001707275200303, 2.811958703674000137, -11.55267125806999928 ) ) ;
#5876=CARTESIAN_POINT ( 'NONE',  ( 24.37816192507718327, -12.29708154334037928, -3.190021095768833082 ) ) ;
#5879=CARTESIAN_POINT ( 'NONE',  ( 23.60000000000000497, -11.54188282345546490, 7.798337198497422129 ) ) ;
#5881=EDGE_LOOP ( 'NONE', ( #68785, #2160, #1312, #17723 ) ) ;
#5902=ADVANCED_FACE ( 'NONE', ( #15044 ), #64790, .F. ) ;
#5904=CARTESIAN_POINT ( 'NONE',  ( 12.17512857912400115, -11.55078329699999884, 4.188961560869000067 ) ) ;
#5909=CARTESIAN_POINT ( 'NONE',  ( 23.95204559793199905, 3.419365875930000076, 12.89885794585999967 ) ) ;
#5914=VERTEX_POINT ( 'NONE', #60456 ) ;
#5919=VERTEX_POINT ( 'NONE', #39129 ) ;
#5920=B_SPLINE_CURVE_WITH_KNOTS ( 'NONE', 3,
 ( #56004, #61249, #18944, #8111, #29454, #50763, #61934, #40273, #51103, #3205, #24532, #19281, #40606, #14047, #36394, #26601, #63978, #51783, #15069, #58402, #57710, #47234 ),
 .UNSPECIFIED., .F., .F.,
 ( 4, 2, 2, 1, 1, 2, 2, 2, 2, 2, 2, 4 ),
 ( 0.000000000000000000, 0.1249999999999412137, 0.1874999999999118205, 0.2187499999999014677, 0.2343749999999007738, 0.2421874999999004130, 0.2499999999999000799, 0.3749999999999177325, 0.4374999999999291123, 0.4687499999999334421, 0.4999999999999377165, 1.000000000000000000 ),
 .UNSPECIFIED. ) ;
#5923=ORIENTED_EDGE ( 'NONE', *, *, #1012, .F. ) ;
#5925=CARTESIAN_POINT ( 'NONE',  ( 17.33333333119166753, 3.345268056437870730, 11.86064107241928411 ) ) ;
#5933=CARTESIAN_POINT ( 'NONE',  ( 13.73854985688900143, 9.171197327466000360, 8.173482659384999849 ) ) ;
#5938=ORIENTED_EDGE ( 'NONE', *, *, #33539, .F. ) ;
#5940=AXIS2_PLACEMENT_3D ( 'NONE', #9837, #10522, #33586 ) ;
#5944=CARTESIAN_POINT ( 'NONE',  ( 11.44438160092000167, 12.37754422778999874, 1.524124373512000030 ) ) ;
#5950=DIRECTION ( 'NONE',  ( -1.000000000000000000, 0.000000000000000000, 0.000000000000000000 ) ) ;
#5951=CARTESIAN_POINT ( 'NONE',  ( 25.50723805854519100, -2.874178715285141905, 11.25475534034192471 ) ) ;
#5952=ORIENTED_EDGE ( 'NONE', *, *, #50358, .F. ) ;
#5955=CARTESIAN_POINT ( 'NONE',  ( 24.25375554908000097, -3.234179890672000290, -12.21792844062999883 ) ) ;
#5967=CARTESIAN_POINT ( 'NONE',  ( 12.08097595789114642, 12.02669421650328019, -3.498808775432329377 ) ) ;
#5973=ORIENTED_EDGE ( 'NONE', *, *, #31205, .F. ) ;
#5975=CARTESIAN_POINT ( 'NONE',  ( 23.60000337037311979, -10.25353992318573759, -9.380071257702633503 ) ) ;
#5976=CARTESIAN_POINT ( 'NONE',  ( 11.92303154622437411, -11.77792023318479586, 4.262523390541344881 ) ) ;
#5984=CARTESIAN_POINT ( 'NONE',  ( 12.48078237941917301, 11.21561491925777432, -3.152940285276780941 ) ) ;
#5985=FACE_OUTER_BOUND ( 'NONE', #30719, .T. ) ;
#5992=CARTESIAN_POINT ( 'NONE',  ( 11.64452043831720829, -3.625675755376928766, 11.98888621914706398 ) ) ;
#5995=CARTESIAN_POINT ( 'NONE',  ( 24.30001129780202263, 8.895961348536667757, 8.895961348536667757 ) ) ;
#5998=EDGE_CURVE ( 'NONE', #64677, #62083, #54736, .T. ) ;
#5999=ORIENTED_EDGE ( 'NONE', *, *, #11208, .T. ) ;
#6010=CARTESIAN_POINT ( 'NONE',  ( 23.60000330292420045, 2.996599131394091842, -13.56986852407293753 ) ) ;
#6011=CARTESIAN_POINT ( 'NONE',  ( 18.44721083353000068, -2.702837639295000205, 11.38762126772000016 ) ) ;
#6014=FACE_OUTER_BOUND ( 'NONE', #31853, .T. ) ;
#6021=CARTESIAN_POINT ( 'NONE',  ( 24.67921580316900076, -12.29514843751999997, 2.979196179828000002 ) ) ;
#6026=CARTESIAN_POINT ( 'NONE',  ( 18.28126625413079154, 11.72532252228423744, -3.796277944706968110 ) ) ;
#6028=B_SPLINE_SURFACE_WITH_KNOTS ( 'NONE', 3, 3, ( 
 ( #59391, #64631, #1358, #17082 ),
 ( #21984, #38415, #11491, #32492 ),
 ( #16737, #32836, #38768, #54148 ),
 ( #44020, #27587, #65671, #22331 ),
 ( #6944, #65323, #39111, #12198 ),
 ( #27938, #33526, #44373, #54845 ),
 ( #43326, #12542, #59740, #6245 ),
 ( #11841, #49249, #43671, #33179 ),
 ( #60435, #49597, #28276, #1704 ),
 ( #48913, #1021, #23023, #5904 ),
 ( #54497, #64968, #48568, #17793 ),
 ( #6597, #22675, #59055, #672 ),
 ( #11157, #53805, #21184, #63480 ),
 ( #43202, #48105, #11041, #4750 ),
 ( #63824, #15256, #15936, #26438 ),
 ( #58589, #36579, #37267, #16281 ) ),
 .UNSPECIFIED., .F., .F., .F.,
 ( 4, 1, 1, 1, 1, 1, 1, 1, 1, 1, 1, 1, 1, 4 ),
 ( 4, 4 ),
 ( 0.02931725585745000029, 0.07692307692307999434, 0.1538461538461999845, 0.2307692307692000011, 0.3076923076922999933, 0.3846153846154000133, 0.4615384615385000333, 0.5384615384614999112, 0.6153846153845999867, 0.6923076923076999512, 0.7692307692308000266, 0.8461538461537999600, 0.9230769230769000355, 0.9830414450855999853 ),
 ( -0.1835260008786999963, 1.183623993927000129 ),
 .UNSPECIFIED. ) ;
#6034=CARTESIAN_POINT ( 'NONE',  ( 12.83523642498299999, 11.49802605210000195, -4.818062943702999590 ) ) ;
#6035=CARTESIAN_POINT ( 'NONE',  ( 17.87004618316199966, 11.92229088141000126, -3.300664210127000064 ) ) ;
#6040=CARTESIAN_POINT ( 'NONE',  ( 18.48724299199999876, -3.206939682244000167, 12.14698705996000072 ) ) ;
#6043=EDGE_LOOP ( 'NONE', ( #34858, #55821, #22919, #31302 ) ) ;
#6053=CONICAL_SURFACE ( 'NONE', #38454, 11.75015521449999945, 0.7854113701714536822 ) ;
#6057=CIRCLE ( 'NONE', #27287, 12.32509977859000827 ) ;
#6060=CARTESIAN_POINT ( 'NONE',  ( 17.60000005322544681, -11.49057892309719264, 4.802228223496430637 ) ) ;
#6063=CARTESIAN_POINT ( 'NONE',  ( 16.29314246895800267, -3.193172571147000038, -11.44978050968999916 ) ) ;
#6071=CARTESIAN_POINT ( 'NONE',  ( 24.55996189763800075, -3.658601031398000192, 12.32999353876000015 ) ) ;
#6076=CARTESIAN_POINT ( 'NONE',  ( 25.19548496669100146, -8.372909214912999332, 8.693259092873001137 ) ) ;
#6079=CARTESIAN_POINT ( 'NONE',  ( 24.74074828464900122, -11.86918666989000037, -3.111331014755999824 ) ) ;
#6084=CARTESIAN_POINT ( 'NONE',  ( 12.99284288850700086, 12.22216846288000092, 1.954503247608000205 ) ) ;
#6086=AXIS2_PLACEMENT_3D ( 'NONE', #4186, #25524, #36011 ) ;
#6087=DIRECTION ( 'NONE',  ( 1.000000000000000000, 0.000000000000000000, 0.000000000000000000 ) ) ;
#6090=EDGE_CURVE ( 'NONE', #23499, #23570, #60834, .T. ) ;
#6092=CARTESIAN_POINT ( 'NONE',  ( 18.28832092538753074, 2.855728056445007823, 11.50255606616314630 ) ) ;
#6094=ORIENTED_EDGE ( 'NONE', *, *, #65735, .T. ) ;
#6097=PLANE ( 'NONE',  #10778 ) ;
#6101=CARTESIAN_POINT ( 'NONE',  ( 25.20468521070600332, 11.19853207827999952, -3.405347367087999899 ) ) ;
#6112=CARTESIAN_POINT ( 'NONE',  ( 24.71426486868732653, 11.77715745911889123, -3.190793282506284800 ) ) ;
#6114=CARTESIAN_POINT ( 'NONE',  ( 13.04552286951900619, -12.39025300375189964, -1.832281502500274772 ) ) ;
#6117=CARTESIAN_POINT ( 'NONE',  ( 24.30000000000000071, 0.000000000000000000, 0.000000000000000000 ) ) ;
#6119=CARTESIAN_POINT ( 'NONE',  ( 25.30000327618300204, -0.7080256801165881742, 11.56241914337144294 ) ) ;
#6121=CARTESIAN_POINT ( 'NONE',  ( 24.30000000000000071, 2.204728229456999866, 11.99913219504999873 ) ) ;
#6127=ORIENTED_EDGE ( 'NONE', *, *, #60927, .F. ) ;
#6146=ADVANCED_FACE ( 'NONE', ( #66379 ), #22840, .F. ) ;
#6153=ORIENTED_EDGE ( 'NONE', *, *, #16948, .T. ) ;
#6159=ORIENTED_EDGE ( 'NONE', *, *, #19091, .F. ) ;
#6163=CARTESIAN_POINT ( 'NONE',  ( 13.69999628573842543, 9.617752440245856960, 8.023770515523496627 ) ) ;
#6169=CARTESIAN_POINT ( 'NONE',  ( 24.87152056774154119, 3.035077187909910545, -11.66328149024612237 ) ) ;
#6170=CARTESIAN_POINT ( 'NONE',  ( 16.43176826122700263, 3.316188843241000050, 11.22344245815999919 ) ) ;
#6176=CARTESIAN_POINT ( 'NONE',  ( 23.58333425578799947, 1.192379528446999839E-13, -4.982680934517999418E-13 ) ) ;
#6177=DIRECTION ( 'NONE',  ( 0.000000000000000000, 0.000000000000000000, -1.000000000000000000 ) ) ;
#6184=CARTESIAN_POINT ( 'NONE',  ( 15.48701341325400094, -9.525963125313998248, -8.191611664426000416 ) ) ;
#6191=DIRECTION ( 'NONE',  ( 1.000000000000000000, 0.000000000000000000, 0.000000000000000000 ) ) ;
#6199=CARTESIAN_POINT ( 'NONE',  ( 11.31944011432000075, -12.15765269271000015, -1.759220518310000037 ) ) ;
#6209=EDGE_CURVE ( 'NONE', #15006, #39410, #13925, .T. ) ;
#6216=CARTESIAN_POINT ( 'NONE',  ( 17.76930066282600151, 3.251864118589000263, -11.33740735155000046 ) ) ;
#6219=CARTESIAN_POINT ( 'NONE',  ( 23.55777338189700032, -10.23214251361999949, -9.679131332715998681 ) ) ;
#6220=B_SPLINE_CURVE_WITH_KNOTS ( 'NONE', 3,
 ( #49148, #26196, #1259, #12096, #54744, #6843, #28177, #20255, #47521, #36337 ),
 .UNSPECIFIED., .F., .F.,
 ( 4, 2, 2, 2, 4 ),
 ( 0.000000000000000000, 0.1249999999532679651, 0.2499999999065359302, 0.3749999998598039230, 0.4999999998130718604 ),
 .UNSPECIFIED. ) ;
#6222=CARTESIAN_POINT ( 'NONE',  ( 25.44993329535400051, 2.258942858049999725, 12.29419282279000036 ) ) ;
#6223=CARTESIAN_POINT ( 'NONE',  ( 20.75138802851920161, 0.000000000000000000, 0.000000000000000000 ) ) ;
#6228=CARTESIAN_POINT ( 'NONE',  ( 24.44917776433500123, 8.894882193901999301, -9.199943407630001957 ) ) ;
#6230=ORIENTED_EDGE ( 'NONE', *, *, #7477, .F. ) ;
#6231=CARTESIAN_POINT ( 'NONE',  ( 24.30001131380927148, -8.895961354869664106, 8.895961354869664106 ) ) ;
#6233=CIRCLE ( 'NONE', #28574, 13.92493900951001073 ) ;
#6235=CARTESIAN_POINT ( 'NONE',  ( 18.29995268966800026, 2.861739928647000220, 11.98821236628000086 ) ) ;
#6244=CARTESIAN_POINT ( 'NONE',  ( 24.36453968238300050, 12.29068757677999990, -3.201420012754999878 ) ) ;
#6245=CARTESIAN_POINT ( 'NONE',  ( 12.18592533278400047, -11.71489335541000010, 3.703722432179000101 ) ) ;
#6251=VERTEX_POINT ( 'NONE', #20206 ) ;
#6268=VERTEX_POINT ( 'NONE', #62844 ) ;
#6274=CARTESIAN_POINT ( 'NONE',  ( 25.29987931604000195, 11.77655473258999841, -4.190794510628000680 ) ) ;
#6282=CARTESIAN_POINT ( 'NONE',  ( 23.56666365135700403, -12.07812737763999955, 3.551569042617998662 ) ) ;
#6284=CARTESIAN_POINT ( 'NONE',  ( 11.80727443316700231, 12.22191286342000005, 1.956148154176999832 ) ) ;
#6309=EDGE_CURVE ( 'NONE', #44124, #7173, #53060, .T. ) ;
#6313=CARTESIAN_POINT ( 'NONE',  ( 17.84552287012693128, 3.595130221969103701, 11.99794414424705025 ) ) ;
#6316=CARTESIAN_POINT ( 'NONE',  ( 24.04053975777259566, -9.302302187229880559, -9.232450872209369663 ) ) ;
#6317=DIRECTION ( 'NONE',  ( -1.000000000000000000, 0.000000000000000000, 0.000000000000000000 ) ) ;
#6321=CARTESIAN_POINT ( 'NONE',  ( 24.33723043407100306, 3.364332162536999959, -12.26583136334000024 ) ) ;
#6323=CARTESIAN_POINT ( 'NONE',  ( 24.30000000000000071, 0.000000000000000000, 0.000000000000000000 ) ) ;
#6326=CARTESIAN_POINT ( 'NONE',  ( 18.47905117804076269, -2.854821129073351837, -11.29488031137822901 ) ) ;
#6329=B_SPLINE_CURVE_WITH_KNOTS ( 'NONE', 3,
 ( #63800, #5426, #65175, #43527 ),
 .UNSPECIFIED., .F., .F.,
 ( 4, 4 ),
 ( 0.000000000000000000, 1.000000000000000000 ),
 .UNSPECIFIED. ) ;
#6334=CARTESIAN_POINT ( 'NONE',  ( 24.30000000000000071, 12.03537377768999939, 3.224868684338999980 ) ) ;
#6337=VECTOR ( 'NONE', #31980, 1000.000000000000227 ) ;
#6338=CARTESIAN_POINT ( 'NONE',  ( 25.44994642811700203, 3.641531520771000022E-14, 3.907985046680999726E-14 ) ) ;
#6345=EDGE_LOOP ( 'NONE', ( #44573, #51982, #18928, #37899 ) ) ;
#6352=CARTESIAN_POINT ( 'NONE',  ( 23.77343880546692034, 3.285534861686421060, -13.18386822430981553 ) ) ;
#6353=CARTESIAN_POINT ( 'NONE',  ( 18.05609597790000009, -3.343430715100999873, 11.12052764821000039 ) ) ;
#6358=AXIS2_PLACEMENT_3D ( 'NONE', #36105, #30868, #58120 ) ;
#6378=CARTESIAN_POINT ( 'NONE',  ( 13.69997185827400266, -11.40547114375999982, -2.374390024598000082 ) ) ;
#6390=FACE_OUTER_BOUND ( 'NONE', #41480, .T. ) ;
#6400=VECTOR ( 'NONE', #52943, 1000.000000000000227 ) ;
#6406=AXIS2_PLACEMENT_3D ( 'NONE', #28934, #22970, #34522 ) ;
#6408=CARTESIAN_POINT ( 'NONE',  ( 24.53429014209899961, 12.47024915613999951, 3.026245713505000268 ) ) ;
#6409=CARTESIAN_POINT ( 'NONE',  ( 11.40162633574000139, 3.633188743968999823, -11.83198634993999931 ) ) ;
#6414=CARTESIAN_POINT ( 'NONE',  ( 11.49999672494999814, 8.721203281753671988, -7.819494091976955552 ) ) ;
#6418=CARTESIAN_POINT ( 'NONE',  ( 24.63408956130300353, -8.686807539907999143, 8.587991764679999918 ) ) ;
#6423=CARTESIAN_POINT ( 'NONE',  ( 24.37897525340100202, -8.840625649873999237, -8.761552777197998410 ) ) ;
#6427=ORIENTED_EDGE ( 'NONE', *, *, #26542, .F. ) ;
#6430=CARTESIAN_POINT ( 'NONE',  ( 23.56666365135700403, 8.673757318230000735, 7.881093921673004488 ) ) ;
#6433=CARTESIAN_POINT ( 'NONE',  ( 14.39999999570800249, 11.53036813819577411, -4.891445144093894193 ) ) ;
#6434=CARTESIAN_POINT ( 'NONE',  ( 18.30003129332100187, 2.732683818840999646, 11.53064095373000164 ) ) ;
#6438=CARTESIAN_POINT ( 'NONE',  ( 23.77345858638861031, -13.06030404894205077, 3.746546544767070497 ) ) ;
#6449=AXIS2_PLACEMENT_3D ( 'NONE', #5055, #43507, #64803 ) ;
#6457=CARTESIAN_POINT ( 'NONE',  ( 24.44496482743900145, 12.03536723905999928, -3.224852005146999989 ) ) ;
#6459=VECTOR ( 'NONE', #41872, 1000.000000000000114 ) ;
#6466=CARTESIAN_POINT ( 'NONE',  ( 24.30000000000000071, 50.08530474119000075, -49.09535524753000146 ) ) ;
#6468=CARTESIAN_POINT ( 'NONE',  ( 17.71367434320026035, -11.53249064895033271, 4.886450710725981139 ) ) ;
#6473=CARTESIAN_POINT ( 'NONE',  ( 24.74446781360200021, -3.238412344267999732, 11.83115098604999993 ) ) ;
#6480=DIRECTION ( 'NONE',  ( 0.000000000000000000, 0.000000000000000000, -1.000000000000000000 ) ) ;
#6486=EDGE_CURVE ( 'NONE', #38535, #39410, #7233, .T. ) ;
#6487=CARTESIAN_POINT ( 'NONE',  ( 24.44916829770000177, -8.894890565782000991, -9.199951775352998240 ) ) ;
#6489=CARTESIAN_POINT ( 'NONE',  ( 23.56681878841384403, 10.34114842139075563, -9.422272710775716931 ) ) ;
#6509=CARTESIAN_POINT ( 'NONE',  ( 15.52913652543167089, -8.833284221180715434, -7.896593172538426408 ) ) ;
#6518=CARTESIAN_POINT ( 'NONE',  ( 16.39932787941000214, -3.295363098100999810, -11.83520513879000013 ) ) ;
#6521=CARTESIAN_POINT ( 'NONE',  ( 24.71429018881659445, 3.125258109923432670, -11.79469236763018181 ) ) ;
#6528=CARTESIAN_POINT ( 'NONE',  ( 17.60000001947600268, -11.86186880240999919, 3.298627760718999991 ) ) ;
#6534=CARTESIAN_POINT ( 'NONE',  ( 24.25866698968500401, -12.09695184427999948, -3.327214749306000030 ) ) ;
#6537=CARTESIAN_POINT ( 'NONE',  ( 15.77677363193000204, -9.321312496448001639, -8.284802892401000207 ) ) ;
#6545=AXIS2_PLACEMENT_3D ( 'NONE', #7893, #2980, #18387 ) ;
#6553=CARTESIAN_POINT ( 'NONE',  ( 11.82330164685100193, -12.43416923969000010, -1.799281280950999928 ) ) ;
#6570=MANIFOLD_SOLID_BREP ( 'Stock-MAS-678-1', #59319 ) ;
#6571=EDGE_CURVE ( 'NONE', #64727, #58276, #54244, .T. ) ;
#6573=CARTESIAN_POINT ( 'NONE',  ( 23.74079507723600102, -9.838286271853998954, -9.517717110099001232 ) ) ;
#6574=CARTESIAN_POINT ( 'NONE',  ( 23.85161546330200011, -9.644042618899000274, 9.632248201521999675 ) ) ;
#6583=CARTESIAN_POINT ( 'NONE',  ( 24.63780974963800219, 3.092545797709000066, -11.81390549036999893 ) ) ;
#6590=AXIS2_PLACEMENT_3D ( 'NONE', #31361, #52674, #53370 ) ;
#6596=CARTESIAN_POINT ( 'NONE',  ( 24.62774583285499830, 12.19917312477000060, -3.045379866085000220 ) ) ;
#6597=CARTESIAN_POINT ( 'NONE',  ( 12.21268235885900033, -11.62758720635999765, 4.758865308234000224 ) ) ;
#6602=ORIENTED_EDGE ( 'NONE', *, *, #18008, .T. ) ;
#6603=CARTESIAN_POINT ( 'NONE',  ( 24.03543920757945074, -9.310452318425328500, 9.237282073437325991 ) ) ;
#6607=ORIENTED_EDGE ( 'NONE', *, *, #16658, .F. ) ;
#6609=EDGE_CURVE ( 'NONE', #58398, #16938, #40825, .T. ) ;
#6616=( BOUNDED_SURFACE ( )  B_SPLINE_SURFACE ( 3, 3, ( 
 ( #52553, #42756, #42070, #13027 ),
 ( #60565, #1837, #796, #33309 ),
 ( #55321, #55673, #54627, #2186 ),
 ( #12673, #64751, #22804, #27369 ) ),
 .UNSPECIFIED., .F., .F., .T. ) 
 B_SPLINE_SURFACE_WITH_KNOTS ( ( 4, 4 ),
 ( 4, 4 ),
 ( 0.000000000000000000, 1.000000000000000000 ),
 ( 0.000000000000000000, 1.000000000000000000 ),
 .UNSPECIFIED. ) 
 GEOMETRIC_REPRESENTATION_ITEM ( )  RATIONAL_B_SPLINE_SURFACE ( (
 ( 1.512182578520000042, 1.160176301760999840, 1.160176301760999840, 1.512182578520000042),
 ( 1.111288591041000196, 0.8526025270081000196, 0.8526025270081000196, 1.111288591041000196),
 ( 1.111288591041000196, 0.8526025270081000196, 0.8526025270081000196, 1.111288591041000196),
 ( 1.512182578520000042, 1.160176301760999840, 1.160176301760999840, 1.512182578520000042) ) ) 
 REPRESENTATION_ITEM ( '' )  SURFACE ( )  );
#6620=ORIENTED_EDGE ( 'NONE', *, *, #15554, .T. ) ;
#6621=CARTESIAN_POINT ( 'NONE',  ( 24.35365242081699932, 12.20235406300999514, 3.288253180468997172 ) ) ;
#6622=CARTESIAN_POINT ( 'NONE',  ( 23.94498321860814727, 9.457022807326861624, 9.320427756281231879 ) ) ;
#6624=B_SPLINE_SURFACE_WITH_KNOTS ( 'NONE', 3, 3, ( 
 ( #67074, #40182, #62853, #30376 ),
 ( #8361, #51684, #25120, #46452 ),
 ( #29707, #34939, #14635, #56939 ),
 ( #35953, #35281, #19876, #51008 ),
 ( #40510, #20215, #46792, #67412 ),
 ( #57614, #57267, #14298, #40855 ),
 ( #31064, #56597, #25460, #56254 ),
 ( #18855, #46106, #3108, #24779 ),
 ( #3442, #8704, #2768, #9367 ),
 ( #30047, #51350, #52023, #4124 ) ),
 .UNSPECIFIED., .F., .F., .F.,
 ( 4, 1, 1, 1, 1, 1, 1, 4 ),
 ( 4, 4 ),
 ( 0.07203983506773999068, 0.1428571428570999946, 0.2857142857143000203, 0.4285714285713999594, 0.5714285714286000406, 0.7142857142856999797, 0.8571428571429000609, 0.9589780836993999635 ),
 ( -0.1900620218102000158, 1.190128522698000069 ),
 .UNSPECIFIED. ) ;
#6629=CARTESIAN_POINT ( 'NONE',  ( 18.19189882637400046, -12.11510371750999937, 3.327574861395000028 ) ) ;
#6630=DIRECTION ( 'NONE',  ( 0.000000000000000000, -0.6460255221484837440, 0.7633158093035797842 ) ) ;
#6639=CARTESIAN_POINT ( 'NONE',  ( 16.39999999347100257, 3.345256695718999751, 11.86066175541999890 ) ) ;
#6644=DIRECTION ( 'NONE',  ( 1.000000000000000000, 0.000000000000000000, 0.000000000000000000 ) ) ;
#6662=CARTESIAN_POINT ( 'NONE',  ( 12.10941530405103173, 10.98038939432486849, -3.892884064768170838 ) ) ;
#6663=CARTESIAN_POINT ( 'NONE',  ( 25.29995873461299993, 11.13046969959000165, 3.427501705020000067 ) ) ;
#6670=CARTESIAN_POINT ( 'NONE',  ( 12.36003207187220809, -11.57530800953469630, 4.784147006776684918 ) ) ;
#6676=CARTESIAN_POINT ( 'NONE',  ( 13.08701341325400236, -12.43401476831999908, -1.800486563913999971 ) ) ;
#6687=EDGE_CURVE ( 'NONE', #41893, #52150, #1758, .T. ) ;
#6688=DIRECTION ( 'NONE',  ( 0.000000000000000000, 0.000000000000000000, -1.000000000000000000 ) ) ;
#6693=CARTESIAN_POINT ( 'NONE',  ( 24.40777907822999993, 12.23846661367000088, 3.187421709680999804 ) ) ;
#6697=VERTEX_POINT ( 'NONE', #48329 ) ;
#6703=CARTESIAN_POINT ( 'NONE',  ( 23.98815239557806223, 3.345691041822517864, -12.76938554867816400 ) ) ;
#6712=ORIENTED_EDGE ( 'NONE', *, *, #13587, .T. ) ;
#6727=CARTESIAN_POINT ( 'NONE',  ( 13.63328756540912323, -11.47070279790941072, -2.387969831734693127 ) ) ;
#6735=CARTESIAN_POINT ( 'NONE',  ( 23.85395620458804800, 3.593169595889099899, 13.20269660471672601 ) ) ;
#6739=CARTESIAN_POINT ( 'NONE',  ( 21.70000039307920048, 13.99999960683000033, 1.736067127764999983E-09 ) ) ;
#6754=LINE ( 'NONE', #28094, #20879 ) ;
#6755=ORIENTED_EDGE ( 'NONE', *, *, #55489, .T. ) ;
#6756=AXIS2_PLACEMENT_3D ( 'NONE', #22405, #43746, #38491 ) ;
#6761=B_SPLINE_SURFACE_WITH_KNOTS ( 'NONE', 3, 3, ( 
 ( #64998, #700, #11871, #31574 ),
 ( #48598, #48944, #57786, #20733 ),
 ( #30887, #49279, #36123, #27617 ),
 ( #15146, #17113, #65355, #63366 ),
 ( #68614, #31237, #57438, #33211 ),
 ( #9542, #38447, #54530, #5933 ),
 ( #15494, #10239, #4641, #52200 ),
 ( #22706, #11520, #53836, #43702 ),
 ( #27275, #22013, #9898, #64661 ) ),
 .UNSPECIFIED., .F., .F., .F.,
 ( 4, 1, 1, 1, 1, 1, 4 ),
 ( 4, 4 ),
 ( 0.05214259105098999897, 0.1666666666667000196, 0.3333333333333000081, 0.5000000000000000000, 0.6666666666667000474, 0.8333333333333000637, 0.9777068595523999983 ),
 ( -0.1900882580235000174, 1.190231865545000156 ),
 .UNSPECIFIED. ) ;
#6763=CARTESIAN_POINT ( 'NONE',  ( 11.49999672495000524, 11.64999999999999680, -1.217117305822887241 ) ) ;
#6770=CARTESIAN_POINT ( 'NONE',  ( 25.36445432553700030, -11.12586087667000001, -3.379826431974999768 ) ) ;
#6771=ADVANCED_FACE ( 'NONE', ( #7756 ), #46424, .T. ) ;
#6774=CARTESIAN_POINT ( 'NONE',  ( 13.99947726215000188, -8.835099311859000437, -7.952110511812001015 ) ) ;
#6776=CARTESIAN_POINT ( 'NONE',  ( 21.05000072320139992, -1.355183834107999921E-13, 1.088018564133000035E-14 ) ) ;
#6778=CARTESIAN_POINT ( 'NONE',  ( 13.21722669115800031, 12.32379348829999977, 1.906876488274000137 ) ) ;
#6782=VERTEX_POINT ( 'NONE', #3872 ) ;
#6783=CARTESIAN_POINT ( 'NONE',  ( 11.30000000000000071, 18.88101580703000337, 3.105963843451999828 ) ) ;
#6784=CARTESIAN_POINT ( 'NONE',  ( 18.23980063339601898, 2.972525812591880534, 11.47315805767759578 ) ) ;
#6797=EDGE_CURVE ( 'NONE', #34183, #44937, #48439, .T. ) ;
#6800=ORIENTED_EDGE ( 'NONE', *, *, #23622, .T. ) ;
#6805=CARTESIAN_POINT ( 'NONE',  ( 16.13837349797499954, 3.856691945087999951, 11.95672051617999898 ) ) ;
#6810=B_SPLINE_CURVE_WITH_KNOTS ( 'NONE', 3,
 ( #5815, #20523, #31712, #47445 ),
 .UNSPECIFIED., .F., .F.,
 ( 4, 4 ),
 ( 0.000000000000000000, 0.5000023781865966521 ),
 .UNSPECIFIED. ) ;
#6814=DIRECTION ( 'NONE',  ( 1.000000000000000000, 0.000000000000000000, 0.000000000000000000 ) ) ;
#6818=CARTESIAN_POINT ( 'NONE',  ( 24.69847935754600243, 3.637896099757999657, 12.18598438281999918 ) ) ;
#6822=B_SPLINE_CURVE_WITH_KNOTS ( 'NONE', 3,
 ( #26648, #42717, #64022, #22415, #48301, #5642, #37812, #32574, #16822, #48993, #53886, #27326, #38148, #1104 ),
 .UNSPECIFIED., .F., .F.,
 ( 4, 2, 2, 2, 2, 2, 4 ),
 ( 0.000000000000000000, 0.1249999999999998335, 0.2499999999999996669, 0.4999999999999993339, 0.6249999999999983347, 0.7499999999999972244, 1.000000000000000000 ),
 .UNSPECIFIED. ) ;
#6823=ORIENTED_EDGE ( 'NONE', *, *, #46237, .F. ) ;
#6826=EDGE_CURVE ( 'NONE', #30666, #24248, #39278, .T. ) ;
#6837=CARTESIAN_POINT ( 'NONE',  ( 24.53428993882599940, 8.855929947951999281, -9.286429770520999938 ) ) ;
#6843=CARTESIAN_POINT ( 'NONE',  ( 18.17745566903306198, 10.88889238843098362, -4.142628063308990249 ) ) ;
#6853=CARTESIAN_POINT ( 'NONE',  ( 24.14647106071498683, -12.47146082256108457, -3.359356504527230225 ) ) ;
#6858=EDGE_CURVE ( 'NONE', #10241, #35517, #7579, .T. ) ;
#6863=VERTEX_POINT ( 'NONE', #29794 ) ;
#6864=DIRECTION ( 'NONE',  ( 0.000000000000000000, 0.4812255921203881792, -0.8765967884314782577 ) ) ;
#6866=ORIENTED_EDGE ( 'NONE', *, *, #24021, .T. ) ;
#6868=CARTESIAN_POINT ( 'NONE',  ( 16.29314246895800267, 3.193172571147000038, 11.44978050968999916 ) ) ;
#6873=CARTESIAN_POINT ( 'NONE',  ( 25.60000000000000142, -2.023988666086999899, -11.01546541709000060 ) ) ;
#6876=LINE ( 'NONE', #39051, #29603 ) ;
#6882=CARTESIAN_POINT ( 'NONE',  ( 15.83019412026500206, -8.948785863751000491, -8.423203147821000769 ) ) ;
#6885=EDGE_CURVE ( 'NONE', #2551, #30098, #14041, .T. ) ;
#6889=CARTESIAN_POINT ( 'NONE',  ( 11.49978667957999967, -12.49365449110754867, -1.022561121909996817 ) ) ;
#6893=ORIENTED_EDGE ( 'NONE', *, *, #14074, .T. ) ;
#6894=DIRECTION ( 'NONE',  ( 0.000000000000000000, 0.000000000000000000, -1.000000000000000000 ) ) ;
#6902=CARTESIAN_POINT ( 'NONE',  ( 27.25811388278000180, 0.000000000000000000, 0.000000000000000000 ) ) ;
#6904=B_SPLINE_CURVE_WITH_KNOTS ( 'NONE', 3,
 ( #52195, #36460, #68261, #29867, #19350, #40672, #57779, #14116 ),
 .UNSPECIFIED., .F., .F.,
 ( 4, 2, 2, 4 ),
 ( 0.000000000000000000, 0.5000000000000005551, 0.7500000000000002220, 1.000000000000000000 ),
 .UNSPECIFIED. ) ;
#6906=CARTESIAN_POINT ( 'NONE',  ( 18.53959992722300143, 2.682146997965999979, 11.29770844980000000 ) ) ;
#6909=CARTESIAN_POINT ( 'NONE',  ( 19.99999987597299977, 0.000000000000000000, 5.040412531797999279E-14 ) ) ;
#6918=CARTESIAN_POINT ( 'NONE',  ( 24.45387054266700133, -8.897469717442998416, -9.225144726131999207 ) ) ;
#6919=CARTESIAN_POINT ( 'NONE',  ( 23.68233444796700127, -9.990153342492000377, 9.401313137095000272 ) ) ;
#6920=DIRECTION ( 'NONE',  ( 1.000000000000000000, 0.000000000000000000, 0.000000000000000000 ) ) ;
#6925=CARTESIAN_POINT ( 'NONE',  ( 23.59999196693599899, 2.915561532799999966, -13.58550759281999909 ) ) ;
#6928=CARTESIAN_POINT ( 'NONE',  ( 25.09299537199500207, 3.211994377626000041, -11.60337666361999887 ) ) ;
#6940=CARTESIAN_POINT ( 'NONE',  ( 24.53429014209899961, 12.47024915613999951, 3.026245713505000268 ) ) ;
#6944=CARTESIAN_POINT ( 'NONE',  ( 12.24011731813700088, -12.12177778538999995, 3.303327906654999868 ) ) ;
#6948=CARTESIAN_POINT ( 'NONE',  ( 23.55757892560500011, 3.265738280757000123, 13.70122728612999907 ) ) ;
#6951=CONICAL_SURFACE ( 'NONE', #32651, 13.94232983116000035, 1.233427434088588903 ) ;
#6952=CARTESIAN_POINT ( 'NONE',  ( 24.26287124489074998, -8.985590579641673514, 8.985591852965418624 ) ) ;
#6958=B_SPLINE_CURVE_WITH_KNOTS ( 'NONE', 3,
 ( #39412, #61761, #13879, #56521 ),
 .UNSPECIFIED., .F., .F.,
 ( 4, 4 ),
 ( 0.000000000000000000, 1.000000000000000000 ),
 .UNSPECIFIED. ) ;
#6960=CARTESIAN_POINT ( 'NONE',  ( 23.91260600754999999, 12.75253188547999983, -3.592041058436000078 ) ) ;
#6963=EDGE_LOOP ( 'NONE', ( #20810, #7046, #27523, #12854 ) ) ;
#6968=CARTESIAN_POINT ( 'NONE',  ( 23.74397628692652518, 9.837201187003470793, 9.448856396694791826 ) ) ;
#6973=CIRCLE ( 'NONE', #63901, 12.42499880353999941 ) ;
#6987=FACE_OUTER_BOUND ( 'NONE', #1290, .T. ) ;
#6988=CARTESIAN_POINT ( 'NONE',  ( 23.64843185931299985, -3.331590877846000165, 13.50015817444000099 ) ) ;
#6990=CARTESIAN_POINT ( 'NONE',  ( 18.44717847589300064, 2.901259342162000543, -12.12894967335999930 ) ) ;
#6993=DIRECTION ( 'NONE',  ( 0.000000000000000000, 0.9421243786071880066, 0.3352635608502960163 ) ) ;
#6997=CARTESIAN_POINT ( 'NONE',  ( 24.66271477989500127, -3.625397779087000227, -12.20587930303000057 ) ) ;
#7016=CARTESIAN_POINT ( 'NONE',  ( 13.00000000001300116, 11.52577654661000039, 1.696746661728000038 ) ) ;
#7017=EDGE_LOOP ( 'NONE', ( #8355, #26327, #34770, #7723 ) ) ;
#7020=CARTESIAN_POINT ( 'NONE',  ( 24.11583679491036136, -9.189166502811682236, -9.154374719221291201 ) ) ;
#7025=CARTESIAN_POINT ( 'NONE',  ( 11.30000000000000071, 12.07633927192662782, 1.479860929215916832 ) ) ;
#7026=CARTESIAN_POINT ( 'NONE',  ( 23.99067072799600098, 3.573053042975999904, -12.95875606115999901 ) ) ;
#7027=CARTESIAN_POINT ( 'NONE',  ( 12.96385332268500079, -12.32790784140999918, -1.878650414825000059 ) ) ;
#7035=CARTESIAN_POINT ( 'NONE',  ( 16.00000000028333602, 12.11987147417543298, -3.159800697744812314 ) ) ;
#7044=CARTESIAN_POINT ( 'NONE',  ( 12.65361177982750185, -10.78680294142912643, 4.401676341558338201 ) ) ;
#7046=ORIENTED_EDGE ( 'NONE', *, *, #53436, .F. ) ;
#7049=CONICAL_SURFACE ( 'NONE', #58399, 8.515178490300000291, 1.329165865441747751 ) ;
#7062=CARTESIAN_POINT ( 'NONE',  ( 25.30000327618300204, -8.756202924575998026, -7.455126447192999883 ) ) ;
#7068=AXIS2_PLACEMENT_3D ( 'NONE', #30556, #41729, #63034 ) ;
#7074=DIRECTION ( 'NONE',  ( -1.000000000000000000, 0.000000000000000000, 0.000000000000000000 ) ) ;
#7079=CARTESIAN_POINT ( 'NONE',  ( 24.56891840910600067, -3.717059876636999771, -12.37205664472999977 ) ) ;
#7087=DIRECTION ( 'NONE',  ( 0.000000000000000000, 0.1807154286439995039, -0.9835354258236027603 ) ) ;
#7090=CARTESIAN_POINT ( 'NONE',  ( 18.30003129332100187, 2.732683818840999646, 11.53064095373000164 ) ) ;
#7093=CARTESIAN_POINT ( 'NONE',  ( 14.70000000000000107, -8.824259102667999954, -7.756628703356000187 ) ) ;
#7113=DIRECTION ( 'NONE',  ( 0.000000000000000000, 0.9421243786072194260, -0.3352635608502069764 ) ) ;
#7126=DIRECTION ( 'NONE',  ( 1.000000000000000000, 0.000000000000000000, 0.000000000000000000 ) ) ;
#7127=CARTESIAN_POINT ( 'NONE',  ( 25.58980421686700168, -8.350728274839999798, -7.985160199510000112 ) ) ;
#7137=EDGE_CURVE ( 'NONE', #5123, #54862, #38875, .T. ) ;
#7139=CARTESIAN_POINT ( 'NONE',  ( 24.04055935422329782, -12.64665599039150479, 3.439787933675944487 ) ) ;
#7148=EDGE_LOOP ( 'NONE', ( #34568, #37429, #33518 ) ) ;
#7157=CARTESIAN_POINT ( 'NONE',  ( 11.68610928851700237, -11.49703662065999943, -1.632765284408000062 ) ) ;
#7163=CIRCLE ( 'NONE', #10547, 0.6999999999999992895 ) ;
#7173=VERTEX_POINT ( 'NONE', #24856 ) ;
#7176=AXIS2_PLACEMENT_3D ( 'NONE', #19326, #55711, #39629 ) ;
#7183=CARTESIAN_POINT ( 'NONE',  ( 25.46372676430900128, 8.354609436172999892, -8.148458316574000548 ) ) ;
#7188=CARTESIAN_POINT ( 'NONE',  ( 24.46580263708699832, -8.828315330680998940, -8.953816637776000675 ) ) ;
#7189=CARTESIAN_POINT ( 'NONE',  ( 18.29995936595984674, 11.60802783711982400, -4.146429233279109283 ) ) ;
#7192=CARTESIAN_POINT ( 'NONE',  ( 23.56665676678100141, -10.37811504717999966, -9.381458738969000066 ) ) ;
#7194=VERTEX_POINT ( 'NONE', #8435 ) ;
#7199=ADVANCED_FACE ( 'NONE', ( #40251 ), #10430, .T. ) ;
#7209=CARTESIAN_POINT ( 'NONE',  ( 23.91316333561315943, -12.85062081998795058, -3.562165271204711825 ) ) ;
#7211=VERTEX_POINT ( 'NONE', #14710 ) ;
#7225=CARTESIAN_POINT ( 'NONE',  ( 18.30017264560541790, -1.838307226984665865, 11.74271423091507494 ) ) ;
#7232=CARTESIAN_POINT ( 'NONE',  ( 24.03127826811100221, -13.13555942676999955, -3.280046834557000413 ) ) ;
#7233=CIRCLE ( 'NONE', #16153, 1.300165623003000981 ) ;
#7237=CARTESIAN_POINT ( 'NONE',  ( 23.77343974722910502, 13.06033031041715020, -3.746575852910564386 ) ) ;
#7241=CARTESIAN_POINT ( 'NONE',  ( 24.44496351116800170, 3.224881296174999967, 12.03535797436000010 ) ) ;
#7247=CARTESIAN_POINT ( 'NONE',  ( 11.56571517796000137, -12.12283255502000046, -1.989142034170999995 ) ) ;
#7251=CARTESIAN_POINT ( 'NONE',  ( 24.37816192318917174, 3.385901465919856523, 12.24459555508155972 ) ) ;
#7256=CARTESIAN_POINT ( 'NONE',  ( 25.60000000000000142, 11.10814700232000085, 2.976419018679000050 ) ) ;
#7268=CARTESIAN_POINT ( 'NONE',  ( 23.58312295925200175, -10.33205725754000071, 9.361132995946999102 ) ) ;
#7269=DIRECTION ( 'NONE',  ( 0.000000000000000000, 0.9630775622489645693, -0.2692240871329898422 ) ) ;
#7275=CARTESIAN_POINT ( 'NONE',  ( 15.90000000000360991, -3.781197540827905712, -11.56430939782970668 ) ) ;
#7278=CARTESIAN_POINT ( 'NONE',  ( 25.57799048303400014, 2.767957921537000043, -11.23360358486999999 ) ) ;
#7280=CARTESIAN_POINT ( 'NONE',  ( 17.85446786537200126, 3.297647132553999771, 11.83458225989999946 ) ) ;
#7286=CARTESIAN_POINT ( 'NONE',  ( 25.00276452419147333, 3.413701559985177436, -11.76138395131285108 ) ) ;
#7291=CARTESIAN_POINT ( 'NONE',  ( 24.54223752888965748, 12.46060277337064370, 3.023618805785813990 ) ) ;
#7292=AXIS2_PLACEMENT_3D ( 'NONE', #9645, #36922, #58237 ) ;
#7296=CARTESIAN_POINT ( 'NONE',  ( 23.63066751290400092, 3.422883563399000018, 13.57573942691999846 ) ) ;
#7298=VERTEX_POINT ( 'NONE', #24166 ) ;
#7299=CARTESIAN_POINT ( 'NONE',  ( 23.67317744432095949, -9.998263301726394658, 9.464660330969566715 ) ) ;
#7305=CARTESIAN_POINT ( 'NONE',  ( 15.40000000009400161, -8.833277835210999740, -7.896561221812000930 ) ) ;
#7314=ORIENTED_EDGE ( 'NONE', *, *, #47552, .T. ) ;
#7320=CARTESIAN_POINT ( 'NONE',  ( 18.21401021018400002, -11.54142174797000031, 4.213216475886000012 ) ) ;
#7333=CARTESIAN_POINT ( 'NONE',  ( 18.31587707751100069, 3.089759977613000252, -11.98885651319999823 ) ) ;
#7340=ADVANCED_FACE ( 'NONE', ( #16416 ), #40583, .F. ) ;
#7350=VERTEX_POINT ( 'NONE', #68517 ) ;
#7353=DIRECTION ( 'NONE',  ( 0.000000000000000000, 0.2437104050146043921, -0.9698480491745176124 ) ) ;
#7354=CARTESIAN_POINT ( 'NONE',  ( 11.79999999550100220, -3.351258778187000242, 11.15757272551999968 ) ) ;
#7361=CARTESIAN_POINT ( 'NONE',  ( 24.01909549956856793, -9.335994749712794416, -9.253314179451693988 ) ) ;
#7363=CARTESIAN_POINT ( 'NONE',  ( 25.46373185538400463, 11.23406899464000119, 3.161078463958999496 ) ) ;
#7365=B_SPLINE_CURVE_WITH_KNOTS ( 'NONE', 3,
 ( #16723, #5550, #10114, #31445 ),
 .UNSPECIFIED., .F., .F.,
 ( 4, 4 ),
 ( 0.000000000000000000, 1.000000000000000000 ),
 .UNSPECIFIED. ) ;
#7367=CARTESIAN_POINT ( 'NONE',  ( 24.55996189856299949, -12.50738814765000129, 2.996555333579999925 ) ) ;
#7372=B_SPLINE_CURVE_WITH_KNOTS ( 'NONE', 3,
 ( #16329, #37658, #64214, #48499, #11091, #5500 ),
 .UNSPECIFIED., .F., .F.,
 ( 4, 2, 4 ),
 ( 0.000000000000000000, 0.5000000000000000000, 1.000000000000000000 ),
 .UNSPECIFIED. ) ;
#7376=DIRECTION ( 'NONE',  ( -1.000000000000000000, 0.000000000000000000, 0.000000000000000000 ) ) ;
#7379=VERTEX_POINT ( 'NONE', #5242 ) ;
#7381=CARTESIAN_POINT ( 'NONE',  ( 17.68665174764113246, -11.41076566300253425, 4.624016165095039099 ) ) ;
#7395=CARTESIAN_POINT ( 'NONE',  ( 24.79997670811756194, -3.079643851578497848, -11.72208648962189415 ) ) ;
#7403=CARTESIAN_POINT ( 'NONE',  ( 11.26374551471000274, 3.753781600817000186, -11.28122097457000095 ) ) ;
#7406=VERTEX_POINT ( 'NONE', #20986 ) ;
#7408=CARTESIAN_POINT ( 'NONE',  ( 20.00000000000000000, 11.79499999999999993, 0.000000000000000000 ) ) ;
#7420=ORIENTED_EDGE ( 'NONE', *, *, #66623, .T. ) ;
#7422=EDGE_CURVE ( 'NONE', #54502, #28894, #40160, .T. ) ;
#7424=CARTESIAN_POINT ( 'NONE',  ( 24.02031753346800258, -3.259282138741000256, -12.61500720365999939 ) ) ;
#7431=CARTESIAN_POINT ( 'NONE',  ( 15.40000000000000036, -40.50079594190999899, -35.53525775058000136 ) ) ;
#7448=AXIS2_PLACEMENT_3D ( 'NONE', #26036, #31290, #64795 ) ;
#7450=CARTESIAN_POINT ( 'NONE',  ( 11.60578299225600141, 3.447612089971000326, -11.88742905964999963 ) ) ;
#7451=VERTEX_POINT ( 'NONE', #38082 ) ;
#7457=CARTESIAN_POINT ( 'NONE',  ( 11.49999672495000347, 10.14910021683508567, -5.848045769722699738 ) ) ;
#7461=CARTESIAN_POINT ( 'NONE',  ( 25.40241868561099992, 11.40895027791000160, 3.011581611870999708 ) ) ;
#7463=CARTESIAN_POINT ( 'NONE',  ( 24.69847945454000282, -12.37231998179999870, -2.942481676297000082 ) ) ;
#7466=DIRECTION ( 'NONE',  ( 0.000000000000000000, -0.8077502949377767250, 0.5895247755844827964 ) ) ;
#7469=CARTESIAN_POINT ( 'NONE',  ( 13.15534550153200044, 12.11329499872000071, 2.052871598439000245 ) ) ;
#7474=DIRECTION ( 'NONE',  ( 0.000000000000000000, 0.000000000000000000, 1.000000000000000000 ) ) ;
#7475=CARTESIAN_POINT ( 'NONE',  ( 24.98038038036339969, 8.548001386182342287, -8.348258811873629170 ) ) ;
#7477=EDGE_CURVE ( 'NONE', #20699, #5868, #36090, .T. ) ;
#7489=AXIS2_PLACEMENT_3D ( 'NONE', #29115, #3548, #14406 ) ;
#7495=DIRECTION ( 'NONE',  ( 0.000000000000000000, -1.000000000000000000, 0.000000000000000000 ) ) ;
#7496=CARTESIAN_POINT ( 'NONE',  ( 11.71278712779700015, -11.72302084951000190, -1.966028253584000129 ) ) ;
#7509=CARTESIAN_POINT ( 'NONE',  ( 24.87965846251700341, -2.960046916869999656, 11.62351360425999935 ) ) ;
#7511=EDGE_LOOP ( 'NONE', ( #11837, #65314, #18952, #24131 ) ) ;
#7538=FACE_OUTER_BOUND ( 'NONE', #42085, .T. ) ;
#7545=CARTESIAN_POINT ( 'NONE',  ( 23.78804302077149302, -13.03937298471759654, -3.724210977727982819 ) ) ;
#7547=FACE_OUTER_BOUND ( 'NONE', #9975, .T. ) ;
#7555=CONICAL_SURFACE ( 'NONE', #36554, 1.150083888163000223, 0.7854614995501695285 ) ;
#7561=CARTESIAN_POINT ( 'NONE',  ( 16.27289819560299833, 3.403267206945999934, 11.10251878130000058 ) ) ;
#7573=ORIENTED_EDGE ( 'NONE', *, *, #9709, .F. ) ;
#7577=PRESENTATION_STYLE_ASSIGNMENT (( #2676 ) ) ;
#7579=B_SPLINE_CURVE_WITH_KNOTS ( 'NONE', 3,
 ( #45516, #3532, #66826, #51097 ),
 .UNSPECIFIED., .F., .F.,
 ( 4, 4 ),
 ( 0.000000000000000000, 1.000000000000000000 ),
 .UNSPECIFIED. ) ;
#7581=DIRECTION ( 'NONE',  ( 1.000000000000000000, 0.000000000000000000, 0.000000000000000000 ) ) ;
#7584=CARTESIAN_POINT ( 'NONE',  ( 23.85847252464887802, -3.325664090202163248, -13.01555661423517485 ) ) ;
#7591=ORIENTED_EDGE ( 'NONE', *, *, #15083, .F. ) ;
#7592=ADVANCED_FACE ( 'NONE', ( #2675 ), #358, .T. ) ;
#7599=CARTESIAN_POINT ( 'NONE',  ( 24.02995475322400054, 13.13684421285999981, 3.281205399872999973 ) ) ;
#7603=CARTESIAN_POINT ( 'NONE',  ( 17.60000001287599858, 11.53033693765999779, -4.891431908114999949 ) ) ;
#7619=ORIENTED_EDGE ( 'NONE', *, *, #25356, .T. ) ;
#7622=CARTESIAN_POINT ( 'NONE',  ( 23.89320776801300283, -2.594336453560998734, 11.06325219636999435 ) ) ;
#7625=CARTESIAN_POINT ( 'NONE',  ( 17.88701341325399952, 3.642483061606999861, 12.02409215997000125 ) ) ;
#7638=B_SPLINE_CURVE_WITH_KNOTS ( 'NONE', 3,
 ( #6434, #48752, #6092, #6784, #44216, #17982, #65511, #37912 ),
 .UNSPECIFIED., .F., .F.,
 ( 4, 2, 2, 4 ),
 ( 0.000000000000000000, 0.2500000000000000000, 0.5000000000000000000, 1.000000000000000000 ),
 .UNSPECIFIED. ) ;
#7652=DIRECTION ( 'NONE',  ( 0.000000000000000000, 0.000000000000000000, -1.000000000000000000 ) ) ;
#7659=ORIENTED_EDGE ( 'NONE', *, *, #18538, .F. ) ;
#7661=AXIS2_PLACEMENT_3D ( 'NONE', #52698, #35349, #26482 ) ;
#7664=CARTESIAN_POINT ( 'NONE',  ( 25.39991507554827521, -8.680020025995577981, 7.390263434114647367 ) ) ;
#7671=CARTESIAN_POINT ( 'NONE',  ( 18.36455407565900089, -12.06439799272000002, 3.505004330567000004 ) ) ;
#7681=CIRCLE ( 'NONE', #64599, 0.6999999999999992895 ) ;
#7683=DIRECTION ( 'NONE',  ( 0.000000000000000000, 2.692747184616903860E-07, -0.9999999999999636957 ) ) ;
#7685=CARTESIAN_POINT ( 'NONE',  ( 23.61357289147300165, -3.134997397370999916, 13.53670803788000043 ) ) ;
#7688=CARTESIAN_POINT ( 'NONE',  ( 18.40156003475500057, 3.148349829928000165, -12.06792178657999948 ) ) ;
#7697=B_SPLINE_CURVE_WITH_KNOTS ( 'NONE', 3,
 ( #5283, #53532, #64341, #26965, #16458, #10190, #53186, #15778, #22044, #5967, #57731, #47256, #27305, #68910, #20681, #31187, #58087, #732, #15093, #36417, #42012, #15441, #36766, #52842, #4937, #26277 ),
 .UNSPECIFIED., .F., .F.,
 ( 4, 2, 2, 2, 2, 2, 2, 2, 2, 2, 2, 2, 4 ),
 ( 0.000000000000000000, 0.06249999999999739098, 0.09374999999999711342, 0.1249999999999968359, 0.2499999999999964473, 0.3749999999999960032, 0.4999999999999955591, 0.6249999999999951150, 0.7499999999999946709, 0.8124999999999942268, 0.8437499999999948930, 0.8749999999999954481, 1.000000000000000000 ),
 .UNSPECIFIED. ) ;
#7708=DIRECTION ( 'NONE',  ( 1.000000000000000000, 0.000000000000000000, 0.000000000000000000 ) ) ;
#7713=ORIENTED_EDGE ( 'NONE', *, *, #24719, .F. ) ;
#7715=CARTESIAN_POINT ( 'NONE',  ( 12.71442162208154691, 11.86191914805647230, -3.298674357357656906 ) ) ;
#7717=CARTESIAN_POINT ( 'NONE',  ( 18.29999330150736014, 11.02846243710159868, -3.754394858750199848 ) ) ;
#7718=CARTESIAN_POINT ( 'NONE',  ( 24.50399615207700066, -12.34862307763000011, 3.085465605386000121 ) ) ;
#7723=ORIENTED_EDGE ( 'NONE', *, *, #10751, .F. ) ;
#7735=CARTESIAN_POINT ( 'NONE',  ( 18.30003129332100187, -2.732683818840999646, -11.53064095373000164 ) ) ;
#7740=EDGE_CURVE ( 'NONE', #59934, #60441, #26647, .T. ) ;
#7743=EDGE_CURVE ( 'NONE', #20902, #37580, #30624, .T. ) ;
#7748=ORIENTED_EDGE ( 'NONE', *, *, #51855, .T. ) ;
#7749=CARTESIAN_POINT ( 'NONE',  ( 24.66908130708416635, -3.147928273865472804, -11.83338230875681418 ) ) ;
#7756=FACE_OUTER_BOUND ( 'NONE', #37370, .T. ) ;
#7769=ORIENTED_EDGE ( 'NONE', *, *, #41995, .F. ) ;
#7773=ORIENTED_EDGE ( 'NONE', *, *, #43227, .F. ) ;
#7777=CARTESIAN_POINT ( 'NONE',  ( 23.54916697122300207, -2.964289671590000008, -13.72170765701000050 ) ) ;
#7792=CARTESIAN_POINT ( 'NONE',  ( 23.59396203638712919, -13.38681815648950035, 4.024094169786141428 ) ) ;
#7796=EDGE_CURVE ( 'NONE', #56866, #54214, #22528, .T. ) ;
#7803=ORIENTED_EDGE ( 'NONE', *, *, #65075, .F. ) ;
#7809=CARTESIAN_POINT ( 'NONE',  ( 11.79999999771000141, -3.595163221087000149, 11.99793848941000007 ) ) ;
#7813=CARTESIAN_POINT ( 'NONE',  ( 29.60000000000000142, 0.000000000000000000, 0.000000000000000000 ) ) ;
#7815=CARTESIAN_POINT ( 'NONE',  ( 24.95408811465000198, -12.04589448677999997, -2.875991317726000140 ) ) ;
#7817=DIRECTION ( 'NONE',  ( 0.000000000000000000, -0.2588190451024932059, 0.9659258262890756397 ) ) ;
#7821=FACE_OUTER_BOUND ( 'NONE', #67419, .T. ) ;
#7825=CARTESIAN_POINT ( 'NONE',  ( 13.60156003475500164, 12.26415473033000048, 2.266572665737999870 ) ) ;
#7827=EDGE_CURVE ( 'NONE', #28283, #9687, #10042, .T. ) ;
#7847=ORIENTED_EDGE ( 'NONE', *, *, #41512, .F. ) ;
#7853=FACE_OUTER_BOUND ( 'NONE', #14405, .T. ) ;
#7867=ORIENTED_EDGE ( 'NONE', *, *, #49435, .F. ) ;
#7870=FACE_OUTER_BOUND ( 'NONE', #46432, .T. ) ;
#7874=CARTESIAN_POINT ( 'NONE',  ( 18.44720874474599981, -2.702894824448000222, -11.38760777189999907 ) ) ;
#7875=CONICAL_SURFACE ( 'NONE', #64787, 11.75015521449999945, 0.7854113701714536822 ) ;
#7877=CARTESIAN_POINT ( 'NONE',  ( 16.39999997324030190, 3.261216865579172008, 11.32142606715090061 ) ) ;
#7887=ORIENTED_EDGE ( 'NONE', *, *, #62507, .T. ) ;
#7891=CARTESIAN_POINT ( 'NONE',  ( 25.60000000000000142, 0.000000000000000000, 0.000000000000000000 ) ) ;
#7893=CARTESIAN_POINT ( 'NONE',  ( 25.60000000000000142, -9.899494936611999307, -9.899494936611999307 ) ) ;
#7899=CARTESIAN_POINT ( 'NONE',  ( 23.59999445750599989, -13.22316420035999940, -4.267800004853000040 ) ) ;
#7900=CARTESIAN_POINT ( 'NONE',  ( 24.40628504395400000, 3.359328441570999857, -12.19433831731000062 ) ) ;
#7915=CARTESIAN_POINT ( 'NONE',  ( 15.86018463513499910, 3.716003765078999876, 11.29289727949000088 ) ) ;
#7922=CARTESIAN_POINT ( 'NONE',  ( 24.96666885033332761, 2.078227436549349605, -11.31065739565387496 ) ) ;
#7923=CARTESIAN_POINT ( 'NONE',  ( 18.05828166255871636, -3.296090596061253652, 11.87625419658844805 ) ) ;
#7924=ORIENTED_EDGE ( 'NONE', *, *, #58830, .T. ) ;
#7926=CARTESIAN_POINT ( 'NONE',  ( 23.83637917632099956, -13.03948500899999985, -3.620862819564000468 ) ) ;
#7930=VERTEX_POINT ( 'NONE', #11013 ) ;
#7931=CARTESIAN_POINT ( 'NONE',  ( 25.29995422340600086, 2.596935224161999844, 11.35301931920000129 ) ) ;
#7932=EDGE_CURVE ( 'NONE', #7930, #36190, #11003, .T. ) ;
#7935=CARTESIAN_POINT ( 'NONE',  ( 24.00938379501951658, -3.345592699034538153, -12.72992676416136604 ) ) ;
#7936=CARTESIAN_POINT ( 'NONE',  ( 11.49978667957999967, -12.43119799159999950, -1.530013559959999991 ) ) ;
#7939=ORIENTED_EDGE ( 'NONE', *, *, #30558, .T. ) ;
#7953=B_SPLINE_CURVE_WITH_KNOTS ( 'NONE', 3,
 ( #2831, #29428, #55979, #38868, #33968, #1803 ),
 .UNSPECIFIED., .F., .F.,
 ( 4, 2, 4 ),
 ( 0.000000000000000000, 0.5000000000000000000, 1.000000000000000000 ),
 .UNSPECIFIED. ) ;
#7959=DIRECTION ( 'NONE',  ( -1.000000000000000000, 0.000000000000000000, 0.000000000000000000 ) ) ;
#7964=CARTESIAN_POINT ( 'NONE',  ( 17.79999999998900151, 3.595165934733000057, 11.99793354950999991 ) ) ;
#7968=VERTEX_POINT ( 'NONE', #28484 ) ;
#7971=EDGE_CURVE ( 'NONE', #31995, #38535, #33336, .T. ) ;
#7980=ORIENTED_EDGE ( 'NONE', *, *, #18573, .F. ) ;
#7988=FACE_OUTER_BOUND ( 'NONE', #25873, .T. ) ;
#7996=DIRECTION ( 'NONE',  ( 0.000000000000000000, 0.7614089499631907509, -0.6482718649732928107 ) ) ;
#7999=CARTESIAN_POINT ( 'NONE',  ( 16.10005255078199937, -3.632778330393000132, -11.06917548872000090 ) ) ;
#8017=FACE_OUTER_BOUND ( 'NONE', #6043, .T. ) ;
#8030=CARTESIAN_POINT ( 'NONE',  ( 24.25970375843899873, -3.166447075414999812, 12.13786225095999960 ) ) ;
#8045=B_SPLINE_CURVE_WITH_KNOTS ( 'NONE', 3,
 ( #62879, #68125, #2198, #50426 ),
 .UNSPECIFIED., .F., .F.,
 ( 4, 4 ),
 ( 0.000000000000000000, 1.000000000000000000 ),
 .UNSPECIFIED. ) ;
#8048=CARTESIAN_POINT ( 'NONE',  ( 25.25798339014900051, 8.562781525512001224, 7.910461493226999430 ) ) ;
#8059=VECTOR ( 'NONE', #29857, 1000.000000000000114 ) ;
#8061=DIRECTION ( 'NONE',  ( 0.000000000000000000, -1.000000000000000000, 0.000000000000000000 ) ) ;
#8064=CARTESIAN_POINT ( 'NONE',  ( 24.41456973747800063, -12.00390065690999997, 3.256048965932000439 ) ) ;
#8066=CARTESIAN_POINT ( 'NONE',  ( 44.24148000000000280, 11.77655473258999841, -4.190794510628000680 ) ) ;
#8067=DIRECTION ( 'NONE',  ( -8.953094821931283005E-11, 0.9867385579967302700, 0.1623176458754050089 ) ) ;
#8069=ORIENTED_EDGE ( 'NONE', *, *, #30622, .F. ) ;
#8077=ORIENTED_EDGE ( 'NONE', *, *, #34512, .T. ) ;
#8080=DIRECTION ( 'NONE',  ( 0.000000000000000000, -0.1807154286440004198, -0.9835354258236025382 ) ) ;
#8093=ORIENTED_EDGE ( 'NONE', *, *, #5814, .F. ) ;
#8094=DIRECTION ( 'NONE',  ( 1.267684193041221762E-20, 0.9999999999999997780, 2.657887364712999055E-08 ) ) ;
#8103=EDGE_CURVE ( 'NONE', #20902, #16735, #66763, .T. ) ;
#8106=CARTESIAN_POINT ( 'NONE',  ( 25.29987667925500361, 11.77655473258999841, 4.190794510628000680 ) ) ;
#8107=ORIENTED_EDGE ( 'NONE', *, *, #41759, .T. ) ;
#8111=CARTESIAN_POINT ( 'NONE',  ( 24.63610587989722234, 8.692490458917935925, 8.668794396725420626 ) ) ;
#8116=VERTEX_POINT ( 'NONE', #17909 ) ;
#8121=DIRECTION ( 'NONE',  ( 0.000000000000000000, -0.9659258262890757507, -0.2588190451024934835 ) ) ;
#8122=CARTESIAN_POINT ( 'NONE',  ( 24.21979545967400327, -3.760914022703000459, -12.77961884926999936 ) ) ;
#8124=AXIS2_PLACEMENT_3D ( 'NONE', #66391, #43700, #34602 ) ;
#8126=CARTESIAN_POINT ( 'NONE',  ( 24.44496488009700030, 8.810487470433001178, 8.810507756548000557 ) ) ;
#8133=EDGE_CURVE ( 'NONE', #36015, #38805, #31140, .T. ) ;
#8137=CARTESIAN_POINT ( 'NONE',  ( 16.04504292973000190, -8.364028678926000993, -8.186631590245999845 ) ) ;
#8139=CARTESIAN_POINT ( 'NONE',  ( 23.64971691489271421, -13.39987426919188707, 3.835034287296173350 ) ) ;
#8141=DIRECTION ( 'NONE',  ( 0.000000000000000000, -0.9466492601157001641, 0.3222656952305000266 ) ) ;
#8148=ADVANCED_FACE ( 'NONE', ( #34342 ), #65785, .T. ) ;
#8150=AXIS2_PLACEMENT_3D ( 'NONE', #53023, #921, #42534 ) ;
#8157=CONICAL_SURFACE ( 'NONE', #68420, 12.42515511468000078, 0.7854106315584118425 ) ;
#8161=ORIENTED_EDGE ( 'NONE', *, *, #15940, .F. ) ;
#8164=CARTESIAN_POINT ( 'NONE',  ( 13.70003001321900271, 9.668726926528000476, 7.961868161445000425 ) ) ;
#8165=CARTESIAN_POINT ( 'NONE',  ( 20.00000000000000000, 0.000000000000000000, 0.000000000000000000 ) ) ;
#8166=CARTESIAN_POINT ( 'NONE',  ( 24.74439240416100105, -8.626915347824999358, -8.720184348590999335 ) ) ;
#8167=CARTESIAN_POINT ( 'NONE',  ( 17.60000000000000142, -11.23412379136000006, 3.084957477885999833 ) ) ;
#8169=AXIS2_PLACEMENT_3D ( 'NONE', #29257, #39048, #2326 ) ;
#8173=EDGE_LOOP ( 'NONE', ( #26537, #34674, #40491, #36390 ) ) ;
#8175=CARTESIAN_POINT ( 'NONE',  ( 25.26126129534557307, 2.660454058625374874, 11.37585472950963883 ) ) ;
#8177=CARTESIAN_POINT ( 'NONE',  ( 24.60115027442303770, 8.755275597086985329, -9.042371280549295065 ) ) ;
#8183=CARTESIAN_POINT ( 'NONE',  ( 24.30000000000000071, -12.03537377768999939, 3.224868684338999980 ) ) ;
#8184=CARTESIAN_POINT ( 'NONE',  ( 25.60000000000000142, -8.527654132749999505, 7.260537518967999482 ) ) ;
#8195=CARTESIAN_POINT ( 'NONE',  ( 24.40777907822999993, -12.23846661367000088, -3.187421709680999804 ) ) ;
#8203=AXIS2_PLACEMENT_3D ( 'NONE', #40802, #35571, #50954 ) ;
#8208=ORIENTED_EDGE ( 'NONE', *, *, #51566, .F. ) ;
#8216=CARTESIAN_POINT ( 'NONE',  ( 24.22085326866800159, 9.185890470428999421, -9.646242683205999313 ) ) ;
#8217=CARTESIAN_POINT ( 'NONE',  ( 18.40429364930200151, -2.938801558760000265, -11.32979830910000096 ) ) ;
#8238=VERTEX_POINT ( 'NONE', #41295 ) ;
#8241=CARTESIAN_POINT ( 'NONE',  ( 23.71889146657003167, -13.13858983292066718, -3.830114772933163270 ) ) ;
#8242=CARTESIAN_POINT ( 'NONE',  ( 24.35145719007200071, 3.377064811435000369, -12.26055847765000095 ) ) ;
#8244=ORIENTED_EDGE ( 'NONE', *, *, #20066, .T. ) ;
#8259=CARTESIAN_POINT ( 'NONE',  ( 24.32156006308829888, -9.044158311594529209, -9.474452558964053139 ) ) ;
#8262=CARTESIAN_POINT ( 'NONE',  ( 25.29987654162099986, 8.533547811387000692, 7.925584028117998336 ) ) ;
#8265=CARTESIAN_POINT ( 'NONE',  ( 23.61806551351500261, -13.16805540424999954, -4.269441848944000029 ) ) ;
#8267=( LENGTH_UNIT ( ) NAMED_UNIT ( * ) SI_UNIT ( .MILLI., .METRE. ) );
#8271=VERTEX_POINT ( 'NONE', #57704 ) ;
#8272=CARTESIAN_POINT ( 'NONE',  ( 25.46371819568200223, 2.879482785682999868, 11.30954024936000124 ) ) ;
#8273=AXIS2_PLACEMENT_3D ( 'NONE', #35603, #15299, #10388 ) ;
#8288=DIRECTION ( 'NONE',  ( -1.000000000000000000, 0.000000000000000000, 0.000000000000000000 ) ) ;
#8293=CARTESIAN_POINT ( 'NONE',  ( 23.55066246010500208, 13.34856924552999935, 4.338579446700999931 ) ) ;
#8324=B_SPLINE_CURVE_WITH_KNOTS ( 'NONE', 3,
 ( #50629, #28978, #55877, #39798 ),
 .UNSPECIFIED., .F., .F.,
 ( 4, 4 ),
 ( 0.000000000000000000, 1.000000000000000000 ),
 .UNSPECIFIED. ) ;
#8326=CARTESIAN_POINT ( 'NONE',  ( 24.84574153431059429, 3.513914038403941564, -11.93620105921934638 ) ) ;
#8331=CARTESIAN_POINT ( 'NONE',  ( 11.55259020248000112, -3.617313325735000085, 11.93403632987999963 ) ) ;
#8339=CARTESIAN_POINT ( 'NONE',  ( 19.39373726536100051, 0.000000000000000000, 0.000000000000000000 ) ) ;
#8341=CARTESIAN_POINT ( 'NONE',  ( 16.13140881196668630, -3.487052973475988527, -11.11602635788098148 ) ) ;
#8342=EDGE_LOOP ( 'NONE', ( #53348, #49608, #5197, #35275 ) ) ;
#8350=EDGE_LOOP ( 'NONE', ( #35809, #43896, #34833, #30574 ) ) ;
#8352=AXIS2_PLACEMENT_3D ( 'NONE', #15701, #26541, #65221 ) ;
#8354=CARTESIAN_POINT ( 'NONE',  ( 24.13560165115514167, 9.160542504100666505, 9.132857127789494101 ) ) ;
#8355=ORIENTED_EDGE ( 'NONE', *, *, #38511, .F. ) ;
#8356=B_SPLINE_SURFACE_WITH_KNOTS ( 'NONE', 3, 3, ( 
 ( #53046, #5829, #69117, #48488 ),
 ( #31381, #21225, #5141, #64892 ),
 ( #48144, #59315, #32416, #594 ),
 ( #58979, #37305, #32076, #15977 ),
 ( #53730, #27166, #10730, #26478 ),
 ( #21903, #63525, #26132, #10043 ),
 ( #54070, #31725, #43242, #247 ),
 ( #21561, #16663, #64549, #64204 ),
 ( #4790, #17006, #37988, #47458 ) ),
 .UNSPECIFIED., .F., .F., .F.,
 ( 4, 1, 1, 1, 1, 1, 4 ),
 ( 4, 4 ),
 ( 0.05136528901824000126, 0.1666666666667000196, 0.3333333333333000081, 0.5000000000000000000, 0.6666666666667000474, 0.8333333333333000637, 0.9784615765758000183 ),
 ( -0.1917159053268999991, 1.191863452461999984 ),
 .UNSPECIFIED. ) ;
#8361=CARTESIAN_POINT ( 'NONE',  ( 17.79046541331000242, -3.643254180937999909, -12.02383733079000017 ) ) ;
#8370=DIRECTION ( 'NONE',  ( 0.000000000000000000, -0.7071067811865475727, 0.7071067811865475727 ) ) ;
#8376=CARTESIAN_POINT ( 'NONE',  ( 24.57034142978699975, -3.716692469271000387, 12.37044818449999894 ) ) ;
#8377=CARTESIAN_POINT ( 'NONE',  ( 13.00000000009400303, 11.69118001589999878, 1.923222888683999932 ) ) ;
#8398=CARTESIAN_POINT ( 'NONE',  ( 24.57709918591382348, 11.91258060227069393, 3.191967924368984466 ) ) ;
#8402=B_SPLINE_CURVE_WITH_KNOTS ( 'NONE', 3,
 ( #42952, #11134, #5879, #48544, #43994, #21960 ),
 .UNSPECIFIED., .F., .F.,
 ( 4, 2, 4 ),
 ( 0.000000000000000000, 0.5000000000000000000, 1.000000000000000000 ),
 .UNSPECIFIED. ) ;
#8406=CARTESIAN_POINT ( 'NONE',  ( 25.00270149670823017, 11.89258197074110335, 2.924337394597763318 ) ) ;
#8408=CARTESIAN_POINT ( 'NONE',  ( 13.56683625432869178, 9.108504156368613991, 7.475700167246387196 ) ) ;
#8416=CARTESIAN_POINT ( 'NONE',  ( 13.49999720188825769, -11.61513859405366844, -2.353594668653351096 ) ) ;
#8420=ORIENTED_EDGE ( 'NONE', *, *, #31889, .F. ) ;
#8428=CARTESIAN_POINT ( 'NONE',  ( 18.29995268966800026, -2.861739928647000220, -11.98821236628000086 ) ) ;
#8430=CARTESIAN_POINT ( 'NONE',  ( 15.96663596566263976, -3.844870426479619852, -11.78010250471071174 ) ) ;
#8435=CARTESIAN_POINT ( 'NONE',  ( 25.59997324745700098, -8.218963665681000563, -8.043524865771999544 ) ) ;
#8438=CARTESIAN_POINT ( 'NONE',  ( 24.74122145672611239, -3.111613011112996041, -11.77168806187908778 ) ) ;
#8443=FACE_BOUND ( 'NONE', #4996, .T. ) ;
#8447=CARTESIAN_POINT ( 'NONE',  ( 24.30001683613300045, -12.21047198529999989, -3.271805531187999883 ) ) ;
#8453=STYLED_ITEM ( 'NONE', ( #7577 ), #6570 ) ;
#8464=ORIENTED_EDGE ( 'NONE', *, *, #18006, .F. ) ;
#8465=DIRECTION ( 'NONE',  ( -1.000000000000000000, 0.000000000000000000, 0.000000000000000000 ) ) ;
#8467=EDGE_CURVE ( 'NONE', #2511, #28950, #17738, .T. ) ;
#8472=CARTESIAN_POINT ( 'NONE',  ( 23.59999441188499958, 10.30760541648000128, -9.317696302454001156 ) ) ;
#8483=CARTESIAN_POINT ( 'NONE',  ( 23.56669596105687248, -13.32134171675407686, 4.273005797680200502 ) ) ;
#8491=CARTESIAN_POINT ( 'NONE',  ( 13.50018479229797386, 9.763984779744731668, 6.782114604289404269 ) ) ;
#8495=FACE_OUTER_BOUND ( 'NONE', #53902, .T. ) ;
#8505=CARTESIAN_POINT ( 'NONE',  ( 23.60000000000000142, -9.517611874540000017, -8.103398312166000039 ) ) ;
#8506=CARTESIAN_POINT ( 'NONE',  ( 23.58937261997547807, 13.38214254373811407, 4.047428957154697748 ) ) ;
#8508=DIRECTION ( 'NONE',  ( 1.000000000000000000, 0.000000000000000000, 0.000000000000000000 ) ) ;
#8515=ORIENTED_EDGE ( 'NONE', *, *, #3228, .T. ) ;
#8517=CARTESIAN_POINT ( 'NONE',  ( 24.89161351175072312, 3.022277498610428825, 11.64684786725776533 ) ) ;
#8521=ADVANCED_BREP_SHAPE_REPRESENTATION ( '', ( #6570, #9676 ), #42081 ) ;
#8524=ORIENTED_EDGE ( 'NONE', *, *, #13444, .F. ) ;
#8526=ADVANCED_FACE ( 'NONE', ( #47061 ), #55666, .T. ) ;
#8535=CARTESIAN_POINT ( 'NONE',  ( 16.09999335515345464, 3.810015139075933366, 11.93171563566236948 ) ) ;
#8542=B_SPLINE_CURVE_WITH_KNOTS ( 'NONE', 3,
 ( #51291, #67355, #34193, #45368 ),
 .UNSPECIFIED., .F., .F.,
 ( 4, 4 ),
 ( 0.000000000000000000, 1.000000000000000000 ),
 .UNSPECIFIED. ) ;
#8547=EDGE_CURVE ( 'NONE', #37826, #13082, #22111, .T. ) ;
#8556=CARTESIAN_POINT ( 'NONE',  ( 25.08237298766499990, 8.543494775977999112, -8.158987811473000562 ) ) ;
#8557=B_SPLINE_CURVE_WITH_KNOTS ( 'NONE', 3,
 ( #7062, #18251, #65437, #60208 ),
 .UNSPECIFIED., .F., .F.,
 ( 4, 4 ),
 ( 0.000000000000000000, 1.000000000000000000 ),
 .UNSPECIFIED. ) ;
#8558=CARTESIAN_POINT ( 'NONE',  ( 25.27000123253231223, -3.169726888505174145, -11.48329030453897914 ) ) ;
#8563=VERTEX_POINT ( 'NONE', #14898 ) ;
#8566=CARTESIAN_POINT ( 'NONE',  ( 23.60205915885299888, -11.56239291746998710, -3.974820703396001242 ) ) ;
#8569=CARTESIAN_POINT ( 'NONE',  ( 25.59994555223599733, -2.024003533649000097, 11.01554633311000053 ) ) ;
#8571=FACE_OUTER_BOUND ( 'NONE', #17035, .T. ) ;
#8582=LINE ( 'NONE', #25003, #31240 ) ;
#8584=ORIENTED_EDGE ( 'NONE', *, *, #23148, .T. ) ;
#8588=CARTESIAN_POINT ( 'NONE',  ( 13.09162860438300058, -11.49399796109000071, -1.653788228654999859 ) ) ;
#8592=AXIS2_PLACEMENT_3D ( 'NONE', #19642, #8465, #50773 ) ;
#8608=EDGE_CURVE ( 'NONE', #45386, #855, #19954, .T. ) ;
#8614=VERTEX_POINT ( 'NONE', #14052 ) ;
#8617=CARTESIAN_POINT ( 'NONE',  ( 24.14104189581271953, -3.327735444545656840, -12.48993067524683021 ) ) ;
#8626=CYLINDRICAL_SURFACE ( 'NONE', #22189, 12.52500000000000036 ) ;
#8629=EDGE_CURVE ( 'NONE', #45182, #48412, #14395, .T. ) ;
#8631=DIRECTION ( 'NONE',  ( 2.186520856378935359E-10, -0.9979498542811711115, 0.06400069015400811079 ) ) ;
#8632=CARTESIAN_POINT ( 'NONE',  ( 23.62001755077699983, 13.19613008251999986, 4.178531453471999946 ) ) ;
#8636=CARTESIAN_POINT ( 'NONE',  ( 15.72310803393400036, 9.201544169428000686, 8.280720087647999605 ) ) ;
#8639=CARTESIAN_POINT ( 'NONE',  ( 17.80000000005199823, -3.345268251980999974, 11.86064071431999878 ) ) ;
#8645=CARTESIAN_POINT ( 'NONE',  ( 24.66271477989500127, 3.625397779087000227, 12.20587930303000057 ) ) ;
#8647=CARTESIAN_POINT ( 'NONE',  ( 23.50387503050299998, 0.01709925755191780278, -13.79998940635069005 ) ) ;
#8649=CARTESIAN_POINT ( 'NONE',  ( 23.74238067972500232, 9.838688633414999885, 9.383767474846001377 ) ) ;
#8650=EDGE_LOOP ( 'NONE', ( #1762, #68053, #10448, #45691 ) ) ;
#8671=CARTESIAN_POINT ( 'NONE',  ( 11.84748603848200155, -3.299681227315999887, 11.83395064283000053 ) ) ;
#8685=CARTESIAN_POINT ( 'NONE',  ( 18.50001572531400029, 2.908166856580999937, -12.18270046149000052 ) ) ;
#8687=AXIS2_PLACEMENT_3D ( 'NONE', #67329, #52293, #4388 ) ;
#8697=DIRECTION ( 'NONE',  ( -0.9486832980505238710, -8.389522287884208957E-10, 0.3162277660168079652 ) ) ;
#8698=ORIENTED_EDGE ( 'NONE', *, *, #28343, .F. ) ;
#8701=CONICAL_SURFACE ( 'NONE', #28830, 8.515178490300000291, 1.329165865441747751 ) ;
#8703=CARTESIAN_POINT ( 'NONE',  ( 14.46666666253433498, 8.815232490335741744, 7.616703758276837988 ) ) ;
#8704=CARTESIAN_POINT ( 'NONE',  ( 18.44718133169100227, -2.901187496916000086, -12.12896678136999995 ) ) ;
#8705=CARTESIAN_POINT ( 'NONE',  ( 24.61098151485200347, -8.751788807863999153, 9.056922189874999418 ) ) ;
#8709=CARTESIAN_POINT ( 'NONE',  ( 24.30000000000000071, 9.305479840184000651, -8.315530346521999405 ) ) ;
#8710=ORIENTED_EDGE ( 'NONE', *, *, #65643, .F. ) ;
#8739=CARTESIAN_POINT ( 'NONE',  ( 24.72252720687009386, 11.76897357382126685, 3.190821958176780715 ) ) ;
#8750=CARTESIAN_POINT ( 'NONE',  ( 16.10004050617000004, 3.886235259787000018, 11.90683839252000098 ) ) ;
#8751=AXIS2_PLACEMENT_3D ( 'NONE', #35731, #56022, #9149 ) ;
#8752=CARTESIAN_POINT ( 'NONE',  ( 16.10006098462790902, 8.380959734829373176, 8.092216891312055793 ) ) ;
#8753=DIRECTION ( 'NONE',  ( -1.000000000000000000, 0.000000000000000000, 0.000000000000000000 ) ) ;
#8759=CARTESIAN_POINT ( 'NONE',  ( 24.72252701717521006, -8.647819769236338772, 8.596819301983423145 ) ) ;
#8761=AXIS2_PLACEMENT_3D ( 'NONE', #13693, #54954, #45842 ) ;
#8773=DIRECTION ( 'NONE',  ( 1.000000000000000000, 0.000000000000000000, 0.000000000000000000 ) ) ;
#8776=EDGE_LOOP ( 'NONE', ( #37083, #19165, #53632, #41820 ) ) ;
#8797=EDGE_CURVE ( 'NONE', #55894, #34904, #44111, .T. ) ;
#8823=CARTESIAN_POINT ( 'NONE',  ( 23.60648250789430236, -13.39605720553294432, 3.969101063526361273 ) ) ;
#8829=ADVANCED_FACE ( 'NONE', ( #64591 ), #16565, .T. ) ;
#8842=FACE_OUTER_BOUND ( 'NONE', #25375, .T. ) ;
#8851=DIRECTION ( 'NONE',  ( -1.000000000000000000, 0.000000000000000000, 0.000000000000000000 ) ) ;
#8875=( NAMED_UNIT ( * ) PLANE_ANGLE_UNIT ( ) SI_UNIT ( $, .RADIAN. ) );
#8877=EDGE_LOOP ( 'NONE', ( #53539, #16072, #61479, #31907 ) ) ;
#8898=CARTESIAN_POINT ( 'NONE',  ( 25.40238653257500090, 8.312591668607000273, -8.374698588276999089 ) ) ;
#8899=FACE_OUTER_BOUND ( 'NONE', #44955, .T. ) ;
#8900=CARTESIAN_POINT ( 'NONE',  ( 18.23887202961200060, -3.252214874110999965, -11.14733497513999971 ) ) ;
#8910=CARTESIAN_POINT ( 'NONE',  ( 11.79999998400527517, 11.58088844914904314, 1.772255231651886254 ) ) ;
#8915=AXIS2_PLACEMENT_3D ( 'NONE', #52599, #20443, #48048 ) ;
#8916=CARTESIAN_POINT ( 'NONE',  ( 16.09999335515346885, -3.810015139062473466, -11.93171563566676419 ) ) ;
#8925=CARTESIAN_POINT ( 'NONE',  ( 24.44916829770000177, 3.519946668155999880, -12.30317708153000034 ) ) ;
#8932=CARTESIAN_POINT ( 'NONE',  ( 13.38404792230800133, -11.55332361678999931, -1.871151989399000071 ) ) ;
#8953=VERTEX_POINT ( 'NONE', #44679 ) ;
#8954=CARTESIAN_POINT ( 'NONE',  ( 23.80818184942661730, 13.01048713944770441, -3.693375169791979662 ) ) ;
#8966=FACE_OUTER_BOUND ( 'NONE', #23300, .T. ) ;
#8969=DIRECTION ( 'NONE',  ( 2.887772199312943602E-10, -0.4812251768484908099, -0.8765970164032835799 ) ) ;
#8971=CARTESIAN_POINT ( 'NONE',  ( 23.62925782967800004, 13.46920268230999973, 3.826620036219000376 ) ) ;
#8979=CARTESIAN_POINT ( 'NONE',  ( 24.35365242081699932, -1.906711579079999552, -11.36048031428999572 ) ) ;
#8981=CARTESIAN_POINT ( 'NONE',  ( 24.78226685285000386, -12.26744358842999993, 2.911641580551999731 ) ) ;
#8984=CARTESIAN_POINT ( 'NONE',  ( 24.31006797060300073, 3.215953369236999926, 12.14991815011999954 ) ) ;
#8986=CARTESIAN_POINT ( 'NONE',  ( 23.58473471199800287, 10.19686565968999936, 9.579920953980000320 ) ) ;
#8989=EDGE_CURVE ( 'NONE', #15838, #35693, #44333, .T. ) ;
#8992=PLANE ( 'NONE',  #42346 ) ;
#9002=CARTESIAN_POINT ( 'NONE',  ( 17.60000000000000142, -10.78295181803999903, 4.410266442048000002 ) ) ;
#9005=CARTESIAN_POINT ( 'NONE',  ( 11.56599877858000092, -3.774257655232999831, 11.98333518513999962 ) ) ;
#9018=ORIENTED_EDGE ( 'NONE', *, *, #60871, .F. ) ;
#9026=ORIENTED_EDGE ( 'NONE', *, *, #63603, .T. ) ;
#9027=DIRECTION ( 'NONE',  ( 2.888706471568024494E-10, -0.06432770287657048336, -0.9979288284455077873 ) ) ;
#9035=CARTESIAN_POINT ( 'NONE',  ( 17.61265229197699966, -11.81477306456000065, 3.322807805102999890 ) ) ;
#9036=CARTESIAN_POINT ( 'NONE',  ( 24.53002386606399909, -8.771528676250001766, 8.897041952682000598 ) ) ;
#9077=CARTESIAN_POINT ( 'NONE',  ( 24.54174074856956267, 8.849271461504201852, 9.279828214275216425 ) ) ;
#9082=CARTESIAN_POINT ( 'NONE',  ( 12.37336427446297016, 11.82897199538926358, -3.432444870274659277 ) ) ;
#9084=CARTESIAN_POINT ( 'NONE',  ( 13.99955778315600163, -9.394084143528001363, -8.201088258230999628 ) ) ;
#9086=CARTESIAN_POINT ( 'NONE',  ( 15.89979320885400327, 3.824231472901999496, 11.71686814605000038 ) ) ;
#9089=CARTESIAN_POINT ( 'NONE',  ( 24.95277496327178213, -11.53322809624908274, 3.220796833695926953 ) ) ;
#9094=FACE_OUTER_BOUND ( 'NONE', #31983, .T. ) ;
#9106=CARTESIAN_POINT ( 'NONE',  ( 18.26079396959535828, 3.428468831596959365, -12.04667397462516298 ) ) ;
#9131=B_SPLINE_CURVE_WITH_KNOTS ( 'NONE', 3,
 ( #62558, #35998, #52417, #62897 ),
 .UNSPECIFIED., .F., .F.,
 ( 4, 4 ),
 ( 0.000000000000000000, 1.000000000000000000 ),
 .UNSPECIFIED. ) ;
#9140=ORIENTED_EDGE ( 'NONE', *, *, #41706, .F. ) ;
#9149=DIRECTION ( 'NONE',  ( 0.000000000000000000, 1.000000000000000000, 0.000000000000000000 ) ) ;
#9152=FACE_OUTER_BOUND ( 'NONE', #41111, .T. ) ;
#9160=EDGE_CURVE ( 'NONE', #20915, #63154, #43221, .T. ) ;
#9164=DIRECTION ( 'NONE',  ( 0.000000000000000000, -0.4595937023756062056, -0.8881292860483110951 ) ) ;
#9165=CARTESIAN_POINT ( 'NONE',  ( 23.60205915885299888, 11.53346724329999873, -4.150849519444998137 ) ) ;
#9166=FACE_OUTER_BOUND ( 'NONE', #65473, .T. ) ;
#9168=FACE_OUTER_BOUND ( 'NONE', #33717, .T. ) ;
#9179=CARTESIAN_POINT ( 'NONE',  ( 24.63409004136600089, 11.78082236971000007, 3.229000081171000236 ) ) ;
#9182=CARTESIAN_POINT ( 'NONE',  ( 23.59108006868057572, 13.38394536322959283, 4.038510903308840660 ) ) ;
#9193=CARTESIAN_POINT ( 'NONE',  ( 18.48326398027718653, 2.855662837657351183, -11.29488646771110893 ) ) ;
#9194=CARTESIAN_POINT ( 'NONE',  ( 13.73886390325583484, 9.223149073484993465, 8.172668166918892751 ) ) ;
#9203=SURFACE_STYLE_USAGE ( .BOTH. , #26332 ) ;
#9207=CARTESIAN_POINT ( 'NONE',  ( 11.35563158142000262, -11.71552011691000139, -1.381878615183999903 ) ) ;
#9220=FACE_OUTER_BOUND ( 'NONE', #41042, .T. ) ;
#9223=EDGE_LOOP ( 'NONE', ( #48877, #25276, #33251 ) ) ;
#9228=CARTESIAN_POINT ( 'NONE',  ( 24.84733913753600021, 8.571409823520001581, -8.858777810802999753 ) ) ;
#9229=CARTESIAN_POINT ( 'NONE',  ( 24.08756655391700008, 9.258138178154998954, -9.301679906964000821 ) ) ;
#9230=CARTESIAN_POINT ( 'NONE',  ( 18.35192027319500241, -2.803655468537999962, -11.45922931039000048 ) ) ;
#9243=CARTESIAN_POINT ( 'NONE',  ( 13.92975648157900004, 8.821327856275999579, 7.690719526968000430 ) ) ;
#9247=CARTESIAN_POINT ( 'NONE',  ( 15.40000000001299973, -8.815237407733999220, -7.616696375847999967 ) ) ;
#9260=CARTESIAN_POINT ( 'NONE',  ( 13.51802873821100270, -11.59174185862000073, -2.195273509308000026 ) ) ;
#9268=CARTESIAN_POINT ( 'NONE',  ( 21.72233714749290101, 0.000000000000000000, 0.000000000000000000 ) ) ;
#9286=ORIENTED_EDGE ( 'NONE', *, *, #39309, .T. ) ;
#9287=CARTESIAN_POINT ( 'NONE',  ( 23.98813794683320921, 12.73148067554796725, -3.487252914621118638 ) ) ;
#9291=EDGE_CURVE ( 'NONE', #60176, #51578, #55744, .T. ) ;
#9293=EDGE_CURVE ( 'NONE', #35342, #26251, #64873, .T. ) ;
#9310=CARTESIAN_POINT ( 'NONE',  ( 15.45446786537200090, 9.133287421996001854, 8.216743560820999548 ) ) ;
#9314=CARTESIAN_POINT ( 'NONE',  ( 23.89320776801300283, -3.226867021103002831, -11.46303308828999867 ) ) ;
#9316=DIRECTION ( 'NONE',  ( 0.000000000000000000, 0.000000000000000000, -1.000000000000000000 ) ) ;
#9324=DIRECTION ( 'NONE',  ( -0.000000000000000000, 0.3222656952305000266, 0.9466492601157001641 ) ) ;
#9326=ORIENTED_EDGE ( 'NONE', *, *, #50455, .F. ) ;
#9331=VERTEX_POINT ( 'NONE', #1469 ) ;
#9332=LINE ( 'NONE', #13917, #46244 ) ;
#9336=CARTESIAN_POINT ( 'NONE',  ( 23.50387503050299998, 6.998357211011000167, -12.12530396926999998 ) ) ;
#9340=CARTESIAN_POINT ( 'NONE',  ( 15.80279819343546244, 8.703657694420872559, 8.043987028914530768 ) ) ;
#9349=CIRCLE ( 'NONE', #49536, 0.6999999999999992895 ) ;
#9367=CARTESIAN_POINT ( 'NONE',  ( 18.26281931570200356, -2.856833007231000199, -11.95042392763000016 ) ) ;
#9368=FACE_OUTER_BOUND ( 'NONE', #65845, .T. ) ;
#9379=VECTOR ( 'NONE', #65471, 1000.000000000000114 ) ;
#9384=CARTESIAN_POINT ( 'NONE',  ( 13.48832048419379426, 11.62805077016393440, 2.291814632468947899 ) ) ;
#9389=ORIENTED_EDGE ( 'NONE', *, *, #66517, .T. ) ;
#9391=CARTESIAN_POINT ( 'NONE',  ( 13.73895793914716634, 8.868838256396804454, 7.856013393113998156 ) ) ;
#9399=CARTESIAN_POINT ( 'NONE',  ( 25.29881401420400167, 8.389234982073000779, 8.297993602990999307 ) ) ;
#9404=CARTESIAN_POINT ( 'NONE',  ( 14.93333333161133503, 9.471995579709359347, 8.194932869644874884 ) ) ;
#9412=EDGE_LOOP ( 'NONE', ( #33382, #41495, #64323, #47840 ) ) ;
#9417=CARTESIAN_POINT ( 'NONE',  ( 13.91137892731300063, -9.265832517555999459, -8.206449300197000696 ) ) ;
#9419=ORIENTED_EDGE ( 'NONE', *, *, #53518, .F. ) ;
#9423=CARTESIAN_POINT ( 'NONE',  ( 24.63612324460100211, -11.85362448828802151, 3.193519006004666316 ) ) ;
#9439=B_SPLINE_CURVE_WITH_KNOTS ( 'NONE', 3,
 ( #19550, #35296, #41556, #57628 ),
 .UNSPECIFIED., .F., .F.,
 ( 4, 4 ),
 ( 0.000000000000000000, 1.000000000000000000 ),
 .UNSPECIFIED. ) ;
#9440=CARTESIAN_POINT ( 'NONE',  ( 24.11583145280971507, -3.333338908579203341, 12.53524871031152088 ) ) ;
#9443=CARTESIAN_POINT ( 'NONE',  ( 25.19548435074899828, -3.342129198621000441, -11.59778229319999987 ) ) ;
#9445=CARTESIAN_POINT ( 'NONE',  ( 24.38453341727200296, -12.23039280200000078, -3.201153185139999913 ) ) ;
#9468=LINE ( 'NONE', #55399, #46152 ) ;
#9473=ORIENTED_EDGE ( 'NONE', *, *, #11814, .T. ) ;
#9477=CARTESIAN_POINT ( 'NONE',  ( 24.50399615158200106, 8.846403136021999458, 9.151488484734001005 ) ) ;
#9482=B_SPLINE_SURFACE_WITH_KNOTS ( 'NONE', 3, 3, ( 
 ( #38941, #12366, #55016, #22495 ),
 ( #64792, #53966, #1878, #6071 ),
 ( #27409, #38583, #22152, #16903 ),
 ( #23196, #65839, #38233, #11659 ),
 ( #59907, #12015, #33351, #56746 ),
 ( #24918, #66529, #14095, #18305 ) ),
 .UNSPECIFIED., .F., .F., .F.,
 ( 4, 1, 1, 4 ),
 ( 4, 4 ),
 ( 0.1811037619699999990, 0.3333333333333000081, 0.6666666666667000474, 0.8725156331704999602 ),
 ( -0.1256563615239000009, 1.125656361510000147 ),
 .UNSPECIFIED. ) ;
#9484=CARTESIAN_POINT ( 'NONE',  ( 23.60000000000000497, 11.54188747559392958, -7.798329221074294715 ) ) ;
#9487=CARTESIAN_POINT ( 'NONE',  ( 24.30000000000000071, 9.289189189551001036, 7.908916752674000072 ) ) ;
#9491=CARTESIAN_POINT ( 'NONE',  ( 17.92628981779796860, 3.345291551605440894, 11.86067033226837708 ) ) ;
#9499=FACE_OUTER_BOUND ( 'NONE', #50283, .T. ) ;
#9505=CARTESIAN_POINT ( 'NONE',  ( 15.90003771078200145, -3.695138809391000034, -11.25918926437999978 ) ) ;
#9508=CARTESIAN_POINT ( 'NONE',  ( 23.73961666470999887, 3.322481645952000129, -13.28128432273999948 ) ) ;
#9521=CARTESIAN_POINT ( 'NONE',  ( 24.48514021601400259, 12.12976263849000169, 3.164527443243999816 ) ) ;
#9522=DIRECTION ( 'NONE',  ( 0.000000000000000000, -1.000000000000000000, 0.000000000000000000 ) ) ;
#9525=CARTESIAN_POINT ( 'NONE',  ( 23.60864783563093638, 13.39760228683210741, 3.959825147115396238 ) ) ;
#9531=CARTESIAN_POINT ( 'NONE',  ( 13.35060253487349335, 12.37707099949019707, 1.919647290784784133 ) ) ;
#9539=CARTESIAN_POINT ( 'NONE',  ( 23.66004879239100234, 9.998910715289998308, -9.691527791130999603 ) ) ;
#9542=CARTESIAN_POINT ( 'NONE',  ( 13.87269624719400163, 9.544758557629000606, 8.169753052074002042 ) ) ;
#9543=B_SPLINE_CURVE_WITH_KNOTS ( 'NONE', 3,
 ( #7735, #40579, #18578, #8428 ),
 .UNSPECIFIED., .F., .F.,
 ( 4, 4 ),
 ( 0.000000000000000000, 1.000000000000000000 ),
 .UNSPECIFIED. ) ;
#9549=SURFACE_STYLE_FILL_AREA ( #57105 ) ;
#9551=ORIENTED_EDGE ( 'NONE', *, *, #29876, .T. ) ;
#9554=AXIS2_PLACEMENT_3D ( 'NONE', #17357, #17713, #39036 ) ;
#9560=CARTESIAN_POINT ( 'NONE',  ( 12.50062609531600089, 11.46460001353999836, -4.648225426428999718 ) ) ;
#9566=CARTESIAN_POINT ( 'NONE',  ( 18.40429364930200151, 2.938801558760000265, 11.32979830910000096 ) ) ;
#9573=CARTESIAN_POINT ( 'NONE',  ( 25.48369865294700176, 8.423008303568998656, -7.952430695590999576 ) ) ;
#9579=VERTEX_POINT ( 'NONE', #66735 ) ;
#9588=CARTESIAN_POINT ( 'NONE',  ( 13.73862479881500143, 8.949604875896001843, 7.398842444207000213 ) ) ;
#9595=ORIENTED_EDGE ( 'NONE', *, *, #40876, .F. ) ;
#9600=PLANE ( 'NONE',  #24219 ) ;
#9608=CARTESIAN_POINT ( 'NONE',  ( 12.97447410014400226, -11.72278459482000024, -1.967342116188999679 ) ) ;
#9611=ORIENTED_EDGE ( 'NONE', *, *, #67215, .T. ) ;
#9616=CARTESIAN_POINT ( 'NONE',  ( 15.78404792230800346, 8.744893293839998805, 7.778646260181000471 ) ) ;
#9618=CARTESIAN_POINT ( 'NONE',  ( 23.58038622399895701, 10.23758691150733036, 9.527246697258645369 ) ) ;
#9631=ORIENTED_EDGE ( 'NONE', *, *, #17757, .T. ) ;
#9632=CARTESIAN_POINT ( 'NONE',  ( 23.61278980179503151, -10.11611562016859445, 9.631329498146783408 ) ) ;
#9636=CARTESIAN_POINT ( 'NONE',  ( 11.79999999742034511, -12.31348763297674331, -1.888274624276562896 ) ) ;
#9637=DIRECTION ( 'NONE',  ( 1.000000000000000000, 0.000000000000000000, 0.000000000000000000 ) ) ;
#9645=CARTESIAN_POINT ( 'NONE',  ( 23.60000000000000142, 0.000000000000000000, 0.000000000000000000 ) ) ;
#9649=CARTESIAN_POINT ( 'NONE',  ( 25.47112285341500026, 2.702203117016999556, 11.27946744962999936 ) ) ;
#9650=EDGE_CURVE ( 'NONE', #56347, #33649, #63270, .T. ) ;
#9657=FACE_OUTER_BOUND ( 'NONE', #41993, .T. ) ;
#9662=CARTESIAN_POINT ( 'NONE',  ( 14.46666666253433498, -8.815232490335725757, -7.616703758276854863 ) ) ;
#9667=CARTESIAN_POINT ( 'NONE',  ( 23.58444450794900149, 10.35808252348000025, 9.328052187805999651 ) ) ;
#9674=CIRCLE ( 'NONE', #4083, 13.98989063585999837 ) ;
#9676=AXIS2_PLACEMENT_3D ( 'NONE', #40345, #19020, #18341 ) ;
#9680=ADVANCED_FACE ( 'NONE', ( #8017 ), #24778, .F. ) ;
#9684=CARTESIAN_POINT ( 'NONE',  ( 13.69999628573842543, -9.617752440245887158, -8.023770515523462876 ) ) ;
#9687=VERTEX_POINT ( 'NONE', #39487 ) ;
#9698=EDGE_LOOP ( 'NONE', ( #7573, #67176, #29673, #22140, #61349, #34525 ) ) ;
#9699=CARTESIAN_POINT ( 'NONE',  ( 16.10005255078199937, -3.632778330393000132, -11.06917548872000090 ) ) ;
#9700=CARTESIAN_POINT ( 'NONE',  ( 16.39999999231800132, -3.216285993016000155, -11.40340220863999932 ) ) ;
#9706=CARTESIAN_POINT ( 'NONE',  ( 24.44496350777200178, -12.03536639536000052, -3.224849854974999985 ) ) ;
#9709=EDGE_CURVE ( 'NONE', #47311, #50417, #35952, .T. ) ;
#9710=VERTEX_POINT ( 'NONE', #58303 ) ;
#9717=CARTESIAN_POINT ( 'NONE',  ( 17.57198699599700120, -11.81437355489000041, 3.324579570925000116 ) ) ;
#9718=CARTESIAN_POINT ( 'NONE',  ( 23.61718184453616942, -13.40540285613228910, -3.918713763237630765 ) ) ;
#9721=CARTESIAN_POINT ( 'NONE',  ( 24.34832118744133211, -3.224867653600234529, -12.03536993091778129 ) ) ;
#9733=CARTESIAN_POINT ( 'NONE',  ( 17.75883778089099962, 3.641526152925000037, -12.02434993381999995 ) ) ;
#9746=CARTESIAN_POINT ( 'NONE',  ( 24.52301487189109253, 8.782814486076295779, 8.926451907308345923 ) ) ;
#9760=ORIENTED_EDGE ( 'NONE', *, *, #16089, .F. ) ;
#9764=CARTESIAN_POINT ( 'NONE',  ( 13.73732479921000049, -9.700721122729000001, -7.982825098500999417 ) ) ;
#9767=CARTESIAN_POINT ( 'NONE',  ( 25.46372797112000086, -8.354608193938998895, 8.148457429720000533 ) ) ;
#9775=EDGE_CURVE ( 'NONE', #10227, #18501, #16974, .T. ) ;
#9776=EDGE_CURVE ( 'NONE', #10297, #26251, #56704, .T. ) ;
#9781=CARTESIAN_POINT ( 'NONE',  ( 23.85292962156700014, 3.520417378894999949, 13.16609032570999993 ) ) ;
#9790=CARTESIAN_POINT ( 'NONE',  ( 23.94495401785119171, -3.343212669807313020, 12.85029054808020987 ) ) ;
#9795=DIRECTION ( 'NONE',  ( 0.000000000000000000, -0.2588190451024934835, 0.9659258262890757507 ) ) ;
#9796=CIRCLE ( 'NONE', #52216, 0.3000000000000007105 ) ;
#9803=ORIENTED_EDGE ( 'NONE', *, *, #23440, .T. ) ;
#9811=AXIS2_PLACEMENT_3D ( 'NONE', #53204, #64360, #27679 ) ;
#9819=DIRECTION ( 'NONE',  ( 0.000000000000000000, -0.9127899773906427150, -0.4084292560226189250 ) ) ;
#9827=CARTESIAN_POINT ( 'NONE',  ( 24.41456973790700147, 8.821771448540999927, 8.767658430047001517 ) ) ;
#9831=CARTESIAN_POINT ( 'NONE',  ( 16.09996065438095414, 9.056490835163806707, 8.652417574211018092 ) ) ;
#9834=CARTESIAN_POINT ( 'NONE',  ( 23.66004879239100234, 9.998910715289998308, -9.691527791130999603 ) ) ;
#9837=CARTESIAN_POINT ( 'NONE',  ( 11.40000717739000002, 3.090860900556000105E-13, -1.000866056699999936E-13 ) ) ;
#9838=VECTOR ( 'NONE', #65464, 1000.000000000000227 ) ;
#9840=DIRECTION ( 'NONE',  ( 0.000000000000000000, 0.9840640231862776144, 0.1778145052306959739 ) ) ;
#9855=CARTESIAN_POINT ( 'NONE',  ( 23.58931645927405896, -3.186881233604905272, -13.61284225936185166 ) ) ;
#9864=CARTESIAN_POINT ( 'NONE',  ( 17.92913687513156873, -3.216295279492283665, 11.40344415250781118 ) ) ;
#9866=B_SPLINE_CURVE_WITH_KNOTS ( 'NONE', 3,
 ( #22506, #11671, #5738, #33010 ),
 .UNSPECIFIED., .F., .F.,
 ( 4, 4 ),
 ( 0.5000000000000298650, 1.000000000000000000 ),
 .UNSPECIFIED. ) ;
#9876=CARTESIAN_POINT ( 'NONE',  ( 24.39664237511399847, -8.810499461477174776, 8.810499461443630054 ) ) ;
#9880=EDGE_LOOP ( 'NONE', ( #31444, #34198, #47144, #16840 ) ) ;
#9886=ORIENTED_EDGE ( 'NONE', *, *, #58007, .T. ) ;
#9887=EDGE_CURVE ( 'NONE', #64134, #57964, #20327, .T. ) ;
#9894=CARTESIAN_POINT ( 'NONE',  ( 24.14470172087083455, 9.246870630047478556, -9.586744156808173045 ) ) ;
#9896=CARTESIAN_POINT ( 'NONE',  ( 12.99229341877100019, 11.49414526569999850, 1.652619848542000058 ) ) ;
#9898=CARTESIAN_POINT ( 'NONE',  ( 14.03986884071600016, 9.265369649631999494, 8.206962993589000277 ) ) ;
#9901=ORIENTED_EDGE ( 'NONE', *, *, #9887, .F. ) ;
#9903=EDGE_LOOP ( 'NONE', ( #12999, #34948, #61448, #14604, #30563, #9389, #62828, #67746, #19544, #30818, #3185, #63526, #28765, #31204, #58648, #3972, #17854 ) ) ;
#9908=LINE ( 'NONE', #58148, #40408 ) ;
#9909=ORIENTED_EDGE ( 'NONE', *, *, #53656, .T. ) ;
#9910=CARTESIAN_POINT ( 'NONE',  ( 12.69408977940800121, 11.93156085714000092, -3.263088413970000268 ) ) ;
#9911=CARTESIAN_POINT ( 'NONE',  ( 17.89937390468400125, 11.46460001353999836, -4.648225426428999718 ) ) ;
#9916=CARTESIAN_POINT ( 'NONE',  ( 18.44717847589300064, -2.901259342162000543, 12.12894967335999930 ) ) ;
#9920=ORIENTED_EDGE ( 'NONE', *, *, #49256, .F. ) ;
#9925=CARTESIAN_POINT ( 'NONE',  ( 25.27035628967400172, 8.566978069849998434, -7.889731756040999855 ) ) ;
#9956=ORIENTED_EDGE ( 'NONE', *, *, #44943, .F. ) ;
#9960=CARTESIAN_POINT ( 'NONE',  ( 13.44051303026600053, -11.61511980691000012, -2.065108503055999911 ) ) ;
#9969=FACE_OUTER_BOUND ( 'NONE', #28768, .T. ) ;
#9971=CARTESIAN_POINT ( 'NONE',  ( 23.60854598900385781, 10.12895705728418960, 9.621631069965385308 ) ) ;
#9973=CARTESIAN_POINT ( 'NONE',  ( 20.75138802851920161, 0.000000000000000000, 0.000000000000000000 ) ) ;
#9975=EDGE_LOOP ( 'NONE', ( #65606, #32788, #9760, #45834 ) ) ;
#9979=ORIENTED_EDGE ( 'NONE', *, *, #44597, .F. ) ;
#9987=DIRECTION ( 'NONE',  ( 1.000000000000000000, 0.000000000000000000, 0.000000000000000000 ) ) ;
#9992=ORIENTED_EDGE ( 'NONE', *, *, #66046, .T. ) ;
#10002=ORIENTED_EDGE ( 'NONE', *, *, #13586, .F. ) ;
#10006=CARTESIAN_POINT ( 'NONE',  ( 15.37415039705200215, 9.132871822554998076, 8.217191491449000296 ) ) ;
#10012=CARTESIAN_POINT ( 'NONE',  ( 25.19966571366900254, -11.70908055238000145, 2.905889386239000061 ) ) ;
#10017=CARTESIAN_POINT ( 'NONE',  ( 23.51705919471800144, 10.50857783028999926, 9.449538485383000008 ) ) ;
#10021=B_SPLINE_CURVE_WITH_KNOTS ( 'NONE', 3,
 ( #46561, #57040, #45870, #56362 ),
 .UNSPECIFIED., .F., .F.,
 ( 4, 4 ),
 ( 0.000000000000000000, 1.000000000000000000 ),
 .UNSPECIFIED. ) ;
#10023=FACE_OUTER_BOUND ( 'NONE', #27442, .T. ) ;
#10024=ORIENTED_EDGE ( 'NONE', *, *, #51714, .T. ) ;
#10026=DIRECTION ( 'NONE',  ( 0.000000000000000000, -0.8764402124317022258, 0.4815106998112011483 ) ) ;
#10033=CARTESIAN_POINT ( 'NONE',  ( 24.30000564797063234, -12.09374148493534840, 3.240508264358131107 ) ) ;
#10041=CARTESIAN_POINT ( 'NONE',  ( 16.13854985688900001, -3.352851047014000052, -11.81842075147999971 ) ) ;
#10042=B_SPLINE_CURVE_WITH_KNOTS ( 'NONE', 3,
 ( #522, #59937, #54698, #32009 ),
 .UNSPECIFIED., .F., .F.,
 ( 4, 4 ),
 ( 0.000000000000000000, 1.000000000000000000 ),
 .UNSPECIFIED. ) ;
#10043=CARTESIAN_POINT ( 'NONE',  ( 11.31919037786000182, 11.76444917719000038, 1.692529869092999961 ) ) ;
#10071=FACE_OUTER_BOUND ( 'NONE', #6345, .T. ) ;
#10079=CARTESIAN_POINT ( 'NONE',  ( 18.28771814374053761, 2.987295517884132501, -11.95930540589378488 ) ) ;
#10088=EDGE_CURVE ( 'NONE', #59692, #33837, #22056, .T. ) ;
#10089=VERTEX_POINT ( 'NONE', #20135 ) ;
#10096=CARTESIAN_POINT ( 'NONE',  ( 24.67559749782400047, 8.698784986637999594, 9.015141820286999064 ) ) ;
#10097=AXIS2_PLACEMENT_3D ( 'NONE', #21308, #4876, #47199 ) ;
#10105=ADVANCED_FACE ( 'NONE', ( #20822 ), #33244, .T. ) ;
#10114=CARTESIAN_POINT ( 'NONE',  ( 15.96647867633516427, -8.895858221259741683, -8.626805212950843682 ) ) ;
#10118=CARTESIAN_POINT ( 'NONE',  ( 11.25950692870000047, 3.811441498709999820, -11.68087307222999982 ) ) ;
#10132=CARTESIAN_POINT ( 'NONE',  ( 24.08756693569399943, 3.426422008827000099, 12.66862219457000016 ) ) ;
#10141=CARTESIAN_POINT ( 'NONE',  ( 23.71152327822508354, -3.235048976924307595, 13.31086256645365928 ) ) ;
#10146=CARTESIAN_POINT ( 'NONE',  ( 24.98214466478799878, -3.089315488182000191, -11.61702660961000078 ) ) ;
#10149=ORIENTED_EDGE ( 'NONE', *, *, #52872, .F. ) ;
#10152=AXIS2_PLACEMENT_3D ( 'NONE', #46804, #62863, #26510 ) ;
#10161=VECTOR ( 'NONE', #50186, 1000.000000000000000 ) ;
#10170=CARTESIAN_POINT ( 'NONE',  ( 11.79999998109721204, -11.63601885445003248, -1.847750289993327133 ) ) ;
#10172=CARTESIAN_POINT ( 'NONE',  ( 11.36663496983795874, -3.844885926410422705, 11.78015091829274752 ) ) ;
#10173=DIRECTION ( 'NONE',  ( -1.000000000000000000, 0.000000000000000000, 0.000000000000000000 ) ) ;
#10177=ADVANCED_FACE ( 'NONE', ( #31666 ), #46714, .F. ) ;
#10179=CARTESIAN_POINT ( 'NONE',  ( 24.36453968238300050, 8.917854847619999248, 9.043337665091998545 ) ) ;
#10186=CARTESIAN_POINT ( 'NONE',  ( 25.29987333571600061, -10.83443035398000021, -3.855530949778000149 ) ) ;
#10190=CARTESIAN_POINT ( 'NONE',  ( 12.52002425203523650, 12.10842255864620753, -3.203403679956843941 ) ) ;
#10196=CARTESIAN_POINT ( 'NONE',  ( 25.44993984453400060, 11.77655473258999841, 4.190794510628000680 ) ) ;
#10199=CARTESIAN_POINT ( 'NONE',  ( 23.73953418927302650, -9.827640250138356848, 9.725489356616225933 ) ) ;
#10204=CARTESIAN_POINT ( 'NONE',  ( 23.57792053481616534, -3.138450412106891463, 13.63071449664701085 ) ) ;
#10205=CARTESIAN_POINT ( 'NONE',  ( 23.58664969842400083, 3.018451562790000153, -13.60679499663999970 ) ) ;
#10219=CARTESIAN_POINT ( 'NONE',  ( 24.53429011008099891, 3.614318944477000084, -12.31267538233000103 ) ) ;
#10223=CARTESIAN_POINT ( 'NONE',  ( 23.61700585920300099, 13.18055929188999897, -4.241175825786999809 ) ) ;
#10227=VERTEX_POINT ( 'NONE', #30296 ) ;
#10233=FACE_OUTER_BOUND ( 'NONE', #55910, .T. ) ;
#10234=CARTESIAN_POINT ( 'NONE',  ( 14.93333333161133503, -9.471995579709343360, -8.194932869644890872 ) ) ;
#10237=CARTESIAN_POINT ( 'NONE',  ( 13.64720874474600087, 11.45913667646999912, 2.381478076492999918 ) ) ;
#10239=CARTESIAN_POINT ( 'NONE',  ( 13.92966272177200260, 9.396431546200000540, 8.198412206645000921 ) ) ;
#10241=VERTEX_POINT ( 'NONE', #51600 ) ;
#10246=CARTESIAN_POINT ( 'NONE',  ( 13.49980696792483137, 10.68794281923483780, 6.218617845733617422 ) ) ;
#10250=CARTESIAN_POINT ( 'NONE',  ( 11.79999999550100220, -11.52577121388000059, -1.696750555870000010 ) ) ;
#10253=CARTESIAN_POINT ( 'NONE',  ( 12.40355051044899959, 11.78614875273999907, -3.442261952866000119 ) ) ;
#10257=AXIS2_PLACEMENT_3D ( 'NONE', #4235, #8121, #24544 ) ;
#10258=CARTESIAN_POINT ( 'NONE',  ( 12.24143698068809982, -11.79508855325971162, 3.559061050736494813 ) ) ;
#10259=CARTESIAN_POINT ( 'NONE',  ( 17.85449583315300259, -3.297641659324999974, 11.83458394846000061 ) ) ;
#10282=CARTESIAN_POINT ( 'NONE',  ( 16.39947726215000046, -3.188035298175999621, -11.45126509954999960 ) ) ;
#10283=CARTESIAN_POINT ( 'NONE',  ( 13.64514873068900158, 9.050862583665999495, 7.420564490681000436 ) ) ;
#10288=CARTESIAN_POINT ( 'NONE',  ( 25.44993329535400051, 2.258942858049999725, 12.29419282279000036 ) ) ;
#10290=DIRECTION ( 'NONE',  ( 1.000000000000000000, 0.000000000000000000, 0.000000000000000000 ) ) ;
#10297=VERTEX_POINT ( 'NONE', #61333 ) ;
#10313=ORIENTED_EDGE ( 'NONE', *, *, #28144, .T. ) ;
#10314=CARTESIAN_POINT ( 'NONE',  ( 23.57438223407208966, 10.27284394070036555, 9.492890931809894184 ) ) ;
#10319=ORIENTED_EDGE ( 'NONE', *, *, #41824, .F. ) ;
#10321=CARTESIAN_POINT ( 'NONE',  ( 24.78225873320400297, 12.26745412634999965, -2.911642956740000177 ) ) ;
#10326=CARTESIAN_POINT ( 'NONE',  ( 23.58536431466287553, -10.21357488779519684, 9.549750708585223791 ) ) ;
#10328=CARTESIAN_POINT ( 'NONE',  ( 18.43329252113700889, 2.892698357136549880, -12.11790064375146336 ) ) ;
#10330=CARTESIAN_POINT ( 'NONE',  ( 24.30000000000000071, -11.77655473258999841, 4.190794510628000680 ) ) ;
#10355=CONICAL_SURFACE ( 'NONE', #59461, 11.75017108327000059, 0.7854127224616339609 ) ;
#10358=CARTESIAN_POINT ( 'NONE',  ( 25.20466218340900255, -11.19856126556000042, 3.405324039013999826 ) ) ;
#10362=CARTESIAN_POINT ( 'NONE',  ( 24.42336652060700075, 8.981205186855000022, 9.518213142638000335 ) ) ;
#10363=EDGE_LOOP ( 'NONE', ( #65329, #10808, #35851, #36160 ) ) ;
#10369=CARTESIAN_POINT ( 'NONE',  ( 18.23019412026599895, 3.031170125296999807, 11.90979123982999965 ) ) ;
#10372=VERTEX_POINT ( 'NONE', #1563 ) ;
#10374=B_SPLINE_CURVE_WITH_KNOTS ( 'NONE', 3,
 ( #42387, #4973, #26993, #26306, #11245, #21392, #32583, #37138, #58455, #38156 ),
 .UNSPECIFIED., .F., .F.,
 ( 4, 2, 2, 2, 4 ),
 ( 0.000000000000000000, 0.2500000000000001110, 0.5000000000000000000, 0.7500000000000000000, 1.000000000000000000 ),
 .UNSPECIFIED. ) ;
#10380=CARTESIAN_POINT ( 'NONE',  ( 25.26995798061230403, -11.52974591960634143, -2.996559586417926191 ) ) ;
#10385=CARTESIAN_POINT ( 'NONE',  ( 16.39944283128300029, -3.410739012457999930, -11.89826262991000050 ) ) ;
#10388=DIRECTION ( 'NONE',  ( 0.000000000000000000, -1.000000000000000000, 0.000000000000000000 ) ) ;
#10394=CARTESIAN_POINT ( 'NONE',  ( 24.37808884581836111, -8.911082519650753042, -9.054599882782522258 ) ) ;
#10398=CARTESIAN_POINT ( 'NONE',  ( 24.67921311619700120, 3.567517360056999820, 12.13750603036999998 ) ) ;
#10407=CARTESIAN_POINT ( 'NONE',  ( 18.47905117804075914, 2.854821129078588982, 11.29488031137690207 ) ) ;
#10409=CARTESIAN_POINT ( 'NONE',  ( 23.56682100824491144, -13.33070654784838993, -4.243923923310612523 ) ) ;
#10412=CARTESIAN_POINT ( 'NONE',  ( 18.48260618742725114, 3.086131726339705672, 12.13914505220553686 ) ) ;
#10420=EDGE_CURVE ( 'NONE', #24248, #28381, #35852, .T. ) ;
#10422=CARTESIAN_POINT ( 'NONE',  ( 12.79999999914999975, -12.11987927271999865, 3.159802730921999814 ) ) ;
#10429=CARTESIAN_POINT ( 'NONE',  ( 13.86904166957594953, 8.833215535550262842, 7.896538540699785003 ) ) ;
#10430=CONICAL_SURFACE ( 'NONE', #68459, 12.47499939740000130, 0.7853981102588313279 ) ;
#10440=CARTESIAN_POINT ( 'NONE',  ( 15.39999999998900293, 9.471998555523999386, 8.194929586088999685 ) ) ;
#10446=CARTESIAN_POINT ( 'NONE',  ( 24.26733149983100191, 8.951944080867999531, -8.897842724163000483 ) ) ;
#10448=ORIENTED_EDGE ( 'NONE', *, *, #16807, .F. ) ;
#10454=CARTESIAN_POINT ( 'NONE',  ( 13.50567905817900183, -9.332645239999999731, -7.987984570204999635 ) ) ;
#10469=ORIENTED_EDGE ( 'NONE', *, *, #60409, .T. ) ;
#10471=B_SPLINE_CURVE_WITH_KNOTS ( 'NONE', 3,
 ( #36181, #40393, #14521, #51233, #2986, #3662 ),
 .UNSPECIFIED., .F., .F.,
 ( 4, 2, 4 ),
 ( 0.000000000000000000, 0.5000000000000000000, 1.000000000000000000 ),
 .UNSPECIFIED. ) ;
#10475=ORIENTED_EDGE ( 'NONE', *, *, #75, .F. ) ;
#10477=EDGE_CURVE ( 'NONE', #31379, #60315, #64515, .T. ) ;
#10478=B_SPLINE_SURFACE_WITH_KNOTS ( 'NONE', 3, 3, ( 
 ( #24730, #9667, #40804, #10017 ),
 ( #46747, #14586, #67702, #20166 ),
 ( #35573, #50956, #68052, #41494 ),
 ( #61784, #3054, #8986, #30328 ),
 ( #19829, #13903, #56543, #41160 ),
 ( #8649, #51636, #3733, #25067 ),
 ( #62466, #35904, #62805, #15614 ),
 ( #69093, #59285, #32391, #37281 ),
 ( #53706, #63837, #917, #53363 ),
 ( #21197, #11390, #63494, #10362 ),
 ( #42872, #31697, #52669, #5466 ),
 ( #47784, #10702, #38310, #54044 ) ),
 .UNSPECIFIED., .F., .F., .F.,
 ( 4, 1, 1, 1, 1, 1, 1, 1, 1, 4 ),
 ( 4, 4 ),
 ( 0.5527793964264999804, 0.5999999999999999778, 0.6500000000000000222, 0.6999999999999999556, 0.7500000000000000000, 0.8000000000000000444, 0.8499999999999999778, 0.9000000000000000222, 0.9499999999999999556, 0.9893861203041000030 ),
 ( -0.2706700323135999842, 1.270791129485999926 ),
 .UNSPECIFIED. ) ;
#10483=CARTESIAN_POINT ( 'NONE',  ( 24.39664803201866405, -8.853227592127330681, 8.853227592127330681 ) ) ;
#10489=CARTESIAN_POINT ( 'NONE',  ( 13.43777338887480610, -12.12041883920679730, -2.246947635350974970 ) ) ;
#10491=PLANE ( 'NONE',  #13814 ) ;
#10504=CARTESIAN_POINT ( 'NONE',  ( 24.70905524881975523, -3.127839019168523027, 11.79917697410494171 ) ) ;
#10514=CARTESIAN_POINT ( 'NONE',  ( 24.60999195316300003, 8.752663949940000521, 9.057796881813999335 ) ) ;
#10516=CARTESIAN_POINT ( 'NONE',  ( 18.30000000000000071, 0.000000000000000000, 0.000000000000000000 ) ) ;
#10522=DIRECTION ( 'NONE',  ( 1.000000000000000000, 0.000000000000000000, 0.000000000000000000 ) ) ;
#10534=ORIENTED_EDGE ( 'NONE', *, *, #49708, .T. ) ;
#10540=CARTESIAN_POINT ( 'NONE',  ( 23.56664322114200161, -2.935586410151000081, -13.67842711829000102 ) ) ;
#10545=B_SPLINE_CURVE_WITH_KNOTS ( 'NONE', 3,
 ( #11550, #48627, #32551, #26623, #16797, #730, #28000, #59109, #42, #49309, #43389, #65029, #53864, #43035 ),
 .UNSPECIFIED., .F., .F.,
 ( 4, 2, 2, 2, 2, 2, 4 ),
 ( 0.000000000000000000, 0.1250000000000030809, 0.2500000000000061617, 0.5000000000000043299, 0.6250000000000035527, 0.7500000000000026645, 1.000000000000000000 ),
 .UNSPECIFIED. ) ;
#10547=AXIS2_PLACEMENT_3D ( 'NONE', #28825, #1202, #13080 ) ;
#10557=CARTESIAN_POINT ( 'NONE',  ( 24.39664890306633183, 3.240506439362909497, -12.09373467396045854 ) ) ;
#10558=DIRECTION ( 'NONE',  ( 0.000000000000000000, 0.000000000000000000, -1.000000000000000000 ) ) ;
#10564=CARTESIAN_POINT ( 'NONE',  ( 23.63098021901300072, 13.46819232204000016, -3.822892805028000218 ) ) ;
#10566=ORIENTED_EDGE ( 'NONE', *, *, #67862, .F. ) ;
#10570=CARTESIAN_POINT ( 'NONE',  ( 13.04552286951901330, 12.39025300375190142, 1.832281502500254566 ) ) ;
#10573=CARTESIAN_POINT ( 'NONE',  ( 12.79999999468004646, -11.20144845259485678, 4.552734317499857575 ) ) ;
#10575=CARTESIAN_POINT ( 'NONE',  ( 18.18404792230800382, -3.205001206845999651, 11.25648540289999922 ) ) ;
#10580=CARTESIAN_POINT ( 'NONE',  ( 12.99325612864500279, 11.57041205278999918, 1.757148387262999822 ) ) ;
#10594=CARTESIAN_POINT ( 'NONE',  ( 12.17512857912400115, 11.55078329699999884, -4.188961560869000067 ) ) ;
#10595=CARTESIAN_POINT ( 'NONE',  ( 18.13017043268600048, 11.56648533137999912, -4.655999611355000845 ) ) ;
#10600=CARTESIAN_POINT ( 'NONE',  ( 17.60000000085000238, 12.11987927271999865, -3.159802730921999814 ) ) ;
#10622=CARTESIAN_POINT ( 'NONE',  ( 23.50387503050299998, 0.000000000000000000, 0.000000000000000000 ) ) ;
#10623=AXIS2_PLACEMENT_3D ( 'NONE', #35592, #30014, #69109 ) ;
#10624=CARTESIAN_POINT ( 'NONE',  ( 25.30000327618300204, 10.83443035398000021, -3.855530949778000149 ) ) ;
#10631=FACE_OUTER_BOUND ( 'NONE', #42504, .T. ) ;
#10635=CARTESIAN_POINT ( 'NONE',  ( 12.80000000000000071, -11.23412379136000006, 3.084957477885999833 ) ) ;
#10638=ORIENTED_EDGE ( 'NONE', *, *, #66802, .T. ) ;
#10650=CARTESIAN_POINT ( 'NONE',  ( 13.69997185827400266, 11.40547114375999982, 2.374390024598000082 ) ) ;
#10653=DIRECTION ( 'NONE',  ( 0.000000000000000000, 0.000000000000000000, -1.000000000000000000 ) ) ;
#10658=CARTESIAN_POINT ( 'NONE',  ( 12.80000000000000071, -11.23412379136000006, 3.084957477885999833 ) ) ;
#10661=CARTESIAN_POINT ( 'NONE',  ( 24.87965957765100100, 11.54628040307999903, -3.248281071505000117 ) ) ;
#10665=CARTESIAN_POINT ( 'NONE',  ( 15.90003771078200145, 3.695138809391000034, 11.25918926437999978 ) ) ;
#10670=ADVANCED_FACE ( 'NONE', ( #27976 ), #3952, .F. ) ;
#10675=CARTESIAN_POINT ( 'NONE',  ( 23.80953365092410579, 13.00795969425658249, 3.692987363579084192 ) ) ;
#10677=CARTESIAN_POINT ( 'NONE',  ( 12.99999999998900080, -12.39025855408000076, -1.832244667012999928 ) ) ;
#10681=CARTESIAN_POINT ( 'NONE',  ( 24.30000000000000071, 0.000000000000000000, 0.000000000000000000 ) ) ;
#10689=CARTESIAN_POINT ( 'NONE',  ( 24.39664176096000148, 8.810499011074819364, -8.810499011034677252 ) ) ;
#10697=CARTESIAN_POINT ( 'NONE',  ( 25.25798371868100034, -11.13205096074000089, 3.460355926395999759 ) ) ;
#10702=CARTESIAN_POINT ( 'NONE',  ( 24.38581293668700312, 8.886045982725999437, 8.989759919345001293 ) ) ;
#10718=CARTESIAN_POINT ( 'NONE',  ( 13.99999999231800096, -8.833253877201999060, -7.896562762484000686 ) ) ;
#10719=VERTEX_POINT ( 'NONE', #18174 ) ;
#10725=CARTESIAN_POINT ( 'NONE',  ( 11.49978667957999967, -12.43119799159999950, -1.530013559959999991 ) ) ;
#10726=ORIENTED_EDGE ( 'NONE', *, *, #5481, .T. ) ;
#10727=CARTESIAN_POINT ( 'NONE',  ( 16.04647714749799903, -3.814092932148000159, -11.87318743920999964 ) ) ;
#10729=B_SPLINE_CURVE_WITH_KNOTS ( 'NONE', 3,
 ( #60419, #23700, #33855, #40137, #28614, #24044, #50275, #55171, #44353, #2377 ),
 .UNSPECIFIED., .F., .F.,
 ( 4, 2, 2, 2, 4 ),
 ( 0.000000000000000000, 0.2499999999999967804, 0.3749999999999971689, 0.4999999999999975575, 1.000000000000000000 ),
 .UNSPECIFIED. ) ;
#10730=CARTESIAN_POINT ( 'NONE',  ( 11.48831242699000121, 11.66400889920000061, 1.747256858593000173 ) ) ;
#10731=ORIENTED_EDGE ( 'NONE', *, *, #57541, .T. ) ;
#10739=CARTESIAN_POINT ( 'NONE',  ( 23.85399111800575156, -13.23042136191713958, 3.489530933266961288 ) ) ;
#10744=ORIENTED_EDGE ( 'NONE', *, *, #36072, .F. ) ;
#10747=CARTESIAN_POINT ( 'NONE',  ( 15.86281931570199966, -8.823480018325001950, -8.551042465543998716 ) ) ;
#10748=DIRECTION ( 'NONE',  ( 0.000000000000000000, 0.000000000000000000, 1.000000000000000000 ) ) ;
#10751=EDGE_CURVE ( 'NONE', #47043, #64287, #27630, .T. ) ;
#10759=B_SPLINE_CURVE_WITH_KNOTS ( 'NONE', 3,
 ( #619, #43267, #64574, #16685, #38013, #59338, #35541, #35201, #56511, #8617, #3025, #61752, #66654, #29966, #13870, #55831, #7935, #19104, #40770, #51267, #7584, #50583, #45345, #40426, #39753, #29271, #12838, #14212, #28933, #62094, #3363 ),
 .UNSPECIFIED., .F., .F.,
 ( 4, 2, 2, 1, 1, 2, 2, 2, 1, 2, 2, 2, 2, 2, 2, 2, 4 ),
 ( 0.000000000000000000, 0.06250000000002108036, 0.09375000000003078093, 0.1093750000000356382, 0.1171875000000380668, 0.1210937500000392325, 0.1250000000000403844, 0.1875000000000528744, 0.2187500000000581757, 0.2343750000000596745, 0.2500000000000611733, 0.3750000000000564548, 0.4375000000000552891, 0.4687500000000547340, 0.5000000000000541789, 0.7500000000000270894, 1.000000000000000000 ),
 .UNSPECIFIED. ) ;
#10769=CARTESIAN_POINT ( 'NONE',  ( 23.68247649694000145, -13.13665233500999996, 3.950736996479999874 ) ) ;
#10776=CARTESIAN_POINT ( 'NONE',  ( 18.53960231418900051, 2.682082126742999950, -11.29772413421000188 ) ) ;
#10778=AXIS2_PLACEMENT_3D ( 'NONE', #27790, #17285, #54691 ) ;
#10781=STYLED_ITEM ( 'NONE', ( #46969 ), #8521 ) ;
#10787=VERTEX_POINT ( 'NONE', #27284 ) ;
#10808=ORIENTED_EDGE ( 'NONE', *, *, #59257, .T. ) ;
#10811=EDGE_CURVE ( 'NONE', #10372, #47157, #15743, .T. ) ;
#10812=CARTESIAN_POINT ( 'NONE',  ( 13.70003001321900271, 10.86123379505843545, 6.319444516909296539 ) ) ;
#10816=CARTESIAN_POINT ( 'NONE',  ( 24.56914408408099959, 3.716987283419999955, 12.37180464569999927 ) ) ;
#10819=EDGE_CURVE ( 'NONE', #7211, #55031, #42739, .T. ) ;
#10822=ORIENTED_EDGE ( 'NONE', *, *, #17260, .F. ) ;
#10827=CARTESIAN_POINT ( 'NONE',  ( 24.77999963990900056, -3.612931897559000127, -12.08259271626999976 ) ) ;
#10830=ORIENTED_EDGE ( 'NONE', *, *, #44622, .T. ) ;
#10832=CARTESIAN_POINT ( 'NONE',  ( 23.58885147429595719, 10.33108476000267828, 9.338978122152829187 ) ) ;
#10852=CARTESIAN_POINT ( 'NONE',  ( 19.99999987597299977, 1.497200531649000015E-13, 3.463895836829999943E-14 ) ) ;
#10858=CARTESIAN_POINT ( 'NONE',  ( 24.60170725920900026, 8.811863727701000570, 9.296544040758000449 ) ) ;
#10865=ADVANCED_FACE ( 'NONE', ( #25129 ), #67762, .T. ) ;
#10868=FACE_OUTER_BOUND ( 'NONE', #60542, .T. ) ;
#10877=CARTESIAN_POINT ( 'NONE',  ( 12.09999999995609521, 11.00695867686506269, -3.817557009248758959 ) ) ;
#10883=CARTESIAN_POINT ( 'NONE',  ( 23.60000000000000142, -9.289189189551001036, 7.908916752675001050 ) ) ;
#10887=AXIS2_PLACEMENT_3D ( 'NONE', #62049, #25328, #35491 ) ;
#10891=ORIENTED_EDGE ( 'NONE', *, *, #65478, .F. ) ;
#10894=CONICAL_SURFACE ( 'NONE', #15347, 12.47499939740000130, 0.7853981102588313279 ) ;
#10895=CARTESIAN_POINT ( 'NONE',  ( 25.26995024675264290, 3.169784517860001039, 11.48334038991926320 ) ) ;
#10905=B_SPLINE_SURFACE_WITH_KNOTS ( 'NONE', 3, 3, ( 
 ( #57282, #35298, #56613, #41559 ),
 ( #67428, #30731, #19553, #40871 ),
 ( #52038, #25477, #46809, #14315 ),
 ( #35641, #68115, #5527, #47498 ),
 ( #10769, #32453, #26867, #59018 ),
 ( #64589, #42593, #63207, #63902 ),
 ( #48181, #4830, #31419, #636 ),
 ( #52736, #68452, #47847, #16016 ),
 ( #285, #16699, #21944, #38026 ),
 ( #52387, #59353, #31082, #26517 ),
 ( #43283, #20574, #57984, #4482 ),
 ( #32114, #16359, #25822, #47153 ) ),
 .UNSPECIFIED., .F., .F., .F.,
 ( 4, 1, 1, 1, 1, 1, 1, 1, 1, 4 ),
 ( 4, 4 ),
 ( 0.5527591097492000616, 0.5999999999999999778, 0.6500000000000000222, 0.6999999999999999556, 0.7500000000000000000, 0.8000000000000000444, 0.8499999999999999778, 0.9000000000000000222, 0.9499999999999999556, 0.9893860793656999997 ),
 ( -0.2706700118377999842, 1.270791066829999982 ),
 .UNSPECIFIED. ) ;
#10906=CARTESIAN_POINT ( 'NONE',  ( 25.60000000000000142, 2.023980670379999847, 11.01542190082000161 ) ) ;
#10907=CARTESIAN_POINT ( 'NONE',  ( 24.41555930013399944, 12.00270549100999951, 3.255728780632000330 ) ) ;
#10908=CARTESIAN_POINT ( 'NONE',  ( 17.80000000005199823, -3.345268251980999974, 11.86064071431999878 ) ) ;
#10913=CARTESIAN_POINT ( 'NONE',  ( 25.30000327618300204, 10.83443035398000021, -3.855530949778000149 ) ) ;
#10918=ADVANCED_FACE ( 'NONE', ( #67423 ), #18522, .F. ) ;
#10919=CARTESIAN_POINT ( 'NONE',  ( 23.94496671461785198, 3.343214108386058037, -12.85026700558185020 ) ) ;
#10921=B_SPLINE_CURVE_WITH_KNOTS ( 'NONE', 3,
 ( #19220, #2458, #19574, #50013 ),
 .UNSPECIFIED., .F., .F.,
 ( 4, 4 ),
 ( 0.000000000000000000, 1.000000000000000000 ),
 .UNSPECIFIED. ) ;
#10926=CARTESIAN_POINT ( 'NONE',  ( 13.46242637979000101, 11.63956415132000011, 2.420148064723000481 ) ) ;
#10933=VERTEX_POINT ( 'NONE', #34950 ) ;
#10936=AXIS2_PLACEMENT_3D ( 'NONE', #37296, #38323, #16996 ) ;
#10937=CARTESIAN_POINT ( 'NONE',  ( 16.39999999231800132, 3.216285993016000155, 11.40340220863999932 ) ) ;
#10943=CARTESIAN_POINT ( 'NONE',  ( 18.36290965255400209, 11.69601057336999972, -4.586677359659000253 ) ) ;
#10948=CARTESIAN_POINT ( 'NONE',  ( 18.31992917194613213, 12.02644019082415738, -3.499704873216455070 ) ) ;
#10951=EDGE_CURVE ( 'NONE', #59568, #20805, #35329, .T. ) ;
#10958=ADVANCED_FACE ( 'NONE', ( #60819 ), #23575, .T. ) ;
#10960=CARTESIAN_POINT ( 'NONE',  ( 24.48513460874600156, 8.805438997290998770, -8.922423169716999780 ) ) ;
#10967=AXIS2_PLACEMENT_3D ( 'NONE', #64081, #5706, #32635 ) ;
#10974=ADVANCED_FACE ( 'NONE', ( #66748 ), #31364, .T. ) ;
#10978=LINE ( 'NONE', #144, #6400 ) ;
#10988=CARTESIAN_POINT ( 'NONE',  ( 25.52347087181200180, -11.21067381750000003, -3.136870539691000381 ) ) ;
#10992=CARTESIAN_POINT ( 'NONE',  ( 11.49999672494999992, -11.45771900890041906, 2.434039779710992502 ) ) ;
#10995=VERTEX_POINT ( 'NONE', #25472 ) ;
#10999=CARTESIAN_POINT ( 'NONE',  ( 13.31007343200417736, 11.51543253752112150, 1.765677284072383557 ) ) ;
#11003=CIRCLE ( 'NONE', #13275, 0.9999999999999993339 ) ;
#11009=DIRECTION ( 'NONE',  ( -1.000000000000000000, 0.000000000000000000, 0.000000000000000000 ) ) ;
#11013=CARTESIAN_POINT ( 'NONE',  ( 20.75138802851920161, 0.000000000000000000, 5.760713961201000544 ) ) ;
#11014=VERTEX_POINT ( 'NONE', #58662 ) ;
#11018=DIRECTION ( 'NONE',  ( 0.000000000000000000, 0.9659258262890757507, 0.2588190451024934835 ) ) ;
#11022=CARTESIAN_POINT ( 'NONE',  ( 16.07476513888299863, 3.720976809451999934, 11.90233817890000090 ) ) ;
#11024=DIRECTION ( 'NONE',  ( -8.952907862884936298E-11, -0.7455324205424948003, -0.6664693615763958023 ) ) ;
#11028=EDGE_LOOP ( 'NONE', ( #54856, #49361, #10002, #39288, #62233, #20784 ) ) ;
#11032=CARTESIAN_POINT ( 'NONE',  ( 17.71485163640869587, -12.11985299911213154, 3.159871563571859276 ) ) ;
#11034=CARTESIAN_POINT ( 'NONE',  ( 24.57937622052195437, -12.41575245050226606, -3.011584258247195223 ) ) ;
#11035=B_SPLINE_CURVE_WITH_KNOTS ( 'NONE', 3,
 ( #45628, #24639, #15171, #46994, #30915, #19385, #52572, #36153, #68296, #56801, #45960, #3638, #3305, #40370, #67269, #46308, #13809, #67609, #14495, #57816, #14152, #14833, #4326, #67959, #31261, #66931, #19734, #41404, #20075, #57465, #61691 ),
 .UNSPECIFIED., .F., .F.,
 ( 4, 2, 2, 1, 1, 2, 2, 2, 1, 2, 2, 2, 2, 2, 2, 2, 4 ),
 ( 0.000000000000000000, 0.06249999999998517852, 0.09374999999997776778, 0.1093749999999739375, 0.1171874999999719807, 0.1210937499999709954, 0.1249999999999700101, 0.1874999999999709677, 0.2187499999999734934, 0.2343749999999746592, 0.2499999999999758526, 0.3749999999999817368, 0.4374999999999846234, 0.4687499999999846789, 0.4999999999999847899, 0.7499999999999924505, 1.000000000000000000 ),
 .UNSPECIFIED. ) ;
#11041=CARTESIAN_POINT ( 'NONE',  ( 12.67430611818100061, -11.44505085583999993, 4.692779640757001047 ) ) ;
#11049=CARTESIAN_POINT ( 'NONE',  ( 18.17737860441035380, 11.15478131644621840, -3.361574628444541357 ) ) ;
#11055=B_SPLINE_SURFACE_WITH_KNOTS ( 'NONE', 3, 3, ( 
 ( #4361, #42127, #68330, #63434 ),
 ( #20449, #67643, #30268, #35171 ),
 ( #25349, #36531, #57499, #41775 ),
 ( #36187, #14530, #9260, #56484 ),
 ( #57855, #15205, #9960, #24671 ),
 ( #56834, #8932, #51575, #25010 ),
 ( #3669, #45991, #31297, #67304 ),
 ( #8588, #52607, #46341, #40744 ),
 ( #30601, #19767, #4700, #41092 ),
 ( #26046, #62409, #35846, #9608 ) ),
 .UNSPECIFIED., .F., .F., .F.,
 ( 4, 1, 1, 1, 1, 1, 1, 4 ),
 ( 4, 4 ),
 ( 0.04183311431308000400, 0.1428571428570999946, 0.2857142857143000203, 0.4285714285713999594, 0.5714285714286000406, 0.7142857142856999797, 0.8571428571429000609, 0.9292981235707000742 ),
 ( -0.1917799910644000239, 1.191756862851000021 ),
 .UNSPECIFIED. ) ;
#11062=ADVANCED_FACE ( 'NONE', ( #57277, #52382 ), #42254, .F. ) ;
#11073=ORIENTED_EDGE ( 'NONE', *, *, #22102, .T. ) ;
#11079=DIRECTION ( 'NONE',  ( -1.000000000000000000, 0.000000000000000000, 0.000000000000000000 ) ) ;
#11083=CARTESIAN_POINT ( 'NONE',  ( 24.81126491645922982, 3.073463793308780279, -11.71256572910995963 ) ) ;
#11084=DIRECTION ( 'NONE',  ( 0.000000000000000000, 0.4595926418529958646, 0.8881298348521931008 ) ) ;
#11086=ORIENTED_EDGE ( 'NONE', *, *, #37913, .T. ) ;
#11091=CARTESIAN_POINT ( 'NONE',  ( 11.66889198463462662, 3.216368914751021268, -11.40336763631111339 ) ) ;
#11093=ORIENTED_EDGE ( 'NONE', *, *, #13301, .T. ) ;
#11097=CARTESIAN_POINT ( 'NONE',  ( 16.13936233968600220, -9.023335130797001113, -8.741328814538000813 ) ) ;
#11102=CARTESIAN_POINT ( 'NONE',  ( 23.56666365135700403, -9.114812703071004663, 8.684180617907001576 ) ) ;
#11103=DIRECTION ( 'NONE',  ( 0.000000000000000000, 0.000000000000000000, 1.000000000000000000 ) ) ;
#11107=CARTESIAN_POINT ( 'NONE',  ( 24.44496356232399847, -3.224881240379999792, -12.03535804424000055 ) ) ;
#11110=( BOUNDED_SURFACE ( )  B_SPLINE_SURFACE ( 3, 3, ( 
 ( #54329, #28470, #1895, #23555 ),
 ( #12381, #11677, #6430, #33015 ),
 ( #27780, #12033, #65855, #49090 ),
 ( #65154, #18321, #44896, #44212 ) ),
 .UNSPECIFIED., .F., .F., .T. ) 
 B_SPLINE_SURFACE_WITH_KNOTS ( ( 4, 4 ),
 ( 4, 4 ),
 ( 0.000000000000000000, 1.000000000000000000 ),
 ( 0.000000000000000000, 1.000000000000000000 ),
 .UNSPECIFIED. ) 
 GEOMETRIC_REPRESENTATION_ITEM ( )  RATIONAL_B_SPLINE_SURFACE ( (
 ( 1.512182578520000042, 1.160176301760999840, 1.160176301760999840, 1.512182578520000042),
 ( 1.111288591041000196, 0.8526025270081000196, 0.8526025270081000196, 1.111288591041000196),
 ( 1.111288591041000196, 0.8526025270081000196, 0.8526025270081000196, 1.111288591041000196),
 ( 1.512182578520000042, 1.160176301760999840, 1.160176301760999840, 1.512182578520000042) ) ) 
 REPRESENTATION_ITEM ( '' )  SURFACE ( )  );
#11114=B_SPLINE_CURVE_WITH_KNOTS ( 'NONE', 3,
 ( #7241, #61074, #2685, #23324 ),
 .UNSPECIFIED., .F., .F.,
 ( 4, 4 ),
 ( 0.000000000000000000, 1.000000000000000000 ),
 .UNSPECIFIED. ) ;
#11115=CARTESIAN_POINT ( 'NONE',  ( 25.30000327618300204, -1.393126554761421110, -11.43653827017141111 ) ) ;
#11127=CARTESIAN_POINT ( 'NONE',  ( 11.79999999550100220, 3.351258778187000242, -11.15757272551999968 ) ) ;
#11129=CARTESIAN_POINT ( 'NONE',  ( 18.24051303026600124, 3.055556278716000218, -11.39470302754000031 ) ) ;
#11132=CARTESIAN_POINT ( 'NONE',  ( 24.15440335769899960, -9.221781890355002176, -9.473822549412000527 ) ) ;
#11134=CARTESIAN_POINT ( 'NONE',  ( 23.60000000000000142, -10.96647536436334391, 8.588749203884328054 ) ) ;
#11135=ORIENTED_EDGE ( 'NONE', *, *, #50970, .T. ) ;
#11155=ORIENTED_EDGE ( 'NONE', *, *, #49991, .T. ) ;
#11157=CARTESIAN_POINT ( 'NONE',  ( 12.42828976145100128, -11.57811841779999895, 4.879106015068000346 ) ) ;
#11162=VERTEX_POINT ( 'NONE', #31760 ) ;
#11163=CARTESIAN_POINT ( 'NONE',  ( 24.98032374313059023, -11.50386448131031791, -3.228640037327431767 ) ) ;
#11182=DIRECTION ( 'NONE',  ( 1.000000000000000000, 0.000000000000000000, 0.000000000000000000 ) ) ;
#11184=B_SPLINE_CURVE_WITH_KNOTS ( 'NONE', 3,
 ( #58770, #10877, #6662, #44439, #1425, #22739, #44089, #53535, #5627, #43040 ),
 .UNSPECIFIED., .F., .F.,
 ( 4, 2, 2, 2, 4 ),
 ( 0.4999999997123694695, 0.6249999997842766719, 0.7499999998561844849, 0.8749999999280921870, 1.000000000000000000 ),
 .UNSPECIFIED. ) ;
#11208=EDGE_CURVE ( 'NONE', #65259, #33492, #22289, .T. ) ;
#11226=CARTESIAN_POINT ( 'NONE',  ( 23.80818154638642881, -9.703800845197944724, -9.420725050333308204 ) ) ;
#11227=CARTESIAN_POINT ( 'NONE',  ( 11.30000000000000071, 0.000000000000000000, 0.000000000000000000 ) ) ;
#11232=ORIENTED_EDGE ( 'NONE', *, *, #66802, .F. ) ;
#11234=CARTESIAN_POINT ( 'NONE',  ( 18.29999999997146887, -11.00695868226778629, 3.817556993357585249 ) ) ;
#11237=TOROIDAL_SURFACE ( 'NONE', #50336, 12.20000000000000107, 0.6999999999999999556 ) ;
#11241=CIRCLE ( 'NONE', #58161, 14.00000000000000000 ) ;
#11245=CARTESIAN_POINT ( 'NONE',  ( 11.50001544675000176, -9.368387413360784066, 8.415797411343536538 ) ) ;
#11251=ORIENTED_EDGE ( 'NONE', *, *, #6090, .F. ) ;
#11259=CARTESIAN_POINT ( 'NONE',  ( 13.60016906737400078, 3.366196210663000557E-13, 1.969535645684999935E-13 ) ) ;
#11260=EDGE_CURVE ( 'NONE', #10787, #15277, #26896, .T. ) ;
#11263=CARTESIAN_POINT ( 'NONE',  ( 23.56665676678100141, -2.935523947847999970, 13.67844066972000050 ) ) ;
#11265=CARTESIAN_POINT ( 'NONE',  ( 12.95917414208900098, 11.49387908994000007, 1.654391991822000030 ) ) ;
#11268=ORIENTED_EDGE ( 'NONE', *, *, #17210, .F. ) ;
#11281=EDGE_CURVE ( 'NONE', #39483, #6863, #58587, .T. ) ;
#11282=CARTESIAN_POINT ( 'NONE',  ( 18.21407466721599988, 11.71489335541000010, -3.703722432179000101 ) ) ;
#11285=ADVANCED_FACE ( 'NONE', ( #16693 ), #21803, .F. ) ;
#11287=CARTESIAN_POINT ( 'NONE',  ( 18.49969735796901205, 11.81669335334967386, -4.154069657518311587 ) ) ;
#11289=ORIENTED_EDGE ( 'NONE', *, *, #40346, .F. ) ;
#11302=EDGE_CURVE ( 'NONE', #37325, #68067, #48559, .T. ) ;
#11315=CARTESIAN_POINT ( 'NONE',  ( 11.49999672495000524, 4.789193247147742305, -10.68959786790916588 ) ) ;
#11318=CARTESIAN_POINT ( 'NONE',  ( 13.70003001321900271, -9.668726926528000476, -7.961868161445000425 ) ) ;
#11319=CARTESIAN_POINT ( 'NONE',  ( 24.39664325317268734, 3.224866859135877117, -12.03536696594411914 ) ) ;
#11320=CARTESIAN_POINT ( 'NONE',  ( 24.77999985543100081, -8.657366092043000450, 9.170186965892000330 ) ) ;
#11321=DIRECTION ( 'NONE',  ( 0.000000000000000000, 0.01629188381079070894, -0.9998672784534433644 ) ) ;
#11323=CARTESIAN_POINT ( 'NONE',  ( 24.87547883224999978, -11.55042359755999826, -3.247369794756999717 ) ) ;
#11327=CARTESIAN_POINT ( 'NONE',  ( 11.29996849689000271, 12.23272706294999956, 1.505586356912999912 ) ) ;
#11334=LINE ( 'NONE', #64810, #57413 ) ;
#11338=EDGE_LOOP ( 'NONE', ( #13904, #36654, #68852, #33894 ) ) ;
#11339=CARTESIAN_POINT ( 'NONE',  ( 23.59999193302000364, -13.22318594659000013, 4.267778254689999606 ) ) ;
#11340=ADVANCED_FACE ( 'NONE', ( #8966 ), #66662, .F. ) ;
#11344=ADVANCED_FACE ( 'NONE', ( #61081, #45009 ), #8626, .T. ) ;
#11350=ORIENTED_EDGE ( 'NONE', *, *, #53705, .T. ) ;
#11353=ORIENTED_EDGE ( 'NONE', *, *, #26753, .T. ) ;
#11359=CARTESIAN_POINT ( 'NONE',  ( 24.68353902991545468, 11.80738835872714176, -3.191231336988252565 ) ) ;
#11360=CARTESIAN_POINT ( 'NONE',  ( 11.49999035076000276, -3.886252136122000156, 11.90689009355000039 ) ) ;
#11362=CARTESIAN_POINT ( 'NONE',  ( 13.21911358530772773, -12.38522838340864851, -1.866030466704243551 ) ) ;
#11363=ORIENTED_EDGE ( 'NONE', *, *, #66913, .T. ) ;
#11365=B_SPLINE_CURVE_WITH_KNOTS ( 'NONE', 3,
 ( #41200, #14965, #63186, #3776 ),
 .UNSPECIFIED., .F., .F.,
 ( 4, 4 ),
 ( 0.000000000000000000, 1.000000000000000000 ),
 .UNSPECIFIED. ) ;
#11366=CARTESIAN_POINT ( 'NONE',  ( 17.79663207835866956, -11.53878384028511306, 4.871562533345485946 ) ) ;
#11371=CARTESIAN_POINT ( 'NONE',  ( 25.58980475334900362, -2.739986445787999436, 11.22452250057999912 ) ) ;
#11373=EDGE_LOOP ( 'NONE', ( #57939, #22315, #27172, #17037 ) ) ;
#11381=CARTESIAN_POINT ( 'NONE',  ( 17.74639017890714499, 11.23193386242191139, -3.094113022443028882 ) ) ;
#11383=AXIS2_PLACEMENT_3D ( 'NONE', #17270, #29159, #7466 ) ;
#11385=ADVANCED_FACE ( 'NONE', ( #35550 ), #40078, .T. ) ;
#11390=CARTESIAN_POINT ( 'NONE',  ( 24.23233723912900217, 9.064763380006999327, 9.162364161575000665 ) ) ;
#11412=CARTESIAN_POINT ( 'NONE',  ( 13.70003001321900271, 9.668726926528000476, 7.961868161445000425 ) ) ;
#11414=CARTESIAN_POINT ( 'NONE',  ( 24.30000000000000071, 11.77655473258999841, 4.190794510628000680 ) ) ;
#11417=CARTESIAN_POINT ( 'NONE',  ( 24.76777373405924720, 3.098484992731120435, -11.74891855520822403 ) ) ;
#11420=ORIENTED_EDGE ( 'NONE', *, *, #4466, .F. ) ;
#11421=CARTESIAN_POINT ( 'NONE',  ( 15.86547101025739792, -8.701845401024742799, -7.746061882572572443 ) ) ;
#11422=EDGE_CURVE ( 'NONE', #33943, #40655, #6958, .T. ) ;
#11431=ORIENTED_EDGE ( 'NONE', *, *, #23060, .F. ) ;
#11432=CARTESIAN_POINT ( 'NONE',  ( 16.09992084546400193, 8.991497430826001391, 8.719551690569000257 ) ) ;
#11433=CARTESIAN_POINT ( 'NONE',  ( 15.45446786537200090, -9.133287421996001854, -8.216743560820999548 ) ) ;
#11441=B_SPLINE_CURVE_WITH_KNOTS ( 'NONE', 3,
 ( #5865, #37344, #21943, #59352 ),
 .UNSPECIFIED., .F., .F.,
 ( 4, 4 ),
 ( 0.000000000000000000, 1.000000000000000000 ),
 .UNSPECIFIED. ) ;
#11448=EDGE_CURVE ( 'NONE', #1716, #16591, #7681, .T. ) ;
#11450=CARTESIAN_POINT ( 'NONE',  ( 11.44438160092000167, -12.37754422778999874, -1.524124373512000030 ) ) ;
#11455=CARTESIAN_POINT ( 'NONE',  ( 24.38452416568300052, 12.23040738833000063, 3.201157652712999901 ) ) ;
#11458=FACE_OUTER_BOUND ( 'NONE', #36302, .T. ) ;
#11465=CARTESIAN_POINT ( 'NONE',  ( 23.95224662109200153, -9.460740396185999046, -9.410539229647000070 ) ) ;
#11470=ORIENTED_EDGE ( 'NONE', *, *, #33144, .T. ) ;
#11474=CARTESIAN_POINT ( 'NONE',  ( 24.40777907822999993, 8.879621479992000133, -9.005112135964999709 ) ) ;
#11478=CARTESIAN_POINT ( 'NONE',  ( 24.30000000000000071, -8.810505093353000916, 8.810505093353000916 ) ) ;
#11482=CARTESIAN_POINT ( 'NONE',  ( 25.46373024410000241, -11.23407150414000100, 3.161076981347000103 ) ) ;
#11489=ORIENTED_EDGE ( 'NONE', *, *, #24621, .F. ) ;
#11490=CARTESIAN_POINT ( 'NONE',  ( 24.44916829770000177, 12.41483723393999838, -3.103225306172999964 ) ) ;
#11491=CARTESIAN_POINT ( 'NONE',  ( 12.79413755118400253, -11.93226572510000061, 3.260039893805000144 ) ) ;
#11497=ORIENTED_EDGE ( 'NONE', *, *, #42141, .T. ) ;
#11507=EDGE_CURVE ( 'NONE', #58173, #66927, #52998, .T. ) ;
#11509=DIRECTION ( 'NONE',  ( 1.000000000000000000, 0.000000000000000000, 0.000000000000000000 ) ) ;
#11510=ORIENTED_EDGE ( 'NONE', *, *, #17755, .F. ) ;
#11516=DIRECTION ( 'NONE',  ( -1.000000000000000000, 0.000000000000000000, 5.204170427930416866E-14 ) ) ;
#11520=CARTESIAN_POINT ( 'NONE',  ( 13.99955778315600163, 9.394084143528001363, 8.201088258230999628 ) ) ;
#11528=AXIS2_PLACEMENT_3D ( 'NONE', #55435, #24302, #39353 ) ;
#11534=DIRECTION ( 'NONE',  ( 0.000000000000000000, -1.000000000000000000, 0.000000000000000000 ) ) ;
#11537=CARTESIAN_POINT ( 'NONE',  ( 25.59997295081500113, -11.07537799752999952, 3.096069084855000320 ) ) ;
#11543=CONICAL_SURFACE ( 'NONE', #3708, 1.150084366271999725, 0.7854618604935084125 ) ;
#11546=AXIS2_PLACEMENT_3D ( 'NONE', #26511, #20570, #58663 ) ;
#11550=CARTESIAN_POINT ( 'NONE',  ( 17.79999999998900151, -3.595165934733000057, -11.99793354950999991 ) ) ;
#11557=CARTESIAN_POINT ( 'NONE',  ( 17.79999999998900151, 3.595165934733000057, 11.99793354950999991 ) ) ;
#11559=DIRECTION ( 'NONE',  ( -1.000000000000000000, 0.000000000000000000, 0.000000000000000000 ) ) ;
#11560=CARTESIAN_POINT ( 'NONE',  ( 23.91426698951526220, -9.509256905776609869, -9.346090767248723452 ) ) ;
#11561=PLANE ( 'NONE',  #67541 ) ;
#11566=CARTESIAN_POINT ( 'NONE',  ( 24.23232808299099972, 3.402461458659999494, -12.43151225365000023 ) ) ;
#11568=ORIENTED_EDGE ( 'NONE', *, *, #48217, .T. ) ;
#11571=AXIS2_PLACEMENT_3D ( 'NONE', #52650, #14571, #20493 ) ;
#11574=CARTESIAN_POINT ( 'NONE',  ( 11.79999999684100054, -3.345264396959000130, 11.86064773189999855 ) ) ;
#11582=CARTESIAN_POINT ( 'NONE',  ( 24.51327040776200050, 12.11106229541000090, 3.153269560843000363 ) ) ;
#11608=CARTESIAN_POINT ( 'NONE',  ( 24.66708179642670373, -12.30983497500974622, 2.983163088799908103 ) ) ;
#11617=B_SPLINE_SURFACE_WITH_KNOTS ( 'NONE', 3, 3, ( 
 ( #6423, #69029, #21142, #42468 ),
 ( #34056, #17628, #23550, #38954 ),
 ( #49779, #8166, #2235, #60615 ),
 ( #65501, #44890, #50467, #22855 ),
 ( #66194, #60960, #60271, #50131 ),
 ( #2569, #55026, #29515, #18316 ),
 ( #1890, #43848, #50818, #13075 ),
 ( #33708, #2913, #59917, #7127 ) ),
 .UNSPECIFIED., .F., .F., .F.,
 ( 4, 1, 1, 1, 1, 4 ),
 ( 4, 4 ),
 ( 0.008358950191421000986, 0.05882352941176000050, 0.1176470588234999892, 0.1764705882353000133, 0.2352941176471000095, 0.2534938933614000467 ),
 ( -0.1830994283965000080, 1.182949771275999984 ),
 .UNSPECIFIED. ) ;
#11622=CARTESIAN_POINT ( 'NONE',  ( 12.83903456837200174, 11.55258133652000119, -4.939873833509000889 ) ) ;
#11623=CARTESIAN_POINT ( 'NONE',  ( 17.57230163855200189, 11.81435006507999930, -3.324773181547000078 ) ) ;
#11633=LINE ( 'NONE', #59537, #9838 ) ;
#11636=CARTESIAN_POINT ( 'NONE',  ( 23.60000000000000142, -9.517611874540000017, 8.103398312166998352 ) ) ;
#11641=CONICAL_SURFACE ( 'NONE', #21673, 13.94999929345000211, 0.7853981072369679017 ) ;
#11647=CARTESIAN_POINT ( 'NONE',  ( 24.67921321800200118, -8.727630028894999725, 9.158313644156001132 ) ) ;
#11654=CARTESIAN_POINT ( 'NONE',  ( 30.60000000000000142, -2.052081084281999983E-07, 7.720759220056000238 ) ) ;
#11659=CARTESIAN_POINT ( 'NONE',  ( 24.66122485234200212, -3.625879222137000202, 12.20767898207999913 ) ) ;
#11663=CARTESIAN_POINT ( 'NONE',  ( 25.57778492944800064, -8.344458803148999237, 8.014471200166999765 ) ) ;
#11666=CARTESIAN_POINT ( 'NONE',  ( 25.41680095681100227, -11.20712209151000138, -3.225979711303999853 ) ) ;
#11671=CARTESIAN_POINT ( 'NONE',  ( 25.59994555223600088, -0.6783951095372073858, -11.19994871957819704 ) ) ;
#11673=CARTESIAN_POINT ( 'NONE',  ( 13.18628609634500215, 12.21854424350999935, 1.979874043355999813 ) ) ;
#11674=ORIENTED_EDGE ( 'NONE', *, *, #52036, .F. ) ;
#11675=AXIS2_PLACEMENT_3D ( 'NONE', #15722, #52430, #63605 ) ;
#11676=ADVANCED_FACE ( 'NONE', ( #25737 ), #15592, .T. ) ;
#11677=CARTESIAN_POINT ( 'NONE',  ( 23.89320776801300283, 8.283889223751996767, 7.778387372934005839 ) ) ;
#11684=CARTESIAN_POINT ( 'NONE',  ( 23.76529063391505758, -13.07188707895195456, 3.759452220472195627 ) ) ;
#11687=CARTESIAN_POINT ( 'NONE',  ( 11.50029455687000102, -11.56505190006999939, -1.404305717648999918 ) ) ;
#11702=CARTESIAN_POINT ( 'NONE',  ( 24.70905576447193752, 11.78230593457693942, -3.190800434545450592 ) ) ;
#11709=DIRECTION ( 'NONE',  ( 0.000000000000000000, 0.7614089499631908620, -0.6482718649732929217 ) ) ;
#11712=CARTESIAN_POINT ( 'NONE',  ( 25.08881765777200457, 3.215721225475999923, 11.60740081808000035 ) ) ;
#11714=CARTESIAN_POINT ( 'NONE',  ( 25.36466043037300011, -2.635483744749000046, 11.32507393831999920 ) ) ;
#11721=CARTESIAN_POINT ( 'NONE',  ( 16.03314433152364771, 8.943717616153273653, 8.673217039016851260 ) ) ;
#11727=B_SPLINE_CURVE_WITH_KNOTS ( 'NONE', 3,
 ( #57301, #20943, #9404, #10440 ),
 .UNSPECIFIED., .F., .F.,
 ( 4, 4 ),
 ( 0.000000000000000000, 1.000000000000000000 ),
 .UNSPECIFIED. ) ;
#11738=EDGE_CURVE ( 'NONE', #63300, #21757, #55250, .T. ) ;
#11739=LINE ( 'NONE', #33082, #39398 ) ;
#11740=CARTESIAN_POINT ( 'NONE',  ( 23.60205915885299888, 9.223492163361996177, -8.025915643364996299 ) ) ;
#11741=B_SPLINE_CURVE_WITH_KNOTS ( 'NONE', 3,
 ( #6639, #37766, #17125, #22716 ),
 .UNSPECIFIED., .F., .F.,
 ( 4, 4 ),
 ( 0.000000000000000000, 1.000000000000000000 ),
 .UNSPECIFIED. ) ;
#11748=CARTESIAN_POINT ( 'NONE',  ( 24.34833211465999980, 8.895958282168665576, -8.895958282168665576 ) ) ;
#11752=ORIENTED_EDGE ( 'NONE', *, *, #21874, .T. ) ;
#11759=VERTEX_POINT ( 'NONE', #27457 ) ;
#11764=CARTESIAN_POINT ( 'NONE',  ( 25.29987654162099986, -8.533547851352999203, -7.925583806936000286 ) ) ;
#11766=B_SPLINE_CURVE_WITH_KNOTS ( 'NONE', 3,
 ( #2482, #7035, #28721, #33961 ),
 .UNSPECIFIED., .F., .F.,
 ( 4, 4 ),
 ( 0.000000000000000000, 1.000000000000000000 ),
 .UNSPECIFIED. ) ;
#11769=CARTESIAN_POINT ( 'NONE',  ( 17.60000002773078975, -12.03387896817346281, 3.206083673428302028 ) ) ;
#11771=CARTESIAN_POINT ( 'NONE',  ( 24.44496356299600137, 12.03536643057000077, 3.224849944858999784 ) ) ;
#11778=AXIS2_PLACEMENT_3D ( 'NONE', #18767, #13184, #2336 ) ;
#11779=CARTESIAN_POINT ( 'NONE',  ( 15.36385332268500115, -9.394483288005998745, -8.200629419667000874 ) ) ;
#11781=ORIENTED_EDGE ( 'NONE', *, *, #11820, .F. ) ;
#11782=B_SPLINE_SURFACE_WITH_KNOTS ( 'NONE', 3, 3, ( 
 ( #61972, #35408, #56734, #46584 ),
 ( #30171, #35745, #67891, #25246 ),
 ( #49639, #12934, #50335, #24452 ),
 ( #2779, #7685, #39154, #23065 ),
 ( #24105, #12585, #6988, #13627 ),
 ( #1745, #34260, #55583, #28674 ),
 ( #34952, #44414, #56266, #29027 ),
 ( #45777, #18524, #2433, #61169 ),
 ( #13290, #50683, #55232, #23761 ),
 ( #33567, #3121, #33915, #67088 ),
 ( #66750, #60822, #51021, #8376 ),
 ( #8030, #65714, #29719, #60478 ) ),
 .UNSPECIFIED., .F., .F., .F.,
 ( 4, 1, 1, 1, 1, 1, 1, 1, 1, 4 ),
 ( 4, 4 ),
 ( 0.5515740600308000063, 0.5999999999999999778, 0.6500000000000000222, 0.6999999999999999556, 0.7500000000000000000, 0.8000000000000000444, 0.8499999999999999778, 0.9000000000000000222, 0.9499999999999999556, 0.9893625964778000048 ),
 ( -0.2706692301633999986, 1.270787907492000102 ),
 .UNSPECIFIED. ) ;
#11784=EDGE_CURVE ( 'NONE', #16879, #36918, #50863, .T. ) ;
#11789=EDGE_CURVE ( 'NONE', #30003, #25573, #19572, .T. ) ;
#11796=CARTESIAN_POINT ( 'NONE',  ( 11.68591862085600219, -12.43715917574999885, -1.778745665763999950 ) ) ;
#11803=FACE_OUTER_BOUND ( 'NONE', #66462, .T. ) ;
#11810=CARTESIAN_POINT ( 'NONE',  ( 18.07439970769999960, 3.110573872314000177, -11.47478625844000177 ) ) ;
#11813=CARTESIAN_POINT ( 'NONE',  ( 23.86978363481900089, -9.627977290743000793, -9.781481518887000348 ) ) ;
#11814=EDGE_CURVE ( 'NONE', #64287, #12534, #29386, .T. ) ;
#11815=CARTESIAN_POINT ( 'NONE',  ( 24.42275932749500100, -8.981807471221001649, 9.518608303324000985 ) ) ;
#11820=EDGE_CURVE ( 'NONE', #33864, #41132, #32991, .T. ) ;
#11821=EDGE_CURVE ( 'NONE', #36754, #68281, #4336, .T. ) ;
#11823=CARTESIAN_POINT ( 'NONE',  ( 24.51327040776200050, 8.786342692376999608, -8.911852834221001274 ) ) ;
#11826=CARTESIAN_POINT ( 'NONE',  ( 25.29881353977600256, 2.991656389957999984, -11.41428782199000125 ) ) ;
#11829=CARTESIAN_POINT ( 'NONE',  ( 24.67921139482200132, 8.727627377900999406, -9.158314240160001063 ) ) ;
#11837=ORIENTED_EDGE ( 'NONE', *, *, #38747, .T. ) ;
#11838=CARTESIAN_POINT ( 'NONE',  ( 24.60170725920900026, 12.45697517054999892, -2.983025822496999879 ) ) ;
#11841=CARTESIAN_POINT ( 'NONE',  ( 11.86287780003600112, -11.93788271774999998, 3.912105503483000124 ) ) ;
#11845=CARTESIAN_POINT ( 'NONE',  ( 23.52062801899400313, 3.100976312918000133, 13.78346562762999916 ) ) ;
#11847=CARTESIAN_POINT ( 'NONE',  ( 24.08707339289249916, -9.231394016030909810, 9.185131054776540793 ) ) ;
#11852=ORIENTED_EDGE ( 'NONE', *, *, #59211, .F. ) ;
#11854=CARTESIAN_POINT ( 'NONE',  ( 24.42400777655799970, 12.73291499258000137, -3.018588619611000112 ) ) ;
#11860=CARTESIAN_POINT ( 'NONE',  ( 23.89320776801300283, 11.54071136943000297, 2.936967729234000402 ) ) ;
#11861=B_SPLINE_CURVE_WITH_KNOTS ( 'NONE', 3,
 ( #13485, #8910, #51894, #14166 ),
 .UNSPECIFIED., .F., .F.,
 ( 4, 4 ),
 ( 0.000000000000000000, 1.000000000000000000 ),
 .UNSPECIFIED. ) ;
#11863=ORIENTED_EDGE ( 'NONE', *, *, #63116, .T. ) ;
#11869=CARTESIAN_POINT ( 'NONE',  ( 18.26272493605000236, -11.59941211794000004, 4.057574997846999487 ) ) ;
#11871=CARTESIAN_POINT ( 'NONE',  ( 13.55563772304700088, 9.581334502426001265, 7.839063693813000278 ) ) ;
#11877=ORIENTED_EDGE ( 'NONE', *, *, #22358, .F. ) ;
#11885=CARTESIAN_POINT ( 'NONE',  ( 24.53429014209899961, 12.47024915613999951, 3.026245713505000268 ) ) ;
#11891=B_SPLINE_CURVE_WITH_KNOTS ( 'NONE', 3,
 ( #33739, #18687, #28143, #23241 ),
 .UNSPECIFIED., .F., .F.,
 ( 4, 4 ),
 ( 0.000000000000000000, 1.000000000000000000 ),
 .UNSPECIFIED. ) ;
#11893=CARTESIAN_POINT ( 'NONE',  ( 24.40777907822999993, -3.358845133677000216, -12.19253384565000076 ) ) ;
#11894=DIRECTION ( 'NONE',  ( 0.000000000000000000, -2.657874751134998991E-08, 0.9999999999999996669 ) ) ;
#11911=CARTESIAN_POINT ( 'NONE',  ( 11.79999999684100054, 12.15995044155999949, 2.000340912084999978 ) ) ;
#11914=CARTESIAN_POINT ( 'NONE',  ( 23.72389630350670586, -9.881498421283909650, -9.454772414382880186 ) ) ;
#11915=CARTESIAN_POINT ( 'NONE',  ( 11.90028836426309589, -11.81686663804793724, 4.153560932553760132 ) ) ;
#11917=B_SPLINE_CURVE_WITH_KNOTS ( 'NONE', 3,
 ( #61501, #10328, #63804, #15913 ),
 .UNSPECIFIED., .F., .F.,
 ( 4, 4 ),
 ( 0.000000000000000000, 1.000000000000000000 ),
 .UNSPECIFIED. ) ;
#11922=CARTESIAN_POINT ( 'NONE',  ( 13.21722669115800031, -12.32379348829999977, -1.906876488274000137 ) ) ;
#11931=CARTESIAN_POINT ( 'NONE',  ( 18.30000103245939158, -11.66744832144745203, 3.971921730545766138 ) ) ;
#11933=COLOUR_RGB ( '', 0.66274510, 0.83137255, 0.94901961) ;
#11938=DIRECTION ( 'NONE',  ( 0.000000000000000000, -0.4595937023756062056, -0.8881292860483110951 ) ) ;
#11940=DIRECTION ( 'NONE',  ( 8.953188301455325544E-11, 0.2714597137498098722, -0.9624498032681346738 ) ) ;
#11943=EDGE_LOOP ( 'NONE', ( #30382, #37142, #32762, #15048 ) ) ;
#11945=B_SPLINE_CURVE_WITH_KNOTS ( 'NONE', 3,
 ( #10650, #31996, #16921, #21150, #58896, #42477, #15896, #58206, #31643, #33019, #10999, #48063, #52966, #27428 ),
 .UNSPECIFIED., .F., .F.,
 ( 4, 2, 2, 2, 2, 2, 4 ),
 ( 0.000000000000000000, 0.1250000000000008327, 0.2500000000000016653, 0.5000000000000029976, 0.6250000000000021094, 0.7500000000000014433, 1.000000000000000000 ),
 .UNSPECIFIED. ) ;
#11951=CARTESIAN_POINT ( 'NONE',  ( 23.71151258249847871, 3.235038466978575666, -13.31088662455443128 ) ) ;
#11953=CARTESIAN_POINT ( 'NONE',  ( 24.34832137511671135, -8.810502415987484071, -8.810502415987484071 ) ) ;
#11955=CARTESIAN_POINT ( 'NONE',  ( 11.60581233665799950, 3.287326773434000149, -11.32699406611000015 ) ) ;
#11972=DIRECTION ( 'NONE',  ( -1.000000000000000000, 0.000000000000000000, 0.000000000000000000 ) ) ;
#11976=CARTESIAN_POINT ( 'NONE',  ( 17.56088320631100075, 12.16696388215000013, -3.135175697041999499 ) ) ;
#11987=FACE_OUTER_BOUND ( 'NONE', #9223, .T. ) ;
#11988=DIRECTION ( 'NONE',  ( 0.000000000000000000, -1.000000000000000000, 0.000000000000000000 ) ) ;
#11989=PLANE ( 'NONE',  #67047 ) ;
#11990=CARTESIAN_POINT ( 'NONE',  ( 24.45617572362546355, 12.38364420599299898, -3.108063458830152115 ) ) ;
#12008=ORIENTED_EDGE ( 'NONE', *, *, #58641, .F. ) ;
#12009=EDGE_CURVE ( 'NONE', #8238, #28950, #1009, .T. ) ;
#12011=DIRECTION ( 'NONE',  ( -1.000000000000000000, 0.000000000000000000, 0.000000000000000000 ) ) ;
#12015=CARTESIAN_POINT ( 'NONE',  ( 24.51228084553499897, -3.325039717427999975, 12.06631758408999922 ) ) ;
#12022=CARTESIAN_POINT ( 'NONE',  ( 11.49978667957999967, -12.43119799159999950, -1.530013559959999991 ) ) ;
#12023=AXIS2_PLACEMENT_3D ( 'NONE', #46368, #62435, #47401 ) ;
#12025=CARTESIAN_POINT ( 'NONE',  ( 14.03176826122700227, -8.820984799833000878, -7.691098505213000536 ) ) ;
#12026=DIRECTION ( 'NONE',  ( 1.000000000000000000, 0.000000000000000000, 0.000000000000000000 ) ) ;
#12033=CARTESIAN_POINT ( 'NONE',  ( 23.89320776801300283, 8.313844348291002717, 8.526065358951003148 ) ) ;
#12037=CARTESIAN_POINT ( 'NONE',  ( 24.73254324275212213, 8.642950426568003053, -8.588141212706347005 ) ) ;
#12058=CARTESIAN_POINT ( 'NONE',  ( 24.92738949723038999, 11.56001277368646640, -3.214474823069669807 ) ) ;
#12067=CARTESIAN_POINT ( 'NONE',  ( 18.31644260632910814, -11.66217921385985079, 4.569092474540076054 ) ) ;
#12081=ADVANCED_FACE ( 'NONE', ( #28503 ), #30223, .T. ) ;
#12083=CARTESIAN_POINT ( 'NONE',  ( 24.84547362285450234, 8.580307739459316352, -9.011481308573959126 ) ) ;
#12092=CIRCLE ( 'NONE', #47833, 0.2000000000000004274 ) ;
#12096=CARTESIAN_POINT ( 'NONE',  ( 17.91920925550502020, 10.80976535600978572, -4.345114692431126358 ) ) ;
#12101=CARTESIAN_POINT ( 'NONE',  ( 13.49980696793000057, -9.514462421839999351, -7.834836582454001608 ) ) ;
#12108=CARTESIAN_POINT ( 'NONE',  ( 24.39664737804999817, 8.853227125957333854, -8.853227125957333854 ) ) ;
#12112=ORIENTED_EDGE ( 'NONE', *, *, #15139, .T. ) ;
#12115=B_SPLINE_CURVE_WITH_KNOTS ( 'NONE', 3,
 ( #28011, #65043, #59124, #33258 ),
 .UNSPECIFIED., .F., .F.,
 ( 4, 4 ),
 ( 0.000000000000000000, 1.000000000000000000 ),
 .UNSPECIFIED. ) ;
#12119=VERTEX_POINT ( 'NONE', #41728 ) ;
#12124=CARTESIAN_POINT ( 'NONE',  ( 16.31144947526900069, 3.254927130315000028, 11.33654363332999893 ) ) ;
#12127=CARTESIAN_POINT ( 'NONE',  ( 16.01451879247663967, -8.585242134254837509, -7.875498515381707421 ) ) ;
#12143=EDGE_CURVE ( 'NONE', #39483, #61665, #30751, .T. ) ;
#12154=CARTESIAN_POINT ( 'NONE',  ( 25.29989727901499919, -2.078227429405999693, -11.31065739696999906 ) ) ;
#12158=DIRECTION ( 'NONE',  ( -0.9999999999995587974, -4.522743910995809051E-07, -8.233165796359658046E-07 ) ) ;
#12167=CARTESIAN_POINT ( 'NONE',  ( 18.35192688406300121, 2.803631260452999818, -11.45923525916999886 ) ) ;
#12169=EDGE_CURVE ( 'NONE', #16567, #62492, #57453, .T. ) ;
#12173=CARTESIAN_POINT ( 'NONE',  ( 23.54905859008200153, -10.40163749118999981, -9.427750568795000063 ) ) ;
#12175=CARTESIAN_POINT ( 'NONE',  ( 24.57788509281051148, 3.600249671649326189, -12.25995025209595646 ) ) ;
#12180=CARTESIAN_POINT ( 'NONE',  ( 23.60205915885299888, -2.338900754078999444, 12.00073634674999212 ) ) ;
#12183=CARTESIAN_POINT ( 'NONE',  ( 24.30001697071400457, -8.938702858184001343, 8.938676113071998941 ) ) ;
#12189=EDGE_LOOP ( 'NONE', ( #7887, #32701, #55199, #22501 ) ) ;
#12196=EDGE_LOOP ( 'NONE', ( #65186, #56702, #63964, #42047 ) ) ;
#12197=CARTESIAN_POINT ( 'NONE',  ( 24.50399615158200106, 12.34862307823000016, -3.085465605547000223 ) ) ;
#12198=CARTESIAN_POINT ( 'NONE',  ( 12.40355051044899959, -11.78614875273999907, 3.442261952866000119 ) ) ;
#12205=CARTESIAN_POINT ( 'NONE',  ( 23.91319624006256461, -9.510189266786756690, 9.347864195410048538 ) ) ;
#12209=VERTEX_POINT ( 'NONE', #67949 ) ;
#12212=CARTESIAN_POINT ( 'NONE',  ( 23.64843174477000076, 13.35727533436999792, -3.864837375578999978 ) ) ;
#12216=DIRECTION ( 'NONE',  ( 0.000000000000000000, 0.1807154286440004198, 0.9835354258236025382 ) ) ;
#12222=B_SPLINE_SURFACE_WITH_KNOTS ( 'NONE', 3, 3, ( 
 ( #46399, #56541, #51295, #29653 ),
 ( #3391, #56199, #66680, #51634 ),
 ( #62124, #28962, #45373, #8645 ),
 ( #8984, #19827, #40455, #45028 ),
 ( #14243, #18803, #41158, #50267 ),
 ( #2370, #67358, #56887, #19132 ) ),
 .UNSPECIFIED., .F., .F., .F.,
 ( 4, 1, 1, 4 ),
 ( 4, 4 ),
 ( 0.1423941366080999915, 0.3333333333333000081, 0.6666666666667000474, 0.8219462302419999755 ),
 ( -0.1256563615234000120, 1.125656361508000192 ),
 .UNSPECIFIED. ) ;
#12227=FACE_OUTER_BOUND ( 'NONE', #31742, .T. ) ;
#12238=ORIENTED_EDGE ( 'NONE', *, *, #22304, .F. ) ;
#12244=CARTESIAN_POINT ( 'NONE',  ( 18.44496314779700086, 2.860815007322000447, -12.13831535021000008 ) ) ;
#12251=FACE_OUTER_BOUND ( 'NONE', #42973, .T. ) ;
#12270=B_SPLINE_CURVE_WITH_KNOTS ( 'NONE', 3,
 ( #65490, #39281, #33000, #1527 ),
 .UNSPECIFIED., .F., .F.,
 ( 4, 4 ),
 ( 0.000000000000000000, 1.000000000000000000 ),
 .UNSPECIFIED. ) ;
#12274=DIRECTION ( 'NONE',  ( 0.000000000000000000, 0.000000000000000000, 1.000000000000000000 ) ) ;
#12280=CARTESIAN_POINT ( 'NONE',  ( 24.25968945202800242, 3.166454503780999907, -12.13789061559999993 ) ) ;
#12281=CARTESIAN_POINT ( 'NONE',  ( 12.99284288850700086, -12.22216846288000092, -1.954503247608000205 ) ) ;
#12282=VERTEX_POINT ( 'NONE', #27034 ) ;
#12292=CARTESIAN_POINT ( 'NONE',  ( 15.83777337640987781, 9.021763928136897093, 8.400065602738665760 ) ) ;
#12301=DIRECTION ( 'NONE',  ( 0.7071058810607747658, -0.7071076813111745185, 3.975037112901852268E-09 ) ) ;
#12309=CARTESIAN_POINT ( 'NONE',  ( 11.74274107869599959, 3.315287298500999569, -11.22371330986000082 ) ) ;
#12311=CARTESIAN_POINT ( 'NONE',  ( 13.49994651945300284, -12.07042783918999795, -2.492331243371999960 ) ) ;
#12315=ORIENTED_EDGE ( 'NONE', *, *, #33538, .T. ) ;
#12316=CONICAL_SURFACE ( 'NONE', #64742, 11.74991359182999950, 0.7853990805437361944 ) ;
#12322=CARTESIAN_POINT ( 'NONE',  ( 23.59999462723899910, 13.22316330987000121, -4.267799687262000319 ) ) ;
#12325=ORIENTED_EDGE ( 'NONE', *, *, #1674, .F. ) ;
#12330=CARTESIAN_POINT ( 'NONE',  ( 17.60750054167100132, 12.16746880438999945, -3.133263442192999904 ) ) ;
#12331=ADVANCED_FACE ( 'NONE', ( #34704 ), #35, .F. ) ;
#12337=DIRECTION ( 'NONE',  ( 1.000000000000000000, 0.000000000000000000, 0.000000000000000000 ) ) ;
#12358=ORIENTED_EDGE ( 'NONE', *, *, #18673, .F. ) ;
#12366=CARTESIAN_POINT ( 'NONE',  ( 24.35145719007200071, -3.377064811435000369, 12.26055847765000095 ) ) ;
#12370=CARTESIAN_POINT ( 'NONE',  ( 25.37703487173499894, -8.494994160653000392, 7.921071945508999512 ) ) ;
#12381=CARTESIAN_POINT ( 'NONE',  ( 24.35365242081700288, 8.326148686889998984, 7.789520173161003314 ) ) ;
#12407=CARTESIAN_POINT ( 'NONE',  ( 16.39955778315600199, 3.526114926816000139, 11.96132012103000086 ) ) ;
#12418=EDGE_CURVE ( 'NONE', #48090, #64727, #63530, .T. ) ;
#12422=CARTESIAN_POINT ( 'NONE',  ( 24.48565841925800157, -3.324180655266999906, 12.08642999707000065 ) ) ;
#12429=CARTESIAN_POINT ( 'NONE',  ( 23.63861704028150612, 3.356905873913091920, -13.53849385471555244 ) ) ;
#12435=CARTESIAN_POINT ( 'NONE',  ( 24.72545694048200104, -8.702406706990998941, -9.187175443698999189 ) ) ;
#12441=CARTESIAN_POINT ( 'NONE',  ( 24.32155146060084050, -3.683040365894125756, 12.56970734039675008 ) ) ;
#12445=CARTESIAN_POINT ( 'NONE',  ( 24.35365242081700288, 8.326148686863003689, -7.789520173261992753 ) ) ;
#12447=CARTESIAN_POINT ( 'NONE',  ( 17.80000000005199823, -3.345268251980999974, -11.86064071431999878 ) ) ;
#12466=DIRECTION ( 'NONE',  ( 1.000000000000000000, 0.000000000000000000, 0.000000000000000000 ) ) ;
#12467=CARTESIAN_POINT ( 'NONE',  ( 15.86222979673600264, 3.623677739266000231, 11.32125985288999992 ) ) ;
#12478=EDGE_CURVE ( 'NONE', #45907, #40201, #35199, .T. ) ;
#12480=CARTESIAN_POINT ( 'NONE',  ( 23.58435508815700032, -13.25843894756000019, -4.303664095111000343 ) ) ;
#12481=SURFACE_STYLE_FILL_AREA ( #27524 ) ;
#12484=CARTESIAN_POINT ( 'NONE',  ( 23.75090057454168146, 13.09200471557739220, -3.783062315943054088 ) ) ;
#12488=CARTESIAN_POINT ( 'NONE',  ( 24.30001680106099826, 12.21047197645999915, -3.271805488357999891 ) ) ;
#12493=VERTEX_POINT ( 'NONE', #8685 ) ;
#12499=EDGE_CURVE ( 'NONE', #51109, #1148, #39688, .T. ) ;
#12502=CARTESIAN_POINT ( 'NONE',  ( 24.33639490202200406, 12.30598233413000031, 3.219714224404999658 ) ) ;
#12505=DIRECTION ( 'NONE',  ( 1.000000000000000000, 0.000000000000000000, 0.000000000000000000 ) ) ;
#12509=CARTESIAN_POINT ( 'NONE',  ( 25.46372189163300348, -2.879475976718999686, 11.30953721564000070 ) ) ;
#12518=CARTESIAN_POINT ( 'NONE',  ( 23.55356531116300189, -10.33133730171999964, 9.496498206886998972 ) ) ;
#12524=CARTESIAN_POINT ( 'NONE',  ( 15.90018573812068325, -5.468217585226445188, -10.55609518975756345 ) ) ;
#12526=ORIENTED_EDGE ( 'NONE', *, *, #6571, .F. ) ;
#12528=CARTESIAN_POINT ( 'NONE',  ( 24.48566039390000171, 3.324180779519999795, -12.08642902895999782 ) ) ;
#12534=VERTEX_POINT ( 'NONE', #55554 ) ;
#12541=CARTESIAN_POINT ( 'NONE',  ( 24.70770306079000278, 12.32897093721000026, -2.948671852896999734 ) ) ;
#12542=CARTESIAN_POINT ( 'NONE',  ( 12.01716035628400192, -11.91307312420999942, 3.686993282830000052 ) ) ;
#12550=CARTESIAN_POINT ( 'NONE',  ( 24.17844123396919542, -9.099783653359832414, 9.084867597324226551 ) ) ;
#12553=CARTESIAN_POINT ( 'NONE',  ( 12.80000000000000071, 11.23412379136000006, -3.084957477885999833 ) ) ;
#12563=EDGE_CURVE ( 'NONE', #8116, #32306, #16847, .T. ) ;
#12566=CARTESIAN_POINT ( 'NONE',  ( 24.11585380241538701, 9.189141416228876480, 9.154356187537644018 ) ) ;
#12567=EDGE_LOOP ( 'NONE', ( #29757, #36518, #56031, #32286, #36477 ) ) ;
#12571=CARTESIAN_POINT ( 'NONE',  ( 24.35365242081699932, 3.253466243134998326, -12.21167519469000240 ) ) ;
#12573=CARTESIAN_POINT ( 'NONE',  ( 18.10229711294200072, -11.55827859785000022, 4.675888931126000791 ) ) ;
#12585=CARTESIAN_POINT ( 'NONE',  ( 23.66588336739700082, -3.239807211238000306, 13.42507355106999967 ) ) ;
#12586=ADVANCED_FACE ( 'NONE', ( #35266 ), #34584, .F. ) ;
#12588=CARTESIAN_POINT ( 'NONE',  ( 18.35309808591700076, 2.844562563850999926, -12.04738788559999918 ) ) ;
#12593=EDGE_LOOP ( 'NONE', ( #49950, #20767, #11073, #41099, #26352 ) ) ;
#12597=B_SPLINE_CURVE_WITH_KNOTS ( 'NONE', 3,
 ( #1983, #44645, #39382, #27867 ),
 .UNSPECIFIED., .F., .F.,
 ( 4, 4 ),
 ( 0.000000000000000000, 1.000000000000000000 ),
 .UNSPECIFIED. ) ;
#12604=VERTEX_POINT ( 'NONE', #61483 ) ;
#12625=ADVANCED_FACE ( 'NONE', ( #18842 ), #47798, .F. ) ;
#12636=CARTESIAN_POINT ( 'NONE',  ( 18.50001572531400384, 0.9783175634148698618, 12.52499999877128722 ) ) ;
#12648=ORIENTED_EDGE ( 'NONE', *, *, #68468, .F. ) ;
#12651=CARTESIAN_POINT ( 'NONE',  ( 23.63923232067427094, 13.40729140062978075, -3.856841352120893074 ) ) ;
#12656=CARTESIAN_POINT ( 'NONE',  ( 11.56631965465000178, 3.502676170607000206, -11.07146920481999963 ) ) ;
#12661=CARTESIAN_POINT ( 'NONE',  ( 24.30000000000000071, 2.078227429405999693, -11.31065739696999906 ) ) ;
#12666=CIRCLE ( 'NONE', #24938, 14.00000000000000533 ) ;
#12672=EDGE_CURVE ( 'NONE', #25788, #17060, #13940, .T. ) ;
#12673=CARTESIAN_POINT ( 'NONE',  ( 24.35365242081699932, -8.948887819794997256, -8.923422014253004519 ) ) ;
#12678=CARTESIAN_POINT ( 'NONE',  ( 23.58437025649000063, -2.901519131754999758, -13.63407372122000005 ) ) ;
#12682=DIRECTION ( 'NONE',  ( 0.000000000000000000, 0.7180578485451756254, 0.6959834237556764558 ) ) ;
#12705=VERTEX_POINT ( 'NONE', #52863 ) ;
#12707=ADVANCED_FACE ( 'NONE', ( #406 ), #20997, .T. ) ;
#12710=DIRECTION ( 'NONE',  ( 0.000000000000000000, -0.001485959642859940649, 0.9999988959613604900 ) ) ;
#12714=CARTESIAN_POINT ( 'NONE',  ( 11.49999672495000169, 7.851643750443685121, -8.692270414123809630 ) ) ;
#12719=CARTESIAN_POINT ( 'NONE',  ( 25.57778554945400273, 11.11296393906000013, 3.219278657787000064 ) ) ;
#12724=CARTESIAN_POINT ( 'NONE',  ( 14.04832727683000115, -8.838110522795000534, -7.948685794524999793 ) ) ;
#12725=DIRECTION ( 'NONE',  ( -1.000000000000000000, 0.000000000000000000, 0.000000000000000000 ) ) ;
#12730=VERTEX_POINT ( 'NONE', #31893 ) ;
#12734=DIRECTION ( 'NONE',  ( 0.000000000000000000, 0.1623203401144080182, -0.9867381147929490393 ) ) ;
#12746=VERTEX_POINT ( 'NONE', #43416 ) ;
#12752=B_SPLINE_CURVE_WITH_KNOTS ( 'NONE', 3,
 ( #51287, #56191, #4064, #30317 ),
 .UNSPECIFIED., .F., .F.,
 ( 4, 4 ),
 ( 0.4999999894681322887, 1.000000000000000000 ),
 .UNSPECIFIED. ) ;
#12753=CARTESIAN_POINT ( 'NONE',  ( 24.51105662686868669, -3.208409238885217896, 11.97394890221126751 ) ) ;
#12754=CYLINDRICAL_SURFACE ( 'NONE', #43910, 14.00000000000000000 ) ;
#12755=CARTESIAN_POINT ( 'NONE',  ( 24.35365242081700288, 2.582848009905001074, 11.10541636514000174 ) ) ;
#12759=ORIENTED_EDGE ( 'NONE', *, *, #55009, .T. ) ;
#12770=CARTESIAN_POINT ( 'NONE',  ( 24.69899731016300137, -3.637719133123000326, 12.18533670124999979 ) ) ;
#12772=ORIENTED_EDGE ( 'NONE', *, *, #48128, .F. ) ;
#12790=VERTEX_POINT ( 'NONE', #47624 ) ;
#12798=CARTESIAN_POINT ( 'NONE',  ( 13.70005190196300227, -9.005348107749998832, -7.391036106496999381 ) ) ;
#12802=ORIENTED_EDGE ( 'NONE', *, *, #12143, .T. ) ;
#12805=CARTESIAN_POINT ( 'NONE',  ( 24.16198515854589246, -12.44540882913624635, -3.348940053833783015 ) ) ;
#12811=FACE_OUTER_BOUND ( 'NONE', #57862, .T. ) ;
#12818=EDGE_CURVE ( 'NONE', #54214, #42540, #6822, .T. ) ;
#12820=FACE_OUTER_BOUND ( 'NONE', #39149, .T. ) ;
#12823=VERTEX_POINT ( 'NONE', #11574 ) ;
#12825=CARTESIAN_POINT ( 'NONE',  ( 18.30003129332100187, 2.732683818840999646, 11.53064095373000164 ) ) ;
#12838=CARTESIAN_POINT ( 'NONE',  ( 23.71897770753286849, -3.252386419300755893, -13.29323848889808701 ) ) ;
#12839=CARTESIAN_POINT ( 'NONE',  ( 24.59999999957999961, 2.749830087550999854E-09, -4.999999999859999988 ) ) ;
#12840=EDGE_CURVE ( 'NONE', #37115, #28639, #40143, .T. ) ;
#12854=ORIENTED_EDGE ( 'NONE', *, *, #35325, .T. ) ;
#12855=CARTESIAN_POINT ( 'NONE',  ( 18.02410434383600091, 3.285250940561000199, 11.23276246309000115 ) ) ;
#12858=LINE ( 'NONE', #50946, #50494 ) ;
#12861=B_SPLINE_CURVE_WITH_KNOTS ( 'NONE', 3,
 ( #58921, #63462, #20824, #42161, #15585, #537, #43184, #26423, #42840, #63809, #64150, #31668, #64488, #16610, #52990, #5086, #47749, #69064, #37935, #31324, #5435, #21170, #15918, #10675, #32022, #26775, #66442, #18214, #29063, #38852, #28018 ),
 .UNSPECIFIED., .F., .F.,
 ( 4, 2, 2, 1, 1, 2, 2, 2, 1, 2, 2, 2, 2, 2, 2, 2, 4 ),
 ( 0.000000000000000000, 0.06250000000001527944, 0.09375000000002210732, 0.1093750000000244527, 0.1171875000000244943, 0.1210937500000246470, 0.1250000000000247857, 0.1875000000000223710, 0.2187500000000211775, 0.2343750000000196232, 0.2500000000000180966, 0.3750000000000170974, 0.4375000000000169309, 0.4687500000000165978, 0.5000000000000163203, 0.7500000000000081046, 1.000000000000000000 ),
 .UNSPECIFIED. ) ;
#12866=CARTESIAN_POINT ( 'NONE',  ( 23.61807764069600069, -10.28177138180000050, 9.268757862392000391 ) ) ;
#12867=B_SPLINE_CURVE_WITH_KNOTS ( 'NONE', 3,
 ( #68341, #35857, #63092, #52970 ),
 .UNSPECIFIED., .F., .F.,
 ( 4, 4 ),
 ( 0.000000000000000000, 1.000000000000000000 ),
 .UNSPECIFIED. ) ;
#12875=CARTESIAN_POINT ( 'NONE',  ( 23.60205915885299888, -2.171992490524999209, 12.06370038613999718 ) ) ;
#12877=ORIENTED_EDGE ( 'NONE', *, *, #42020, .T. ) ;
#12878=EDGE_CURVE ( 'NONE', #25292, #48209, #11766, .T. ) ;
#12898=CARTESIAN_POINT ( 'NONE',  ( 24.74119899597345551, -11.75041001041740429, -3.191107525484343732 ) ) ;
#12902=CARTESIAN_POINT ( 'NONE',  ( 18.36651216305132905, -2.877244130631001262, -12.05316132863760181 ) ) ;
#12907=CARTESIAN_POINT ( 'NONE',  ( 24.30000000000000071, 2.204728229456999866, -11.99913219504999873 ) ) ;
#12918=CIRCLE ( 'NONE', #54218, 12.20000000000000107 ) ;
#12920=CARTESIAN_POINT ( 'NONE',  ( 23.60205915885299888, 2.171992490524999209, -12.06370038613999718 ) ) ;
#12923=CARTESIAN_POINT ( 'NONE',  ( 18.14133394217200390, -11.74923367482999836, 3.582907174652000037 ) ) ;
#12930=ORIENTED_EDGE ( 'NONE', *, *, #37092, .T. ) ;
#12932=CARTESIAN_POINT ( 'NONE',  ( 24.63002439619599926, 0.000000000000000000, 0.000000000000000000 ) ) ;
#12934=CARTESIAN_POINT ( 'NONE',  ( 23.58682091624699950, -3.020374421963000433, 13.60611292239000036 ) ) ;
#12960=ADVANCED_FACE ( 'NONE', ( #33615 ), #67892, .T. ) ;
#12963=CARTESIAN_POINT ( 'NONE',  ( 25.09890003032761641, 11.37374245467410461, 3.274683916523300375 ) ) ;
#12966=ORIENTED_EDGE ( 'NONE', *, *, #56357, .F. ) ;
#12967=CONICAL_SURFACE ( 'NONE', #29698, 12.47499939740000130, 0.7853981102588313279 ) ;
#12968=EDGE_CURVE ( 'NONE', #56572, #26364, #54473, .T. ) ;
#12970=CARTESIAN_POINT ( 'NONE',  ( 12.62607976188088799, 11.85836615252178916, -3.313854784738079484 ) ) ;
#12971=CIRCLE ( 'NONE', #21876, 1.000000000000000000 ) ;
#12976=CARTESIAN_POINT ( 'NONE',  ( 24.30001697352500045, -3.271769158411000245, -12.21048181092999840 ) ) ;
#12978=CARTESIAN_POINT ( 'NONE',  ( 13.26944243593800010, -12.10482456369999937, -2.110592202804000284 ) ) ;
#12988=DIRECTION ( 'NONE',  ( -1.000000000000000000, 0.000000000000000000, 0.000000000000000000 ) ) ;
#12989=CYLINDRICAL_SURFACE ( 'NONE', #3061, 0.5000000000000028866 ) ;
#12993=CARTESIAN_POINT ( 'NONE',  ( 15.89979320884932967, -8.154023814690269489, -9.295983641917322515 ) ) ;
#12997=B_SPLINE_CURVE_WITH_KNOTS ( 'NONE', 3,
 ( #63275, #3862, #47218, #42325 ),
 .UNSPECIFIED., .F., .F.,
 ( 4, 4 ),
 ( 0.000000000000000000, 1.000000000000000000 ),
 .UNSPECIFIED. ) ;
#12999=ORIENTED_EDGE ( 'NONE', *, *, #47460, .T. ) ;
#13006=FACE_OUTER_BOUND ( 'NONE', #43824, .T. ) ;
#13014=CARTESIAN_POINT ( 'NONE',  ( 23.56664309646999911, -10.37807348783000094, 9.381504613656002078 ) ) ;
#13015=ORIENTED_EDGE ( 'NONE', *, *, #7740, .T. ) ;
#13016=CIRCLE ( 'NONE', #724, 12.20000000000000639 ) ;
#13027=CARTESIAN_POINT ( 'NONE',  ( 23.60205915885299888, -9.361474752776006270, -7.912850866691996998 ) ) ;
#13031=CARTESIAN_POINT ( 'NONE',  ( 17.60604090556100232, 11.93226446383000017, -3.260045347513999658 ) ) ;
#13032=CARTESIAN_POINT ( 'NONE',  ( 23.74222155833099990, -3.207124327041000367, -13.21279906398999948 ) ) ;
#13038=CARTESIAN_POINT ( 'NONE',  ( 24.30000000000000071, 12.80696435099000041, 50.50083396221000243 ) ) ;
#13047=CARTESIAN_POINT ( 'NONE',  ( 23.57423432650097084, -13.35627592009906550, 4.153587462749816162 ) ) ;
#13048=ORIENTED_EDGE ( 'NONE', *, *, #27470, .F. ) ;
#13049=AXIS2_PLACEMENT_3D ( 'NONE', #45496, #8773, #52094 ) ;
#13051=B_SPLINE_CURVE_WITH_KNOTS ( 'NONE', 3,
 ( #59595, #64478, #26766, #10665 ),
 .UNSPECIFIED., .F., .F.,
 ( 4, 4 ),
 ( 0.000000000000000000, 1.000000000000000000 ),
 .UNSPECIFIED. ) ;
#13071=ORIENTED_EDGE ( 'NONE', *, *, #26837, .T. ) ;
#13072=CARTESIAN_POINT ( 'NONE',  ( 24.56665282559600172, -12.04830931903000035, -3.140565848678999572 ) ) ;
#13075=CARTESIAN_POINT ( 'NONE',  ( 25.57798315594400052, -8.344602483709998353, -8.013942396659000877 ) ) ;
#13080=DIRECTION ( 'NONE',  ( -1.000000000000000000, 3.717264591378875951E-14, -3.221629312528359368E-14 ) ) ;
#13082=VERTEX_POINT ( 'NONE', #31134 ) ;
#13083=DIRECTION ( 'NONE',  ( -1.000000000000000000, 0.000000000000000000, 0.000000000000000000 ) ) ;
#13086=CARTESIAN_POINT ( 'NONE',  ( 24.13227431101038434, -12.49511235236459861, 3.369163575088180984 ) ) ;
#13095=CIRCLE ( 'NONE', #48814, 7.720759220056002903 ) ;
#13099=ORIENTED_EDGE ( 'NONE', *, *, #13213, .T. ) ;
#13104=CARTESIAN_POINT ( 'NONE',  ( 11.56566386073000174, -11.72961781202000076, -1.923363593971999963 ) ) ;
#13110=EDGE_CURVE ( 'NONE', #65247, #27371, #5084, .T. ) ;
#13112=ORIENTED_EDGE ( 'NONE', *, *, #54444, .T. ) ;
#13116=AXIS2_PLACEMENT_3D ( 'NONE', #33169, #37375, #27233 ) ;
#13129=ADVANCED_FACE ( 'NONE', ( #36714 ), #21311, .T. ) ;
#13131=CARTESIAN_POINT ( 'NONE',  ( 15.90007192502618238, -3.569777767583313111, -11.29792192708077181 ) ) ;
#13137=FACE_OUTER_BOUND ( 'NONE', #45392, .T. ) ;
#13145=FACE_OUTER_BOUND ( 'NONE', #66573, .T. ) ;
#13147=AXIS2_PLACEMENT_3D ( 'NONE', #45577, #61304, #7817 ) ;
#13148=CARTESIAN_POINT ( 'NONE',  ( 24.39664803272433247, -3.240506204277676883, -12.09373379660224757 ) ) ;
#13156=EDGE_CURVE ( 'NONE', #31293, #50878, #45954, .T. ) ;
#13168=ORIENTED_EDGE ( 'NONE', *, *, #40961, .F. ) ;
#13170=ORIENTED_EDGE ( 'NONE', *, *, #44118, .F. ) ;
#13171=FACE_OUTER_BOUND ( 'NONE', #51502, .T. ) ;
#13180=CARTESIAN_POINT ( 'NONE',  ( 18.29983863916000075, -2.861762957209999847, 11.98830831200999825 ) ) ;
#13181=ORIENTED_EDGE ( 'NONE', *, *, #42841, .F. ) ;
#13183=CARTESIAN_POINT ( 'NONE',  ( 23.58699641938800085, -13.29334148118999970, -4.186654201655000129 ) ) ;
#13184=DIRECTION ( 'NONE',  ( 1.000000000000000000, 0.000000000000000000, 0.000000000000000000 ) ) ;
#13188=CARTESIAN_POINT ( 'NONE',  ( 25.39410316732910289, 2.774859191736423369, 11.32590268944005629 ) ) ;
#13191=CARTESIAN_POINT ( 'NONE',  ( 24.62620337094597645, 12.35920179424943832, -2.996409964572606555 ) ) ;
#13194=AXIS2_PLACEMENT_3D ( 'NONE', #66390, #46105, #67411 ) ;
#13206=DIRECTION ( 'NONE',  ( -0.9999999999751629787, 5.691912101169789703E-06, -4.156456140529849248E-06 ) ) ;
#13207=CARTESIAN_POINT ( 'NONE',  ( 23.51521036156700006, 13.45800259219000061, 4.320073176091000278 ) ) ;
#13208=ORIENTED_EDGE ( 'NONE', *, *, #33395, .T. ) ;
#13213=EDGE_CURVE ( 'NONE', #55008, #2543, #55636, .T. ) ;
#13214=DIRECTION ( 'NONE',  ( -1.000000000000000000, 9.912705577010336396E-15, 5.699805706780943546E-14 ) ) ;
#13228=CARTESIAN_POINT ( 'NONE',  ( 23.89320776801300283, -3.226867021032998828, 11.46303308821000044 ) ) ;
#13236=EDGE_LOOP ( 'NONE', ( #52465, #38425, #1806 ) ) ;
#13250=ORIENTED_EDGE ( 'NONE', *, *, #41274, .F. ) ;
#13251=DIRECTION ( 'NONE',  ( 8.953094821930460994E-11, -0.2714597137497840040, 0.9624498032681421122 ) ) ;
#13266=AXIS2_PLACEMENT_3D ( 'NONE', #66469, #45508, #49705 ) ;
#13270=ORIENTED_EDGE ( 'NONE', *, *, #28343, .T. ) ;
#13275=AXIS2_PLACEMENT_3D ( 'NONE', #42488, #16599, #27441 ) ;
#13276=CARTESIAN_POINT ( 'NONE',  ( 18.04814306103499888, -11.49796191965999981, 4.570681980344999396 ) ) ;
#13282=EDGE_CURVE ( 'NONE', #34641, #39483, #4261, .T. ) ;
#13284=EDGE_CURVE ( 'NONE', #37826, #13517, #39812, .T. ) ;
#13290=CARTESIAN_POINT ( 'NONE',  ( 24.02106019941100357, -3.259132549667000056, 12.61348568738999987 ) ) ;
#13301=EDGE_CURVE ( 'NONE', #57489, #20902, #882, .T. ) ;
#13308=AXIS2_PLACEMENT_3D ( 'NONE', #45958, #66587, #67267 ) ;
#13318=ORIENTED_EDGE ( 'NONE', *, *, #11507, .T. ) ;
#13323=FACE_OUTER_BOUND ( 'NONE', #22532, .T. ) ;
#13325=DIRECTION ( 'NONE',  ( 0.000000000000000000, -0.9840640631525201520, -0.1778142840487031695 ) ) ;
#13326=CARTESIAN_POINT ( 'NONE',  ( 20.07256264693999981, 0.000000000000000000, 0.000000000000000000 ) ) ;
#13327=CARTESIAN_POINT ( 'NONE',  ( 13.50830001818700055, -12.29143783039000049, -2.111693202397000313 ) ) ;
#13328=ORIENTED_EDGE ( 'NONE', *, *, #17525, .F. ) ;
#13349=VERTEX_POINT ( 'NONE', #40159 ) ;
#13351=CARTESIAN_POINT ( 'NONE',  ( 24.72252647404960513, -3.121154203591807175, -11.78764156663662099 ) ) ;
#13359=CARTESIAN_POINT ( 'NONE',  ( 25.44994642811800034, -1.261213355973999610E-13, 4.884981308350999274E-14 ) ) ;
#13364=ORIENTED_EDGE ( 'NONE', *, *, #26188, .T. ) ;
#13395=CARTESIAN_POINT ( 'NONE',  ( 15.98722619340700213, -8.633165116997000510, -7.765565731395999372 ) ) ;
#13397=CARTESIAN_POINT ( 'NONE',  ( 24.30000000000000071, -11.85420044612000012, 3.901016762742000488 ) ) ;
#13398=ORIENTED_EDGE ( 'NONE', *, *, #38453, .F. ) ;
#13403=CARTESIAN_POINT ( 'NONE',  ( 24.67921569845699992, 12.29514839105000057, -2.979196030862000022 ) ) ;
#13411=DIRECTION ( 'NONE',  ( -1.000000000000000000, -4.212899870229393166E-14, 3.717264591378875951E-14 ) ) ;
#13415=EDGE_CURVE ( 'NONE', #16591, #49775, #48946, .T. ) ;
#13430=DIRECTION ( 'NONE',  ( 0.000000000000000000, 0.001239076634196941687, -0.9999992323442525866 ) ) ;
#13433=CARTESIAN_POINT ( 'NONE',  ( 25.27003374619006948, -8.359947296913826875, -8.486664668671879852 ) ) ;
#13434=CARTESIAN_POINT ( 'NONE',  ( 24.66906608026770442, 3.147934860013589464, 11.83339566522958464 ) ) ;
#13436=CARTESIAN_POINT ( 'NONE',  ( 23.98816733236458276, -12.73143379325068025, 3.487225215969183889 ) ) ;
#13444=EDGE_CURVE ( 'NONE', #33492, #7350, #23421, .T. ) ;
#13463=ADVANCED_FACE ( 'NONE', ( #47457 ), #42453, .F. ) ;
#13468=VERTEX_POINT ( 'NONE', #27506 ) ;
#13471=B_SPLINE_CURVE_WITH_KNOTS ( 'NONE', 3,
 ( #58304, #37328, #53413, #43266, #68788, #32097 ),
 .UNSPECIFIED., .F., .F.,
 ( 4, 2, 4 ),
 ( 0.000000000000000000, 0.5000000000000000000, 1.000000000000000000 ),
 .UNSPECIFIED. ) ;
#13474=CARTESIAN_POINT ( 'NONE',  ( 24.15420991129199990, 9.222014324292000964, -9.473961295084999179 ) ) ;
#13475=CARTESIAN_POINT ( 'NONE',  ( 17.79229341877100268, -3.377812583009999869, -11.11021646535000151 ) ) ;
#13480=EDGE_LOOP ( 'NONE', ( #21464, #66860, #35336, #3263 ) ) ;
#13482=CARTESIAN_POINT ( 'NONE',  ( 23.60205915885299888, -11.53346724329999873, -4.150849519424002487 ) ) ;
#13485=CARTESIAN_POINT ( 'NONE',  ( 11.79999999550100220, 11.52577121388000059, 1.696750555870000010 ) ) ;
#13489=CARTESIAN_POINT ( 'NONE',  ( 44.24148000000000280, 2.258942858049999725, -12.29419282279000036 ) ) ;
#13490=DIRECTION ( 'NONE',  ( 1.000000000000000000, 0.000000000000000000, 0.000000000000000000 ) ) ;
#13492=B_SPLINE_CURVE_WITH_KNOTS ( 'NONE', 3,
 ( #52158, #20349, #4262, #41673 ),
 .UNSPECIFIED., .F., .F.,
 ( 4, 4 ),
 ( 0.000000000000000000, 1.000000000000000000 ),
 .UNSPECIFIED. ) ;
#13497=ADVANCED_FACE ( 'NONE', ( #54419 ), #17361, .T. ) ;
#13503=CARTESIAN_POINT ( 'NONE',  ( 18.23980063339601898, -2.972525812591876093, -11.47315805767759755 ) ) ;
#13514=CARTESIAN_POINT ( 'NONE',  ( 25.60000000000000142, 0.000000000000000000, 10.75000000000000000 ) ) ;
#13517=VERTEX_POINT ( 'NONE', #67223 ) ;
#13522=CARTESIAN_POINT ( 'NONE',  ( 25.46372676430900128, 8.354609436172999892, -8.148458316574000548 ) ) ;
#13527=CARTESIAN_POINT ( 'NONE',  ( 23.61341120619100309, -13.29072902885999952, -4.053938077286999508 ) ) ;
#13536=DIRECTION ( 'NONE',  ( 0.000000000000000000, 0.7071067811865475727, -0.7071067811865475727 ) ) ;
#13542=CARTESIAN_POINT ( 'NONE',  ( 21.60000000000000142, 0.000000000000000000, 0.000000000000000000 ) ) ;
#13547=DIRECTION ( 'NONE',  ( 0.000000000000000000, -0.7071067811865475727, 0.7071067811865475727 ) ) ;
#13548=CARTESIAN_POINT ( 'NONE',  ( 23.55654991076200133, 13.49867770468999950, 4.025919757528999554 ) ) ;
#13555=DIRECTION ( 'NONE',  ( 2.887756364190019784E-10, 0.06432770287658050312, 0.9979288284455070102 ) ) ;
#13563=CYLINDRICAL_SURFACE ( 'NONE', #8203, 0.6999999999999992895 ) ;
#13565=CARTESIAN_POINT ( 'NONE',  ( 11.30000000000000071, -4.368599826607999503, -15.48886178036999972 ) ) ;
#13569=CARTESIAN_POINT ( 'NONE',  ( 25.60000000000000142, 11.77655473258999841, -4.190794510628000680 ) ) ;
#13571=ORIENTED_EDGE ( 'NONE', *, *, #6885, .F. ) ;
#13575=AXIS2_PLACEMENT_3D ( 'NONE', #55989, #8094, #29438 ) ;
#13577=ORIENTED_EDGE ( 'NONE', *, *, #58007, .F. ) ;
#13583=DIRECTION ( 'NONE',  ( 1.000000000000000000, 0.000000000000000000, 0.000000000000000000 ) ) ;
#13586=EDGE_CURVE ( 'NONE', #10719, #56062, #42104, .T. ) ;
#13587=EDGE_CURVE ( 'NONE', #35879, #49285, #64434, .T. ) ;
#13597=CARTESIAN_POINT ( 'NONE',  ( 16.32027728219714291, -3.351613101375973791, -11.15747237328656460 ) ) ;
#13602=DIRECTION ( 'NONE',  ( 0.000000000000000000, 0.000000000000000000, -1.000000000000000000 ) ) ;
#13607=VERTEX_POINT ( 'NONE', #2912 ) ;
#13608=CARTESIAN_POINT ( 'NONE',  ( 29.60000000000000142, 0.000000000000000000, 0.000000000000000000 ) ) ;
#13616=CARTESIAN_POINT ( 'NONE',  ( 17.61439135794200084, -11.93243341766000043, 3.259310185281999672 ) ) ;
#13622=DIRECTION ( 'NONE',  ( -1.000000000000000000, 0.000000000000000000, 0.000000000000000000 ) ) ;
#13625=DIRECTION ( 'NONE',  ( -1.000000000000000000, 0.000000000000000000, 0.000000000000000000 ) ) ;
#13627=CARTESIAN_POINT ( 'NONE',  ( 23.63098035122899887, -3.423374544452999935, 13.57524279781000054 ) ) ;
#13628=CARTESIAN_POINT ( 'NONE',  ( 13.43979992210466889, 11.65095899958523340, 2.173573044049638359 ) ) ;
#13630=CARTESIAN_POINT ( 'NONE',  ( 21.72233714749290101, -5.999764115230404649, 0.05320302240984180892 ) ) ;
#13661=DIRECTION ( 'NONE',  ( 0.000000000000000000, -0.9421243786071880066, 0.3352635608502960163 ) ) ;
#13678=CARTESIAN_POINT ( 'NONE',  ( 23.66004879239100234, -9.998911572074998588, 9.691526907171001071 ) ) ;
#13680=CARTESIAN_POINT ( 'NONE',  ( 15.89994436294300151, -8.847904542234999781, -8.580301953175000662 ) ) ;
#13690=EDGE_CURVE ( 'NONE', #18862, #39042, #52127, .T. ) ;
#13693=CARTESIAN_POINT ( 'NONE',  ( 23.56665676678100141, 1.192379528446999839E-13, -4.982680934517999418E-13 ) ) ;
#13699=CARTESIAN_POINT ( 'NONE',  ( 23.59999445750599989, -13.22316420035999940, -4.267800004853000040 ) ) ;
#13718=CARTESIAN_POINT ( 'NONE',  ( 23.64690940319799850, -3.329270756416000232, -13.50285105039000122 ) ) ;
#13727=CARTESIAN_POINT ( 'NONE',  ( 18.29995268966800026, 2.861739928647000220, 11.98821236628000086 ) ) ;
#13741=ORIENTED_EDGE ( 'NONE', *, *, #38169, .F. ) ;
#13742=ADVANCED_FACE ( 'NONE', ( #67913 ), #20029, .F. ) ;
#13745=TOROIDAL_SURFACE ( 'NONE', #51661, 13.79999999999999893, 0.2000000000000000111 ) ;
#13750=CARTESIAN_POINT ( 'NONE',  ( 21.72233714749290101, 5.000000000000000000, 0.000000000000000000 ) ) ;
#13757=CARTESIAN_POINT ( 'NONE',  ( 24.30000000000000071, -8.810505093353000916, -8.810505093353000916 ) ) ;
#13759=DIRECTION ( 'NONE',  ( 0.000000000000000000, 0.9989394889204477046, 0.04604234437292184512 ) ) ;
#13760=CARTESIAN_POINT ( 'NONE',  ( 18.29058462261052753, -11.07487261139573143, 3.615341608536529083 ) ) ;
#13795=CARTESIAN_POINT ( 'NONE',  ( 24.30001685126999789, 8.938702716825000394, -8.938676159935001309 ) ) ;
#13809=CARTESIAN_POINT ( 'NONE',  ( 24.00946664458725266, 3.345587221009647561, 12.72975888196361893 ) ) ;
#13810=CARTESIAN_POINT ( 'NONE',  ( 23.83637295000900025, 9.655512588674998398, -9.482097233574000583 ) ) ;
#13811=CARTESIAN_POINT ( 'NONE',  ( 18.53573769406200356, -2.787008136214999876, -11.27235516822999983 ) ) ;
#13814=AXIS2_PLACEMENT_3D ( 'NONE', #36378, #52806, #14715 ) ;
#13816=ORIENTED_EDGE ( 'NONE', *, *, #3302, .T. ) ;
#13822=PLANE ( 'NONE',  #10887 ) ;
#13825=EDGE_CURVE ( 'NONE', #6251, #60622, #51837, .T. ) ;
#13835=CARTESIAN_POINT ( 'NONE',  ( 13.49994651945300284, 12.07042783918999795, 2.492331243371999960 ) ) ;
#13840=CIRCLE ( 'NONE', #53388, 0.3000000000000004330 ) ;
#13857=CARTESIAN_POINT ( 'NONE',  ( 25.34046362424712839, 8.480593820237956493, -7.990867062144727306 ) ) ;
#13867=CARTESIAN_POINT ( 'NONE',  ( 23.67741368841328864, 13.18816119140440257, -3.924050752104807138 ) ) ;
#13870=CARTESIAN_POINT ( 'NONE',  ( 24.03543971961891401, -3.344494741195767062, -12.68172832290301777 ) ) ;
#13879=CARTESIAN_POINT ( 'NONE',  ( 25.39940339878695852, -11.19882859648231666, 3.252360728051921335 ) ) ;
#13881=B_SPLINE_CURVE_WITH_KNOTS ( 'NONE', 3,
 ( #36371, #10483, #4542, #4890 ),
 .UNSPECIFIED., .F., .F.,
 ( 4, 4 ),
 ( 0.000000000000000000, 1.000000000000000000 ),
 .UNSPECIFIED. ) ;
#13884=CARTESIAN_POINT ( 'NONE',  ( 15.89994436294300151, 8.847904542234999781, 8.580301953175000662 ) ) ;
#13886=EDGE_CURVE ( 'NONE', #46546, #47653, #3727, .T. ) ;
#13892=CARTESIAN_POINT ( 'NONE',  ( 15.86005557146100209, 8.873324881979000267, 8.501367972259000538 ) ) ;
#13898=CARTESIAN_POINT ( 'NONE',  ( 24.59232958921100121, -12.25045686045999993, 3.053350357284999816 ) ) ;
#13901=CARTESIAN_POINT ( 'NONE',  ( 25.49994615398131614, -10.64595569433734390, 3.788460569392772648 ) ) ;
#13903=CARTESIAN_POINT ( 'NONE',  ( 23.66479333458100243, 10.00924341248000005, 9.518029705864998746 ) ) ;
#13904=ORIENTED_EDGE ( 'NONE', *, *, #22304, .T. ) ;
#13917=CARTESIAN_POINT ( 'NONE',  ( 23.59999176271200128, 13.22318677037999812, 4.267778497637999102 ) ) ;
#13923=CARTESIAN_POINT ( 'NONE',  ( 11.48381255716000027, -3.703723199601000271, 11.90766076753999947 ) ) ;
#13925=CIRCLE ( 'NONE', #49651, 11.50000000000000000 ) ;
#13938=CARTESIAN_POINT ( 'NONE',  ( 12.80000000000000071, 10.78295181803999903, -4.410266442048000002 ) ) ;
#13939=DIRECTION ( 'NONE',  ( -1.000000000000000000, 0.000000000000000000, 0.000000000000000000 ) ) ;
#13940=LINE ( 'NONE', #56583, #6459 ) ;
#13943=CARTESIAN_POINT ( 'NONE',  ( 15.20000000000000107, 11.47055000429999971, -4.757693469806000053 ) ) ;
#13945=DIRECTION ( 'NONE',  ( 1.000000000000000000, 0.000000000000000000, 0.000000000000000000 ) ) ;
#13948=CARTESIAN_POINT ( 'NONE',  ( 29.91622776601699840, 0.000000000000000000, 0.000000000000000000 ) ) ;
#13954=CARTESIAN_POINT ( 'NONE',  ( 15.40000000001299973, 8.815237407733999220, 7.616696375847999967 ) ) ;
#13955=FACE_OUTER_BOUND ( 'NONE', #58143, .T. ) ;
#13956=CARTESIAN_POINT ( 'NONE',  ( 24.31006797093800031, -8.914161086992001160, 8.860056389909999552 ) ) ;
#13969=FACE_OUTER_BOUND ( 'NONE', #16692, .T. ) ;
#13975=EDGE_CURVE ( 'NONE', #58018, #32077, #58864, .T. ) ;
#13976=ORIENTED_EDGE ( 'NONE', *, *, #31365, .T. ) ;
#13987=ORIENTED_EDGE ( 'NONE', *, *, #8133, .F. ) ;
#14003=CARTESIAN_POINT ( 'NONE',  ( 16.09997386696500143, 8.350085070477001992, 8.123950967096998710 ) ) ;
#14013=ORIENTED_EDGE ( 'NONE', *, *, #56232, .F. ) ;
#14018=VECTOR ( 'NONE', #67119, 1000.000000000000000 ) ;
#14019=EDGE_CURVE ( 'NONE', #60421, #62492, #59143, .T. ) ;
#14026=CARTESIAN_POINT ( 'NONE',  ( 23.66004879239100234, -3.393652723963000106, -13.50507488346000073 ) ) ;
#14030=CARTESIAN_POINT ( 'NONE',  ( 19.94999927679900154, 0.000000000000000000, 5.040412531797999279E-14 ) ) ;
#14041=LINE ( 'NONE', #35368, #67615 ) ;
#14044=ORIENTED_EDGE ( 'NONE', *, *, #26756, .F. ) ;
#14046=DIRECTION ( 'NONE',  ( -1.000000000000000000, 0.000000000000000000, 0.000000000000000000 ) ) ;
#14047=CARTESIAN_POINT ( 'NONE',  ( 24.87151402923947430, 8.583161980870569252, 8.460101252743749356 ) ) ;
#14052=CARTESIAN_POINT ( 'NONE',  ( 11.49999672495000169, 3.632761979779000061, -11.06912554803999882 ) ) ;
#14056=CARTESIAN_POINT ( 'NONE',  ( 25.00275116957158161, 8.478815136465241764, 8.837059051057721604 ) ) ;
#14059=FACE_BOUND ( 'NONE', #15695, .T. ) ;
#14063=VECTOR ( 'NONE', #24127, 1000.000000000000000 ) ;
#14065=CARTESIAN_POINT ( 'NONE',  ( 15.90018573812399971, -8.493548356068000516, -8.263529029821000904 ) ) ;
#14067=B_SPLINE_CURVE_WITH_KNOTS ( 'NONE', 3,
 ( #25065, #67700, #13901, #67023 ),
 .UNSPECIFIED., .F., .F.,
 ( 4, 4 ),
 ( 0.000000000000000000, 1.000000000000000000 ),
 .UNSPECIFIED. ) ;
#14072=CARTESIAN_POINT ( 'NONE',  ( 18.23777342769928467, 3.105166803968430145, 11.92942855515249967 ) ) ;
#14074=EDGE_CURVE ( 'NONE', #18862, #50564, #18651, .T. ) ;
#14078=CARTESIAN_POINT ( 'NONE',  ( 23.60815875000115582, -13.39692513168543364, 3.962568340425848490 ) ) ;
#14084=CARTESIAN_POINT ( 'NONE',  ( 23.89320776801300283, 10.75689324691000337, -4.023240149132002230 ) ) ;
#14089=CYLINDRICAL_SURFACE ( 'NONE', #56655, 0.5000000000000004441 ) ;
#14095=CARTESIAN_POINT ( 'NONE',  ( 24.62774583285499830, -3.462210234181999802, 12.08748376425999993 ) ) ;
#14103=CARTESIAN_POINT ( 'NONE',  ( 23.60345044734545183, 13.39469792596697673, 3.980595414305586388 ) ) ;
#14106=CARTESIAN_POINT ( 'NONE',  ( 17.66658663920539851, -11.23412379136108719, 3.084957477882974253 ) ) ;
#14108=ORIENTED_EDGE ( 'NONE', *, *, #50455, .T. ) ;
#14109=VECTOR ( 'NONE', #8753, 1000.000000000000000 ) ;
#14116=CARTESIAN_POINT ( 'NONE',  ( 18.30003129334700063, 2.732683817159999862, -11.53064095410000078 ) ) ;
#14124=ORIENTED_EDGE ( 'NONE', *, *, #54128, .T. ) ;
#14131=CARTESIAN_POINT ( 'NONE',  ( 19.99999987597299977, -12.42499880353999941, 0.000000000000000000 ) ) ;
#14133=CARTESIAN_POINT ( 'NONE',  ( 23.60000000000000142, 11.85420044612000012, 3.901016762742000488 ) ) ;
#14136=CARTESIAN_POINT ( 'NONE',  ( 24.57788509278314493, -3.600249671654212058, 12.25995025212536227 ) ) ;
#14144=CARTESIAN_POINT ( 'NONE',  ( 17.82346232393702223, 11.54140747413759449, -4.865347213226944412 ) ) ;
#14147=VERTEX_POINT ( 'NONE', #17541 ) ;
#14149=AXIS2_PLACEMENT_3D ( 'NONE', #4693, #27412, #42118 ) ;
#14152=CARTESIAN_POINT ( 'NONE',  ( 23.85842818131158793, 3.325647356525735621, 13.01563238088372643 ) ) ;
#14153=CARTESIAN_POINT ( 'NONE',  ( 23.61708153891300199, 10.26225109528000168, -9.295033282810001296 ) ) ;
#14155=CARTESIAN_POINT ( 'NONE',  ( 11.49977531252999974, 12.43119799159999950, 1.530013559959999991 ) ) ;
#14159=ORIENTED_EDGE ( 'NONE', *, *, #9293, .F. ) ;
#14166=CARTESIAN_POINT ( 'NONE',  ( 11.79999999471800010, 11.69117318561000118, 1.923227876431999883 ) ) ;
#14189=ORIENTED_EDGE ( 'NONE', *, *, #17611, .T. ) ;
#14196=ORIENTED_EDGE ( 'NONE', *, *, #53122, .T. ) ;
#14209=ORIENTED_EDGE ( 'NONE', *, *, #26188, .F. ) ;
#14212=CARTESIAN_POINT ( 'NONE',  ( 23.67317840412032837, -3.197506257295965604, -13.39107809300776708 ) ) ;
#14218=EDGE_CURVE ( 'NONE', #52300, #30607, #28778, .T. ) ;
#14233=CARTESIAN_POINT ( 'NONE',  ( 16.00156003475500199, 9.132520755637999699, 8.493756974768999157 ) ) ;
#14236=CARTESIAN_POINT ( 'NONE',  ( 23.60205915885299888, -2.338900754103997670, -12.00073634675999834 ) ) ;
#14243=CARTESIAN_POINT ( 'NONE',  ( 24.26733149983100191, 3.229785797570000394, 12.20153234936999986 ) ) ;
#14246=CARTESIAN_POINT ( 'NONE',  ( 24.63002439619599926, 0.000000000000000000, 0.000000000000000000 ) ) ;
#14247=EDGE_LOOP ( 'NONE', ( #14678, #37191, #13250, #48075 ) ) ;
#14254=CARTESIAN_POINT ( 'NONE',  ( 17.76900185986900027, 3.411877013825000304, 11.89794217324999970 ) ) ;
#14258=ORIENTED_EDGE ( 'NONE', *, *, #41187, .F. ) ;
#14260=VECTOR ( 'NONE', #18431, 1000.000000000000000 ) ;
#14264=FACE_OUTER_BOUND ( 'NONE', #55737, .T. ) ;
#14266=CARTESIAN_POINT ( 'NONE',  ( 11.74249537357300177, -3.528133194209999601, 11.96072866431000037 ) ) ;
#14275=EDGE_LOOP ( 'NONE', ( #24337, #22211, #65251, #48026 ) ) ;
#14276=CYLINDRICAL_SURFACE ( 'NONE', #8273, 11.50000000000000000 ) ;
#14277=ORIENTED_EDGE ( 'NONE', *, *, #4466, .T. ) ;
#14279=ADVANCED_FACE ( 'NONE', ( #67064 ), #46439, .T. ) ;
#14281=CARTESIAN_POINT ( 'NONE',  ( 17.60000001072100062, -11.41073498373000028, 4.623967591968000335 ) ) ;
#14285=AXIS2_PLACEMENT_3D ( 'NONE', #26499, #37327, #48164 ) ;
#14292=ORIENTED_EDGE ( 'NONE', *, *, #68079, .T. ) ;
#14298=CARTESIAN_POINT ( 'NONE',  ( 18.23590051321700400, -3.219096189435000088, -11.95421454054999977 ) ) ;
#14306=ORIENTED_EDGE ( 'NONE', *, *, #42020, .F. ) ;
#14309=DIRECTION ( 'NONE',  ( 0.000000000000000000, 0.2588190451024934835, -0.9659258262890757507 ) ) ;
#14313=DIRECTION ( 'NONE',  ( -1.000000000000000000, 0.000000000000000000, 0.000000000000000000 ) ) ;
#14315=CARTESIAN_POINT ( 'NONE',  ( 23.52015599135700086, -13.48676572944000185, 4.209850081331000027 ) ) ;
#14331=CARTESIAN_POINT ( 'NONE',  ( 11.35620373058000077, -3.594096350588000366, 11.23428177897000069 ) ) ;
#14360=B_SPLINE_CURVE_WITH_KNOTS ( 'NONE', 3,
 ( #3393, #57567, #29997, #25760 ),
 .UNSPECIFIED., .F., .F.,
 ( 4, 4 ),
 ( 0.000000000000000000, 1.000000000000000000 ),
 .UNSPECIFIED. ) ;
#14368=CARTESIAN_POINT ( 'NONE',  ( 24.07540675168254651, -3.340246503750487150, 12.60851480763457388 ) ) ;
#14370=EDGE_CURVE ( 'NONE', #9331, #23104, #37178, .T. ) ;
#14371=CARTESIAN_POINT ( 'NONE',  ( 24.44496356299600137, 12.03536643057000077, 3.224849944858999784 ) ) ;
#14372=CARTESIAN_POINT ( 'NONE',  ( 23.73953425137737483, -3.508700594862699695, -13.37373074045048682 ) ) ;
#14393=CARTESIAN_POINT ( 'NONE',  ( 24.94498381146992116, 11.54147255574495823, -3.218772431449972604 ) ) ;
#14395=CIRCLE ( 'NONE', #52307, 12.32510602165000613 ) ;
#14401=ORIENTED_EDGE ( 'NONE', *, *, #50136, .T. ) ;
#14405=EDGE_LOOP ( 'NONE', ( #21632, #45822, #40347, #65632 ) ) ;
#14406=DIRECTION ( 'NONE',  ( 0.000000000000000000, 0.000000000000000000, 1.000000000000000000 ) ) ;
#14412=DIRECTION ( 'NONE',  ( -1.000000000000000000, 0.000000000000000000, 0.000000000000000000 ) ) ;
#14421=CARTESIAN_POINT ( 'NONE',  ( 15.56012107570600023, -8.822147194309000184, -7.967418575816001436 ) ) ;
#14423=CARTESIAN_POINT ( 'NONE',  ( 23.50387503050299998, 14.00000000000000000, 0.000000000000000000 ) ) ;
#14424=ORIENTED_EDGE ( 'NONE', *, *, #68875, .F. ) ;
#14429=CARTESIAN_POINT ( 'NONE',  ( 24.35365242081699932, 12.20235406293000935, -3.288253180433003298 ) ) ;
#14432=VERTEX_POINT ( 'NONE', #2332 ) ;
#14448=CARTESIAN_POINT ( 'NONE',  ( 13.64649313145500109, -9.010717346174999420, -7.468773375841999851 ) ) ;
#14460=CARTESIAN_POINT ( 'NONE',  ( 13.49980696793000057, 9.514462421839999351, 7.834836582454001608 ) ) ;
#14463=B_SPLINE_CURVE_WITH_KNOTS ( 'NONE', 3,
 ( #61402, #13857, #40091, #13522 ),
 .UNSPECIFIED., .F., .F.,
 ( 4, 4 ),
 ( 0.000000000000000000, 1.000000000000000000 ),
 .UNSPECIFIED. ) ;
#14481=ORIENTED_EDGE ( 'NONE', *, *, #65878, .T. ) ;
#14482=CARTESIAN_POINT ( 'NONE',  ( 24.53429011008099891, 3.614318944477000084, -12.31267538233000103 ) ) ;
#14484=DIRECTION ( 'NONE',  ( 0.9999999999990064614, -1.235604879081008633E-06, 6.784100806884041873E-07 ) ) ;
#14487=CARTESIAN_POINT ( 'NONE',  ( 17.90328515628180384, 11.55107739452601834, -4.842351092693065517 ) ) ;
#14495=CARTESIAN_POINT ( 'NONE',  ( 23.95413520383817740, 3.345971697916644949, 12.83256498468845841 ) ) ;
#14496=CARTESIAN_POINT ( 'NONE',  ( 24.51040282428800055, 8.845021705915000254, -9.169845360568999126 ) ) ;
#14497=CARTESIAN_POINT ( 'NONE',  ( 11.29998578400000042, -3.824193979571000046, 11.71675423233000046 ) ) ;
#14503=DIRECTION ( 'NONE',  ( -1.000000000000000000, 0.000000000000000000, 0.000000000000000000 ) ) ;
#14510=CARTESIAN_POINT ( 'NONE',  ( 13.80679720086500062, 8.861764092194999165, 7.504495031742999700 ) ) ;
#14515=B_SPLINE_SURFACE_WITH_KNOTS ( 'NONE', 3, 3, ( 
 ( #3388, #40797, #13898, #28959 ),
 ( #19475, #62121, #50262, #8981 ),
 ( #3725, #67697, #45025, #18452 ),
 ( #47084, #52322, #57913, #10012 ),
 ( #31350, #63833, #21193, #48112 ),
 ( #10358, #58254, #31692, #57559 ),
 ( #10697, #36939, #41153, #41831 ),
 ( #35898, #20161, #15608, #52663 ) ),
 .UNSPECIFIED., .F., .F., .F.,
 ( 4, 1, 1, 1, 1, 4 ),
 ( 4, 4 ),
 ( 0.008355503774731999275, 0.05882352941176000050, 0.1176470588234999892, 0.1764705882353000133, 0.2352941176471000095, 0.2534843214274999923 ),
 ( -0.1830816817365999993, 1.182949857538000193 ),
 .UNSPECIFIED. ) ;
#14521=CARTESIAN_POINT ( 'NONE',  ( 16.09997386696500143, 5.375854662731813782, 10.37779375783400937 ) ) ;
#14530=CARTESIAN_POINT ( 'NONE',  ( 13.60429364930200080, -11.50682694388999927, -2.143319390578000139 ) ) ;
#14537=CARTESIAN_POINT ( 'NONE',  ( 15.86376629110799996, 3.753680978508000088, 11.28125155222999787 ) ) ;
#14538=CARTESIAN_POINT ( 'NONE',  ( 15.98722619340700213, 8.633165116997000510, 7.765565731395999372 ) ) ;
#14544=CARTESIAN_POINT ( 'NONE',  ( 24.67921311619700120, 3.567517360056999820, 12.13750603036999998 ) ) ;
#14553=ORIENTED_EDGE ( 'NONE', *, *, #61485, .T. ) ;
#14561=ORIENTED_EDGE ( 'NONE', *, *, #10477, .T. ) ;
#14565=AXIS2_PLACEMENT_3D ( 'NONE', #53283, #47699, #4344 ) ;
#14570=LINE ( 'NONE', #46381, #42143 ) ;
#14571=DIRECTION ( 'NONE',  ( -1.000000000000000000, 0.000000000000000000, 0.000000000000000000 ) ) ;
#14586=CARTESIAN_POINT ( 'NONE',  ( 23.58305362212199796, 10.33301849453000010, 9.360217489553999570 ) ) ;
#14589=CARTESIAN_POINT ( 'NONE',  ( 24.30000000000000071, 11.85420044612000012, -3.901016762742000488 ) ) ;
#14591=B_SPLINE_CURVE_WITH_KNOTS ( 'NONE', 3,
 ( #63592, #68147, #3828, #30424, #57661, #20610 ),
 .UNSPECIFIED., .F., .F.,
 ( 4, 2, 4 ),
 ( 0.000000000000000000, 0.5000000000000000000, 1.000000000000000000 ),
 .UNSPECIFIED. ) ;
#14602=CARTESIAN_POINT ( 'NONE',  ( 13.70003001321900271, -9.668726926528000476, -7.961868161445000425 ) ) ;
#14603=CARTESIAN_POINT ( 'NONE',  ( 14.46666666233133469, 9.187454791078208061, 8.213178404136472821 ) ) ;
#14604=ORIENTED_EDGE ( 'NONE', *, *, #43257, .F. ) ;
#14605=CARTESIAN_POINT ( 'NONE',  ( 11.53898808224000128, -3.920528549154999709, 11.93545759853000021 ) ) ;
#14629=EDGE_LOOP ( 'NONE', ( #41244, #13181, #40432, #63949 ) ) ;
#14635=CARTESIAN_POINT ( 'NONE',  ( 17.86531638133300248, -3.412592442238999713, -11.89775222658999887 ) ) ;
#14636=CARTESIAN_POINT ( 'NONE',  ( 24.54688887196200042, -8.860350057919001543, 9.344992028423000363 ) ) ;
#14651=CARTESIAN_POINT ( 'NONE',  ( 17.79408754209099897, 3.298114924730999764, -11.83441383768999877 ) ) ;
#14658=CARTESIAN_POINT ( 'NONE',  ( 23.61748067083564351, -10.10092716189297235, -9.643545208109760125 ) ) ;
#14663=CARTESIAN_POINT ( 'NONE',  ( 25.19966511448500057, 8.371114574844000344, 8.687417344736999780 ) ) ;
#14671=ORIENTED_EDGE ( 'NONE', *, *, #53652, .T. ) ;
#14674=CARTESIAN_POINT ( 'NONE',  ( 24.53429010005800137, -12.47024913742999885, 3.026245653581999928 ) ) ;
#14678=ORIENTED_EDGE ( 'NONE', *, *, #5842, .T. ) ;
#14682=CARTESIAN_POINT ( 'NONE',  ( 11.44792571093000255, 3.801678398496999733, -11.87711516161999903 ) ) ;
#14689=ORIENTED_EDGE ( 'NONE', *, *, #32281, .T. ) ;
#14704=CIRCLE ( 'NONE', #59300, 11.79499999999999993 ) ;
#14706=CARTESIAN_POINT ( 'NONE',  ( 18.22497476944389661, 3.457026130725855850, -12.03849088744170004 ) ) ;
#14708=CARTESIAN_POINT ( 'NONE',  ( 24.69847986554200148, -3.637895343793999814, -12.18598392984999990 ) ) ;
#14710=CARTESIAN_POINT ( 'NONE',  ( 23.60001133530950668, -1.983597864821140026E-14, -13.89477126879791058 ) ) ;
#14715=DIRECTION ( 'NONE',  ( 1.000000000000000000, 0.000000000000000000, 0.000000000000000000 ) ) ;
#14716=EDGE_CURVE ( 'NONE', #60364, #44668, #45491, .T. ) ;
#14728=B_SPLINE_CURVE_WITH_KNOTS ( 'NONE', 3,
 ( #52804, #4897, #57345, #25887, #10489, #26236, #40936, #41622 ),
 .UNSPECIFIED., .F., .F.,
 ( 4, 2, 2, 4 ),
 ( 0.000000000000000000, 0.5000000000000026645, 0.7500000000000013323, 1.000000000000000000 ),
 .UNSPECIFIED. ) ;
#14738=FACE_OUTER_BOUND ( 'NONE', #52187, .T. ) ;
#14741=CARTESIAN_POINT ( 'NONE',  ( 11.79999999471800010, 11.69117318561000118, 1.923227876431999883 ) ) ;
#14742=CARTESIAN_POINT ( 'NONE',  ( 16.08259915475489521, 9.118254932978883787, 8.587227412616197597 ) ) ;
#14744=AXIS2_PLACEMENT_3D ( 'NONE', #50992, #13939, #28999 ) ;
#14745=CARTESIAN_POINT ( 'NONE',  ( 20.75138802851920161, 0.000000000000000000, 0.000000000000000000 ) ) ;
#14748=DIRECTION ( 'NONE',  ( 0.000000000000000000, 0.9659258262890756397, -0.2588190451024932059 ) ) ;
#14754=CARTESIAN_POINT ( 'NONE',  ( 24.30000000000000071, 0.000000000000000000, 0.000000000000000000 ) ) ;
#14758=CYLINDRICAL_SURFACE ( 'NONE', #55210, 0.5000000000000004441 ) ;
#14771=CARTESIAN_POINT ( 'NONE',  ( 23.61276350013500291, 3.132797279252000244, -13.53855344537999983 ) ) ;
#14785=CARTESIAN_POINT ( 'NONE',  ( 13.46376629110800138, -9.221173139870998625, -7.505113150216000228 ) ) ;
#14786=CARTESIAN_POINT ( 'NONE',  ( 21.10000033274619824, -12.52499966719000035, -3.709625656131999791E-10 ) ) ;
#14794=ORIENTED_EDGE ( 'NONE', *, *, #31061, .F. ) ;
#14798=CARTESIAN_POINT ( 'NONE',  ( 17.98087424866222506, 3.330341796646840713, -11.16384340189072333 ) ) ;
#14802=EDGE_CURVE ( 'NONE', #47324, #37325, #37858, .T. ) ;
#14808=CIRCLE ( 'NONE', #56124, 9.250000000000000000 ) ;
#14810=VERTEX_POINT ( 'NONE', #3611 ) ;
#14813=CARTESIAN_POINT ( 'NONE',  ( 25.60000000000000142, 2.258942858049999725, 12.29419282279000036 ) ) ;
#14814=CARTESIAN_POINT ( 'NONE',  ( 24.35146665670700017, -12.30647607894000117, -3.205652257177999953 ) ) ;
#14816=ORIENTED_EDGE ( 'NONE', *, *, #45922, .T. ) ;
#14821=B_SPLINE_CURVE_WITH_KNOTS ( 'NONE', 3,
 ( #25745, #42515, #53349, #31684 ),
 .UNSPECIFIED., .F., .F.,
 ( 4, 4 ),
 ( 0.000000000000000000, 1.000000000000000000 ),
 .UNSPECIFIED. ) ;
#14823=CARTESIAN_POINT ( 'NONE',  ( 17.88018231457700224, 3.314507696643999690, 11.22393832560999982 ) ) ;
#14826=VERTEX_POINT ( 'NONE', #36820 ) ;
#14831=ADVANCED_FACE ( 'NONE', ( #36465 ), #6761, .F. ) ;
#14833=CARTESIAN_POINT ( 'NONE',  ( 23.84129534145970553, 3.319672314572660987, 13.04905549722290381 ) ) ;
#14834=CARTESIAN_POINT ( 'NONE',  ( 23.74313043943600121, 9.836954956339999612, -9.383370562020999728 ) ) ;
#14843=CARTESIAN_POINT ( 'NONE',  ( 11.79999999771000141, -12.39026187696000036, -1.832249219479999969 ) ) ;
#14853=CYLINDRICAL_SURFACE ( 'NONE', #1586, 1.000000000000001332 ) ;
#14873=CARTESIAN_POINT ( 'NONE',  ( 15.76715644869600119, 8.722854347492999594, 8.080426068599999567 ) ) ;
#14875=CARTESIAN_POINT ( 'NONE',  ( 25.29986734212600297, -2.258942858049999725, 11.29419282279013004 ) ) ;
#14879=DIRECTION ( 'NONE',  ( 1.000000000000000000, 0.000000000000000000, 0.000000000000000000 ) ) ;
#14880=CARTESIAN_POINT ( 'NONE',  ( 12.80000000000000071, 50.14170351282000127, -17.06962823869000090 ) ) ;
#14890=ORIENTED_EDGE ( 'NONE', *, *, #67603, .T. ) ;
#14891=CARTESIAN_POINT ( 'NONE',  ( 11.79999999771000141, 12.39026187696000036, 1.832249219479999969 ) ) ;
#14892=CARTESIAN_POINT ( 'NONE',  ( 23.84018977933850891, 12.96271613198936734, -3.649568246013530803 ) ) ;
#14898=CARTESIAN_POINT ( 'NONE',  ( 21.60000000000000142, 12.52500000000000036, 0.000000000000000000 ) ) ;
#14903=AXIS2_PLACEMENT_3D ( 'NONE', #16759, #1383, #16077 ) ;
#14914=CARTESIAN_POINT ( 'NONE',  ( 15.39046541331000029, 9.526477069417000010, 8.190982836632000996 ) ) ;
#14915=CARTESIAN_POINT ( 'NONE',  ( 24.32158589636341262, 9.044138011824934154, 9.474428460952893261 ) ) ;
#14924=DIRECTION ( 'NONE',  ( 0.000000000000000000, -0.9466492601157001641, 0.3222656952305000266 ) ) ;
#14929=DIRECTION ( 'NONE',  ( 1.000000000000000000, 0.000000000000000000, 0.000000000000000000 ) ) ;
#14932=CARTESIAN_POINT ( 'NONE',  ( 17.95534550153200115, 3.277905616156999713, 11.84067279748999901 ) ) ;
#14937=CARTESIAN_POINT ( 'NONE',  ( 24.67921321800200118, -8.727630028894999725, 9.158313644156001132 ) ) ;
#14942=CARTESIAN_POINT ( 'NONE',  ( 11.50001496184999894, 8.431319371474298663, -9.354420476537780971 ) ) ;
#14949=B_SPLINE_CURVE_WITH_KNOTS ( 'NONE', 3,
 ( #47895, #22251, #52788, #25532, #4882, #52439 ),
 .UNSPECIFIED., .F., .F.,
 ( 4, 2, 4 ),
 ( 0.000000000000000000, 0.5000000000000000000, 1.000000000000000000 ),
 .UNSPECIFIED. ) ;
#14950=DIRECTION ( 'NONE',  ( 0.000000000000000000, 0.5393449376833056030, -0.8420849352621094797 ) ) ;
#14951=ORIENTED_EDGE ( 'NONE', *, *, #10819, .T. ) ;
#14952=DIRECTION ( 'NONE',  ( -1.000000000000000000, 0.000000000000000000, 0.000000000000000000 ) ) ;
#14953=ORIENTED_EDGE ( 'NONE', *, *, #39541, .T. ) ;
#14954=CARTESIAN_POINT ( 'NONE',  ( 18.30000103245939158, -11.66744832144745203, 3.971921730545766138 ) ) ;
#14965=CARTESIAN_POINT ( 'NONE',  ( 15.90000000000000036, -8.611670352360746961, -8.369116320314965662 ) ) ;
#14975=CARTESIAN_POINT ( 'NONE',  ( 24.39664237488266707, -3.224866622838412411, -12.03536608415421050 ) ) ;
#14986=CARTESIAN_POINT ( 'NONE',  ( 17.76396973669300294, 3.526704268670000086, -11.96114524401999901 ) ) ;
#14993=EDGE_CURVE ( 'NONE', #31587, #35662, #11114, .T. ) ;
#15002=CIRCLE ( 'NONE', #477, 10.75000000000000000 ) ;
#15004=CARTESIAN_POINT ( 'NONE',  ( 18.36663043076582724, -2.717294527786511704, -11.46570543779412787 ) ) ;
#15005=CARTESIAN_POINT ( 'NONE',  ( 11.42387073792000152, -3.325692027085000113, 11.41083924281000073 ) ) ;
#15006=VERTEX_POINT ( 'NONE', #1652 ) ;
#15011=EDGE_CURVE ( 'NONE', #37580, #47653, #5310, .T. ) ;
#15019=CARTESIAN_POINT ( 'NONE',  ( 13.87269624719400163, -9.544758557629000606, -8.169753052074002042 ) ) ;
#15033=CYLINDRICAL_SURFACE ( 'NONE', #63686, 0.6999999999999992895 ) ;
#15035=ORIENTED_EDGE ( 'NONE', *, *, #32625, .F. ) ;
#15044=FACE_OUTER_BOUND ( 'NONE', #5071, .T. ) ;
#15048=ORIENTED_EDGE ( 'NONE', *, *, #33666, .F. ) ;
#15051=VERTEX_POINT ( 'NONE', #61418 ) ;
#15057=EDGE_CURVE ( 'NONE', #68067, #7298, #19842, .T. ) ;
#15068=DIRECTION ( 'NONE',  ( 0.7071060218675898623, -0.7071075405046897133, 8.464214322710876718E-10 ) ) ;
#15069=CARTESIAN_POINT ( 'NONE',  ( 24.95273178630209898, 8.555918886037284565, 8.377715515261876078 ) ) ;
#15070=CARTESIAN_POINT ( 'NONE',  ( 21.05000000000000426, 0.000000000000000000, 0.000000000000000000 ) ) ;
#15077=CARTESIAN_POINT ( 'NONE',  ( 24.30857393632600250, 8.915481952665000875, 8.861377372684998477 ) ) ;
#15079=CARTESIAN_POINT ( 'NONE',  ( 13.99999999379500082, -8.815218614167999789, -7.616697584347000394 ) ) ;
#15081=CARTESIAN_POINT ( 'NONE',  ( 15.92727146503378499, 9.312591611299771088, 8.375703117199133629 ) ) ;
#15083=EDGE_CURVE ( 'NONE', #6863, #42044, #56194, .T. ) ;
#15093=CARTESIAN_POINT ( 'NONE',  ( 12.25964841771339309, 11.59985379594652599, -4.724415456179380968 ) ) ;
#15099=ORIENTED_EDGE ( 'NONE', *, *, #6571, .T. ) ;
#15106=CARTESIAN_POINT ( 'NONE',  ( 23.59433343020063845, -3.211148892941130928, -13.60463507072412703 ) ) ;
#15124=CARTESIAN_POINT ( 'NONE',  ( 24.14474055218938986, 3.678932468831995539, -12.80134587320634054 ) ) ;
#15136=ORIENTED_EDGE ( 'NONE', *, *, #1656, .F. ) ;
#15139=EDGE_CURVE ( 'NONE', #47642, #25573, #33662, .T. ) ;
#15140=DIRECTION ( 'NONE',  ( 0.000000000000000000, -0.9466492601157000530, 0.3222656952305000266 ) ) ;
#15141=EDGE_CURVE ( 'NONE', #54978, #63863, #23662, .T. ) ;
#15146=CARTESIAN_POINT ( 'NONE',  ( 13.75930817923600102, 9.623971528738000103, 8.076134841847999013 ) ) ;
#15153=CIRCLE ( 'NONE', #20741, 14.00000000000000000 ) ;
#15156=CARTESIAN_POINT ( 'NONE',  ( 24.34832161043337351, -3.224867767510426919, 12.03537035604409056 ) ) ;
#15158=CARTESIAN_POINT ( 'NONE',  ( 12.42828976145100128, 11.57811841779999895, -4.879106015068000346 ) ) ;
#15159=CARTESIAN_POINT ( 'NONE',  ( 17.73161317130500336, 12.16650445177999984, -3.137092607272999878 ) ) ;
#15164=CARTESIAN_POINT ( 'NONE',  ( 17.85728973496400229, 3.190139087762999814, 11.45065787240999988 ) ) ;
#15171=CARTESIAN_POINT ( 'NONE',  ( 24.23036338817854585, 3.301121323903743576, 12.33133795113440456 ) ) ;
#15180=CONICAL_SURFACE ( 'NONE', #54251, 1.150081673463000165, 0.7854598275718697176 ) ;
#15186=CARTESIAN_POINT ( 'NONE',  ( 25.29987931604000195, 11.13052921044000065, -3.427478701325000099 ) ) ;
#15187=CARTESIAN_POINT ( 'NONE',  ( 13.73763077846600034, 8.978479145825000174, 7.363267546620999582 ) ) ;
#15188=DIRECTION ( 'NONE',  ( -1.000000000000000000, 0.000000000000000000, 0.000000000000000000 ) ) ;
#15189=VECTOR ( 'NONE', #18212, 999.9999999999998863 ) ;
#15198=DIRECTION ( 'NONE',  ( -1.000000000000000000, 0.000000000000000000, 0.000000000000000000 ) ) ;
#15205=CARTESIAN_POINT ( 'NONE',  ( 13.51386961183700031, -11.53357255609999932, -1.992589078083000009 ) ) ;
#15207=CARTESIAN_POINT ( 'NONE',  ( 13.05446786537200232, 12.11615129267999968, 2.032410325197000045 ) ) ;
#15208=VERTEX_POINT ( 'NONE', #12488 ) ;
#15210=ORIENTED_EDGE ( 'NONE', *, *, #26802, .T. ) ;
#15211=DIRECTION ( 'NONE',  ( 1.000000000000000000, 0.000000000000000000, 0.000000000000000000 ) ) ;
#15231=ORIENTED_EDGE ( 'NONE', *, *, #5613, .F. ) ;
#15232=CARTESIAN_POINT ( 'NONE',  ( 24.30000000000000071, -50.50083396221999976, -14.25635100356000073 ) ) ;
#15233=CARTESIAN_POINT ( 'NONE',  ( 24.04053420818027575, 12.64669712376688793, -3.439809266941736166 ) ) ;
#15253=CARTESIAN_POINT ( 'NONE',  ( 25.30000327618300204, 10.83443035398000021, -3.855530949778000149 ) ) ;
#15256=CARTESIAN_POINT ( 'NONE',  ( 12.78268972790800184, -11.49710380946999955, 4.820178426657999005 ) ) ;
#15262=CARTESIAN_POINT ( 'NONE',  ( 23.60205915885299888, -2.504446818062000535, -12.27382285989999566 ) ) ;
#15271=CARTESIAN_POINT ( 'NONE',  ( 12.10000000000000142, 50.14170351282000127, -17.06962823869000090 ) ) ;
#15276=DIRECTION ( 'NONE',  ( 2.887756364190075102E-10, -0.5897878662160149776, -0.8075582163933199276 ) ) ;
#15277=VERTEX_POINT ( 'NONE', #63110 ) ;
#15287=CARTESIAN_POINT ( 'NONE',  ( 17.60000000714711277, -11.20147114780081843, 4.552742043578180464 ) ) ;
#15299=DIRECTION ( 'NONE',  ( 1.000000000000000000, 0.000000000000000000, 0.000000000000000000 ) ) ;
#15301=ORIENTED_EDGE ( 'NONE', *, *, #21955, .T. ) ;
#15312=EDGE_CURVE ( 'NONE', #8614, #2551, #31193, .T. ) ;
#15317=ORIENTED_EDGE ( 'NONE', *, *, #69042, .T. ) ;
#15320=CYLINDRICAL_SURFACE ( 'NONE', #31579, 0.5000000000000004441 ) ;
#15321=CYLINDRICAL_SURFACE ( 'NONE', #28592, 9.250000000000000000 ) ;
#15324=CARTESIAN_POINT ( 'NONE',  ( 17.97784399489228946, 3.574258648614753398, 12.00418160090821473 ) ) ;
#15336=CARTESIAN_POINT ( 'NONE',  ( 16.13895793972310599, 3.268072512451278389, 11.38828084065380608 ) ) ;
#15339=ORIENTED_EDGE ( 'NONE', *, *, #34102, .F. ) ;
#15341=ORIENTED_EDGE ( 'NONE', *, *, #41232, .T. ) ;
#15342=CARTESIAN_POINT ( 'NONE',  ( 18.29991931957795259, -1.031823913341759950E-13, -12.32514597914127563 ) ) ;
#15343=CARTESIAN_POINT ( 'NONE',  ( 23.60754984838813186, -10.12980629292501078, -9.622309725513526146 ) ) ;
#15347=AXIS2_PLACEMENT_3D ( 'NONE', #6776, #28114, #49425 ) ;
#15349=CARTESIAN_POINT ( 'NONE',  ( 24.37899127803200372, 8.840620920327999954, 8.761547301204000604 ) ) ;
#15356=ORIENTED_EDGE ( 'NONE', *, *, #61114, .T. ) ;
#15359=FACE_OUTER_BOUND ( 'NONE', #29763, .T. ) ;
#15361=CARTESIAN_POINT ( 'NONE',  ( 24.67921580255100267, 8.727633792449999817, 9.158312800479000870 ) ) ;
#15365=CARTESIAN_POINT ( 'NONE',  ( 13.99999999379500082, 8.815218614167999789, 7.616697584347000394 ) ) ;
#15382=TOROIDAL_SURFACE ( 'NONE', #3098, 10.75000000000000000, 1.500000000000000000 ) ;
#15384=CARTESIAN_POINT ( 'NONE',  ( 24.22085374770700028, 3.760945907258999465, 12.77833517530000051 ) ) ;
#15395=CARTESIAN_POINT ( 'NONE',  ( 24.39664803136666649, 12.09373379607674082, 3.240506204136868185 ) ) ;
#15399=CARTESIAN_POINT ( 'NONE',  ( 25.29574788798400320, -2.995621132715000190, -11.41693952213999985 ) ) ;
#15403=EDGE_LOOP ( 'NONE', ( #43688, #24286, #40641, #27438 ) ) ;
#15407=CARTESIAN_POINT ( 'NONE',  ( 15.90018573812067260, 7.083264066697978478, 9.547770387690125204 ) ) ;
#15417=EDGE_CURVE ( 'NONE', #7173, #17632, #4731, .T. ) ;
#15418=CARTESIAN_POINT ( 'NONE',  ( 25.29986734212600297, -2.596989636639000398, 11.35306351421000137 ) ) ;
#15426=CARTESIAN_POINT ( 'NONE',  ( 25.46373154986600085, 8.354608910739999672, 8.148450287869000164 ) ) ;
#15433=B_SPLINE_CURVE_WITH_KNOTS ( 'NONE', 3,
 ( #33354, #34397, #23890, #65493 ),
 .UNSPECIFIED., .F., .F.,
 ( 4, 4 ),
 ( 0.000000000000000000, 1.000000000000000000 ),
 .UNSPECIFIED. ) ;
#15441=CARTESIAN_POINT ( 'NONE',  ( 12.41307909110098429, 11.56466389787666493, -4.809819853923482214 ) ) ;
#15455=PLANE ( 'NONE',  #66740 ) ;
#15459=ORIENTED_EDGE ( 'NONE', *, *, #22950, .F. ) ;
#15471=DIRECTION ( 'NONE',  ( 1.000000000000000000, 0.000000000000000000, 0.000000000000000000 ) ) ;
#15473=CARTESIAN_POINT ( 'NONE',  ( 24.01983374632887092, 9.335054998824150019, -9.252342060729551676 ) ) ;
#15475=CARTESIAN_POINT ( 'NONE',  ( 24.30000000000000071, -8.810505093353000916, 8.810505093353000916 ) ) ;
#15477=FACE_OUTER_BOUND ( 'NONE', #58993, .T. ) ;
#15487=CYLINDRICAL_SURFACE ( 'NONE', #4085, 0.6999999999999992895 ) ;
#15494=CARTESIAN_POINT ( 'NONE',  ( 13.94794651623100101, 9.527030574842997979, 8.190375113092999371 ) ) ;
#15505=CARTESIAN_POINT ( 'NONE',  ( 13.86904166957592999, -8.833215535550223763, -7.896538540699776121 ) ) ;
#15507=CARTESIAN_POINT ( 'NONE',  ( 12.32697677577000128, 11.50538345640999971, -4.553133914476999777 ) ) ;
#15508=CARTESIAN_POINT ( 'NONE',  ( 17.75588107601699761, 11.55446208650999829, -4.935524324464999779 ) ) ;
#15510=DIRECTION ( 'NONE',  ( 1.000000000000000000, 0.000000000000000000, 0.000000000000000000 ) ) ;
#15513=CARTESIAN_POINT ( 'NONE',  ( 18.44330693167099966, -2.998553466420000202, 12.10578145104000036 ) ) ;
#15516=ORIENTED_EDGE ( 'NONE', *, *, #26439, .F. ) ;
#15518=CARTESIAN_POINT ( 'NONE',  ( 25.60000000000000142, -8.131727983644998048, 8.131727983644998048 ) ) ;
#15526=ORIENTED_EDGE ( 'NONE', *, *, #8629, .F. ) ;
#15527=CARTESIAN_POINT ( 'NONE',  ( 25.00275061277693567, -11.89252591243665869, 2.924339798584659977 ) ) ;
#15530=EDGE_CURVE ( 'NONE', #28381, #10297, #51096, .T. ) ;
#15533=CIRCLE ( 'NONE', #19984, 0.3000000000000000444 ) ;
#15536=FACE_OUTER_BOUND ( 'NONE', #30790, .T. ) ;
#15537=CARTESIAN_POINT ( 'NONE',  ( 15.79991751193277416, -9.060349897821465603, -8.357793075677504291 ) ) ;
#15554=EDGE_CURVE ( 'NONE', #20236, #36843, #12861, .T. ) ;
#15555=CARTESIAN_POINT ( 'NONE',  ( 24.30001680216799897, -3.271769318036999774, 12.21048166890999909 ) ) ;
#15557=CARTESIAN_POINT ( 'NONE',  ( 11.49999672494999636, -10.70720904779669524, 4.749689352253898988 ) ) ;
#15566=DIRECTION ( 'NONE',  ( -1.000000000000000000, 0.000000000000000000, 0.000000000000000000 ) ) ;
#15570=CARTESIAN_POINT ( 'NONE',  ( 18.50003594170800270, 2.686563649653999963, -11.33603604535000109 ) ) ;
#15585=CARTESIAN_POINT ( 'NONE',  ( 24.17844067670218777, 12.41761889074214587, 3.338210367410554991 ) ) ;
#15592=PLANE ( 'NONE',  #7292 ) ;
#15595=FACE_OUTER_BOUND ( 'NONE', #3081, .T. ) ;
#15604=CIRCLE ( 'NONE', #21188, 1.000000000000000000 ) ;
#15608=CARTESIAN_POINT ( 'NONE',  ( 25.48313768079200159, -11.09944635839999982, 3.317483465242999863 ) ) ;
#15610=ADVANCED_FACE ( 'NONE', ( #34300 ), #65376, .F. ) ;
#15614=CARTESIAN_POINT ( 'NONE',  ( 23.86819263930300394, 9.630286858308998887, 9.781782771855001002 ) ) ;
#15615=VERTEX_POINT ( 'NONE', #2136 ) ;
#15635=CARTESIAN_POINT ( 'NONE',  ( 13.99999999485600277, 9.471999751521998689, 8.194948195317001804 ) ) ;
#15639=ORIENTED_EDGE ( 'NONE', *, *, #60871, .T. ) ;
#15649=ORIENTED_EDGE ( 'NONE', *, *, #44195, .T. ) ;
#15652=AXIS2_PLACEMENT_3D ( 'NONE', #13948, #23045, #17817 ) ;
#15670=ORIENTED_EDGE ( 'NONE', *, *, #19336, .T. ) ;
#15675=LINE ( 'NONE', #47150, #53260 ) ;
#15695=EDGE_LOOP ( 'NONE', ( #38598, #56424 ) ) ;
#15699=ADVANCED_FACE ( 'NONE', ( #45734 ), #34567, .T. ) ;
#15701=CARTESIAN_POINT ( 'NONE',  ( 19.39373726536100051, 0.000000000000000000, 0.000000000000000000 ) ) ;
#15704=ORIENTED_EDGE ( 'NONE', *, *, #22214, .F. ) ;
#15705=CARTESIAN_POINT ( 'NONE',  ( 24.44496412535000118, -8.810486166165000910, -8.810507954003998776 ) ) ;
#15709=CARTESIAN_POINT ( 'NONE',  ( 11.53898808224000128, 3.920528549154999709, -11.93545759853000021 ) ) ;
#15711=ORIENTED_EDGE ( 'NONE', *, *, #386, .T. ) ;
#15717=VERTEX_POINT ( 'NONE', #67043 ) ;
#15722=CARTESIAN_POINT ( 'NONE',  ( 13.59982064663300072, -2.380318164795999883E-13, -1.474376176701999879E-13 ) ) ;
#15726=ORIENTED_EDGE ( 'NONE', *, *, #57706, .T. ) ;
#15733=CARTESIAN_POINT ( 'NONE',  ( 24.09351851543715384, -3.337598052541425719, 12.57555534302550448 ) ) ;
#15737=CARTESIAN_POINT ( 'NONE',  ( 25.08881450776800293, -3.215722343401999694, -11.60740445141000166 ) ) ;
#15739=CARTESIAN_POINT ( 'NONE',  ( 25.39940292809759370, -8.416043265628282199, -8.072286559073248213 ) ) ;
#15743=CIRCLE ( 'NONE', #44802, 14.00000000000000533 ) ;
#15778=CARTESIAN_POINT ( 'NONE',  ( 12.35268573731032227, 12.09127048605807353, -3.267865047144104640 ) ) ;
#15782=CARTESIAN_POINT ( 'NONE',  ( 18.30000786429387816, -11.69700901162388185, 3.885059408455575625 ) ) ;
#15785=ORIENTED_EDGE ( 'NONE', *, *, #50292, .T. ) ;
#15793=CARTESIAN_POINT ( 'NONE',  ( 23.54908214757200113, 2.962708511087999597, -13.72216420026999906 ) ) ;
#15803=CARTESIAN_POINT ( 'NONE',  ( 13.99999999347100044, -9.187456302440001110, -8.213201953411001455 ) ) ;
#15812=ORIENTED_EDGE ( 'NONE', *, *, #58862, .T. ) ;
#15816=DIRECTION ( 'NONE',  ( -0.000000000000000000, 0.2588190451024934280, 0.9659258262890756397 ) ) ;
#15819=VERTEX_POINT ( 'NONE', #41175 ) ;
#15822=CARTESIAN_POINT ( 'NONE',  ( 18.02410434383600091, -3.285250940561000199, 11.23276246309000115 ) ) ;
#15827=ORIENTED_EDGE ( 'NONE', *, *, #13825, .F. ) ;
#15838=VERTEX_POINT ( 'NONE', #2733 ) ;
#15839=CARTESIAN_POINT ( 'NONE',  ( 12.56257882282300109, 11.80639483233000142, -3.358960109135999961 ) ) ;
#15840=CARTESIAN_POINT ( 'NONE',  ( 18.54135782960599954, 11.85700164854999983, -4.150661879143999755 ) ) ;
#15842=CARTESIAN_POINT ( 'NONE',  ( 23.56664322114200161, -2.935586410151000081, -13.67842711829000102 ) ) ;
#15845=CARTESIAN_POINT ( 'NONE',  ( 17.79173234077999766, -3.528207283916999781, 11.96069632439000152 ) ) ;
#15846=AXIS2_PLACEMENT_3D ( 'NONE', #48786, #26085, #22206 ) ;
#15848=VERTEX_POINT ( 'NONE', #35248 ) ;
#15852=CARTESIAN_POINT ( 'NONE',  ( 11.29996849689000271, 12.23272706294999956, 1.505586356912999912 ) ) ;
#15868=CARTESIAN_POINT ( 'NONE',  ( 16.39956681845000119, -3.250692199830000018, -11.33777344299000056 ) ) ;
#15869=CARTESIAN_POINT ( 'NONE',  ( 15.89998535262538581, -8.893549080881243185, -8.534693534631728085 ) ) ;
#15874=EDGE_CURVE ( 'NONE', #45907, #15819, #22741, .T. ) ;
#15876=CARTESIAN_POINT ( 'NONE',  ( 44.24148000000000280, 9.517611874540000017, -8.103398312166000039 ) ) ;
#15879=CARTESIAN_POINT ( 'NONE',  ( 23.60000000000000497, 10.96672402886443187, 8.588474120523409638 ) ) ;
#15881=FACE_OUTER_BOUND ( 'NONE', #38018, .T. ) ;
#15884=CARTESIAN_POINT ( 'NONE',  ( 18.30017264560542145, -0.9191760160195996399, -11.85014035451979630 ) ) ;
#15888=DIRECTION ( 'NONE',  ( 0.000000000000000000, 0.000000000000000000, -1.000000000000000000 ) ) ;
#15889=DIRECTION ( 'NONE',  ( 1.000000000000000000, 0.000000000000000000, 0.000000000000000000 ) ) ;
#15896=CARTESIAN_POINT ( 'NONE',  ( 13.56457200098428117, 11.48338024779088862, 1.964390585080378226 ) ) ;
#15913=CARTESIAN_POINT ( 'NONE',  ( 18.29983863916000075, 2.861762957209999847, -11.98830831200999825 ) ) ;
#15915=ADVANCED_FACE ( 'NONE', ( #66702, #14264 ), #61464, .T. ) ;
#15916=CARTESIAN_POINT ( 'NONE',  ( 44.24148000000000280, -9.517611874540000017, -8.103398312166000039 ) ) ;
#15918=CARTESIAN_POINT ( 'NONE',  ( 23.81728141243367602, 12.99649529944050030, 3.682154768044699988 ) ) ;
#15921=ORIENTED_EDGE ( 'NONE', *, *, #20131, .T. ) ;
#15930=CIRCLE ( 'NONE', #8150, 5.000000000000000000 ) ;
#15936=CARTESIAN_POINT ( 'NONE',  ( 12.78455560662700208, -11.44263450739000021, 4.698119303721000506 ) ) ;
#15940=EDGE_CURVE ( 'NONE', #45376, #35517, #25426, .T. ) ;
#15943=CARTESIAN_POINT ( 'NONE',  ( 24.53428991195500330, 3.614319144953999530, 12.31267516478999902 ) ) ;
#15946=EDGE_CURVE ( 'NONE', #31242, #28639, #61878, .T. ) ;
#15951=CYLINDRICAL_SURFACE ( 'NONE', #55574, 0.5000000000000004441 ) ;
#15962=ORIENTED_EDGE ( 'NONE', *, *, #15940, .T. ) ;
#15970=B_SPLINE_CURVE_WITH_KNOTS ( 'NONE', 3,
 ( #12322, #43794, #59863, #50414 ),
 .UNSPECIFIED., .F., .F.,
 ( 4, 4 ),
 ( 0.000000000000000000, 1.000000000000000000 ),
 .UNSPECIFIED. ) ;
#15976=CARTESIAN_POINT ( 'NONE',  ( 16.39955778315600199, -3.526114926816000139, -11.96132012103000086 ) ) ;
#15977=CARTESIAN_POINT ( 'NONE',  ( 11.56566386073000174, 11.72961781202000076, 1.923363593971999963 ) ) ;
#15978=EDGE_LOOP ( 'NONE', ( #30371, #52965, #54261, #5325 ) ) ;
#15979=CARTESIAN_POINT ( 'NONE',  ( 24.92741773699590624, 2.996169077880856957, -11.61847982281971881 ) ) ;
#15980=DIRECTION ( 'NONE',  ( 1.000000000000000000, 0.000000000000000000, 0.000000000000000000 ) ) ;
#15999=DIRECTION ( 'NONE',  ( 0.000000000000000000, -0.008867170401640422917, -0.9999606858717338120 ) ) ;
#16006=ORIENTED_EDGE ( 'NONE', *, *, #45095, .T. ) ;
#16007=( BOUNDED_SURFACE ( )  B_SPLINE_SURFACE ( 3, 3, ( 
 ( #35073, #49152, #40640, #22578 ),
 ( #43920, #38315, #3244, #65224 ),
 ( #12445, #2895, #17339, #11740 ),
 ( #33083, #38669, #56738, #59988 ) ),
 .UNSPECIFIED., .F., .F., .F. ) 
 B_SPLINE_SURFACE_WITH_KNOTS ( ( 4, 4 ),
 ( 4, 4 ),
 ( 0.000000000000000000, 1.000000000000000000 ),
 ( 0.000000000000000000, 1.000000000000000000 ),
 .UNSPECIFIED. ) 
 GEOMETRIC_REPRESENTATION_ITEM ( )  RATIONAL_B_SPLINE_SURFACE ( (
 ( 1.512182578520000042, 1.160176301760999840, 1.160176301760999840, 1.512182578520000042),
 ( 1.111288591041000196, 0.8526025270081000196, 0.8526025270081000196, 1.111288591041000196),
 ( 1.111288591041000196, 0.8526025270081000196, 0.8526025270081000196, 1.111288591041000196),
 ( 1.512182578520000042, 1.160176301760999840, 1.160176301760999840, 1.512182578520000042) ) ) 
 REPRESENTATION_ITEM ( '' )  SURFACE ( )  );
#16016=CARTESIAN_POINT ( 'NONE',  ( 24.03017386583299952, -13.13663164873999989, 3.281013120054999899 ) ) ;
#16023=CARTESIAN_POINT ( 'NONE',  ( 18.44383669537300108, 2.795303817231000298, -11.36579926027000020 ) ) ;
#16030=CARTESIAN_POINT ( 'NONE',  ( 11.80600022547799988, -3.313997181012000137, 11.22408540768999963 ) ) ;
#16032=CARTESIAN_POINT ( 'NONE',  ( 25.29986325275000070, 2.258942858049999725, 11.29419282279020287 ) ) ;
#16036=CARTESIAN_POINT ( 'NONE',  ( 24.56500367226799852, 8.792450275430001128, -9.097562849135000462 ) ) ;
#16041=CARTESIAN_POINT ( 'NONE',  ( 13.84412491599044337, 8.835575362389644027, 7.593298916478570249 ) ) ;
#16042=EDGE_CURVE ( 'NONE', #30003, #33549, #8582, .T. ) ;
#16045=CARTESIAN_POINT ( 'NONE',  ( 25.00272599386161332, 11.89255749221432623, -2.924338816029021348 ) ) ;
#16054=B_SPLINE_CURVE_WITH_KNOTS ( 'NONE', 3,
 ( #41109, #57178, #51589, #40414 ),
 .UNSPECIFIED., .F., .F.,
 ( 4, 4 ),
 ( 0.000000000000000000, 1.000000000000000000 ),
 .UNSPECIFIED. ) ;
#16069=CARTESIAN_POINT ( 'NONE',  ( 24.56665995394800106, -3.304342232863999751, -12.00441819182999836 ) ) ;
#16070=AXIS2_PLACEMENT_3D ( 'NONE', #284, #48874, #32452 ) ;
#16072=ORIENTED_EDGE ( 'NONE', *, *, #48928, .T. ) ;
#16073=CARTESIAN_POINT ( 'NONE',  ( 16.09996065438095769, -9.056490835163780062, -8.652417574211050066 ) ) ;
#16075=CARTESIAN_POINT ( 'NONE',  ( 23.96074334152477192, 9.430604214506258742, 9.306875196542495843 ) ) ;
#16077=DIRECTION ( 'NONE',  ( -1.000000000000000000, 0.000000000000000000, 0.000000000000000000 ) ) ;
#16079=DIRECTION ( 'NONE',  ( 0.000000000000000000, -0.1807154286440006141, -0.9835354258236025382 ) ) ;
#16082=ADVANCED_FACE ( 'NONE', ( #7547 ), #37435, .F. ) ;
#16089=EDGE_CURVE ( 'NONE', #23400, #14432, #21016, .T. ) ;
#16094=CARTESIAN_POINT ( 'NONE',  ( 24.71765875488695485, -3.123588627309684895, 11.79180799685195780 ) ) ;
#16099=CARTESIAN_POINT ( 'NONE',  ( 11.49999035076000276, -3.886252136122000156, 11.90689009355000039 ) ) ;
#16133=B_SPLINE_CURVE_WITH_KNOTS ( 'NONE', 3,
 ( #67724, #52346, #62485, #4097, #9340, #36964, #31038, #20186 ),
 .UNSPECIFIED., .F., .F.,
 ( 4, 2, 2, 4 ),
 ( 0.000000000000000000, 0.2499999999999992228, 0.4999999999999984457, 1.000000000000000000 ),
 .UNSPECIFIED. ) ;
#16140=CIRCLE ( 'NONE', #55228, 13.89999856298999958 ) ;
#16147=CARTESIAN_POINT ( 'NONE',  ( 11.53142637459347775, -3.735369041114874111, 11.95516355327115399 ) ) ;
#16150=CARTESIAN_POINT ( 'NONE',  ( 24.53428985175800037, 12.47024902693999948, -3.026245299674999778 ) ) ;
#16151=CARTESIAN_POINT ( 'NONE',  ( 23.60000334400854527, 10.25389668638031004, -9.379908238711360369 ) ) ;
#16153=AXIS2_PLACEMENT_3D ( 'NONE', #37322, #38705, #49190 ) ;
#16159=CARTESIAN_POINT ( 'NONE',  ( 13.68260097612285264, 12.30227370000273268, 2.353106563168188003 ) ) ;
#16161=EDGE_LOOP ( 'NONE', ( #44764, #20117, #24015, #52131 ) ) ;
#16163=CARTESIAN_POINT ( 'NONE',  ( 24.30001680216799897, -3.271769318036999774, 12.21048166890999909 ) ) ;
#16164=CARTESIAN_POINT ( 'NONE',  ( 18.31802873821099809, -2.927761598026000112, 11.42873208727000112 ) ) ;
#16168=CARTESIAN_POINT ( 'NONE',  ( 13.36715644869600084, 11.69666705770999826, 2.137627928029000035 ) ) ;
#16184=CARTESIAN_POINT ( 'NONE',  ( 12.25978835901500119, 11.49417283396999956, -4.331891014347999835 ) ) ;
#16185=FACE_OUTER_BOUND ( 'NONE', #29640, .T. ) ;
#16192=CARTESIAN_POINT ( 'NONE',  ( 18.44496314779700086, -2.860815007322000447, 12.13831535021000008 ) ) ;
#16195=ORIENTED_EDGE ( 'NONE', *, *, #22725, .F. ) ;
#16197=CARTESIAN_POINT ( 'NONE',  ( 11.50004197952388552, 11.55567553918560542, 1.481524017262679127 ) ) ;
#16199=CARTESIAN_POINT ( 'NONE',  ( 13.55563472374800149, 9.144188282469000839, 7.452974878632000255 ) ) ;
#16201=CARTESIAN_POINT ( 'NONE',  ( 24.84557873272407136, -3.513964920196102071, -11.93639205272353010 ) ) ;
#16206=ORIENTED_EDGE ( 'NONE', *, *, #26881, .T. ) ;
#16219=DIRECTION ( 'NONE',  ( -1.000000000000000000, 0.000000000000000000, 0.000000000000000000 ) ) ;
#16228=CARTESIAN_POINT ( 'NONE',  ( 25.25778441053600076, -11.13231713549000013, -3.460093662997999697 ) ) ;
#16244=FACE_OUTER_BOUND ( 'NONE', #152, .T. ) ;
#16248=ORIENTED_EDGE ( 'NONE', *, *, #134, .T. ) ;
#16250=EDGE_CURVE ( 'NONE', #1910, #29725, #65802, .T. ) ;
#16252=CARTESIAN_POINT ( 'NONE',  ( 25.57800075372000137, 11.11254651097000057, -3.219695634887000057 ) ) ;
#16262=CARTESIAN_POINT ( 'NONE',  ( 16.15930817923600316, 3.787151970053999950, 11.97924296128000066 ) ) ;
#16270=FACE_OUTER_BOUND ( 'NONE', #26819, .T. ) ;
#16272=CARTESIAN_POINT ( 'NONE',  ( 18.19067337301504494, -12.06199139229578066, 3.374301501848208762 ) ) ;
#16276=LINE ( 'NONE', #21519, #27620 ) ;
#16281=CARTESIAN_POINT ( 'NONE',  ( 12.82764013820600013, -11.38891548326999903, 4.574441164091999745 ) ) ;
#16286=CARTESIAN_POINT ( 'NONE',  ( 18.22958618735997049, 11.12724485990802847, -3.450621024319545427 ) ) ;
#16289=CARTESIAN_POINT ( 'NONE',  ( 24.55996189763800075, -8.848787117368999589, -9.333438204885000644 ) ) ;
#16290=AXIS2_PLACEMENT_3D ( 'NONE', #15916, #36561, #36912 ) ;
#16294=CARTESIAN_POINT ( 'NONE',  ( 17.89107826690531056, -3.595094513005585135, 11.99795484439375848 ) ) ;
#16295=ORIENTED_EDGE ( 'NONE', *, *, #41039, .T. ) ;
#16299=CARTESIAN_POINT ( 'NONE',  ( 17.60000000798000386, 11.41069016990000051, -4.623987642516999230 ) ) ;
#16304=ADVANCED_FACE ( 'NONE', ( #15881 ), #26849, .F. ) ;
#16305=ORIENTED_EDGE ( 'NONE', *, *, #64949, .T. ) ;
#16321=CARTESIAN_POINT ( 'NONE',  ( 25.22253823781074900, 2.724025653123483881, -11.39869274941884392 ) ) ;
#16328=CARTESIAN_POINT ( 'NONE',  ( 23.73953470779122554, -13.33634092520827252, 3.648239340457724467 ) ) ;
#16329=CARTESIAN_POINT ( 'NONE',  ( 11.29998636608000062, 3.695122995756999984, -11.25914041192000070 ) ) ;
#16337=VECTOR ( 'NONE', #5299, 1000.000000000000227 ) ;
#16348=CARTESIAN_POINT ( 'NONE',  ( 13.69997185827399910, -9.599065136398367670, -6.667560658748436175 ) ) ;
#16353=CARTESIAN_POINT ( 'NONE',  ( 11.26490954471000094, -12.17992731521000138, -1.606774076355000025 ) ) ;
#16359=CARTESIAN_POINT ( 'NONE',  ( 24.38581461189300015, -12.22838082518000036, 3.200660937889999946 ) ) ;
#16361=ORIENTED_EDGE ( 'NONE', *, *, #11281, .T. ) ;
#16372=CARTESIAN_POINT ( 'NONE',  ( 23.58566160172500048, -10.19392717108999946, -9.581222027289999943 ) ) ;
#16374=CARTESIAN_POINT ( 'NONE',  ( 11.84835150974899953, -3.192438788486000156, 11.44998398973999976 ) ) ;
#16416=FACE_OUTER_BOUND ( 'NONE', #66201, .T. ) ;
#16426=CARTESIAN_POINT ( 'NONE',  ( 25.59997277611800115, 2.578802611042650509E-13, -11.19994871957399241 ) ) ;
#16434=AXIS2_PLACEMENT_3D ( 'NONE', #10622, #59207, #21122 ) ;
#16436=CARTESIAN_POINT ( 'NONE',  ( 24.54174074855145804, -8.849271461538792849, -9.279828214374076012 ) ) ;
#16437=CARTESIAN_POINT ( 'NONE',  ( 11.82330164685100193, 12.43416923969000010, 1.799281280950999928 ) ) ;
#16453=DIRECTION ( 'NONE',  ( 0.7071068208980029191, 0.000000000000000000, -0.7071067414750898950 ) ) ;
#16454=CARTESIAN_POINT ( 'NONE',  ( 24.96658222323440057, -10.83443034510523617, -3.855530974724861615 ) ) ;
#16458=CARTESIAN_POINT ( 'NONE',  ( 12.57461732485479899, 12.11259905827362182, -3.187575261700099638 ) ) ;
#16461=CARTESIAN_POINT ( 'NONE',  ( 17.60000000000000142, -10.78295181803999903, 4.410266442048000002 ) ) ;
#16463=CARTESIAN_POINT ( 'NONE',  ( 11.35393383743268103, 12.19578912482747590, 1.764073084349790266 ) ) ;
#16464=VERTEX_POINT ( 'NONE', #52177 ) ;
#16478=EDGE_CURVE ( 'NONE', #39483, #20439, #19683, .T. ) ;
#16480=DIRECTION ( 'NONE',  ( 0.000000000000000000, 1.000000000000000000, 0.000000000000000000 ) ) ;
#16483=CARTESIAN_POINT ( 'NONE',  ( 18.20279897579440131, -3.027817980922570484, 11.45825916412429812 ) ) ;
#16489=CARTESIAN_POINT ( 'NONE',  ( 15.79991751193278482, 9.060349897821472709, 8.357793075677504291 ) ) ;
#16492=B_SPLINE_SURFACE_WITH_KNOTS ( 'NONE', 3, 3, ( 
 ( #39769, #11455, #1667, #39074 ),
 ( #54803, #12502, #32795, #59701 ),
 ( #22635, #38376, #43979, #27547 ),
 ( #48875, #28238, #65286, #34181 ),
 ( #17400, #22294, #43634, #7599 ),
 ( #64928, #49554, #22984, #65630 ),
 ( #60397, #65971, #18099, #56527 ),
 ( #24025, #3377, #35215, #8971 ),
 ( #61431, #30647, #3038, #13548 ),
 ( #8632, #24714, #41141, #30310 ),
 ( #51957, #46730, #62451, #13207 ),
 ( #67345, #56873, #8293, #35556 ) ),
 .UNSPECIFIED., .F., .F., .F.,
 ( 4, 1, 1, 1, 1, 1, 1, 1, 1, 4 ),
 ( 4, 4 ),
 ( 0.01095835123444999920, 0.05000000000000000278, 0.1000000000000000056, 0.1499999999999999944, 0.2000000000000000111, 0.2500000000000000000, 0.2999999999999999889, 0.3499999999999999778, 0.4000000000000000222, 0.4461837860292000024 ),
 ( -0.2706701102521000268, 1.270791538669000076 ),
 .UNSPECIFIED. ) ;
#16493=CARTESIAN_POINT ( 'NONE',  ( 25.49995441705259935, 2.042062856630685097, 11.11383374566986326 ) ) ;
#16494=CARTESIAN_POINT ( 'NONE',  ( 24.11241132672047272, 9.193877876179779918, -9.158456253082972509 ) ) ;
#16495=CARTESIAN_POINT ( 'NONE',  ( 27.09999999999999787, 4.013733789776000248E-13, 10.75000000000000000 ) ) ;
#16506=CARTESIAN_POINT ( 'NONE',  ( 18.53960231418900051, -2.682082126742999950, 11.29772413421000188 ) ) ;
#16511=CARTESIAN_POINT ( 'NONE',  ( 13.55481756226799916, 11.54935041389000006, 2.400813070608000199 ) ) ;
#16523=CARTESIAN_POINT ( 'NONE',  ( 13.49980696793000057, 9.514462421839999351, 7.834836582454001608 ) ) ;
#16526=AXIS2_PLACEMENT_3D ( 'NONE', #6223, #38742, #27562 ) ;
#16530=CARTESIAN_POINT ( 'NONE',  ( 12.53679426224900162, 11.40784081139999984, -4.532785132108998916 ) ) ;
#16531=CARTESIAN_POINT ( 'NONE',  ( 18.39660364871399878, 11.70009917314000170, -4.315816162729000816 ) ) ;
#16535=CARTESIAN_POINT ( 'NONE',  ( 25.60000000000000142, 2.023980670379999847, 11.01542190082000161 ) ) ;
#16536=CARTESIAN_POINT ( 'NONE',  ( 17.98972740837745476, 12.09687365817480575, -3.246763311060390844 ) ) ;
#16540=CARTESIAN_POINT ( 'NONE',  ( 25.29995823066400362, -11.13046982544999963, 3.427501264366999756 ) ) ;
#16542=CARTESIAN_POINT ( 'NONE',  ( 18.30000000000000071, 14.70300865175000027, -5.744762642578000289 ) ) ;
#16555=CARTESIAN_POINT ( 'NONE',  ( 11.66883611674750654, -3.345348949920207815, 11.86065797283158929 ) ) ;
#16559=CARTESIAN_POINT ( 'NONE',  ( 16.07059379716000080, -3.381060347337999872, -11.29912544500000138 ) ) ;
#16561=EDGE_CURVE ( 'NONE', #48552, #6251, #1109, .T. ) ;
#16565=CONICAL_SURFACE ( 'NONE', #40050, 12.47499939740000130, 0.7853981102588313279 ) ;
#16567=VERTEX_POINT ( 'NONE', #17536 ) ;
#16575=CARTESIAN_POINT ( 'NONE',  ( 11.49999144015000319, 3.886253129992999877, -11.90689313971000018 ) ) ;
#16588=CARTESIAN_POINT ( 'NONE',  ( 24.97040879175293426, 8.550777727342323331, -8.358969513697752873 ) ) ;
#16589=CARTESIAN_POINT ( 'NONE',  ( 15.45728973496400194, 8.836548693809998412, 7.950469186927999310 ) ) ;
#16591=VERTEX_POINT ( 'NONE', #6334 ) ;
#16592=CARTESIAN_POINT ( 'NONE',  ( 23.58888338209971991, -2.922255725552524996, -13.61648187270552945 ) ) ;
#16596=EDGE_LOOP ( 'NONE', ( #18675, #38433, #40416, #47022 ) ) ;
#16598=CARTESIAN_POINT ( 'NONE',  ( 25.09299849713500308, 11.65481204179000052, -3.020019037700000020 ) ) ;
#16599=DIRECTION ( 'NONE',  ( 4.399946526753046019E-15, -1.000000000000000000, -1.785362917591035329E-14 ) ) ;
#16610=CARTESIAN_POINT ( 'NONE',  ( 24.05220180837281063, 12.62753229755031015, 3.430343039253267445 ) ) ;
#16611=EDGE_CURVE ( 'NONE', #5014, #60256, #5159, .T. ) ;
#16631=CARTESIAN_POINT ( 'NONE',  ( 18.01256889503158121, 11.20125638878172936, -3.203298770437340348 ) ) ;
#16642=ADVANCED_FACE ( 'NONE', ( #64365 ), #37903, .F. ) ;
#16645=CARTESIAN_POINT ( 'NONE',  ( 25.55274001713692655, -11.13099802292605389, -3.116587923746078292 ) ) ;
#16658=EDGE_CURVE ( 'NONE', #15819, #56117, #54451, .T. ) ;
#16662=CARTESIAN_POINT ( 'NONE',  ( 16.18326532032400067, -3.458591647041000083, -11.88419159288000060 ) ) ;
#16663=CARTESIAN_POINT ( 'NONE',  ( 11.44446504844000145, 11.61858443320999967, 1.410913393917999858 ) ) ;
#16666=CARTESIAN_POINT ( 'NONE',  ( 24.51106247826800910, 3.208407811236159812, -11.97394356203530030 ) ) ;
#16675=ORIENTED_EDGE ( 'NONE', *, *, #55741, .F. ) ;
#16679=CARTESIAN_POINT ( 'NONE',  ( 15.46531638133300035, -9.264179323101998875, -8.208366262023000459 ) ) ;
#16685=CARTESIAN_POINT ( 'NONE',  ( 24.19055685125828603, -3.314211647974591113, -12.40155450095146428 ) ) ;
#16692=EDGE_LOOP ( 'NONE', ( #1348, #16837, #42301, #4864, #7420 ) ) ;
#16693=FACE_OUTER_BOUND ( 'NONE', #39133, .T. ) ;
#16696=CARTESIAN_POINT ( 'NONE',  ( 23.59999467231800097, -10.30760443253999981, -9.317695455237998914 ) ) ;
#16699=CARTESIAN_POINT ( 'NONE',  ( 24.08696074224200245, -12.68545904450999906, 3.367396192228000018 ) ) ;
#16710=CARTESIAN_POINT ( 'NONE',  ( 23.66585382769999768, -10.00662356887000115, -9.518285594139999972 ) ) ;
#16711=CARTESIAN_POINT ( 'NONE',  ( 23.81895245337700118, -9.670840248742999634, 9.333086655847001367 ) ) ;
#16721=ORIENTED_EDGE ( 'NONE', *, *, #59302, .F. ) ;
#16723=CARTESIAN_POINT ( 'NONE',  ( 16.09992084546400193, -8.991497430826001391, -8.719551690569000257 ) ) ;
#16729=B_SPLINE_CURVE_WITH_KNOTS ( 'NONE', 3,
 ( #46760, #53033, #36261, #30678 ),
 .UNSPECIFIED., .F., .F.,
 ( 4, 4 ),
 ( 0.000000000000000000, 1.000000000000000000 ),
 .UNSPECIFIED. ) ;
#16735=VERTEX_POINT ( 'NONE', #27684 ) ;
#16737=CARTESIAN_POINT ( 'NONE',  ( 12.66849918197500102, -12.16651130357000099, 3.137066692814999946 ) ) ;
#16739=AXIS2_PLACEMENT_3D ( 'NONE', #66549, #29524, #19347 ) ;
#16757=CARTESIAN_POINT ( 'NONE',  ( 16.86666666233133327, 3.345268057356068692, 11.86064107292373571 ) ) ;
#16759=CARTESIAN_POINT ( 'NONE',  ( 11.30000000000000071, 11.28618258042000022, 10.08934826511999994 ) ) ;
#16761=DIRECTION ( 'NONE',  ( 1.000000000000000000, 0.000000000000000000, 0.000000000000000000 ) ) ;
#16770=ORIENTED_EDGE ( 'NONE', *, *, #48313, .T. ) ;
#16772=CARTESIAN_POINT ( 'NONE',  ( 24.35365242081700288, -11.54878985755999388, 2.979915831581000152 ) ) ;
#16781=PLANE ( 'NONE',  #42497 ) ;
#16783=CARTESIAN_POINT ( 'NONE',  ( 25.55266313104714726, -2.866471730758334058, 11.19811586864718933 ) ) ;
#16788=CIRCLE ( 'NONE', #27991, 1.000000000000000222 ) ;
#16789=B_SPLINE_CURVE_WITH_KNOTS ( 'NONE', 3,
 ( #67922, #10573, #63708, #20380 ),
 .UNSPECIFIED., .F., .F.,
 ( 4, 4 ),
 ( 0.000000000000000000, 1.000000000000000000 ),
 .UNSPECIFIED. ) ;
#16797=CARTESIAN_POINT ( 'NONE',  ( 18.01911383344807405, -3.562435417629448597, -12.00770609665208966 ) ) ;
#16806=EDGE_LOOP ( 'NONE', ( #5243, #20594, #61152, #57204 ) ) ;
#16807=EDGE_CURVE ( 'NONE', #26903, #62306, #22288, .T. ) ;
#16810=CARTESIAN_POINT ( 'NONE',  ( 23.89491306796949033, -9.543190063518746769, -9.361237058299565206 ) ) ;
#16811=CARTESIAN_POINT ( 'NONE',  ( 12.41307909110101804, -11.56466389787636473, 4.809819853924211408 ) ) ;
#16812=DIRECTION ( 'NONE',  ( -1.000000000000000000, 0.000000000000000000, 0.000000000000000000 ) ) ;
#16822=CARTESIAN_POINT ( 'NONE',  ( 18.36030550607078737, -3.088870463273618139, 11.23311224736321101 ) ) ;
#16833=FACE_OUTER_BOUND ( 'NONE', #67517, .T. ) ;
#16835=B_SPLINE_CURVE_WITH_KNOTS ( 'NONE', 3,
 ( #9767, #3493, #46502, #67122 ),
 .UNSPECIFIED., .F., .F.,
 ( 4, 4 ),
 ( 0.000000000000000000, 1.000000000000000000 ),
 .UNSPECIFIED. ) ;
#16837=ORIENTED_EDGE ( 'NONE', *, *, #41377, .F. ) ;
#16840=ORIENTED_EDGE ( 'NONE', *, *, #7932, .T. ) ;
#16846=CARTESIAN_POINT ( 'NONE',  ( 24.13790633822682352, 3.328477659013978407, -12.49555518615514949 ) ) ;
#16847=B_SPLINE_CURVE_WITH_KNOTS ( 'NONE', 3,
 ( #60452, #23731, #49958, #2072 ),
 .UNSPECIFIED., .F., .F.,
 ( 4, 4 ),
 ( 0.000000000000000000, 1.000000000000000000 ),
 .UNSPECIFIED. ) ;
#16848=DIRECTION ( 'NONE',  ( -1.000000000000000000, 0.000000000000000000, 0.000000000000000000 ) ) ;
#16856=EDGE_LOOP ( 'NONE', ( #12112, #50354, #24190 ) ) ;
#16861=CARTESIAN_POINT ( 'NONE',  ( 25.29995737991200144, -8.533537546129998930, 7.925519566782000425 ) ) ;
#16865=EDGE_CURVE ( 'NONE', #6782, #13349, #59393, .T. ) ;
#16877=CARTESIAN_POINT ( 'NONE',  ( 18.31684170297491576, 11.66237234948261836, -4.568609802378666984 ) ) ;
#16879=VERTEX_POINT ( 'NONE', #36277 ) ;
#16882=CARTESIAN_POINT ( 'NONE',  ( 13.69997185827400266, -11.40547114375999982, -2.374390024598000082 ) ) ;
#16903=CARTESIAN_POINT ( 'NONE',  ( 24.60170725920900026, -3.645111442846999950, 12.27956986324999988 ) ) ;
#16908=CARTESIAN_POINT ( 'NONE',  ( 24.69847988401100380, -8.734423968153000928, 9.243501732991999731 ) ) ;
#16910=ORIENTED_EDGE ( 'NONE', *, *, #62093, .T. ) ;
#16916=CARTESIAN_POINT ( 'NONE',  ( 13.64331666222400052, 12.23490852752999913, 2.418322770048999981 ) ) ;
#16921=CARTESIAN_POINT ( 'NONE',  ( 13.69586690835513210, 11.42311322218458969, 2.288407577489913525 ) ) ;
#16923=CARTESIAN_POINT ( 'NONE',  ( 15.65609597790000151, 8.788746246889001412, 7.589637905006999752 ) ) ;
#16925=CARTESIAN_POINT ( 'NONE',  ( 23.74397595434759722, -13.10155070693668122, 3.794838497900099750 ) ) ;
#16933=CARTESIAN_POINT ( 'NONE',  ( 25.36466183423599929, 11.12554151139999981, -3.380142950005000202 ) ) ;
#16935=ORIENTED_EDGE ( 'NONE', *, *, #48313, .F. ) ;
#16936=CARTESIAN_POINT ( 'NONE',  ( 11.66889198463462840, -3.216368914751022157, 11.40336763631111516 ) ) ;
#16938=VERTEX_POINT ( 'NONE', #13678 ) ;
#16944=CARTESIAN_POINT ( 'NONE',  ( 24.87149320935953156, 11.61826505781595742, -3.203182254666349316 ) ) ;
#16947=ADVANCED_FACE ( 'NONE', ( #45828 ), #63528, .F. ) ;
#16948=EDGE_CURVE ( 'NONE', #40442, #57158, #19278, .T. ) ;
#16950=ORIENTED_EDGE ( 'NONE', *, *, #63620, .T. ) ;
#16957=CARTESIAN_POINT ( 'NONE',  ( 25.48313530789599923, -2.676704236843000295, 11.27114544762000037 ) ) ;
#16959=VERTEX_POINT ( 'NONE', #37308 ) ;
#16970=CARTESIAN_POINT ( 'NONE',  ( 13.56663524094155626, 11.53596571847202767, 2.401556225329833705 ) ) ;
#16974=B_SPLINE_CURVE_WITH_KNOTS ( 'NONE', 3,
 ( #36293, #57613, #31063, #10407, #52371, #47137, #68438, #20558, #47481, #68787, #42242, #31749, #53067, #5166 ),
 .UNSPECIFIED., .F., .F.,
 ( 4, 2, 2, 2, 2, 2, 4 ),
 ( 0.000000000000000000, 0.1249999999999983624, 0.2499999999999967248, 0.4999999999999945599, 0.6249999999999958922, 0.7499999999999972244, 1.000000000000000000 ),
 .UNSPECIFIED. ) ;
#16978=CARTESIAN_POINT ( 'NONE',  ( 18.49995202021990082, -2.953582884391593222, 12.17185907300070902 ) ) ;
#16980=PLANE ( 'NONE',  #66497 ) ;
#16982=CARTESIAN_POINT ( 'NONE',  ( 24.96658174203486169, 8.756202942073826989, -7.455126426642118886 ) ) ;
#16995=EDGE_CURVE ( 'NONE', #41132, #35889, #15604, .T. ) ;
#16996=DIRECTION ( 'NONE',  ( 0.000000000000000000, -0.9617682489148012825, 0.2738646296610005582 ) ) ;
#17003=CARTESIAN_POINT ( 'NONE',  ( 11.72001955192552280, -12.39031618367880938, -1.831854259321207490 ) ) ;
#17005=CARTESIAN_POINT ( 'NONE',  ( 16.43986884071599874, -3.414349888938000177, -11.89720686373000191 ) ) ;
#17006=CARTESIAN_POINT ( 'NONE',  ( 11.44750515593000095, 11.62256912479000093, 1.379235499629000161 ) ) ;
#17009=CARTESIAN_POINT ( 'NONE',  ( 16.44004776902900034, 3.254301421112999915, 11.33671678219000079 ) ) ;
#17020=ORIENTED_EDGE ( 'NONE', *, *, #62182, .F. ) ;
#17023=CARTESIAN_POINT ( 'NONE',  ( 18.90826270587400160, 0.000000000000000000, 0.000000000000000000 ) ) ;
#17025=ORIENTED_EDGE ( 'NONE', *, *, #24455, .F. ) ;
#17035=EDGE_LOOP ( 'NONE', ( #6602, #2614, #55867, #14561, #16295, #58977 ) ) ;
#17037=ORIENTED_EDGE ( 'NONE', *, *, #46879, .F. ) ;
#17039=CARTESIAN_POINT ( 'NONE',  ( 25.39938977705818957, 2.782691790074335092, -11.32464129750441373 ) ) ;
#17043=CARTESIAN_POINT ( 'NONE',  ( 20.00000000000000000, 11.79499999999999993, 0.000000000000000000 ) ) ;
#17052=CARTESIAN_POINT ( 'NONE',  ( 18.05609597790000009, 3.343430715100999873, -11.12052764821000039 ) ) ;
#17054=CARTESIAN_POINT ( 'NONE',  ( 24.45625562770040773, -12.38367834655976907, -3.108174973275622310 ) ) ;
#17055=CARTESIAN_POINT ( 'NONE',  ( 24.32839125186500340, -9.022429054383998448, -9.339811860416999068 ) ) ;
#17057=B_SPLINE_CURVE_WITH_KNOTS ( 'NONE', 3,
 ( #49180, #27173, #1291, #17724, #22604, #12127, #48496, #11421, #43948, #26832, #253, #65252, #58634, #54771 ),
 .UNSPECIFIED., .F., .F.,
 ( 4, 2, 2, 2, 2, 2, 4 ),
 ( 0.000000000000000000, 0.1250000000000005274, 0.2500000000000010547, 0.5000000000000021094, 0.6250000000000014433, 0.7500000000000006661, 1.000000000000000000 ),
 .UNSPECIFIED. ) ;
#17060=VERTEX_POINT ( 'NONE', #4793 ) ;
#17064=CARTESIAN_POINT ( 'NONE',  ( 12.99999999998900080, -12.39025855408000076, -1.832244667012999928 ) ) ;
#17080=ORIENTED_EDGE ( 'NONE', *, *, #14019, .T. ) ;
#17082=CARTESIAN_POINT ( 'NONE',  ( 12.82792991967100171, -11.81434786598999942, 3.324782598720999793 ) ) ;
#17089=CARTESIAN_POINT ( 'NONE',  ( 24.14319173801533935, -9.149649622521751624, 9.124492735417254252 ) ) ;
#17096=CARTESIAN_POINT ( 'NONE',  ( 23.62003806996300170, 13.19646996404000028, -4.177448498581999736 ) ) ;
#17102=CARTESIAN_POINT ( 'NONE',  ( 24.30000000000000071, 0.000000000000000000, 0.000000000000000000 ) ) ;
#17105=CARTESIAN_POINT ( 'NONE',  ( 23.91429184840559685, 9.509214059390449947, 9.346071062481517089 ) ) ;
#17106=ORIENTED_EDGE ( 'NONE', *, *, #41377, .T. ) ;
#17111=CARTESIAN_POINT ( 'NONE',  ( 18.19494255922599990, -11.55196140944999961, 4.440362831676999633 ) ) ;
#17113=CARTESIAN_POINT ( 'NONE',  ( 13.67476513888300005, 9.526862765824999357, 8.046751417967000108 ) ) ;
#17117=EDGE_CURVE ( 'NONE', #13349, #25042, #78, .T. ) ;
#17119=EDGE_CURVE ( 'NONE', #43628, #27393, #18997, .T. ) ;
#17121=VECTOR ( 'NONE', #21495, 1000.000000000000114 ) ;
#17123=CARTESIAN_POINT ( 'NONE',  ( 23.89320776801300283, -12.21745654473000542, 3.256241354580001524 ) ) ;
#17125=CARTESIAN_POINT ( 'NONE',  ( 16.39999999270239428, 3.259293166955308685, 11.55581727975966544 ) ) ;
#17128=B_SPLINE_CURVE_WITH_KNOTS ( 'NONE', 3,
 ( #49722, #54622, #445, #10937 ),
 .UNSPECIFIED., .F., .F.,
 ( 4, 4 ),
 ( 0.000000000000000000, 1.000000000000000000 ),
 .UNSPECIFIED. ) ;
#17135=CARTESIAN_POINT ( 'NONE',  ( 24.62773497368900166, -3.462213745051000213, -12.08749688049000071 ) ) ;
#17138=EDGE_CURVE ( 'NONE', #35342, #54502, #62605, .T. ) ;
#17160=CARTESIAN_POINT ( 'NONE',  ( 20.00000000000000000, -11.79499999999999993, 0.000000000000000000 ) ) ;
#17161=CARTESIAN_POINT ( 'NONE',  ( 24.15344905084700144, 3.593700277778999919, -12.72454352958999912 ) ) ;
#17162=CARTESIAN_POINT ( 'NONE',  ( 13.43043922992600159, -12.41458792447999926, -1.928118222792999825 ) ) ;
#17165=CARTESIAN_POINT ( 'NONE',  ( 12.10941541367886209, 11.07487266647606816, -3.615341446703132622 ) ) ;
#17168=CARTESIAN_POINT ( 'NONE',  ( 17.80000000001300009, -3.351264566333000072, -11.15757590352999884 ) ) ;
#17171=CARTESIAN_POINT ( 'NONE',  ( 18.02490773331091134, -11.46571851143742826, 4.499230601365909799 ) ) ;
#17183=EDGE_LOOP ( 'NONE', ( #26998, #64931, #53816, #59598, #15812, #3875, #693, #15099, #54259, #58499, #26313, #22851, #49679, #36637, #20756, #63954, #29203, #12802, #13112, #24910 ) ) ;
#17184=B_SPLINE_CURVE_WITH_KNOTS ( 'NONE', 3,
 ( #47134, #57608, #56931, #67406 ),
 .UNSPECIFIED., .F., .F.,
 ( 4, 4 ),
 ( 0.000000000000000000, 1.000000000000000000 ),
 .UNSPECIFIED. ) ;
#17192=CIRCLE ( 'NONE', #56284, 5.000000000000000000 ) ;
#17205=EDGE_CURVE ( 'NONE', #15208, #38268, #12597, .T. ) ;
#17210=EDGE_CURVE ( 'NONE', #7298, #37494, #67678, .T. ) ;
#17211=ORIENTED_EDGE ( 'NONE', *, *, #8629, .T. ) ;
#17214=CARTESIAN_POINT ( 'NONE',  ( 25.21375942257175495, -8.515658397323806028, 8.063058284021709099 ) ) ;
#17219=FACE_OUTER_BOUND ( 'NONE', #11373, .T. ) ;
#17227=B_SPLINE_SURFACE_WITH_KNOTS ( 'NONE', 3, 3, ( 
 ( #63257, #36359, #53809, #21309 ),
 ( #4530, #63948, #58712, #10816 ),
 ( #47200, #57673, #32158, #31810 ),
 ( #48223, #10132, #330, #15384 ),
 ( #36712, #5909, #21644, #46856 ),
 ( #20279, #62913, #9781, #31132 ),
 ( #58032, #52783, #26219, #47548 ),
 ( #20971, #17797, #65327, #7296 ),
 ( #60439, #27249, #43675, #6948 ),
 ( #48917, #33877, #17446, #11845 ),
 ( #55194, #23028, #33530, #32840 ),
 ( #44377, #28637, #39461, #54849 ) ),
 .UNSPECIFIED., .F., .F., .F.,
 ( 4, 1, 1, 1, 1, 1, 1, 1, 1, 4 ),
 ( 4, 4 ),
 ( 0.01098173103564000115, 0.05000000000000000278, 0.1000000000000000056, 0.1499999999999999944, 0.2000000000000000111, 0.2500000000000000000, 0.2999999999999999889, 0.3499999999999999778, 0.4000000000000000222, 0.4470370502493000164 ),
 ( -0.2706693728835000146, 1.270788559091000192 ),
 .UNSPECIFIED. ) ;
#17228=ADVANCED_FACE ( 'NONE', ( #12820 ), #32434, .F. ) ;
#17238=CARTESIAN_POINT ( 'NONE',  ( 24.37808884332112314, 12.29705478244968830, -3.189923896649337731 ) ) ;
#17245=ORIENTED_EDGE ( 'NONE', *, *, #54400, .T. ) ;
#17260=EDGE_CURVE ( 'NONE', #22975, #7379, #37596, .T. ) ;
#17264=CARTESIAN_POINT ( 'NONE',  ( 24.67333001244800172, -8.700662965794998982, 9.017020110425999491 ) ) ;
#17270=CARTESIAN_POINT ( 'NONE',  ( 12.40000000000000213, -12.27510221496999954, -1.916289661941000144 ) ) ;
#17276=CARTESIAN_POINT ( 'NONE',  ( 25.59994555223700274, -10.55174472786000095, 3.754934689065000164 ) ) ;
#17280=CARTESIAN_POINT ( 'NONE',  ( 25.05006280129954277, 8.531455033317872250, -8.270352402647430878 ) ) ;
#17285=DIRECTION ( 'NONE',  ( 0.000000000000000000, 0.9624505444715651947, -0.2714570858282905341 ) ) ;
#17309=CARTESIAN_POINT ( 'NONE',  ( 17.96054543402357595, -12.10037373249118886, 3.233681995861158676 ) ) ;
#17313=EDGE_CURVE ( 'NONE', #68412, #31887, #7638, .T. ) ;
#17315=CARTESIAN_POINT ( 'NONE',  ( 25.57799932127799991, -2.767938380759999983, 11.23359650972000168 ) ) ;
#17316=ORIENTED_EDGE ( 'NONE', *, *, #28012, .T. ) ;
#17330=CARTESIAN_POINT ( 'NONE',  ( 23.61660710412960995, 10.09774633507085539, -9.649252052224994713 ) ) ;
#17338=DIRECTION ( 'NONE',  ( 1.000000000000000000, 0.000000000000000000, 0.000000000000000000 ) ) ;
#17339=CARTESIAN_POINT ( 'NONE',  ( 23.56666365135700403, 8.673757318211000822, -7.881093921744994901 ) ) ;
#17350=CARTESIAN_POINT ( 'NONE',  ( 24.19015434441247692, -12.39791403410435322, -3.330852224754460078 ) ) ;
#17355=ADVANCED_FACE ( 'NONE', ( #35438 ), #56764, .F. ) ;
#17357=CARTESIAN_POINT ( 'NONE',  ( 25.60000000000000142, 0.000000000000000000, 0.000000000000000000 ) ) ;
#17361=PLANE ( 'NONE',  #45607 ) ;
#17363=VERTEX_POINT ( 'NONE', #60969 ) ;
#17364=CARTESIAN_POINT ( 'NONE',  ( 24.68356055557331885, 3.139996735530106609, -11.82109522866602447 ) ) ;
#17365=CARTESIAN_POINT ( 'NONE',  ( 16.00249209530700156, 3.346223412964000055, 11.40475585647000045 ) ) ;
#17367=ORIENTED_EDGE ( 'NONE', *, *, #18227, .T. ) ;
#17368=CARTESIAN_POINT ( 'NONE',  ( 13.49980696793000057, 9.514462421839999351, 7.834836582454001608 ) ) ;
#17372=CARTESIAN_POINT ( 'NONE',  ( 18.29998515896361866, -2.924733550950529448, 11.97422828356911317 ) ) ;
#17375=CARTESIAN_POINT ( 'NONE',  ( 23.61708161427199926, -13.18086190930000079, -4.239849120749999756 ) ) ;
#17378=CARTESIAN_POINT ( 'NONE',  ( 15.61722669115800066, -9.375864875015000877, -8.222239459497000524 ) ) ;
#17389=ORIENTED_EDGE ( 'NONE', *, *, #15011, .F. ) ;
#17391=ORIENTED_EDGE ( 'NONE', *, *, #21955, .F. ) ;
#17392=CARTESIAN_POINT ( 'NONE',  ( 11.74257329013500240, -12.32813410531000109, -1.877195977750000022 ) ) ;
#17397=CIRCLE ( 'NONE', #59812, 1.000000000000000888 ) ;
#17400=CARTESIAN_POINT ( 'NONE',  ( 23.91167052346600386, 12.75422773238000040, 3.593058583353999857 ) ) ;
#17406=B_SPLINE_CURVE_WITH_KNOTS ( 'NONE', 3,
 ( #56673, #24160, #8430, #25188 ),
 .UNSPECIFIED., .F., .F.,
 ( 4, 4 ),
 ( 0.000000000000000000, 1.000000000000000000 ),
 .UNSPECIFIED. ) ;
#17410=CARTESIAN_POINT ( 'NONE',  ( 18.12922381500399993, 3.157787539580000136, -11.36563583066999961 ) ) ;
#17414=CARTESIAN_POINT ( 'NONE',  ( 23.82000366591099905, -9.668684621276998570, -9.332229521209001177 ) ) ;
#17415=CARTESIAN_POINT ( 'NONE',  ( 24.56892343362300224, -8.855981324802000287, 9.405092422590000112 ) ) ;
#17416=CARTESIAN_POINT ( 'NONE',  ( 11.80912799980900019, -3.189026639965999443, 11.45098040807999951 ) ) ;
#17424=CARTESIAN_POINT ( 'NONE',  ( 25.26979871721500359, 2.550136720506999577, -11.36439046742999892 ) ) ;
#17430=ORIENTED_EDGE ( 'NONE', *, *, #48297, .F. ) ;
#17437=DIRECTION ( 'NONE',  ( -1.000000000000000000, 0.000000000000000000, 0.000000000000000000 ) ) ;
#17439=EDGE_CURVE ( 'NONE', #4322, #31587, #29323, .T. ) ;
#17446=CARTESIAN_POINT ( 'NONE',  ( 23.55381184191400123, 3.060945918118999742, 13.69458336343999960 ) ) ;
#17449=CARTESIAN_POINT ( 'NONE',  ( 24.14104147839731240, -9.152730137167427671, 9.126869235150973481 ) ) ;
#17456=CARTESIAN_POINT ( 'NONE',  ( 23.55075825960500069, 13.34757147688000067, -4.341189614811999498 ) ) ;
#17459=B_SPLINE_CURVE_WITH_KNOTS ( 'NONE', 3,
 ( #7090, #45878, #54991, #61609 ),
 .UNSPECIFIED., .F., .F.,
 ( 4, 4 ),
 ( 0.000000000000000000, 1.000000000000000000 ),
 .UNSPECIFIED. ) ;
#17461=ORIENTED_EDGE ( 'NONE', *, *, #63680, .T. ) ;
#17466=CARTESIAN_POINT ( 'NONE',  ( 23.57773536430026695, 10.35457686501782604, 9.360237667582394394 ) ) ;
#17470=CARTESIAN_POINT ( 'NONE',  ( 24.35365242081699932, 1.906711579001001189, -11.36048031431998595 ) ) ;
#17472=CARTESIAN_POINT ( 'NONE',  ( 17.73384588713700083, -11.55359908321999995, 4.937673966378999246 ) ) ;
#17484=CARTESIAN_POINT ( 'NONE',  ( 11.71271957899600125, 12.11624328427999941, 2.031646723569000113 ) ) ;
#17490=CARTESIAN_POINT ( 'NONE',  ( 25.60000000000000142, 9.899494936611999307, 9.899494936611999307 ) ) ;
#17507=DIRECTION ( 'NONE',  ( -1.000000000000000000, 0.000000000000000000, 0.000000000000000000 ) ) ;
#17515=CARTESIAN_POINT ( 'NONE',  ( 23.71152083938696009, -9.910026289319734616, -9.457066222056473848 ) ) ;
#17516=CARTESIAN_POINT ( 'NONE',  ( 12.49459120400055667, -12.10614746208238302, 3.212001293532054103 ) ) ;
#17522=CARTESIAN_POINT ( 'NONE',  ( 13.60156003475500164, -12.26415473033000048, -2.266572665737999870 ) ) ;
#17525=EDGE_CURVE ( 'NONE', #19259, #48851, #16789, .T. ) ;
#17526=EDGE_CURVE ( 'NONE', #21757, #42930, #34639, .T. ) ;
#17529=CARTESIAN_POINT ( 'NONE',  ( 18.26547113879619033, -3.186161613544661098, -11.20588962290425528 ) ) ;
#17532=CARTESIAN_POINT ( 'NONE',  ( 24.30001697352500045, -3.271769158411000245, -12.21048181092999840 ) ) ;
#17533=FACE_OUTER_BOUND ( 'NONE', #26483, .T. ) ;
#17536=CARTESIAN_POINT ( 'NONE',  ( 11.79999999471800010, -3.216299622513999701, 11.40340969442000052 ) ) ;
#17541=CARTESIAN_POINT ( 'NONE',  ( 24.67921570607400383, -3.567514742249000115, 12.13750887372000165 ) ) ;
#17553=CARTESIAN_POINT ( 'NONE',  ( 24.04054642575986378, 3.344385333844766883, -12.67224307145318818 ) ) ;
#17557=CARTESIAN_POINT ( 'NONE',  ( 11.83178351958400043, 3.316209711830000018, -11.22342786695999983 ) ) ;
#17558=AXIS2_PLACEMENT_3D ( 'NONE', #54763, #54069, #40323 ) ;
#17561=ORIENTED_EDGE ( 'NONE', *, *, #68895, .F. ) ;
#17573=CARTESIAN_POINT ( 'NONE',  ( 12.10000669845703847, -11.02846243759423039, 3.754394857303111621 ) ) ;
#17575=ORIENTED_EDGE ( 'NONE', *, *, #44232, .T. ) ;
#17578=CARTESIAN_POINT ( 'NONE',  ( 23.62920471791399990, -3.420566888407999606, -13.57806623620999886 ) ) ;
#17608=CARTESIAN_POINT ( 'NONE',  ( 11.71260115691700143, 3.298410940261000235, -11.83433202606999934 ) ) ;
#17610=EDGE_CURVE ( 'NONE', #42540, #10227, #53451, .T. ) ;
#17611=EDGE_CURVE ( 'NONE', #7298, #15615, #25963, .T. ) ;
#17628=CARTESIAN_POINT ( 'NONE',  ( 24.56885749267500074, -8.742331804604999590, -8.862243903196000971 ) ) ;
#17629=CARTESIAN_POINT ( 'NONE',  ( 13.35262485425710999, -11.51206127779176036, -1.787622147836161579 ) ) ;
#17630=CARTESIAN_POINT ( 'NONE',  ( 18.29999330150736014, -11.02846243710336616, 3.754394858745019103 ) ) ;
#17632=VERTEX_POINT ( 'NONE', #18929 ) ;
#17633=AXIS2_PLACEMENT_3D ( 'NONE', #65061, #49695, #23815 ) ;
#17657=CARTESIAN_POINT ( 'NONE',  ( 16.34794651623100137, 3.644047358192000097, 12.02362153922000054 ) ) ;
#17662=FACE_OUTER_BOUND ( 'NONE', #22210, .T. ) ;
#17664=CARTESIAN_POINT ( 'NONE',  ( 17.87831314280386152, -11.54767577568710557, 4.850450964119741748 ) ) ;
#17672=EDGE_LOOP ( 'NONE', ( #22115, #7847, #40691, #1669 ) ) ;
#17680=CARTESIAN_POINT ( 'NONE',  ( 24.67921139482200132, 8.727627377900999406, -9.158314240160001063 ) ) ;
#17689=CIRCLE ( 'NONE', #35558, 8.250000000000000000 ) ;
#17702=CARTESIAN_POINT ( 'NONE',  ( 25.30000327618300204, -8.756202924575998026, -7.455126447192999883 ) ) ;
#17713=DIRECTION ( 'NONE',  ( 1.000000000000000000, 0.000000000000000000, 0.000000000000000000 ) ) ;
#17719=EDGE_CURVE ( 'NONE', #63101, #60029, #14728, .T. ) ;
#17720=CARTESIAN_POINT ( 'NONE',  ( 16.39999999439439549, -3.511866690759578802, -11.95216930658972032 ) ) ;
#17723=ORIENTED_EDGE ( 'NONE', *, *, #46796, .F. ) ;
#17724=CARTESIAN_POINT ( 'NONE',  ( 16.07905395910119850, -8.470000438687037558, -7.998963526368340737 ) ) ;
#17732=CARTESIAN_POINT ( 'NONE',  ( 24.32784151249200377, -12.60041493477000074, -3.144063045006000312 ) ) ;
#17733=CARTESIAN_POINT ( 'NONE',  ( 16.10004050617000360, 8.286228349446574271, 9.446703038322560531 ) ) ;
#17735=B_SPLINE_CURVE_WITH_KNOTS ( 'NONE', 3,
 ( #46570, #9491, #19302, #56374, #14072, #61611, #50787, #13727 ),
 .UNSPECIFIED., .F., .F.,
 ( 4, 2, 2, 4 ),
 ( 0.000000000000000000, 0.4999999999999993339, 0.7499999999999996669, 1.000000000000000000 ),
 .UNSPECIFIED. ) ;
#17737=CARTESIAN_POINT ( 'NONE',  ( 25.34047077108162327, 2.680020306167191446, 11.33984167324305581 ) ) ;
#17738=CIRCLE ( 'NONE', #36692, 0.6999999999999992895 ) ;
#17749=CARTESIAN_POINT ( 'NONE',  ( 25.46375345652300126, 2.879422156700999658, -11.30951020355999859 ) ) ;
#17755=EDGE_CURVE ( 'NONE', #46470, #1871, #4458, .T. ) ;
#17757=EDGE_CURVE ( 'NONE', #66745, #54548, #12997, .T. ) ;
#17760=ADVANCED_FACE ( 'NONE', ( #68869 ), #12316, .F. ) ;
#17770=CARTESIAN_POINT ( 'NONE',  ( 23.99050544320700240, -9.436313469635999596, 9.573822194107998840 ) ) ;
#17771=DIRECTION ( 'NONE',  ( 0.000000000000000000, 0.9999992323442526976, 0.001239076634196941903 ) ) ;
#17776=CARTESIAN_POINT ( 'NONE',  ( 23.89320776801300283, -3.288740538444000716, 12.20874841465999516 ) ) ;
#17779=CARTESIAN_POINT ( 'NONE',  ( 24.37899125153199975, 3.167412086455000164, -12.03697597459000157 ) ) ;
#17784=ORIENTED_EDGE ( 'NONE', *, *, #56320, .F. ) ;
#17786=VECTOR ( 'NONE', #66689, 1000.000000000000000 ) ;
#17793=CARTESIAN_POINT ( 'NONE',  ( 12.25978835901500119, -11.49417283396999956, 4.331891014347999835 ) ) ;
#17797=CARTESIAN_POINT ( 'NONE',  ( 23.66565973993500194, 3.239486956716000066, 13.42552446105999842 ) ) ;
#17800=CARTESIAN_POINT ( 'NONE',  ( 23.85847181463605438, -9.608971930760668911, 9.387888383478362186 ) ) ;
#17806=B_SPLINE_SURFACE_WITH_KNOTS ( 'NONE', 3, 3, ( 
 ( #67381, #45050, #46075, #8671 ),
 ( #18826, #18134, #40152, #61466 ),
 ( #39456, #14266, #3073, #45736 ),
 ( #56906, #34905, #3751, #50977 ),
 ( #60775, #8331, #29674, #67045 ),
 ( #9005, #13923, #30348, #56564 ),
 ( #55539, #2391, #3414, #24750 ),
 ( #4783, #30683, #52687, #67722 ),
 ( #14605, #4096, #31375, #47805 ) ),
 .UNSPECIFIED., .F., .F., .F.,
 ( 4, 1, 1, 1, 1, 1, 4 ),
 ( 4, 4 ),
 ( 0.05182816266979999725, 0.1666666666667000196, 0.3333333333333000081, 0.5000000000000000000, 0.6666666666667000474, 0.8333333333333000637, 0.9772240888782000034 ),
 ( -0.1900389547208000129, 1.190219847277000031 ),
 .UNSPECIFIED. ) ;
#17809=CARTESIAN_POINT ( 'NONE',  ( 24.32840188601700149, 12.59971520604000084, -3.143741918347000119 ) ) ;
#17813=ORIENTED_EDGE ( 'NONE', *, *, #6609, .T. ) ;
#17817=DIRECTION ( 'NONE',  ( 0.000000000000000000, -1.099932466989999959E-09, 1.000000000000000000 ) ) ;
#17824=CARTESIAN_POINT ( 'NONE',  ( 18.45060561202799931, -11.83531674184000160, 3.931800577755000248 ) ) ;
#17832=CARTESIAN_POINT ( 'NONE',  ( 23.56666365135700403, -11.61524011578000604, 3.333188920255001353 ) ) ;
#17833=CARTESIAN_POINT ( 'NONE',  ( 16.09992084546400193, -8.991497430826001391, -8.719551690569000257 ) ) ;
#17837=CARTESIAN_POINT ( 'NONE',  ( 13.50000000000303224, -9.278109357271722146, -7.623553959385361622 ) ) ;
#17841=EDGE_CURVE ( 'NONE', #36843, #56572, #23881, .T. ) ;
#17847=CARTESIAN_POINT ( 'NONE',  ( 24.46729256464000457, -3.339593025236999857, -12.12065414616999881 ) ) ;
#17854=ORIENTED_EDGE ( 'NONE', *, *, #49130, .T. ) ;
#17859=FACE_OUTER_BOUND ( 'NONE', #33088, .T. ) ;
#17860=CARTESIAN_POINT ( 'NONE',  ( 11.53159663549335967, -3.486713160360387143, 11.11613240505404754 ) ) ;
#17861=CARTESIAN_POINT ( 'NONE',  ( 24.99828551773858010, 11.48454095403716124, 3.234327495894459670 ) ) ;
#17867=CARTESIAN_POINT ( 'NONE',  ( 23.74396121059458409, -9.837233145174325344, -9.448860444549127990 ) ) ;
#17874=CARTESIAN_POINT ( 'NONE',  ( 13.55309301929700005, -12.11670754034000019, -2.533073449765999907 ) ) ;
#17882=CARTESIAN_POINT ( 'NONE',  ( 23.58333423472800305, -7.629452625224000015E-13, 2.908784324518000003E-13 ) ) ;
#17888=DIRECTION ( 'NONE',  ( -1.000000000000000000, 0.000000000000000000, 0.000000000000000000 ) ) ;
#17890=EDGE_CURVE ( 'NONE', #33549, #26364, #22138, .T. ) ;
#17892=CARTESIAN_POINT ( 'NONE',  ( 24.26733149983100191, 12.18172987844000055, 3.303689625207000269 ) ) ;
#17906=CARTESIAN_POINT ( 'NONE',  ( 11.72781722417300188, 3.253150999210000283, -11.33706231867000014 ) ) ;
#17909=CARTESIAN_POINT ( 'NONE',  ( 25.30000327618300204, 8.756202924575998026, 7.455126447192999883 ) ) ;
#17911=AXIS2_PLACEMENT_3D ( 'NONE', #58382, #51765, #47566 ) ;
#17918=CARTESIAN_POINT ( 'NONE',  ( 17.60000000024299993, 11.86189249994999884, -3.298671769835999967 ) ) ;
#17926=ORIENTED_EDGE ( 'NONE', *, *, #60057, .T. ) ;
#17928=CARTESIAN_POINT ( 'NONE',  ( 17.56468935039100288, 12.04942594313000015, -3.198374858544000165 ) ) ;
#17936=DIRECTION ( 'NONE',  ( 0.000000000000000000, 1.000000000000000000, 0.000000000000000000 ) ) ;
#17947=EDGE_CURVE ( 'NONE', #34052, #65107, #61411, .T. ) ;
#17953=B_SPLINE_CURVE_WITH_KNOTS ( 'NONE', 3,
 ( #11557, #6313, #47142, #15324, #36650, #47835, #274, #63889, #26856, #20563, #32441, #10412, #31070, #31754 ),
 .UNSPECIFIED., .F., .F.,
 ( 4, 2, 2, 2, 2, 2, 4 ),
 ( 0.000000000000000000, 0.1250000000000049682, 0.2500000000000099365, 0.5000000000000114353, 0.6250000000000086597, 0.7500000000000056621, 1.000000000000000000 ),
 .UNSPECIFIED. ) ;
#17956=FACE_OUTER_BOUND ( 'NONE', #5881, .T. ) ;
#17969=ORIENTED_EDGE ( 'NONE', *, *, #15530, .T. ) ;
#17972=CARTESIAN_POINT ( 'NONE',  ( 13.80679720086500062, -8.861764092194999165, -7.504495031742999700 ) ) ;
#17976=CARTESIAN_POINT ( 'NONE',  ( 13.73494720760600174, 12.32760134815999997, 2.421442066891999811 ) ) ;
#17982=CARTESIAN_POINT ( 'NONE',  ( 18.06247470437139313, 3.164801830692924867, 11.41978211458705950 ) ) ;
#17984=CARTESIAN_POINT ( 'NONE',  ( 24.67921139482200132, 8.727627377900999406, -9.158314240160001063 ) ) ;
#18002=CARTESIAN_POINT ( 'NONE',  ( 24.62769666374738620, -3.584151135392908305, -12.19978398752706106 ) ) ;
#18006=EDGE_CURVE ( 'NONE', #33549, #9331, #5548, .T. ) ;
#18008=EDGE_CURVE ( 'NONE', #63300, #5868, #58064, .T. ) ;
#18015=CARTESIAN_POINT ( 'NONE',  ( 25.29576976926500009, 2.995598598314000327, 11.41691922160000061 ) ) ;
#18017=CIRCLE ( 'NONE', #13575, 1.000000000000000888 ) ;
#18018=CARTESIAN_POINT ( 'NONE',  ( 25.19216327953800061, -2.891353817808000048, 11.44527084745000067 ) ) ;
#18019=B_SPLINE_CURVE_WITH_KNOTS ( 'NONE', 3,
 ( #60545, #12651, #55651, #23483, #51090, #18245 ),
 .UNSPECIFIED., .F., .F.,
 ( 4, 2, 4 ),
 ( 0.000000000000000000, 0.5000000000000000000, 1.000000000000000000 ),
 .UNSPECIFIED. ) ;
#18028=EDGE_CURVE ( 'NONE', #52150, #41893, #53583, .T. ) ;
#18031=CARTESIAN_POINT ( 'NONE',  ( 16.39999999379500295, 3.351248059343999941, 11.15756683833000018 ) ) ;
#18033=ADVANCED_FACE ( 'NONE', ( #44738 ), #45420, .T. ) ;
#18043=CARTESIAN_POINT ( 'NONE',  ( 24.30000000000000071, 10.83443035398000021, 3.855530949778000149 ) ) ;
#18044=CARTESIAN_POINT ( 'NONE',  ( 24.30000000000000071, -8.810505093353000916, 8.810505093353000916 ) ) ;
#18052=CARTESIAN_POINT ( 'NONE',  ( 24.08742106046339160, -12.56972931058949072, -3.401799986514439045 ) ) ;
#18057=CYLINDRICAL_SURFACE ( 'NONE', #9554, 11.50000000000000178 ) ;
#18063=CIRCLE ( 'NONE', #64941, 12.20000000000000107 ) ;
#18066=EDGE_CURVE ( 'NONE', #41893, #54978, #60459, .T. ) ;
#18075=CARTESIAN_POINT ( 'NONE',  ( 23.99166156695100227, -13.00799102709000010, -3.384109424371999797 ) ) ;
#18079=CARTESIAN_POINT ( 'NONE',  ( 25.46373185538400463, 11.23406899464000119, 3.161078463958999496 ) ) ;
#18086=ORIENTED_EDGE ( 'NONE', *, *, #37253, .F. ) ;
#18090=ORIENTED_EDGE ( 'NONE', *, *, #45479, .T. ) ;
#18094=CIRCLE ( 'NONE', #57148, 1.300160515709999354 ) ;
#18095=EDGE_CURVE ( 'NONE', #55008, #38535, #36391, .T. ) ;
#18099=CARTESIAN_POINT ( 'NONE',  ( 23.73670661716200314, 13.28054472774000061, 3.698137085571999716 ) ) ;
#18106=CARTESIAN_POINT ( 'NONE',  ( 24.30000000000000071, -2.204728229456999866, -11.99913219504999873 ) ) ;
#18119=CARTESIAN_POINT ( 'NONE',  ( 27.09999999999999787, 1.806713620938000108E-12, -9.250000000000000000 ) ) ;
#18121=ORIENTED_EDGE ( 'NONE', *, *, #41537, .T. ) ;
#18122=CARTESIAN_POINT ( 'NONE',  ( 25.37646785958400031, 2.613418185928999993, -11.31776759263999921 ) ) ;
#18129=CARTESIAN_POINT ( 'NONE',  ( 25.37959880612143948, 3.026669825678802273, -11.38055956022503246 ) ) ;
#18134=CARTESIAN_POINT ( 'NONE',  ( 11.80561165699200110, -3.526771526455999783, 11.96112153682000034 ) ) ;
#18142=CARTESIAN_POINT ( 'NONE',  ( 24.14647631174685216, -9.144949018368393467, 9.120856162720306415 ) ) ;
#18156=DIRECTION ( 'NONE',  ( 0.000000000000000000, 0.000000000000000000, -1.000000000000000000 ) ) ;
#18158=VERTEX_POINT ( 'NONE', #25801 ) ;
#18160=DIRECTION ( 'NONE',  ( 1.000000000000000000, 0.000000000000000000, 0.000000000000000000 ) ) ;
#18166=CARTESIAN_POINT ( 'NONE',  ( 18.31117841518900136, -11.80507181181000043, 3.724836393661000056 ) ) ;
#18173=ORIENTED_EDGE ( 'NONE', *, *, #19342, .T. ) ;
#18174=CARTESIAN_POINT ( 'NONE',  ( 23.60000000000000142, 9.289189189551001036, -7.908916752675001050 ) ) ;
#18187=FACE_OUTER_BOUND ( 'NONE', #56680, .T. ) ;
#18191=EDGE_CURVE ( 'NONE', #31999, #13082, #46422, .T. ) ;
#18207=CARTESIAN_POINT ( 'NONE',  ( 12.24143698068993835, 11.79508855326024275, -3.559061050734573683 ) ) ;
#18210=CARTESIAN_POINT ( 'NONE',  ( 17.33333333127366771, 3.351260669886487964, 11.15757822838322433 ) ) ;
#18212=DIRECTION ( 'NONE',  ( 0.9999999999995219380, -9.778750326963210600E-07, 5.518476893961119184E-11 ) ) ;
#18214=CARTESIAN_POINT ( 'NONE',  ( 23.67317737304023595, 13.19576797240445565, 3.926420038237877996 ) ) ;
#18217=CARTESIAN_POINT ( 'NONE',  ( 24.66908015013045130, -8.674046118889807033, 8.642878031199991540 ) ) ;
#18218=CARTESIAN_POINT ( 'NONE',  ( 17.80000000001300009, -3.351264566333000072, -11.15757590352999884 ) ) ;
#18227=EDGE_CURVE ( 'NONE', #56220, #36266, #11365, .T. ) ;
#18231=CARTESIAN_POINT ( 'NONE',  ( 15.89979320884932967, -7.372865056442189591, -9.926947018133246203 ) ) ;
#18233=EDGE_CURVE ( 'NONE', #7194, #28894, #17184, .T. ) ;
#18236=VERTEX_POINT ( 'NONE', #47476 ) ;
#18241=ORIENTED_EDGE ( 'NONE', *, *, #63566, .T. ) ;
#18245=CARTESIAN_POINT ( 'NONE',  ( 23.56665676678199972, 13.31363904818000066, -4.296982115204999175 ) ) ;
#18249=CARTESIAN_POINT ( 'NONE',  ( 11.80443633831200145, 3.376482451534999818, -11.11063790749999924 ) ) ;
#18251=CARTESIAN_POINT ( 'NONE',  ( 25.39994675527849921, -8.680020655622012526, -7.390263983914230117 ) ) ;
#18252=CARTESIAN_POINT ( 'NONE',  ( 23.59999172348799945, -10.30759808834999980, 9.317726582648999667 ) ) ;
#18253=ORIENTED_EDGE ( 'NONE', *, *, #24889, .F. ) ;
#18271=CARTESIAN_POINT ( 'NONE',  ( 23.51695530179700100, -2.932378615205000205, -13.82491157443000063 ) ) ;
#18276=CARTESIAN_POINT ( 'NONE',  ( 24.60109542855846243, 8.755194900634329258, 9.042388595921103445 ) ) ;
#18289=DIRECTION ( 'NONE',  ( 0.000000000000000000, -0.9659258262890757507, 0.2588190451024934835 ) ) ;
#18291=AXIS2_PLACEMENT_3D ( 'NONE', #15070, #46553, #52471 ) ;
#18304=CIRCLE ( 'NONE', #1526, 12.42499880353999941 ) ;
#18305=CARTESIAN_POINT ( 'NONE',  ( 24.72545694048200104, -3.605123969772000336, 12.13009300416999992 ) ) ;
#18309=CARTESIAN_POINT ( 'NONE',  ( 25.25777602213000250, 11.13232791465999938, 3.460084468564999849 ) ) ;
#18311=CARTESIAN_POINT ( 'NONE',  ( 24.45998291059600049, -11.93731034918999967, -3.254645430195999722 ) ) ;
#18315=CARTESIAN_POINT ( 'NONE',  ( 20.00000000000000000, -11.79499999999999993, 0.000000000000000000 ) ) ;
#18316=CARTESIAN_POINT ( 'NONE',  ( 25.52465649271900006, -8.322333800095998768, -8.137666643170000214 ) ) ;
#18319=CARTESIAN_POINT ( 'NONE',  ( 13.37677363193000168, 12.31133347089000019, 1.988942882797000156 ) ) ;
#18321=CARTESIAN_POINT ( 'NONE',  ( 23.89320776801300283, 8.928716006283003992, 8.952507060077003587 ) ) ;
#18323=ORIENTED_EDGE ( 'NONE', *, *, #18399, .F. ) ;
#18337=ORIENTED_EDGE ( 'NONE', *, *, #18573, .T. ) ;
#18339=AXIS2_PLACEMENT_3D ( 'NONE', #54383, #65209, #27134 ) ;
#18341=DIRECTION ( 'NONE',  ( 1.000000000000000000, 0.000000000000000000, 0.000000000000000000 ) ) ;
#18347=CARTESIAN_POINT ( 'NONE',  ( 11.75761329816000078, -11.49411629629000053, -1.653020190619000074 ) ) ;
#18361=B_SPLINE_CURVE_WITH_KNOTS ( 'NONE', 3,
 ( #20524, #35920, #5129, #26466, #62818, #14937 ),
 .UNSPECIFIED., .F., .F.,
 ( 4, 2, 4 ),
 ( 0.000000000000000000, 0.5000000000000000000, 1.000000000000000000 ),
 .UNSPECIFIED. ) ;
#18363=ORIENTED_EDGE ( 'NONE', *, *, #25219, .T. ) ;
#18387=DIRECTION ( 'NONE',  ( -1.000000000000000000, 0.000000000000000000, 0.000000000000000000 ) ) ;
#18394=CARTESIAN_POINT ( 'NONE',  ( 24.14324442345568400, -12.47686306304178139, -3.361569000410982611 ) ) ;
#18399=EDGE_CURVE ( 'NONE', #32077, #43802, #65850, .T. ) ;
#18402=CARTESIAN_POINT ( 'NONE',  ( 24.53429014662800256, -8.855930250654999725, 9.286429702500999639 ) ) ;
#18406=PLANE ( 'NONE',  #21625 ) ;
#18409=CARTESIAN_POINT ( 'NONE',  ( 24.95275982371617118, -8.555910667412625514, -8.377686648711669903 ) ) ;
#18410=AXIS2_PLACEMENT_3D ( 'NONE', #4299, #41372, #63013 ) ;
#18418=ORIENTED_EDGE ( 'NONE', *, *, #19487, .F. ) ;
#18420=CARTESIAN_POINT ( 'NONE',  ( 23.73802563651300090, -13.27927394169999786, -3.696043905241999994 ) ) ;
#18422=CIRCLE ( 'NONE', #45218, 0.6999999999999992895 ) ;
#18431=DIRECTION ( 'NONE',  ( -1.000000000000000000, -9.409886301854999796E-10, -4.862374338246000196E-11 ) ) ;
#18434=ORIENTED_EDGE ( 'NONE', *, *, #2220, .T. ) ;
#18444=ORIENTED_EDGE ( 'NONE', *, *, #20398, .F. ) ;
#18447=CARTESIAN_POINT ( 'NONE',  ( 24.34833259009266726, -8.895958638017500419, -8.895958638017500419 ) ) ;
#18448=LINE ( 'NONE', #55157, #25364 ) ;
#18452=CARTESIAN_POINT ( 'NONE',  ( 24.95781814977000224, -12.04098704729999803, 2.875621858674000109 ) ) ;
#18460=ORIENTED_EDGE ( 'NONE', *, *, #65734, .T. ) ;
#18463=CARTESIAN_POINT ( 'NONE',  ( 23.56666365135700403, -2.963314674619003330, 12.23574966049000423 ) ) ;
#18466=CARTESIAN_POINT ( 'NONE',  ( 17.87616489729400371, 3.527537751923000009, 11.96092219328000006 ) ) ;
#18475=CARTESIAN_POINT ( 'NONE',  ( 30.60000000000000142, 0.000000000000000000, 0.000000000000000000 ) ) ;
#18480=CARTESIAN_POINT ( 'NONE',  ( 13.99999997324030865, 8.827177816329516702, 7.803278505680539823 ) ) ;
#18485=ORIENTED_EDGE ( 'NONE', *, *, #34023, .T. ) ;
#18486=DIRECTION ( 'NONE',  ( -1.000000000000000000, 0.000000000000000000, 0.000000000000000000 ) ) ;
#18487=EDGE_CURVE ( 'NONE', #17632, #36266, #35535, .T. ) ;
#18491=DIRECTION ( 'NONE',  ( 1.000000000000000000, 0.000000000000000000, 0.000000000000000000 ) ) ;
#18494=CARTESIAN_POINT ( 'NONE',  ( 18.50001572531400029, -1.956586073098988354, -12.40985500209093928 ) ) ;
#18501=VERTEX_POINT ( 'NONE', #31969 ) ;
#18506=CARTESIAN_POINT ( 'NONE',  ( 24.01911657365105768, 9.335961567032249775, 9.253293928180594818 ) ) ;
#18509=EDGE_CURVE ( 'NONE', #44907, #62317, #44700, .T. ) ;
#18515=CARTESIAN_POINT ( 'NONE',  ( 24.72544608131900290, -8.702416312033001589, 9.187185040896000743 ) ) ;
#18522=CYLINDRICAL_SURFACE ( 'NONE', #1223, 0.6999999999999992895 ) ;
#18524=CARTESIAN_POINT ( 'NONE',  ( 23.95226462695299929, -3.419397922773000253, 12.89848026480999899 ) ) ;
#18537=AXIS2_PLACEMENT_3D ( 'NONE', #45553, #66859, #18972 ) ;
#18538=EDGE_CURVE ( 'NONE', #61665, #34641, #29103, .T. ) ;
#18547=CARTESIAN_POINT ( 'NONE',  ( 11.50002032348423242, -3.558966193428903413, 11.09334449156782654 ) ) ;
#18551=EDGE_LOOP ( 'NONE', ( #28487, #19341, #21672, #44464, #43433, #43043 ) ) ;
#18560=CARTESIAN_POINT ( 'NONE',  ( 15.96457203294232841, 8.635839794706024364, 7.819790491316798153 ) ) ;
#18563=CARTESIAN_POINT ( 'NONE',  ( 13.58069952315600126, -12.39169461668999972, -2.069104550346000160 ) ) ;
#18564=ORIENTED_EDGE ( 'NONE', *, *, #65878, .F. ) ;
#18566=ADVANCED_FACE ( 'NONE', ( #25333 ), #60378, .F. ) ;
#18567=CARTESIAN_POINT ( 'NONE',  ( 13.00000000009400303, -11.69118001589999878, -1.923222888683999932 ) ) ;
#18573=EDGE_CURVE ( 'NONE', #33733, #66584, #37873, .T. ) ;
#18578=CARTESIAN_POINT ( 'NONE',  ( 18.30000000000000071, -2.818726571106858980, -11.83569999720589294 ) ) ;
#18580=CARTESIAN_POINT ( 'NONE',  ( 12.17041751275704620, -10.92137764442966308, 4.055351144497368665 ) ) ;
#18589=CARTESIAN_POINT ( 'NONE',  ( 18.49996808500599954, -1.807259459756127784, 11.54438823573780759 ) ) ;
#18598=CARTESIAN_POINT ( 'NONE',  ( 11.68610928851700237, 3.397019518052000198, -11.10441497445000003 ) ) ;
#18599=CARTESIAN_POINT ( 'NONE',  ( 23.56664678325900297, -13.31363270032999857, -4.296980171176000063 ) ) ;
#18605=CARTESIAN_POINT ( 'NONE',  ( 24.44496487975900223, 3.224879802562000464, -12.03535984693000138 ) ) ;
#18614=FACE_OUTER_BOUND ( 'NONE', #23978, .T. ) ;
#18621=ADVANCED_FACE ( 'NONE', ( #43116 ), #11989, .T. ) ;
#18628=CARTESIAN_POINT ( 'NONE',  ( 18.39984528086700166, -1.003641614260999896E-13, 7.549516567450998842E-14 ) ) ;
#18633=CARTESIAN_POINT ( 'NONE',  ( 23.62209727552723848, -13.40165364989338137, 3.913322289613119231 ) ) ;
#18634=VERTEX_POINT ( 'NONE', #49393 ) ;
#18641=CIRCLE ( 'NONE', #27563, 13.92493900950999830 ) ;
#18645=CARTESIAN_POINT ( 'NONE',  ( 11.36673756060750939, -11.69736410939764859, -1.420371773397748560 ) ) ;
#18651=CIRCLE ( 'NONE', #27580, 0.6999999999999992895 ) ;
#18653=CARTESIAN_POINT ( 'NONE',  ( 24.87547603600999935, 11.55042631839000045, 3.247370472710000122 ) ) ;
#18657=CARTESIAN_POINT ( 'NONE',  ( 17.60000000000000142, -10.78295181803999903, 4.410266442048000002 ) ) ;
#18661=CARTESIAN_POINT ( 'NONE',  ( 16.39999999347100257, 3.345256695718999751, 11.86066175541999890 ) ) ;
#18663=CARTESIAN_POINT ( 'NONE',  ( 23.50387503050299998, 0.000000000000000000, 0.000000000000000000 ) ) ;
#18667=CARTESIAN_POINT ( 'NONE',  ( 25.12925359016687921, 2.819714440734963024, 11.46538652554768944 ) ) ;
#18670=CARTESIAN_POINT ( 'NONE',  ( 24.12730418717761793, -12.50340476629924780, 3.372662146504148417 ) ) ;
#18673=EDGE_CURVE ( 'NONE', #1379, #13517, #38559, .T. ) ;
#18675=ORIENTED_EDGE ( 'NONE', *, *, #4808, .T. ) ;
#18681=CARTESIAN_POINT ( 'NONE',  ( 25.60000000000000142, 10.55164198324999880, 3.754898126455999741 ) ) ;
#18687=CARTESIAN_POINT ( 'NONE',  ( 11.30000000000000071, 3.781170807299996550, -11.56421779094657332 ) ) ;
#18690=CARTESIAN_POINT ( 'NONE',  ( 24.36958145701300182, -12.05823614978999991, -3.270605474396000023 ) ) ;
#18705=DIRECTION ( 'NONE',  ( 0.000000000000000000, 1.000000000000000000, 0.000000000000000000 ) ) ;
#18710=CARTESIAN_POINT ( 'NONE',  ( 23.64815810203500135, 10.02631040633000126, -9.635204500925999227 ) ) ;
#18711=CARTESIAN_POINT ( 'NONE',  ( 15.90003771078200145, -3.695138809391000034, -11.25918926437999978 ) ) ;
#18715=VERTEX_POINT ( 'NONE', #5705 ) ;
#18729=B_SPLINE_CURVE_WITH_KNOTS ( 'NONE', 3,
 ( #20747, #30218, #24959, #35798 ),
 .UNSPECIFIED., .F., .F.,
 ( 4, 4 ),
 ( 0.000000000000000000, 1.000000000000000000 ),
 .UNSPECIFIED. ) ;
#18732=CARTESIAN_POINT ( 'NONE',  ( 18.19991756629429602, -3.160410836633248621, -11.91446384612378750 ) ) ;
#18738=CARTESIAN_POINT ( 'NONE',  ( 24.00507456979297061, -12.70418999682170913, -3.471506332325644095 ) ) ;
#18740=CARTESIAN_POINT ( 'NONE',  ( 24.70770306079000278, 3.610860736573000107, -12.15153796058999980 ) ) ;
#18752=CARTESIAN_POINT ( 'NONE',  ( 23.66004879239100234, -13.39256420742000131, 3.813548264891000183 ) ) ;
#18756=CARTESIAN_POINT ( 'NONE',  ( 25.29989727901499919, -2.078227429405999693, -11.31065739696999906 ) ) ;
#18758=VECTOR ( 'NONE', #13251, 1000.000000000000114 ) ;
#18762=DIRECTION ( 'NONE',  ( 2.186536431443105034E-10, -0.8764392776392420092, -0.4815124013057229813 ) ) ;
#18767=CARTESIAN_POINT ( 'NONE',  ( 23.66004879239100234, 0.000000000000000000, 0.000000000000000000 ) ) ;
#18770=PRODUCT ( 'Drip Tip - Airflow Cap', 'Drip Tip - Airflow Cap', '', ( #22161 ) ) ;
#18774=CARTESIAN_POINT ( 'NONE',  ( 24.30000000000000071, 2.078227429405999693, 11.31065739696999906 ) ) ;
#18803=CARTESIAN_POINT ( 'NONE',  ( 24.36504260745899941, 3.372670036896999513, 12.24415025393999912 ) ) ;
#18811=CARTESIAN_POINT ( 'NONE',  ( 15.90018573812067615, -4.599694346030117842, -10.96245233228866667 ) ) ;
#18818=CARTESIAN_POINT ( 'NONE',  ( 16.13140881196041221, 3.487052973477671181, 11.11602635788046278 ) ) ;
#18826=CARTESIAN_POINT ( 'NONE',  ( 11.80415302574500203, -3.641975138519000232, 12.02422332381999937 ) ) ;
#18832=ORIENTED_EDGE ( 'NONE', *, *, #63215, .T. ) ;
#18842=FACE_OUTER_BOUND ( 'NONE', #59639, .T. ) ;
#18855=CARTESIAN_POINT ( 'NONE',  ( 18.53494720760600245, -3.035003031749999636, -12.19105792290999979 ) ) ;
#18862=VERTEX_POINT ( 'NONE', #52058 ) ;
#18865=CARTESIAN_POINT ( 'NONE',  ( 12.48078237978696414, -11.21561491931810473, 3.152940285099523621 ) ) ;
#18868=DIRECTION ( 'NONE',  ( 0.000000000000000000, 0.000000000000000000, 1.000000000000000000 ) ) ;
#18883=B_SPLINE_CURVE_WITH_KNOTS ( 'NONE', 3,
 ( #21871, #69084, #16970, #47775 ),
 .UNSPECIFIED., .F., .F.,
 ( 4, 4 ),
 ( 0.000000000000000000, 1.000000000000000000 ),
 .UNSPECIFIED. ) ;
#18884=B_SPLINE_CURVE_WITH_KNOTS ( 'NONE', 3,
 ( #47672, #35803, #26694, #53249 ),
 .UNSPECIFIED., .F., .F.,
 ( 4, 4 ),
 ( 0.000000000000000000, 1.000000000000000000 ),
 .UNSPECIFIED. ) ;
#18901=DIRECTION ( 'NONE',  ( -1.000000000000000000, 0.000000000000000000, 0.000000000000000000 ) ) ;
#18905=CARTESIAN_POINT ( 'NONE',  ( 13.00000000009400303, 11.69118001589999878, 1.923222888683999932 ) ) ;
#18920=CARTESIAN_POINT ( 'NONE',  ( 11.49999144015000319, 3.886253129992999877, -11.90689313971000018 ) ) ;
#18921=FACE_OUTER_BOUND ( 'NONE', #1702, .T. ) ;
#18924=ORIENTED_EDGE ( 'NONE', *, *, #11507, .F. ) ;
#18928=ORIENTED_EDGE ( 'NONE', *, *, #57646, .T. ) ;
#18929=CARTESIAN_POINT ( 'NONE',  ( 15.40000000005200143, -9.187454762873001002, -8.213177997099000649 ) ) ;
#18931=CARTESIAN_POINT ( 'NONE',  ( 24.30000000000000071, 0.000000000000000000, 0.000000000000000000 ) ) ;
#18934=ADVANCED_FACE ( 'NONE', ( #25672 ), #46665, .F. ) ;
#18936=CARTESIAN_POINT ( 'NONE',  ( 16.13886389318898651, -3.397126321181334063, -11.84561170022415766 ) ) ;
#18944=CARTESIAN_POINT ( 'NONE',  ( 24.56710774269708608, 8.731559079190242656, 8.723167087384579688 ) ) ;
#18952=ORIENTED_EDGE ( 'NONE', *, *, #31188, .F. ) ;
#18957=CARTESIAN_POINT ( 'NONE',  ( 23.55356154618500142, -3.058499659814000182, -13.69546366221000078 ) ) ;
#18959=EDGE_CURVE ( 'NONE', #49620, #52300, #12115, .T. ) ;
#18970=DIRECTION ( 'NONE',  ( -8.952907862884472301E-11, 0.2714597137497840040, 0.9624498032681421122 ) ) ;
#18972=DIRECTION ( 'NONE',  ( 0.000000000000000000, 0.000000000000000000, -1.000000000000000000 ) ) ;
#18980=CARTESIAN_POINT ( 'NONE',  ( 13.50018479229797030, 11.10053973472265021, 4.255642710877637569 ) ) ;
#18981=CARTESIAN_POINT ( 'NONE',  ( 23.56665676678700194, 2.935519496638999914, -13.67844162499000049 ) ) ;
#18988=DIRECTION ( 'NONE',  ( 1.000000000000000000, 0.000000000000000000, 0.000000000000000000 ) ) ;
#18992=CARTESIAN_POINT ( 'NONE',  ( 24.37846970953800252, -12.00848455234000056, -3.275549967069999902 ) ) ;
#18995=DIRECTION ( 'NONE',  ( 0.000000000000000000, 1.000000000000000000, 0.000000000000000000 ) ) ;
#18997=CIRCLE ( 'NONE', #61425, 1.300130688722000327 ) ;
#18999=CARTESIAN_POINT ( 'NONE',  ( 15.89979320885400327, 3.824231472901999496, 11.71686814605000038 ) ) ;
#19000=ORIENTED_EDGE ( 'NONE', *, *, #32542, .T. ) ;
#19005=CARTESIAN_POINT ( 'NONE',  ( 24.97034827298988091, 2.963737632979523529, 11.58472174624901285 ) ) ;
#19008=CARTESIAN_POINT ( 'NONE',  ( 13.49980696793000057, -9.514462421839999351, -7.834836582454001608 ) ) ;
#19009=ADVANCED_FACE ( 'NONE', ( #43402 ), #27317, .T. ) ;
#19012=EDGE_CURVE ( 'NONE', #56428, #66584, #65901, .T. ) ;
#19013=CARTESIAN_POINT ( 'NONE',  ( 11.29996927726999978, -12.23272628844000032, -1.505586261403999870 ) ) ;
#19020=DIRECTION ( 'NONE',  ( 0.000000000000000000, 0.000000000000000000, 1.000000000000000000 ) ) ;
#19021=VERTEX_POINT ( 'NONE', #7717 ) ;
#19024=CARTESIAN_POINT ( 'NONE',  ( 11.44446504844000145, -11.61858443320999967, -1.410913393917999858 ) ) ;
#19044=B_SPLINE_CURVE_WITH_KNOTS ( 'NONE', 3,
 ( #7603, #41049, #67262, #19378, #14144, #62371, #14487, #51874, #5012, #16877, #32627, #112, #11287, #32292, #21774, #48012, #10948, #58497, #53253, #26347, #31254, #16536, #64759, #37862, #47676, #10600 ),
 .UNSPECIFIED., .F., .F.,
 ( 4, 2, 2, 2, 2, 2, 2, 2, 2, 2, 2, 2, 4 ),
 ( 0.000000000000000000, 0.06249999999999719669, 0.09374999999999751588, 0.1249999999999978351, 0.2499999999999957812, 0.3749999999999937272, 0.4999999999999916733, 0.6249999999999895639, 0.7499999999999875655, 0.8124999999999880096, 0.8437499999999883427, 0.8749999999999886757, 1.000000000000000000 ),
 .UNSPECIFIED. ) ;
#19051=CARTESIAN_POINT ( 'NONE',  ( 23.56666365135700403, -11.16210620494999439, -3.571147222960000533 ) ) ;
#19060=CARTESIAN_POINT ( 'NONE',  ( 24.34833250312466646, -3.256146816482774486, -12.15210535601315733 ) ) ;
#19068=DIRECTION ( 'NONE',  ( 1.000000000000000000, 0.000000000000000000, 0.000000000000000000 ) ) ;
#19080=DIRECTION ( 'NONE',  ( 0.000000000000000000, 0.000000000000000000, -1.000000000000000000 ) ) ;
#19081=CARTESIAN_POINT ( 'NONE',  ( 16.04750315638899849, 3.679714098878999806, 11.11063745184000062 ) ) ;
#19084=EDGE_LOOP ( 'NONE', ( #1991, #18434, #50907, #55561 ) ) ;
#19091=EDGE_CURVE ( 'NONE', #5123, #14810, #52528, .T. ) ;
#19093=ORIENTED_EDGE ( 'NONE', *, *, #4416, .T. ) ;
#19095=ADVANCED_FACE ( 'NONE', ( #56302 ), #7875, .F. ) ;
#19098=( NAMED_UNIT ( * ) SI_UNIT ( $, .STERADIAN. ) SOLID_ANGLE_UNIT ( ) );
#19100=ORIENTED_EDGE ( 'NONE', *, *, #64483, .T. ) ;
#19104=CARTESIAN_POINT ( 'NONE',  ( 24.00507894008998022, -3.345686396274558216, -12.73791187279332249 ) ) ;
#19105=CARTESIAN_POINT ( 'NONE',  ( 11.64444011873732698, 3.380850026661442964, -11.14878564717023401 ) ) ;
#19118=CARTESIAN_POINT ( 'NONE',  ( 25.30000327618300204, -10.83443035398000021, 3.855530949778000149 ) ) ;
#19119=ORIENTED_EDGE ( 'NONE', *, *, #18066, .T. ) ;
#19128=EDGE_CURVE ( 'NONE', #5014, #12823, #42075, .T. ) ;
#19132=CARTESIAN_POINT ( 'NONE',  ( 24.54688887196200042, 3.662825465818000392, 12.34578425079000041 ) ) ;
#19140=CARTESIAN_POINT ( 'NONE',  ( 13.00000000001300116, -11.52577654661000039, -1.696746661728000038 ) ) ;
#19143=FACE_OUTER_BOUND ( 'NONE', #46429, .T. ) ;
#19154=EDGE_LOOP ( 'NONE', ( #3634, #63893, #5923, #34323 ) ) ;
#19156=CARTESIAN_POINT ( 'NONE',  ( 13.99999999379500082, 8.815218614167999789, 7.616697584347000394 ) ) ;
#19165=ORIENTED_EDGE ( 'NONE', *, *, #52834, .F. ) ;
#19176=EDGE_CURVE ( 'NONE', #5868, #59008, #16788, .T. ) ;
#19187=CARTESIAN_POINT ( 'NONE',  ( 17.61786948987200319, -12.16775412387000088, 3.132314945639000037 ) ) ;
#19195=ORIENTED_EDGE ( 'NONE', *, *, #2778, .T. ) ;
#19198=CARTESIAN_POINT ( 'NONE',  ( 23.60000000000000142, 0.9826074463019562888, -13.89481017416844288 ) ) ;
#19203=CARTESIAN_POINT ( 'NONE',  ( 17.88705809229600163, 3.642474092890999771, -12.02409483768999898 ) ) ;
#19206=ORIENTED_EDGE ( 'NONE', *, *, #27270, .F. ) ;
#19220=CARTESIAN_POINT ( 'NONE',  ( 13.50018479229300006, 11.60142623882999935, 2.415183939829000259 ) ) ;
#19229=CARTESIAN_POINT ( 'NONE',  ( 12.79999999914999975, 12.11987927271999865, -3.159802730921999814 ) ) ;
#19231=DIRECTION ( 'NONE',  ( -1.000000000000000000, 0.000000000000000000, 0.000000000000000000 ) ) ;
#19239=CARTESIAN_POINT ( 'NONE',  ( 25.60000000000000142, -8.527654132749999505, 7.260537518967999482 ) ) ;
#19241=AXIS2_PLACEMENT_3D ( 'NONE', #48942, #31486, #47912 ) ;
#19250=AXIS2_PLACEMENT_3D ( 'NONE', #23766, #6644, #6993 ) ;
#19257=EDGE_CURVE ( 'NONE', #56117, #68518, #14591, .T. ) ;
#19259=VERTEX_POINT ( 'NONE', #19584 ) ;
#19262=ORIENTED_EDGE ( 'NONE', *, *, #58830, .F. ) ;
#19263=VERTEX_POINT ( 'NONE', #40905 ) ;
#19278=B_SPLINE_CURVE_WITH_KNOTS ( 'NONE', 3,
 ( #53049, #4448, #21906, #9700 ),
 .UNSPECIFIED., .F., .F.,
 ( 4, 4 ),
 ( 0.000000000000000000, 1.000000000000000000 ),
 .UNSPECIFIED. ) ;
#19280=AXIS2_PLACEMENT_3D ( 'NONE', #26967, #65736, #65386 ) ;
#19281=CARTESIAN_POINT ( 'NONE',  ( 24.76776889611345922, 8.625621812597076499, 8.557830585166838588 ) ) ;
#19283=CARTESIAN_POINT ( 'NONE',  ( 24.30001683570900184, 3.271769286791000209, 12.21048169671000139 ) ) ;
#19291=CARTESIAN_POINT ( 'NONE',  ( 25.30000327618300204, 2.078227429405999693, -11.31065739696999906 ) ) ;
#19293=CARTESIAN_POINT ( 'NONE',  ( 16.09992084546400193, 8.991497430826001391, 8.719551690569000257 ) ) ;
#19297=CARTESIAN_POINT ( 'NONE',  ( 25.59997384872700010, 11.07537887597999848, -3.096069522331000190 ) ) ;
#19302=CARTESIAN_POINT ( 'NONE',  ( 18.05828223140162692, 3.296090368282508454, 11.87625427050432236 ) ) ;
#19308=ORIENTED_EDGE ( 'NONE', *, *, #55091, .T. ) ;
#19315=CARTESIAN_POINT ( 'NONE',  ( 23.66004879239100234, 9.998911746292000302, 9.691526727427998367 ) ) ;
#19326=CARTESIAN_POINT ( 'NONE',  ( 21.72233714749290101, 6.000000000000000000, -1.351488365663999764E-13 ) ) ;
#19329=CARTESIAN_POINT ( 'NONE',  ( 25.20343682218700110, 11.20004844819000134, 3.404174865946999695 ) ) ;
#19330=VERTEX_POINT ( 'NONE', #4516 ) ;
#19333=CARTESIAN_POINT ( 'NONE',  ( 23.66004879239100234, 13.39256428908000096, 3.813547978107000080 ) ) ;
#19334=EDGE_CURVE ( 'NONE', #37994, #62306, #46295, .T. ) ;
#19336=EDGE_CURVE ( 'NONE', #1910, #40655, #58787, .T. ) ;
#19341=ORIENTED_EDGE ( 'NONE', *, *, #5695, .F. ) ;
#19342=EDGE_CURVE ( 'NONE', #28175, #38133, #47902, .T. ) ;
#19347=DIRECTION ( 'NONE',  ( 0.000000000000000000, -0.7614089499631907509, -0.6482718649732928107 ) ) ;
#19350=CARTESIAN_POINT ( 'NONE',  ( 18.23980063401623752, 2.972525811573667465, -11.47315805793748567 ) ) ;
#19366=CARTESIAN_POINT ( 'NONE',  ( 12.99999999998900080, 12.39025855408000076, 1.832244667012999928 ) ) ;
#19367=CARTESIAN_POINT ( 'NONE',  ( 24.62773497368900166, -12.19918623920000122, -3.045383383698999857 ) ) ;
#19369=ORIENTED_EDGE ( 'NONE', *, *, #58059, .F. ) ;
#19371=AXIS2_PLACEMENT_3D ( 'NONE', #17102, #11509, #12216 ) ;
#19378=CARTESIAN_POINT ( 'NONE',  ( 17.79607173997655423, 11.53879313267151119, -4.871540518365785388 ) ) ;
#19385=CARTESIAN_POINT ( 'NONE',  ( 24.16198533718584684, 3.322437203991291277, 12.45250991497782778 ) ) ;
#19386=CARTESIAN_POINT ( 'NONE',  ( 23.74057427653900021, 9.838736938141998678, -9.517768723660999797 ) ) ;
#19387=CARTESIAN_POINT ( 'NONE',  ( 16.26904166988085620, -3.216266637185321020, -11.40336119490550004 ) ) ;
#19390=VECTOR ( 'NONE', #20225, 1000.000000000000114 ) ;
#19392=EDGE_LOOP ( 'NONE', ( #33100, #48931, #49813, #13741 ) ) ;
#19413=CARTESIAN_POINT ( 'NONE',  ( 13.69992376746900042, 12.26631831379999937, 2.532779022035999805 ) ) ;
#19423=ORIENTED_EDGE ( 'NONE', *, *, #18233, .T. ) ;
#19442=B_SPLINE_CURVE_WITH_KNOTS ( 'NONE', 3,
 ( #53014, #4417, #9662, #213 ),
 .UNSPECIFIED., .F., .F.,
 ( 4, 4 ),
 ( 0.000000000000000000, 1.000000000000000000 ),
 .UNSPECIFIED. ) ;
#19444=ORIENTED_EDGE ( 'NONE', *, *, #23459, .T. ) ;
#19449=CARTESIAN_POINT ( 'NONE',  ( 24.96657550120661995, 2.078227398812693139, 11.31065740259266406 ) ) ;
#19454=ORIENTED_EDGE ( 'NONE', *, *, #35909, .T. ) ;
#19457=ORIENTED_EDGE ( 'NONE', *, *, #12169, .T. ) ;
#19469=CARTESIAN_POINT ( 'NONE',  ( 15.61722669115800066, 9.375864875015000877, 8.222239459497000524 ) ) ;
#19475=CARTESIAN_POINT ( 'NONE',  ( 24.46225942633000017, -11.93531508627000015, 3.254110267536999945 ) ) ;
#19478=B_SPLINE_CURVE_WITH_KNOTS ( 'NONE', 3,
 ( #15555, #27419, #64116, #21474 ),
 .UNSPECIFIED., .F., .F.,
 ( 4, 4 ),
 ( 0.000000000000000000, 1.000000000000000000 ),
 .UNSPECIFIED. ) ;
#19487=EDGE_CURVE ( 'NONE', #54794, #26237, #27102, .T. ) ;
#19493=CARTESIAN_POINT ( 'NONE',  ( 17.86531638133300248, 3.412592442238999713, 11.89775222658999887 ) ) ;
#19498=ORIENTED_EDGE ( 'NONE', *, *, #13415, .T. ) ;
#19504=ORIENTED_EDGE ( 'NONE', *, *, #31067, .T. ) ;
#19514=CARTESIAN_POINT ( 'NONE',  ( 16.09997386696500143, -5.375854662731797795, -10.37779375783402358 ) ) ;
#19536=CARTESIAN_POINT ( 'NONE',  ( 17.90096402402700093, -11.91930970589999994, 3.312615672289999758 ) ) ;
#19543=ORIENTED_EDGE ( 'NONE', *, *, #38747, .F. ) ;
#19544=ORIENTED_EDGE ( 'NONE', *, *, #2442, .T. ) ;
#19547=CARTESIAN_POINT ( 'NONE',  ( 24.30000000000000071, 2.524919604596999712, -12.12772056298999956 ) ) ;
#19550=CARTESIAN_POINT ( 'NONE',  ( 24.44496412535000118, -8.810486166165000910, -8.810507954003998776 ) ) ;
#19552=DIRECTION ( 'NONE',  ( 0.000000000000000000, -0.7146936510866647163, -0.6994376205898656940 ) ) ;
#19553=CARTESIAN_POINT ( 'NONE',  ( 23.54908302934800091, -13.36512341691999950, 4.295216725789000378 ) ) ;
#19558=CARTESIAN_POINT ( 'NONE',  ( 23.56695925801778557, -10.30432770669533404, -9.462935969010649373 ) ) ;
#19572=CIRCLE ( 'NONE', #68710, 0.6999999999999992895 ) ;
#19574=CARTESIAN_POINT ( 'NONE',  ( 13.50000000000000178, 11.91410841793398312, 2.466613755757246285 ) ) ;
#19576=CARTESIAN_POINT ( 'NONE',  ( 24.72675083956480435, 11.76478169716107480, 3.190859653314884081 ) ) ;
#19579=ORIENTED_EDGE ( 'NONE', *, *, #47552, .F. ) ;
#19584=CARTESIAN_POINT ( 'NONE',  ( 12.79999999202000005, -11.41069016990000051, 4.623987642516999230 ) ) ;
#19585=CARTESIAN_POINT ( 'NONE',  ( 16.00000000900400110, -11.53038407186596892, 4.891407584292653432 ) ) ;
#19586=CARTESIAN_POINT ( 'NONE',  ( 15.82968830470293398, 8.721231603648991637, 7.724200095969830038 ) ) ;
#19588=CARTESIAN_POINT ( 'NONE',  ( 24.71805762077055135, -11.77340594384550343, 3.190795258418060776 ) ) ;
#19594=CARTESIAN_POINT ( 'NONE',  ( 13.26247400726062509, -11.68416116973912011, -1.976808445614455900 ) ) ;
#19600=B_SPLINE_CURVE_WITH_KNOTS ( 'NONE', 3,
 ( #61942, #41991, #14056, #56705, #67519, #15426 ),
 .UNSPECIFIED., .F., .F.,
 ( 4, 2, 4 ),
 ( 0.000000000000000000, 0.5000000000000000000, 1.000000000000000000 ),
 .UNSPECIFIED. ) ;
#19602=CARTESIAN_POINT ( 'NONE',  ( 23.59999172237900211, -2.915589696762999949, -13.58550518520000061 ) ) ;
#19615=CARTESIAN_POINT ( 'NONE',  ( 25.02478460520268300, -2.919208160324095580, -11.54269743113043489 ) ) ;
#19624=EDGE_CURVE ( 'NONE', #25967, #57124, #4541, .T. ) ;
#19629=VECTOR ( 'NONE', #12301, 999.9999999999998863 ) ;
#19631=DIRECTION ( 'NONE',  ( 0.000000000000000000, -0.7071067811865475727, -0.7071067811865475727 ) ) ;
#19633=AXIS2_PLACEMENT_3D ( 'NONE', #13397, #18289, #40297 ) ;
#19642=CARTESIAN_POINT ( 'NONE',  ( 23.50387503050299998, 0.000000000000000000, 0.000000000000000000 ) ) ;
#19647=B_SPLINE_CURVE_WITH_KNOTS ( 'NONE', 3,
 ( #61716, #66960, #19760, #30594 ),
 .UNSPECIFIED., .F., .F.,
 ( 4, 4 ),
 ( 0.000000000000000000, 1.000000000000000000 ),
 .UNSPECIFIED. ) ;
#19649=CARTESIAN_POINT ( 'NONE',  ( 16.09997386696500143, -8.350085070477001992, -8.123950967096998710 ) ) ;
#19657=ADVANCED_FACE ( 'NONE', ( #38499 ), #2335, .T. ) ;
#19660=CARTESIAN_POINT ( 'NONE',  ( 16.09055856039299925, -8.515834468357001086, -7.893949987785000566 ) ) ;
#19674=CARTESIAN_POINT ( 'NONE',  ( 17.80000000000000071, -14.76315775485999993, -50.50083396221000243 ) ) ;
#19679=CIRCLE ( 'NONE', #54300, 13.98989063585999837 ) ;
#19682=B_SPLINE_CURVE_WITH_KNOTS ( 'NONE', 3,
 ( #62634, #52499, #4253, #53191 ),
 .UNSPECIFIED., .F., .F.,
 ( 4, 4 ),
 ( 0.000000000000000000, 1.000000000000000000 ),
 .UNSPECIFIED. ) ;
#19683=LINE ( 'NONE', #20024, #54677 ) ;
#19684=DIRECTION ( 'NONE',  ( 1.000000000000000000, 0.000000000000000000, 0.000000000000000000 ) ) ;
#19694=AXIS2_PLACEMENT_3D ( 'NONE', #8066, #67124, #13661 ) ;
#19697=ORIENTED_EDGE ( 'NONE', *, *, #3876, .F. ) ;
#19705=EDGE_LOOP ( 'NONE', ( #40134, #38690, #41737, #66628, #30703, #19423, #12008, #33358, #27017, #59578 ) ) ;
#19706=CARTESIAN_POINT ( 'NONE',  ( 25.39991507555011196, 8.680020025996363131, -7.390263434115322383 ) ) ;
#19707=CARTESIAN_POINT ( 'NONE',  ( 24.44496488041000148, -12.03536727282999941, 3.224852091355999928 ) ) ;
#19709=EDGE_LOOP ( 'NONE', ( #45582, #39316, #12648, #10822 ) ) ;
#19711=FILL_AREA_STYLE_COLOUR ( '', #11933 ) ;
#19724=CONICAL_SURFACE ( 'NONE', #13049, 1.150081764678999585, 0.7854598963975319981 ) ;
#19726=PLANE ( 'NONE',  #65936 ) ;
#19731=CIRCLE ( 'NONE', #58799, 12.20000000000000639 ) ;
#19734=CARTESIAN_POINT ( 'NONE',  ( 23.71889066594441786, 3.252317644464183033, 13.29341160290726798 ) ) ;
#19735=EDGE_CURVE ( 'NONE', #58690, #60460, #55280, .T. ) ;
#19738=CARTESIAN_POINT ( 'NONE',  ( 17.89162860438300129, -3.376692001085000339, -11.11057855219999979 ) ) ;
#19743=CARTESIAN_POINT ( 'NONE',  ( 17.60000001072100062, -11.41073498373000028, 4.623967591968000335 ) ) ;
#19749=CARTESIAN_POINT ( 'NONE',  ( 24.53428985367600390, -3.614319203926000146, 12.31267510079000083 ) ) ;
#19750=CARTESIAN_POINT ( 'NONE',  ( 24.30000000000000071, 12.03537377768999939, 3.224868684338999980 ) ) ;
#19751=CARTESIAN_POINT ( 'NONE',  ( 13.82809631267600103, 8.844623397843001555, 7.663863542600000578 ) ) ;
#19752=CARTESIAN_POINT ( 'NONE',  ( 16.39999999485600313, -3.595156957901000094, -11.99794989424000136 ) ) ;
#19760=CARTESIAN_POINT ( 'NONE',  ( 24.60115016796638088, -8.755275691353283207, 9.042371375187583382 ) ) ;
#19761=CARTESIAN_POINT ( 'NONE',  ( 24.54687940532799928, 3.662828524876999836, -12.34579568540000061 ) ) ;
#19767=CARTESIAN_POINT ( 'NONE',  ( 12.99325612864500279, -11.57041205278999918, -1.757148387262999822 ) ) ;
#19771=AXIS2_PLACEMENT_3D ( 'NONE', #23511, #12337, #2200 ) ;
#19788=ORIENTED_EDGE ( 'NONE', *, *, #12840, .T. ) ;
#19790=CIRCLE ( 'NONE', #16434, 14.00000000000000533 ) ;
#19793=CARTESIAN_POINT ( 'NONE',  ( 24.30001680106099826, 12.21047197645999915, -3.271805488357999891 ) ) ;
#19797=CARTESIAN_POINT ( 'NONE',  ( 11.50002032348423064, 3.558966193428915403, -11.09334449156781943 ) ) ;
#19799=AXIS2_PLACEMENT_3D ( 'NONE', #67564, #8851, #57421 ) ;
#19804=ORIENTED_EDGE ( 'NONE', *, *, #15874, .T. ) ;
#19816=ADVANCED_FACE ( 'NONE', ( #42114 ), #4650, .T. ) ;
#19819=CARTESIAN_POINT ( 'NONE',  ( 13.49980696793000057, 9.514462421839999351, 7.834836582454001608 ) ) ;
#19824=CARTESIAN_POINT ( 'NONE',  ( 25.46372779695100164, -11.23407511953000082, -3.161075425950000017 ) ) ;
#19827=CARTESIAN_POINT ( 'NONE',  ( 24.40777907822999993, 3.358845133677000216, 12.19253384565000076 ) ) ;
#19829=CARTESIAN_POINT ( 'NONE',  ( 23.68246226653500131, 9.989803668321998842, 9.401306877296001119 ) ) ;
#19840=ORIENTED_EDGE ( 'NONE', *, *, #64818, .T. ) ;
#19842=CIRCLE ( 'NONE', #6406, 1.000000000000000222 ) ;
#19855=ORIENTED_EDGE ( 'NONE', *, *, #59134, .T. ) ;
#19857=EDGE_LOOP ( 'NONE', ( #24167, #52908, #49907, #4884 ) ) ;
#19866=ORIENTED_EDGE ( 'NONE', *, *, #18538, .T. ) ;
#19870=VERTEX_POINT ( 'NONE', #2143 ) ;
#19876=CARTESIAN_POINT ( 'NONE',  ( 17.98628609634500108, -3.388648274289000284, -11.90503202562999974 ) ) ;
#19904=CIRCLE ( 'NONE', #64546, 11.50000000000000178 ) ;
#19907=CARTESIAN_POINT ( 'NONE',  ( 24.78226664044499827, 8.655277561894001437, 9.168097195530998889 ) ) ;
#19911=CARTESIAN_POINT ( 'NONE',  ( 11.53971429488000133, -3.572666839320000065, 11.04878221693000029 ) ) ;
#19925=CARTESIAN_POINT ( 'NONE',  ( 13.92966272177200260, -9.396431546200000540, -8.198412206645000921 ) ) ;
#19929=AXIS2_PLACEMENT_3D ( 'NONE', #3908, #67888, #8141 ) ;
#19939=CIRCLE ( 'NONE', #8761, 13.98989063587000281 ) ;
#19942=ORIENTED_EDGE ( 'NONE', *, *, #23488, .F. ) ;
#19952=CARTESIAN_POINT ( 'NONE',  ( 24.59181002256200088, -3.481107758750999537, -12.13646513482999900 ) ) ;
#19954=B_SPLINE_CURVE_WITH_KNOTS ( 'NONE', 3,
 ( #63296, #58070, #35380, #25217, #41989, #36749 ),
 .UNSPECIFIED., .F., .F.,
 ( 4, 2, 4 ),
 ( 0.000000000000000000, 0.5000000000000000000, 1.000000000000000000 ),
 .UNSPECIFIED. ) ;
#19970=CARTESIAN_POINT ( 'NONE',  ( 24.30000000000000071, -12.03537377768999939, -3.224868684338999980 ) ) ;
#19979=CARTESIAN_POINT ( 'NONE',  ( 15.20000000000000107, -11.47055000429999971, 4.757693469806000053 ) ) ;
#19983=ORIENTED_EDGE ( 'NONE', *, *, #12878, .F. ) ;
#19984=AXIS2_PLACEMENT_3D ( 'NONE', #47437, #36949, #58263 ) ;
#19988=CARTESIAN_POINT ( 'NONE',  ( 24.40628504395400000, 8.880942544344001988, 9.006432928708999697 ) ) ;
#19991=CARTESIAN_POINT ( 'NONE',  ( 15.39999999998900293, 9.471998555523999386, 8.194929586088999685 ) ) ;
#19994=CARTESIAN_POINT ( 'NONE',  ( 25.44993329535400051, 2.258942858049999725, 11.14410225571399948 ) ) ;
#20014=CARTESIAN_POINT ( 'NONE',  ( 23.66477443553700155, 3.238206668739000094, -13.42731210495999861 ) ) ;
#20024=CARTESIAN_POINT ( 'NONE',  ( 19.89999966725400071, -12.52499966719000035, -3.709580198520000162E-10 ) ) ;
#20029=CYLINDRICAL_SURFACE ( 'NONE', #19799, 1.000000000000001332 ) ;
#20033=ORIENTED_EDGE ( 'NONE', *, *, #68027, .F. ) ;
#20046=ADVANCED_FACE ( 'NONE', ( #4189 ), #15033, .F. ) ;
#20052=ORIENTED_EDGE ( 'NONE', *, *, #36578, .T. ) ;
#20055=DIRECTION ( 'NONE',  ( 2.186536431443105034E-10, 0.8764392776392420092, -0.4815124013057229813 ) ) ;
#20056=CARTESIAN_POINT ( 'NONE',  ( 24.46729256464000457, -12.16659091368999945, -3.168154674931000336 ) ) ;
#20063=ADVANCED_FACE ( 'NONE', ( #25526 ), #41261, .F. ) ;
#20066=EDGE_CURVE ( 'NONE', #59819, #1148, #4495, .T. ) ;
#20068=CARTESIAN_POINT ( 'NONE',  ( 17.76937411412500367, 3.251867979506000150, 11.33740618442000070 ) ) ;
#20074=CARTESIAN_POINT ( 'NONE',  ( 11.49977531252999974, 12.43119799159999950, 1.530013559959999991 ) ) ;
#20075=CARTESIAN_POINT ( 'NONE',  ( 23.61456370124183124, 3.070877465454437516, 13.52759921014553157 ) ) ;
#20076=CARTESIAN_POINT ( 'NONE',  ( 24.42335439002600239, 8.981275493775999763, -9.518163459556999939 ) ) ;
#20085=CARTESIAN_POINT ( 'NONE',  ( 23.60000000000000142, 9.289189189551001036, 7.908916752675001050 ) ) ;
#20086=CARTESIAN_POINT ( 'NONE',  ( 25.30000327618300204, -2.078227429405999693, 11.31065739696999906 ) ) ;
#20088=DIRECTION ( 'NONE',  ( 0.000000000000000000, -0.2098318009950989882, 0.9777374981512947372 ) ) ;
#20090=CARTESIAN_POINT ( 'NONE',  ( 13.59015267864900345, 8.992820872206999994, 7.631366745126000772 ) ) ;
#20093=CARTESIAN_POINT ( 'NONE',  ( 17.60000003688378811, 11.49036663463118835, -4.802323205938251682 ) ) ;
#20117=ORIENTED_EDGE ( 'NONE', *, *, #32463, .F. ) ;
#20131=EDGE_CURVE ( 'NONE', #27228, #2158, #63371, .T. ) ;
#20135=CARTESIAN_POINT ( 'NONE',  ( 13.50003721581400029, -9.159934378815998812, -7.517910889891000537 ) ) ;
#20156=CARTESIAN_POINT ( 'NONE',  ( 15.83019412026500206, 8.948785863751000491, 8.423203147821000769 ) ) ;
#20161=CARTESIAN_POINT ( 'NONE',  ( 25.37646853861900453, -11.10818234785000058, 3.395598138602999860 ) ) ;
#20166=CARTESIAN_POINT ( 'NONE',  ( 23.51511354854200064, 10.47166404558000075, 9.493607764193999543 ) ) ;
#20170=PLANE ( 'NONE',  #49021 ) ;
#20172=CARTESIAN_POINT ( 'NONE',  ( 18.53494720760600245, 3.035003031749999636, 12.19105792290999979 ) ) ;
#20173=VECTOR ( 'NONE', #65718, 1000.000000000000114 ) ;
#20178=CARTESIAN_POINT ( 'NONE',  ( 11.79999999471800010, 3.216299622513999701, -11.40340969442000052 ) ) ;
#20183=ORIENTED_EDGE ( 'NONE', *, *, #50775, .F. ) ;
#20186=CARTESIAN_POINT ( 'NONE',  ( 15.40000000009400161, 8.833277835210999740, 7.896561221812000930 ) ) ;
#20193=ORIENTED_EDGE ( 'NONE', *, *, #29423, .T. ) ;
#20206=CARTESIAN_POINT ( 'NONE',  ( 21.10000109091659937, -12.52500000000000036, 0.000000000000000000 ) ) ;
#20215=CARTESIAN_POINT ( 'NONE',  ( 18.17677363193000062, -3.419785592864999835, -11.99291007725999947 ) ) ;
#20221=CARTESIAN_POINT ( 'NONE',  ( 13.70005190196300227, -9.005348107749998832, -7.391036106496999381 ) ) ;
#20225=DIRECTION ( 'NONE',  ( -0.7071060218675898623, -0.7071075405046897133, 8.464244187133876641E-10 ) ) ;
#20233=CARTESIAN_POINT ( 'NONE',  ( 17.79173234077999766, 3.528207283916999781, -11.96069632439000152 ) ) ;
#20236=VERTEX_POINT ( 'NONE', #1245 ) ;
#20245=B_SPLINE_CURVE_WITH_KNOTS ( 'NONE', 3,
 ( #10725, #37985, #48141, #32073, #17003, #244 ),
 .UNSPECIFIED., .F., .F.,
 ( 4, 2, 4 ),
 ( 0.000000000000000000, 0.5000000000000000000, 1.000000000000000000 ),
 .UNSPECIFIED. ) ;
#20250=CARTESIAN_POINT ( 'NONE',  ( 11.61719580513100247, -3.441045665385999985, 11.09087012887000157 ) ) ;
#20255=CARTESIAN_POINT ( 'NONE',  ( 18.29058466016600448, 10.98038933999040445, -3.892884224338386989 ) ) ;
#20258=ORIENTED_EDGE ( 'NONE', *, *, #60529, .F. ) ;
#20262=CARTESIAN_POINT ( 'NONE',  ( 11.26489721861000248, 3.710193004830000252, -11.71182445734000055 ) ) ;
#20274=CARTESIAN_POINT ( 'NONE',  ( 13.70003001321900271, 9.668726926528000476, 7.961868161445000425 ) ) ;
#20279=CARTESIAN_POINT ( 'NONE',  ( 23.81982966688499914, 3.247549704558999828, 13.03982134601000098 ) ) ;
#20288=DIRECTION ( 'NONE',  ( 0.000000000000000000, 0.000000000000000000, -1.000000000000000000 ) ) ;
#20290=DIRECTION ( 'NONE',  ( -1.000000000000000000, 0.000000000000000000, 0.000000000000000000 ) ) ;
#20291=CARTESIAN_POINT ( 'NONE',  ( 24.45284546249100188, -12.43926702221000014, -3.093275132500000080 ) ) ;
#20296=DIRECTION ( 'NONE',  ( -1.000000000000000000, 0.000000000000000000, 0.000000000000000000 ) ) ;
#20323=CARTESIAN_POINT ( 'NONE',  ( 15.49019623964617054, 9.469115506160944662, 8.198265202209981339 ) ) ;
#20327=B_SPLINE_CURVE_WITH_KNOTS ( 'NONE', 3,
 ( #22967, #58999, #59336, #54439, #44317, #48509 ),
 .UNSPECIFIED., .F., .F.,
 ( 4, 2, 4 ),
 ( 0.000000000000000000, 0.5000000000000000000, 1.000000000000000000 ),
 .UNSPECIFIED. ) ;
#20329=DIRECTION ( 'NONE',  ( -1.000000000000000000, 0.000000000000000000, 0.000000000000000000 ) ) ;
#20349=CARTESIAN_POINT ( 'NONE',  ( 11.43330212365182952, 3.865573515333838639, -11.84353424803224719 ) ) ;
#20352=CARTESIAN_POINT ( 'NONE',  ( 23.73412239512900257, 3.552994768190999686, -13.41889993560000072 ) ) ;
#20368=CARTESIAN_POINT ( 'NONE',  ( 23.64390295928378904, 13.40130543866907153, 3.849660382617301480 ) ) ;
#20371=EDGE_CURVE ( 'NONE', #51740, #45182, #42586, .T. ) ;
#20372=ORIENTED_EDGE ( 'NONE', *, *, #14716, .F. ) ;
#20376=AXIS2_PLACEMENT_3D ( 'NONE', #6323, #43753, #23106 ) ;
#20380=CARTESIAN_POINT ( 'NONE',  ( 12.80000000000000071, -10.78295181803999903, 4.410266442048000002 ) ) ;
#20384=CARTESIAN_POINT ( 'NONE',  ( 13.49994651945300284, -12.07042783918999795, -2.492331243371999960 ) ) ;
#20398=EDGE_CURVE ( 'NONE', #55782, #25788, #68278, .T. ) ;
#20402=CARTESIAN_POINT ( 'NONE',  ( 12.04183425709900135, 11.69157926155999938, -4.070931047779999368 ) ) ;
#20407=CARTESIAN_POINT ( 'NONE',  ( 17.86873602477000134, 3.252323392204000019, 11.33729809900999896 ) ) ;
#20413=FACE_OUTER_BOUND ( 'NONE', #58284, .T. ) ;
#20415=CARTESIAN_POINT ( 'NONE',  ( 25.37702747131099912, 8.494993186710001254, -7.921081225816001492 ) ) ;
#20429=CARTESIAN_POINT ( 'NONE',  ( 16.07488484168399978, -3.504106430365000246, -11.16639795596000084 ) ) ;
#20432=CARTESIAN_POINT ( 'NONE',  ( 25.39994675531830737, 10.74016667918497525, -3.821986399293599845 ) ) ;
#20439=VERTEX_POINT ( 'NONE', #14131 ) ;
#20443=DIRECTION ( 'NONE',  ( 1.000000000000000000, 0.000000000000000000, 0.000000000000000000 ) ) ;
#20449=CARTESIAN_POINT ( 'NONE',  ( 13.73959992722299894, -11.36892293904000084, -2.362143082378000081 ) ) ;
#20450=DIRECTION ( 'NONE',  ( 0.000000000000000000, -1.000000000000000000, 0.000000000000000000 ) ) ;
#20454=ORIENTED_EDGE ( 'NONE', *, *, #19257, .T. ) ;
#20457=CARTESIAN_POINT ( 'NONE',  ( 15.72922381500400313, 8.763625284509998892, 7.896085856502000233 ) ) ;
#20458=ORIENTED_EDGE ( 'NONE', *, *, #50273, .T. ) ;
#20462=CYLINDRICAL_SURFACE ( 'NONE', #64358, 0.6999999999999992895 ) ;
#20463=CYLINDRICAL_SURFACE ( 'NONE', #46300, 0.6999999999999992895 ) ;
#20469=ORIENTED_EDGE ( 'NONE', *, *, #41537, .F. ) ;
#20471=AXIS2_PLACEMENT_3D ( 'NONE', #36762, #21022, #47598 ) ;
#20473=ORIENTED_EDGE ( 'NONE', *, *, #42342, .F. ) ;
#20493=DIRECTION ( 'NONE',  ( 0.000000000000000000, -0.001485959642859940649, 0.9999988959613604900 ) ) ;
#20494=CIRCLE ( 'NONE', #34985, 1.000000000000000000 ) ;
#20500=CARTESIAN_POINT ( 'NONE',  ( 16.13936233968600220, 9.023335130797001113, 8.741328814538000813 ) ) ;
#20517=ORIENTED_EDGE ( 'NONE', *, *, #54696, .F. ) ;
#20519=CARTESIAN_POINT ( 'NONE',  ( 18.44718133169100227, 2.901187496916000086, 12.12896678136999995 ) ) ;
#20523=CARTESIAN_POINT ( 'NONE',  ( 23.60000000000000142, -1.954837874162284272, -13.79162083333110367 ) ) ;
#20524=CARTESIAN_POINT ( 'NONE',  ( 25.46372797112000086, -8.354608193938998895, 8.148457429720000533 ) ) ;
#20531=ADVANCED_FACE ( 'NONE', ( #51864 ), #56933, .F. ) ;
#20536=CARTESIAN_POINT ( 'NONE',  ( 16.34794651623100137, -3.644047358192000097, -12.02362153922000054 ) ) ;
#20552=ORIENTED_EDGE ( 'NONE', *, *, #14019, .F. ) ;
#20558=CARTESIAN_POINT ( 'NONE',  ( 18.26547113879826867, 3.186161613543892379, 11.20588962290447554 ) ) ;
#20563=CARTESIAN_POINT ( 'NONE',  ( 18.40806533023902603, 3.252985697212876559, 12.09525697359294760 ) ) ;
#20566=ORIENTED_EDGE ( 'NONE', *, *, #46799, .F. ) ;
#20570=DIRECTION ( 'NONE',  ( -1.000000000000000000, 0.000000000000000000, 0.000000000000000000 ) ) ;
#20574=CARTESIAN_POINT ( 'NONE',  ( 24.33723891670900130, -12.30467408780000049, 3.219315065404000364 ) ) ;
#20585=CARTESIAN_POINT ( 'NONE',  ( 11.53935620825161124, -11.69940330537451878, -1.870140110077453732 ) ) ;
#20593=CARTESIAN_POINT ( 'NONE',  ( 11.44446797630000034, -3.649424658612000272, 11.12042579671999931 ) ) ;
#20594=ORIENTED_EDGE ( 'NONE', *, *, #51447, .T. ) ;
#20609=CARTESIAN_POINT ( 'NONE',  ( 13.75930817923600102, -9.623971528738000103, -8.076134841847999013 ) ) ;
#20610=CARTESIAN_POINT ( 'NONE',  ( 15.89979320885400327, 3.824231472901999496, 11.71686814605000038 ) ) ;
#20612=B_SPLINE_CURVE_WITH_KNOTS ( 'NONE', 3,
 ( #15253, #36575, #41140, #46729 ),
 .UNSPECIFIED., .F., .F.,
 ( 4, 4 ),
 ( 0.000000000000000000, 1.000000000000000000 ),
 .UNSPECIFIED. ) ;
#20633=CARTESIAN_POINT ( 'NONE',  ( 16.86666666253433533, -3.351256455363679887, -11.15757949424527595 ) ) ;
#20636=CARTESIAN_POINT ( 'NONE',  ( 25.20343575914399992, -2.651923631867000086, -11.40161457019999958 ) ) ;
#20655=ORIENTED_EDGE ( 'NONE', *, *, #39310, .F. ) ;
#20657=CARTESIAN_POINT ( 'NONE',  ( 24.76774681979610548, -3.098499905868568938, 11.74894159540815508 ) ) ;
#20658=CARTESIAN_POINT ( 'NONE',  ( 21.72233714749290101, 0.000000000000000000, -5.000000000000000000 ) ) ;
#20659=FACE_OUTER_BOUND ( 'NONE', #43787, .T. ) ;
#20667=ORIENTED_EDGE ( 'NONE', *, *, #6687, .F. ) ;
#20681=CARTESIAN_POINT ( 'NONE',  ( 11.92303154622255335, 11.77792023318604286, -4.262523390537997336 ) ) ;
#20693=DIRECTION ( 'NONE',  ( 0.000000000000000000, -0.8765967884314782577, 0.4812255921203881792 ) ) ;
#20699=VERTEX_POINT ( 'NONE', #63026 ) ;
#20710=CARTESIAN_POINT ( 'NONE',  ( 24.30001694968100168, 3.271769180623000040, -12.21048179117000032 ) ) ;
#20713=CARTESIAN_POINT ( 'NONE',  ( 18.30000000000000071, 2.775715947008034146, -11.68320807311170917 ) ) ;
#20714=CARTESIAN_POINT ( 'NONE',  ( 24.43231275843400141, 11.98247113617999915, 3.250307990934000024 ) ) ;
#20716=CARTESIAN_POINT ( 'NONE',  ( 23.64145609567900053, 13.18672912911000061, -4.069240593728999933 ) ) ;
#20730=CARTESIAN_POINT ( 'NONE',  ( 23.73952158721290218, 9.827654401539094309, -9.725498138330634035 ) ) ;
#20732=ORIENTED_EDGE ( 'NONE', *, *, #46236, .T. ) ;
#20733=CARTESIAN_POINT ( 'NONE',  ( 13.46053068095500116, 9.490401724732999256, 7.804222448269000800 ) ) ;
#20741=AXIS2_PLACEMENT_3D ( 'NONE', #40235, #7376, #61552 ) ;
#20746=ADVANCED_FACE ( 'NONE', ( #48342 ), #6616, .F. ) ;
#20747=CARTESIAN_POINT ( 'NONE',  ( 25.46371819568200223, 2.879482785682999868, 11.30954024936000124 ) ) ;
#20749=CARTESIAN_POINT ( 'NONE',  ( 12.79342929296800158, 12.04986812289999953, -3.196648259943000170 ) ) ;
#20750=CARTESIAN_POINT ( 'NONE',  ( 17.57198442900400082, 11.38892236470999997, -4.574426315356000750 ) ) ;
#20754=CARTESIAN_POINT ( 'NONE',  ( 18.12310803393399894, -3.320912951897000198, 11.92519506916999994 ) ) ;
#20756=ORIENTED_EDGE ( 'NONE', *, *, #16611, .T. ) ;
#20759=DIRECTION ( 'NONE',  ( 0.000000000000000000, 0.2714570858282905341, -0.9624505444715651947 ) ) ;
#20761=CARTESIAN_POINT ( 'NONE',  ( 25.60000000000000142, 0.000000000000000000, 0.000000000000000000 ) ) ;
#20767=ORIENTED_EDGE ( 'NONE', *, *, #56671, .F. ) ;
#20768=B_SPLINE_CURVE_WITH_KNOTS ( 'NONE', 3,
 ( #12798, #24312, #34126, #55443 ),
 .UNSPECIFIED., .F., .F.,
 ( 4, 4 ),
 ( 0.000000000000000000, 1.000000000000000000 ),
 .UNSPECIFIED. ) ;
#20776=CARTESIAN_POINT ( 'NONE',  ( 15.89994436294300151, -8.847904542234999781, -8.580301953175000662 ) ) ;
#20784=ORIENTED_EDGE ( 'NONE', *, *, #21909, .T. ) ;
#20787=EDGE_CURVE ( 'NONE', #22779, #5123, #34678, .T. ) ;
#20796=FACE_OUTER_BOUND ( 'NONE', #8342, .T. ) ;
#20797=CARTESIAN_POINT ( 'NONE',  ( 11.49999672495000169, -5.885481364898649481, 10.12743717035876223 ) ) ;
#20804=CARTESIAN_POINT ( 'NONE',  ( 16.09055856039299925, 8.515834468357001086, 7.893949987785000566 ) ) ;
#20805=VERTEX_POINT ( 'NONE', #17573 ) ;
#20810=ORIENTED_EDGE ( 'NONE', *, *, #44475, .T. ) ;
#20817=ORIENTED_EDGE ( 'NONE', *, *, #13284, .F. ) ;
#20818=CARTESIAN_POINT ( 'NONE',  ( 23.66004879239100234, -9.998911572074998588, 9.691526907171001071 ) ) ;
#20819=CARTESIAN_POINT ( 'NONE',  ( 24.09351921955576614, 12.55954825742757208, -3.397332434207054330 ) ) ;
#20822=FACE_OUTER_BOUND ( 'NONE', #9880, .T. ) ;
#20824=CARTESIAN_POINT ( 'NONE',  ( 24.23080198909943306, 12.32902557501668994, 3.306557022674655677 ) ) ;
#20846=CARTESIAN_POINT ( 'NONE',  ( 15.36385332268500115, 9.394483288005998745, 8.200629419667000874 ) ) ;
#20850=CARTESIAN_POINT ( 'NONE',  ( 23.56666365135700403, -2.488348886737001386, -11.45224114470000565 ) ) ;
#20856=CARTESIAN_POINT ( 'NONE',  ( 24.44496488041000148, -12.03536727282999941, 3.224852091355999928 ) ) ;
#20861=CARTESIAN_POINT ( 'NONE',  ( 25.59997255263800042, -11.07537722176000017, -3.096069202785999952 ) ) ;
#20864=CARTESIAN_POINT ( 'NONE',  ( 18.23043922992600230, 3.518658233831999826, 12.06062508533999988 ) ) ;
#20876=CARTESIAN_POINT ( 'NONE',  ( 11.50001496185000072, 5.131800295740712059, -11.50030236647292270 ) ) ;
#20879=VECTOR ( 'NONE', #32990, 1000.000000000000114 ) ;
#20882=CARTESIAN_POINT ( 'NONE',  ( 16.13854177342199847, -3.630911166246999944, -11.92992564462999994 ) ) ;
#20886=CARTESIAN_POINT ( 'NONE',  ( 25.60000000000000142, 2.258942858049999725, -12.29419282279000036 ) ) ;
#20900=B_SPLINE_CURVE_WITH_KNOTS ( 'NONE', 3,
 ( #21779, #31259, #63397, #30912, #16197, #37182 ),
 .UNSPECIFIED., .F., .F.,
 ( 4, 2, 4 ),
 ( 0.000000000000000000, 0.5000000000000000000, 1.000000000000000000 ),
 .UNSPECIFIED. ) ;
#20902=VERTEX_POINT ( 'NONE', #1146 ) ;
#20905=CARTESIAN_POINT ( 'NONE',  ( 24.35365242081700288, -8.355077740100997019, 8.511587483919999642 ) ) ;
#20912=ADVANCED_FACE ( 'NONE', ( #17219 ), #38901, .T. ) ;
#20915=VERTEX_POINT ( 'NONE', #49373 ) ;
#20921=CARTESIAN_POINT ( 'NONE',  ( 18.29998515896363287, 2.924733550950530336, -11.97422828356910607 ) ) ;
#20943=CARTESIAN_POINT ( 'NONE',  ( 14.46666666323366890, 9.471992681081614407, 8.194936219980966996 ) ) ;
#20948=CARTESIAN_POINT ( 'NONE',  ( 16.00000000266000555, 11.41071763148134544, -4.623975354790890613 ) ) ;
#20951=ORIENTED_EDGE ( 'NONE', *, *, #46261, .F. ) ;
#20955=CARTESIAN_POINT ( 'NONE',  ( 11.53681523859000002, 3.897571790034000117, -11.94316735528000173 ) ) ;
#20969=AXIS2_PLACEMENT_3D ( 'NONE', #57006, #25538, #46864 ) ;
#20971=CARTESIAN_POINT ( 'NONE',  ( 23.68315585345000329, 3.147788653374999690, 13.35041697813000106 ) ) ;
#20979=CARTESIAN_POINT ( 'NONE',  ( 23.97708694432106924, -3.345394741305891984, 12.79002816627185091 ) ) ;
#20983=CARTESIAN_POINT ( 'NONE',  ( 25.48370393093700059, -2.675493841248999694, -11.27075153412999953 ) ) ;
#20984=CIRCLE ( 'NONE', #31075, 1.300172478116999208 ) ;
#20986=CARTESIAN_POINT ( 'NONE',  ( 24.53428991268900106, -12.47024905405999995, -3.026245386525999947 ) ) ;
#20990=ORIENTED_EDGE ( 'NONE', *, *, #17119, .F. ) ;
#20997=CONICAL_SURFACE ( 'NONE', #9811, 12.71246950475999959, 0.8960553845711767273 ) ;
#20998=DIRECTION ( 'NONE',  ( 0.9999999999993943733, 9.646910165650955666E-07, -5.296687748115971159E-07 ) ) ;
#21012=ORIENTED_EDGE ( 'NONE', *, *, #31402, .T. ) ;
#21015=FACE_OUTER_BOUND ( 'NONE', #39696, .T. ) ;
#21016=B_SPLINE_CURVE_WITH_KNOTS ( 'NONE', 3,
 ( #52260, #68671, #41428, #30595 ),
 .UNSPECIFIED., .F., .F.,
 ( 4, 4 ),
 ( 0.000000000000000000, 1.000000000000000000 ),
 .UNSPECIFIED. ) ;
#21022=DIRECTION ( 'NONE',  ( -1.000000000000000000, 0.000000000000000000, 0.000000000000000000 ) ) ;
#21032=CARTESIAN_POINT ( 'NONE',  ( 17.79999999998900151, -3.595165934733000057, -11.99793354950999991 ) ) ;
#21034=AXIS2_PLACEMENT_3D ( 'NONE', #9268, #15566, #10653 ) ;
#21040=CARTESIAN_POINT ( 'NONE',  ( 23.60205915885299888, 11.88166580723999921, -3.967996863072999147 ) ) ;
#21053=EDGE_CURVE ( 'NONE', #13607, #5259, #23525, .T. ) ;
#21061=CARTESIAN_POINT ( 'NONE',  ( 24.02106212480699909, 12.55316173831000093, -3.484249586872999682 ) ) ;
#21065=ORIENTED_EDGE ( 'NONE', *, *, #3629, .F. ) ;
#21066=CARTESIAN_POINT ( 'NONE',  ( 13.69992376746900042, 12.26631831379999937, 2.532779022035999805 ) ) ;
#21072=CARTESIAN_POINT ( 'NONE',  ( 17.79416955086200147, -3.253172910778000304, 11.33701170283999993 ) ) ;
#21076=AXIS2_PLACEMENT_3D ( 'NONE', #41167, #47096, #10026 ) ;
#21077=CARTESIAN_POINT ( 'NONE',  ( 13.44051303026600053, 11.61511980691000012, 2.065108503055999911 ) ) ;
#21081=EDGE_LOOP ( 'NONE', ( #45421, #37145, #50647, #67247, #23822 ) ) ;
#21082=CARTESIAN_POINT ( 'NONE',  ( 16.03328789001813703, 8.397841793663578969, 8.170414199808826439 ) ) ;
#21084=ADVANCED_FACE ( 'NONE', ( #21683 ), #11237, .F. ) ;
#21088=CARTESIAN_POINT ( 'NONE',  ( 13.49980696792483137, 11.54838492169066022, 4.420196298692874670 ) ) ;
#21094=CARTESIAN_POINT ( 'NONE',  ( 12.64393528606200334, 11.55448221446000012, -4.935476321030999536 ) ) ;
#21095=CARTESIAN_POINT ( 'NONE',  ( 18.14021164098500094, 11.49417283396999956, -4.331891014347999835 ) ) ;
#21098=ADVANCED_FACE ( 'NONE', ( #53851 ), #16781, .F. ) ;
#21100=CARTESIAN_POINT ( 'NONE',  ( 18.26281727343199890, -2.856883730594999893, 11.95041273044000008 ) ) ;
#21122=DIRECTION ( 'NONE',  ( 0.000000000000000000, 2.692747184616903860E-07, -0.9999999999999636957 ) ) ;
#21123=CARTESIAN_POINT ( 'NONE',  ( 13.73937158902900180, 8.990218567665001714, 7.348698335466000486 ) ) ;
#21129=CARTESIAN_POINT ( 'NONE',  ( 18.11007341752287658, -3.284452655023379908, -11.17744038474783252 ) ) ;
#21131=EDGE_CURVE ( 'NONE', #18501, #31887, #44420, .T. ) ;
#21135=CARTESIAN_POINT ( 'NONE',  ( 16.39999999231800132, -3.216285993016000155, -11.40340220863999932 ) ) ;
#21142=CARTESIAN_POINT ( 'NONE',  ( 24.59231629583900158, -8.769512118076001173, -9.082544788674999481 ) ) ;
#21150=CARTESIAN_POINT ( 'NONE',  ( 13.67905361531532016, 11.43958844919915308, 2.204572756910269771 ) ) ;
#21154=CARTESIAN_POINT ( 'NONE',  ( 24.30000000000000071, 0.000000000000000000, 0.000000000000000000 ) ) ;
#21160=CARTESIAN_POINT ( 'NONE',  ( 24.37898895918399944, 12.00803319959000071, -3.275429579010999959 ) ) ;
#21161=CARTESIAN_POINT ( 'NONE',  ( 11.79999999550100220, -3.351258778187000242, 11.15757272551999968 ) ) ;
#21164=ORIENTED_EDGE ( 'NONE', *, *, #36724, .F. ) ;
#21165=CARTESIAN_POINT ( 'NONE',  ( 24.34832117038932964, 3.224867649022901794, 12.03536991383494303 ) ) ;
#21170=CARTESIAN_POINT ( 'NONE',  ( 23.84134131727602224, 12.96058960459414955, 3.649550007566405352 ) ) ;
#21173=ORIENTED_EDGE ( 'NONE', *, *, #1177, .F. ) ;
#21179=CARTESIAN_POINT ( 'NONE',  ( 25.59994555223600088, -10.09686240769181609, -5.033199831111830669 ) ) ;
#21182=DIRECTION ( 'NONE',  ( -4.063589742475669988E-14, 0.8660931406617480288, 0.4998826579295080341 ) ) ;
#21184=CARTESIAN_POINT ( 'NONE',  ( 12.50062609531600089, -11.46460001353999836, 4.648225426428999718 ) ) ;
#21188=AXIS2_PLACEMENT_3D ( 'NONE', #31046, #64207, #64552 ) ;
#21193=CARTESIAN_POINT ( 'NONE',  ( 25.29881449893400003, -11.38089007393000074, 3.116294150075999969 ) ) ;
#21197=CARTESIAN_POINT ( 'NONE',  ( 24.13682259839000110, 9.106542476583999957, 8.984439671043000786 ) ) ;
#21204=CARTESIAN_POINT ( 'NONE',  ( 18.26122879894100137, 2.828234032943000020, 11.95647652451000020 ) ) ;
#21217=CARTESIAN_POINT ( 'NONE',  ( 29.60000000000000142, 0.000000000000000000, -8.250000000000000000 ) ) ;
#21225=CARTESIAN_POINT ( 'NONE',  ( 11.80585503023100102, 11.57020517019000039, 1.758699328329000222 ) ) ;
#21235=VERTEX_POINT ( 'NONE', #3127 ) ;
#21238=ORIENTED_EDGE ( 'NONE', *, *, #18028, .T. ) ;
#21263=CARTESIAN_POINT ( 'NONE',  ( 23.66004879239100234, -13.39256464007999980, -3.813546745462999876 ) ) ;
#21264=CARTESIAN_POINT ( 'NONE',  ( 15.95377458853735853, 3.445704530244193098, 11.33538647441605640 ) ) ;
#21272=CARTESIAN_POINT ( 'NONE',  ( 18.44503807197100187, 2.664600154114999953, -11.39639460691000039 ) ) ;
#21280=EDGE_LOOP ( 'NONE', ( #608, #31152, #29569, #14306 ) ) ;
#21308=CARTESIAN_POINT ( 'NONE',  ( 25.60000000000000142, 2.976419018679000050, 11.10814700232000085 ) ) ;
#21309=CARTESIAN_POINT ( 'NONE',  ( 24.63626838744500347, 3.694701704419999899, 12.29747005844000007 ) ) ;
#21311=CYLINDRICAL_SURFACE ( 'NONE', #24340, 11.50000000000000178 ) ;
#21320=CARTESIAN_POINT ( 'NONE',  ( 25.27036424497699940, -2.549213983724999633, -11.36408287613999946 ) ) ;
#21324=CARTESIAN_POINT ( 'NONE',  ( 23.76529091359962464, 9.791724092508008681, 9.440860067983548376 ) ) ;
#21326=ORIENTED_EDGE ( 'NONE', *, *, #46796, .T. ) ;
#21329=CARTESIAN_POINT ( 'NONE',  ( 24.63329087101643111, -8.756202933458791193, 7.455126436760659558 ) ) ;
#21340=CARTESIAN_POINT ( 'NONE',  ( 24.53428988874600236, -8.855929874993998752, -9.286429786912000495 ) ) ;
#21353=CARTESIAN_POINT ( 'NONE',  ( 11.43336398472434645, 11.63122337162911002, 1.412340616368904067 ) ) ;
#21367=CARTESIAN_POINT ( 'NONE',  ( 17.60000001947600268, -11.86186880240999919, 3.298627760718999991 ) ) ;
#21372=CARTESIAN_POINT ( 'NONE',  ( 24.32158572772383920, -9.044138607853493994, 9.474428397134387225 ) ) ;
#21389=CARTESIAN_POINT ( 'NONE',  ( 15.40000000005200143, 9.187454762873001002, 8.213177997099000649 ) ) ;
#21392=CARTESIAN_POINT ( 'NONE',  ( 11.50001544675000176, -10.90724927943889710, 6.294778943836956131 ) ) ;
#21393=CARTESIAN_POINT ( 'NONE',  ( 23.81723165750307913, 9.687177923879790598, -9.414241483045064030 ) ) ;
#21396=VERTEX_POINT ( 'NONE', #59705 ) ;
#21403=ADVANCED_FACE ( 'NONE', ( #21948 ), #43288, .F. ) ;
#21404=CARTESIAN_POINT ( 'NONE',  ( 25.29986325275000070, 2.258942858049999725, 12.29419282279000036 ) ) ;
#21405=CARTESIAN_POINT ( 'NONE',  ( 24.07541911252200251, 3.340244713972364998, -12.60849197320232129 ) ) ;
#21406=DIRECTION ( 'NONE',  ( 0.000000000000000000, 0.000000000000000000, -1.000000000000000000 ) ) ;
#21410=CARTESIAN_POINT ( 'NONE',  ( 13.08018231457700153, 11.57028798436999928, 1.758177683552999859 ) ) ;
#21413=VERTEX_POINT ( 'NONE', #49214 ) ;
#21418=CARTESIAN_POINT ( 'NONE',  ( 18.15856293744596783, 11.79508858035351970, -3.559060952131059885 ) ) ;
#21422=CARTESIAN_POINT ( 'NONE',  ( 12.13190478341600098, 11.96733320521999921, -3.503025077341000326 ) ) ;
#21423=CARTESIAN_POINT ( 'NONE',  ( 18.12406690321100200, 11.75515418280000013, -3.561236062516000000 ) ) ;
#21438=CARTESIAN_POINT ( 'NONE',  ( 13.64750315638899991, 9.067203425066999500, 7.400836607049000371 ) ) ;
#21453=CARTESIAN_POINT ( 'NONE',  ( 16.44832727683000329, -3.192413998985999868, -11.44999110620999794 ) ) ;
#21454=ADVANCED_FACE ( 'NONE', ( #54462 ), #39078, .T. ) ;
#21459=AXIS2_PLACEMENT_3D ( 'NONE', #68358, #67077, #42495 ) ;
#21460=ADVANCED_FACE ( 'NONE', ( #11458 ), #44626, .F. ) ;
#21464=ORIENTED_EDGE ( 'NONE', *, *, #12478, .T. ) ;
#21467=DIRECTION ( 'NONE',  ( 1.000000000000000000, 0.000000000000000000, 0.000000000000000000 ) ) ;
#21471=CARTESIAN_POINT ( 'NONE',  ( 25.27036124584200039, -11.11619549273000018, -3.474353012118999828 ) ) ;
#21474=CARTESIAN_POINT ( 'NONE',  ( 24.53428985367600390, -3.614319203926000146, 12.31267510079000083 ) ) ;
#21476=FACE_OUTER_BOUND ( 'NONE', #40164, .T. ) ;
#21488=CARTESIAN_POINT ( 'NONE',  ( 14.93333333119166717, -9.187454790032713703, -8.213178404203524963 ) ) ;
#21495=DIRECTION ( 'NONE',  ( 0.9999999999993943733, -9.646910167131952540E-07, 5.296687751076970703E-07 ) ) ;
#21500=ORIENTED_EDGE ( 'NONE', *, *, #13886, .T. ) ;
#21505=CARTESIAN_POINT ( 'NONE',  ( 15.95458079702100029, 3.771493919207000278, 11.78965436225000118 ) ) ;
#21507=CARTESIAN_POINT ( 'NONE',  ( 24.30000000000000071, 0.000000000000000000, 0.000000000000000000 ) ) ;
#21510=CARTESIAN_POINT ( 'NONE',  ( 13.69996357384221497, -12.28513767539741863, -2.441259368852444211 ) ) ;
#21515=DIRECTION ( 'NONE',  ( -1.000000000000000000, 0.000000000000000000, 0.000000000000000000 ) ) ;
#21519=CARTESIAN_POINT ( 'NONE',  ( 23.59999443371599881, 2.915558930973999985, 13.58549620949000136 ) ) ;
#21530=DIRECTION ( 'NONE',  ( -0.000000000000000000, -0.9999988959613604900, -0.001485959642859940649 ) ) ;
#21533=CARTESIAN_POINT ( 'NONE',  ( 24.26682857475500299, -8.952388712744999921, -8.898287395196000205 ) ) ;
#21552=CARTESIAN_POINT ( 'NONE',  ( 23.56664311700400205, 13.31365802054999925, 4.296923094388999331 ) ) ;
#21560=CARTESIAN_POINT ( 'NONE',  ( 11.66889198508049930, 11.69116221025808322, 1.923144176179721887 ) ) ;
#21561=CARTESIAN_POINT ( 'NONE',  ( 11.53713099069000059, 11.52702260260000067, 1.399766873409999945 ) ) ;
#21562=ORIENTED_EDGE ( 'NONE', *, *, #53436, .T. ) ;
#21565=CARTESIAN_POINT ( 'NONE',  ( 24.71801055494115928, -8.650035796533028787, -8.600711262961937109 ) ) ;
#21578=CARTESIAN_POINT ( 'NONE',  ( 15.91587707751000025, -9.040653309694000939, -8.458480061295000851 ) ) ;
#21584=CARTESIAN_POINT ( 'NONE',  ( 24.67921569845699992, 12.29514839105000057, -2.979196030862000022 ) ) ;
#21585=CARTESIAN_POINT ( 'NONE',  ( 21.72233714749290101, 5.999764115230404649, -0.05320302240984255138 ) ) ;
#21588=DIRECTION ( 'NONE',  ( -0.000000000000000000, 0.3222656952305000266, 0.9466492601157001641 ) ) ;
#21591=DIRECTION ( 'NONE',  ( 1.000000000000000000, 0.000000000000000000, 0.000000000000000000 ) ) ;
#21593=CARTESIAN_POINT ( 'NONE',  ( 11.35642168284000242, -12.27417251877000126, -1.600391102631000040 ) ) ;
#21599=ADVANCED_FACE ( 'NONE', ( #9220 ), #19726, .T. ) ;
#21601=EDGE_CURVE ( 'NONE', #43538, #25292, #19044, .T. ) ;
#21604=CARTESIAN_POINT ( 'NONE',  ( 18.35296092448800209, 2.690559717027000364, 11.48481263514000084 ) ) ;
#21607=EDGE_CURVE ( 'NONE', #54071, #16464, #29840, .T. ) ;
#21611=CARTESIAN_POINT ( 'NONE',  ( 17.76418844530500252, 3.313976920866999798, -11.22406790378000174 ) ) ;
#21612=AXIS2_PLACEMENT_3D ( 'NONE', #42258, #35297, #19552 ) ;
#21615=CARTESIAN_POINT ( 'NONE',  ( 24.42399542544800184, -8.980643143459998257, -9.517742859132999556 ) ) ;
#21617=CARTESIAN_POINT ( 'NONE',  ( 11.60581233665799950, -3.287326773434000149, 11.32699406611000015 ) ) ;
#21618=ORIENTED_EDGE ( 'NONE', *, *, #49164, .F. ) ;
#21622=CARTESIAN_POINT ( 'NONE',  ( 24.70869262301700076, 8.717234922402001374, -9.201991544579998461 ) ) ;
#21625=AXIS2_PLACEMENT_3D ( 'NONE', #60010, #2659, #38689 ) ;
#21628=CIRCLE ( 'NONE', #57365, 1.000000000000000000 ) ;
#21631=CARTESIAN_POINT ( 'NONE',  ( 24.30000000000000071, -10.83443035398000021, 3.855530949778000149 ) ) ;
#21632=ORIENTED_EDGE ( 'NONE', *, *, #23488, .T. ) ;
#21644=CARTESIAN_POINT ( 'NONE',  ( 23.99166244369300216, 3.573271009703999912, 12.95730409900999902 ) ) ;
#21645=ORIENTED_EDGE ( 'NONE', *, *, #40023, .T. ) ;
#21646=CARTESIAN_POINT ( 'NONE',  ( 25.09888444479172520, -11.37375950780082512, -3.274676351230203064 ) ) ;
#21648=ADVANCED_FACE ( 'NONE', ( #42765 ), #33432, .F. ) ;
#21651=B_SPLINE_SURFACE_WITH_KNOTS ( 'NONE', 3, 3, ( 
 ( #40464, #2043, #14254, #3402 ),
 ( #56552, #55524, #66343, #28971 ),
 ( #7625, #18466, #19493, #7280 ),
 ( #4771, #67710, #46410, #14932 ),
 ( #20864, #62472, #26113, #5124 ),
 ( #68058, #62813, #57929, #57228 ),
 ( #30337, #31707, #25075, #10369 ),
 ( #20172, #25766, #42202, #52676 ),
 ( #26460, #20519, #30672, #36952 ),
 ( #36255, #58266, #56896, #21204 ) ),
 .UNSPECIFIED., .F., .F., .F.,
 ( 4, 1, 1, 1, 1, 1, 1, 4 ),
 ( 4, 4 ),
 ( 0.07203983506773999068, 0.1428571428570999946, 0.2857142857143000203, 0.4285714285713999594, 0.5714285714286000406, 0.7142857142856999797, 0.8571428571429000609, 0.9589780836993999635 ),
 ( -0.1900620218102000158, 1.190128522698000069 ),
 .UNSPECIFIED. ) ;
#21659=CARTESIAN_POINT ( 'NONE',  ( 23.56666365135700403, 11.07911597678999271, 4.076188921308005142 ) ) ;
#21672=ORIENTED_EDGE ( 'NONE', *, *, #61788, .F. ) ;
#21673=AXIS2_PLACEMENT_3D ( 'NONE', #28358, #50025, #60857 ) ;
#21677=CARTESIAN_POINT ( 'NONE',  ( 11.83148568236900111, 12.32826180562000040, 1.876276850727000012 ) ) ;
#21683=FACE_OUTER_BOUND ( 'NONE', #35176, .T. ) ;
#21704=CYLINDRICAL_SURFACE ( 'NONE', #49464, 0.6999999999999992895 ) ;
#21732=CARTESIAN_POINT ( 'NONE',  ( 24.14647270089509590, 9.145016144872478492, -9.120921824230352470 ) ) ;
#21735=AXIS2_PLACEMENT_3D ( 'NONE', #38596, #44892, #32669 ) ;
#21751=CARTESIAN_POINT ( 'NONE',  ( 13.32922381500400100, 11.63215034022999994, 1.960198572322999988 ) ) ;
#21757=VERTEX_POINT ( 'NONE', #54638 ) ;
#21768=ORIENTED_EDGE ( 'NONE', *, *, #22869, .T. ) ;
#21769=CARTESIAN_POINT ( 'NONE',  ( 12.66849918197500102, 12.16651130357000099, -3.137066692814999946 ) ) ;
#21770=CARTESIAN_POINT ( 'NONE',  ( 18.38283964371600376, 11.91307312420999942, -3.686993282830000052 ) ) ;
#21773=CARTESIAN_POINT ( 'NONE',  ( 25.59994555223599733, -2.024003533649000097, 11.01554633311000053 ) ) ;
#21774=CARTESIAN_POINT ( 'NONE',  ( 18.47691931228784057, 11.93204885577847030, -3.809797076885868439 ) ) ;
#21779=CARTESIAN_POINT ( 'NONE',  ( 11.79999999550100220, 11.52577121388000059, 1.696750555870000010 ) ) ;
#21782=FACE_OUTER_BOUND ( 'NONE', #31874, .T. ) ;
#21799=CARTESIAN_POINT ( 'NONE',  ( 16.39974593105000267, -3.376006003137999922, -11.11079012987999981 ) ) ;
#21803=B_SPLINE_SURFACE_WITH_KNOTS ( 'NONE', 3, 3, ( 
 ( #21938, #280, #22977, #54797 ),
 ( #1313, #11450, #28233, #49548 ),
 ( #38371, #39069, #21593, #16353 ),
 ( #42932, #33830, #5860, #6199 ),
 ( #32789, #59695, #628, #37682 ),
 ( #11796, #44326, #43974, #7247 ),
 ( #976, #17392, #38722, #48868 ),
 ( #65280, #33136, #54452, #1661 ),
 ( #6553, #55144, #27896, #49206 ) ),
 .UNSPECIFIED., .F., .F., .F.,
 ( 4, 1, 1, 1, 1, 1, 4 ),
 ( 4, 4 ),
 ( 0.02288375853139000202, 0.1666666666667000196, 0.3333333333333000081, 0.5000000000000000000, 0.6666666666667000474, 0.8333333333333000637, 0.9485331614075999118 ),
 ( -0.1900389547208000129, 1.190219847277000031 ),
 .UNSPECIFIED. ) ;
#21807=B_SPLINE_CURVE_WITH_KNOTS ( 'NONE', 3,
 ( #2299, #28534, #61028, #18043 ),
 .UNSPECIFIED., .F., .F.,
 ( 4, 4 ),
 ( 0.000000000000000000, 1.000000000000000000 ),
 .UNSPECIFIED. ) ;
#21818=CARTESIAN_POINT ( 'NONE',  ( 13.69997185827400266, -11.40547114375999982, -2.374390024598000082 ) ) ;
#21824=ORIENTED_EDGE ( 'NONE', *, *, #53131, .F. ) ;
#21827=VECTOR ( 'NONE', #463, 999.9999999999998863 ) ;
#21833=CARTESIAN_POINT ( 'NONE',  ( 15.90006914250090198, -3.698856701507905687, -11.75540275481944619 ) ) ;
#21834=DIRECTION ( 'NONE',  ( 0.000000000000000000, 0.000000000000000000, -1.000000000000000000 ) ) ;
#21837=CARTESIAN_POINT ( 'NONE',  ( 24.56891981372000089, 12.04603233683999974, -3.139955828721999964 ) ) ;
#21839=ORIENTED_EDGE ( 'NONE', *, *, #11738, .T. ) ;
#21843=CARTESIAN_POINT ( 'NONE',  ( 23.58115046238600954, -10.23378857499904804, 9.530750715746675539 ) ) ;
#21847=CARTESIAN_POINT ( 'NONE',  ( 16.39932787941000214, 3.295363098100999810, 11.83520513879000013 ) ) ;
#21854=ORIENTED_EDGE ( 'NONE', *, *, #38511, .T. ) ;
#21858=CARTESIAN_POINT ( 'NONE',  ( 17.60000003185799855, -12.11983897296999935, 3.159727888982000188 ) ) ;
#21864=ORIENTED_EDGE ( 'NONE', *, *, #17138, .F. ) ;
#21871=CARTESIAN_POINT ( 'NONE',  ( 13.69997185827400266, 11.40547114375999982, 2.374390024598000082 ) ) ;
#21873=AXIS2_PLACEMENT_3D ( 'NONE', #62050, #56118, #20088 ) ;
#21874=EDGE_CURVE ( 'NONE', #50564, #59819, #45892, .T. ) ;
#21875=CARTESIAN_POINT ( 'NONE',  ( 24.36809152945900081, -8.862862741694000235, -8.808753452432000586 ) ) ;
#21876=AXIS2_PLACEMENT_3D ( 'NONE', #21585, #15999, #5512 ) ;
#21881=CARTESIAN_POINT ( 'NONE',  ( 12.79999999468004646, 11.20144845259485678, -4.552734317499857575 ) ) ;
#21882=ORIENTED_EDGE ( 'NONE', *, *, #53954, .T. ) ;
#21885=LINE ( 'NONE', #32396, #31608 ) ;
#21903=CARTESIAN_POINT ( 'NONE',  ( 11.56631965465000178, 11.51200727500000021, 1.523108403756999962 ) ) ;
#21904=ORIENTED_EDGE ( 'NONE', *, *, #16042, .T. ) ;
#21905=CARTESIAN_POINT ( 'NONE',  ( 16.10004050617000004, -3.886235259787000018, -11.90683839252000098 ) ) ;
#21906=CARTESIAN_POINT ( 'NONE',  ( 16.39999999270239428, -3.259293166955308685, -11.55581727975966544 ) ) ;
#21909=EDGE_CURVE ( 'NONE', #66745, #47384, #56567, .T. ) ;
#21922=AXIS2_PLACEMENT_3D ( 'NONE', #56318, #12988, #45825 ) ;
#21923=CARTESIAN_POINT ( 'NONE',  ( 15.64816728597000228, -9.503848651356001653, -8.217120907884000403 ) ) ;
#21938=CARTESIAN_POINT ( 'NONE',  ( 11.53898320224999985, -12.47165320829000024, -1.511147746418000093 ) ) ;
#21943=CARTESIAN_POINT ( 'NONE',  ( 24.30000565603569029, 12.09374148929426163, 3.240508265528289744 ) ) ;
#21944=CARTESIAN_POINT ( 'NONE',  ( 24.15348338235900272, -12.81658634417999920, 3.250012531303999808 ) ) ;
#21946=DIRECTION ( 'NONE',  ( 0.000000000000000000, 0.000000000000000000, -1.000000000000000000 ) ) ;
#21948=FACE_OUTER_BOUND ( 'NONE', #24007, .T. ) ;
#21952=CARTESIAN_POINT ( 'NONE',  ( 11.30000285318000230, -11.76356368987999979, -1.428410073821000159 ) ) ;
#21955=EDGE_CURVE ( 'NONE', #50878, #24248, #28216, .T. ) ;
#21958=CARTESIAN_POINT ( 'NONE',  ( 23.85319031184999972, -9.641546400920999460, -9.631730852994000003 ) ) ;
#21959=CARTESIAN_POINT ( 'NONE',  ( 23.83528395833900149, -9.657441433821000842, 9.482667428683999589 ) ) ;
#21960=CARTESIAN_POINT ( 'NONE',  ( 23.59999193302000364, -13.22318594659000013, 4.267778254689999606 ) ) ;
#21961=CIRCLE ( 'NONE', #39854, 0.6999999999999992895 ) ;
#21962=ORIENTED_EDGE ( 'NONE', *, *, #5726, .F. ) ;
#21966=CARTESIAN_POINT ( 'NONE',  ( 21.70000133425200062, -14.00000000000000000, 0.000000000000000000 ) ) ;
#21982=ORIENTED_EDGE ( 'NONE', *, *, #30558, .F. ) ;
#21983=CARTESIAN_POINT ( 'NONE',  ( 24.26682857475500299, 12.18233729078999872, -3.303852352193000108 ) ) ;
#21984=CARTESIAN_POINT ( 'NONE',  ( 12.79272103475300071, -12.16747052068999935, 3.133256626080000107 ) ) ;
#21990=CARTESIAN_POINT ( 'NONE',  ( 25.12925491921549082, -11.33917288839387894, -3.290749069845217978 ) ) ;
#21994=EDGE_CURVE ( 'NONE', #59240, #56220, #49006, .T. ) ;
#21995=EDGE_CURVE ( 'NONE', #63587, #17060, #29139, .T. ) ;
#22001=CARTESIAN_POINT ( 'NONE',  ( 25.29987654162099986, -8.533547851352999203, -7.925583806936000286 ) ) ;
#22009=CARTESIAN_POINT ( 'NONE',  ( 25.29986325275000070, 2.258942858049999725, 12.29419282279000036 ) ) ;
#22013=CARTESIAN_POINT ( 'NONE',  ( 14.03164332880499998, 9.396061154353999356, 8.198822423776999102 ) ) ;
#22022=CARTESIAN_POINT ( 'NONE',  ( 13.69992376746900042, -12.26631831379999937, -2.532779022035999805 ) ) ;
#22034=CARTESIAN_POINT ( 'NONE',  ( 23.60000000000000142, 11.85420044612000012, -3.901016762742000488 ) ) ;
#22044=CARTESIAN_POINT ( 'NONE',  ( 12.25178171628595081, 12.07365382811639165, -3.333154641345941638 ) ) ;
#22050=CARTESIAN_POINT ( 'NONE',  ( 25.60000000000000142, -2.258942858049999725, -12.29419282279000036 ) ) ;
#22053=CARTESIAN_POINT ( 'NONE',  ( 23.75089958727604156, -9.822232532321159226, -9.446477853357983179 ) ) ;
#22056=B_SPLINE_CURVE_WITH_KNOTS ( 'NONE', 3,
 ( #52634, #9636, #57189, #36911 ),
 .UNSPECIFIED., .F., .F.,
 ( 4, 4 ),
 ( 0.000000000000000000, 1.000000000000000000 ),
 .UNSPECIFIED. ) ;
#22059=CARTESIAN_POINT ( 'NONE',  ( 11.30000000000000071, 11.91995148090331291, 1.454135501518458273 ) ) ;
#22063=CARTESIAN_POINT ( 'NONE',  ( 18.22958240947727049, -10.92137759501516747, 4.055351289594743669 ) ) ;
#22067=CARTESIAN_POINT ( 'NONE',  ( 18.22510524369412366, -11.54189923439562016, 4.316434404174353645 ) ) ;
#22080=CARTESIAN_POINT ( 'NONE',  ( 23.91316333055113574, 9.510235985825241656, -9.347881497660901928 ) ) ;
#22091=CARTESIAN_POINT ( 'NONE',  ( 24.22569643261628869, 3.306137007861563060, -12.33866433766620929 ) ) ;
#22092=CARTESIAN_POINT ( 'NONE',  ( 18.12922381500399993, -3.157787539580000136, 11.36563583066999961 ) ) ;
#22097=CARTESIAN_POINT ( 'NONE',  ( 13.46087891924500113, 11.63300053112000043, 2.447944685581000090 ) ) ;
#22102=EDGE_CURVE ( 'NONE', #30666, #7406, #34042, .T. ) ;
#22104=ORIENTED_EDGE ( 'NONE', *, *, #58166, .T. ) ;
#22105=CARTESIAN_POINT ( 'NONE',  ( 11.53144129764059400, -11.54570453160568810, -1.556370871282598101 ) ) ;
#22106=LINE ( 'NONE', #23147, #55080 ) ;
#22108=CARTESIAN_POINT ( 'NONE',  ( 24.74122194148825216, -8.638774282505121249, 8.580579725866343210 ) ) ;
#22109=CARTESIAN_POINT ( 'NONE',  ( 18.21034928235495087, 11.77436611584341009, -3.633175583793197827 ) ) ;
#22111=LINE ( 'NONE', #57536, #63475 ) ;
#22112=AXIS2_PLACEMENT_3D ( 'NONE', #32297, #20759, #26005 ) ;
#22115=ORIENTED_EDGE ( 'NONE', *, *, #26753, .F. ) ;
#22117=CARTESIAN_POINT ( 'NONE',  ( 18.05092722032200214, 11.89802509695999966, -3.395950604129000183 ) ) ;
#22121=CARTESIAN_POINT ( 'NONE',  ( 12.62607976188021119, -11.85836615252176074, 3.313854784738198500 ) ) ;
#22123=CARTESIAN_POINT ( 'NONE',  ( 18.06944243593800081, -3.222040310929999762, 11.85748006108999952 ) ) ;
#22126=CARTESIAN_POINT ( 'NONE',  ( 13.49980696793000057, 9.514462421839999351, 7.834836582454001608 ) ) ;
#22127=AXIS2_PLACEMENT_3D ( 'NONE', #61822, #40168, #13602 ) ;
#22129=EDGE_CURVE ( 'NONE', #35108, #44937, #65987, .T. ) ;
#22131=CARTESIAN_POINT ( 'NONE',  ( 21.60000000000000142, 0.000000000000000000, 0.000000000000000000 ) ) ;
#22138=B_SPLINE_CURVE_WITH_KNOTS ( 'NONE', 3,
 ( #44041, #10832, #17466, #65346 ),
 .UNSPECIFIED., .F., .F.,
 ( 4, 4 ),
 ( 0.000000000000000000, 1.000000000000000000 ),
 .UNSPECIFIED. ) ;
#22140=ORIENTED_EDGE ( 'NONE', *, *, #49385, .T. ) ;
#22152=CARTESIAN_POINT ( 'NONE',  ( 24.50399615158200106, -3.502219942208999903, 12.23695409027999936 ) ) ;
#22156=CARTESIAN_POINT ( 'NONE',  ( 25.47111508646500155, -8.417200813839000872, 7.979926646001998414 ) ) ;
#22157=FACE_OUTER_BOUND ( 'NONE', #34578, .T. ) ;
#22159=CARTESIAN_POINT ( 'NONE',  ( 13.50000000000000178, -11.75776087185402474, -2.440894935388740361 ) ) ;
#22161=PRODUCT_CONTEXT ( 'NONE', #40042, 'mechanical' ) ;
#22167=CIRCLE ( 'NONE', #21034, 5.000000000000000000 ) ;
#22168=CARTESIAN_POINT ( 'NONE',  ( 13.08701341325400236, 12.43401476831999908, 1.800486563913999971 ) ) ;
#22170=FACE_OUTER_BOUND ( 'NONE', #53723, .T. ) ;
#22174=CARTESIAN_POINT ( 'NONE',  ( 24.72251023531952541, 8.647827846133015584, -8.596833533768670321 ) ) ;
#22177=CARTESIAN_POINT ( 'NONE',  ( 23.65871306847106936, -13.20934029255680642, 3.970304306148825013 ) ) ;
#22184=CARTESIAN_POINT ( 'NONE',  ( 25.52469358993199933, 11.20852883979999959, -3.138567732544999878 ) ) ;
#22187=ORIENTED_EDGE ( 'NONE', *, *, #8797, .F. ) ;
#22189=AXIS2_PLACEMENT_3D ( 'NONE', #13542, #24709, #45352 ) ;
#22198=CARTESIAN_POINT ( 'NONE',  ( 16.18326532032400067, 3.458591647041000083, 11.88419159288000060 ) ) ;
#22204=CARTESIAN_POINT ( 'NONE',  ( 18.50055606950828135, -11.89493552632996476, 3.924423580214191798 ) ) ;
#22206=DIRECTION ( 'NONE',  ( 0.000000000000000000, -0.1807154286440006141, 0.9835354258236025382 ) ) ;
#22209=CARTESIAN_POINT ( 'NONE',  ( 24.95780670450700001, -3.530138962360999777, 11.86562507170999936 ) ) ;
#22210=EDGE_LOOP ( 'NONE', ( #9803, #50397, #59429, #48239 ) ) ;
#22211=ORIENTED_EDGE ( 'NONE', *, *, #37057, .T. ) ;
#22214=EDGE_CURVE ( 'NONE', #7968, #25005, #32468, .T. ) ;
#22224=CARTESIAN_POINT ( 'NONE',  ( 24.36453968238300050, -8.917854847619999248, -9.043337665091998545 ) ) ;
#22229=CARTESIAN_POINT ( 'NONE',  ( 11.80000000000000071, 50.50083396221999976, 8.814205526695999993 ) ) ;
#22231=CARTESIAN_POINT ( 'NONE',  ( 23.73952313311524875, -3.508704810469513546, 13.37374458792384679 ) ) ;
#22234=CARTESIAN_POINT ( 'NONE',  ( 13.50018479229300006, -11.60142623882999935, -2.415183939829000259 ) ) ;
#22236=CARTESIAN_POINT ( 'NONE',  ( 19.39373726536100051, -11.26964301940000013, 0.000000000000000000 ) ) ;
#22245=VERTEX_POINT ( 'NONE', #46049 ) ;
#22251=CARTESIAN_POINT ( 'NONE',  ( 11.50000196593843071, 12.42140789277164714, 1.609557074791108988 ) ) ;
#22258=CARTESIAN_POINT ( 'NONE',  ( 24.89078534325364345, -8.576153783899114202, -8.441099479427823127 ) ) ;
#22276=ADVANCED_FACE ( 'NONE', ( #50951 ), #61777, .F. ) ;
#22281=B_SPLINE_CURVE_WITH_KNOTS ( 'NONE', 3,
 ( #19118, #51282, #51618, #25052 ),
 .UNSPECIFIED., .F., .F.,
 ( 4, 4 ),
 ( 0.000000000000000000, 1.000000000000000000 ),
 .UNSPECIFIED. ) ;
#22287=ORIENTED_EDGE ( 'NONE', *, *, #11789, .T. ) ;
#22288=CIRCLE ( 'NONE', #61372, 0.6999999999999992895 ) ;
#22289=LINE ( 'NONE', #27542, #27799 ) ;
#22294=CARTESIAN_POINT ( 'NONE',  ( 23.95109860005200275, 12.88176655920999991, 3.489107522193000133 ) ) ;
#22304=EDGE_CURVE ( 'NONE', #31293, #47655, #242, .T. ) ;
#22305=CARTESIAN_POINT ( 'NONE',  ( 23.61354982155200233, -10.15571182854999854, -9.483312721863999428 ) ) ;
#22306=CARTESIAN_POINT ( 'NONE',  ( 24.45265751162000356, -8.898665285767000555, 9.226266223847000347 ) ) ;
#22307=CARTESIAN_POINT ( 'NONE',  ( 25.59997277611800115, 2.578802611042650509E-13, -11.19994871957399241 ) ) ;
#22315=ORIENTED_EDGE ( 'NONE', *, *, #26881, .F. ) ;
#22319=PLANE ( 'NONE',  #62204 ) ;
#22329=EDGE_CURVE ( 'NONE', #3814, #66584, #11241, .T. ) ;
#22330=EDGE_CURVE ( 'NONE', #37494, #15848, #8542, .T. ) ;
#22331=CARTESIAN_POINT ( 'NONE',  ( 12.56257882282300109, -11.80639483233000142, 3.358960109135999961 ) ) ;
#22336=CARTESIAN_POINT ( 'NONE',  ( 18.50003594167399967, -2.686563651857999613, -11.33603604486000016 ) ) ;
#22337=ORIENTED_EDGE ( 'NONE', *, *, #22873, .F. ) ;
#22338=CARTESIAN_POINT ( 'NONE',  ( 24.76114890596840823, -11.73048710026287722, -3.191743628542212274 ) ) ;
#22339=ADVANCED_FACE ( 'NONE', ( #66330 ), #14515, .F. ) ;
#22347=CARTESIAN_POINT ( 'NONE',  ( 24.45387735997000078, 12.43793564427999954, -3.092859717916999873 ) ) ;
#22357=FACE_OUTER_BOUND ( 'NONE', #13480, .T. ) ;
#22358=EDGE_CURVE ( 'NONE', #44124, #31242, #19442, .T. ) ;
#22360=CARTESIAN_POINT ( 'NONE',  ( 23.89320776801300283, 3.226867021032998828, -11.46303308821000044 ) ) ;
#22362=CARTESIAN_POINT ( 'NONE',  ( 17.99398900912800059, -11.43764524146999939, 4.465475029564999865 ) ) ;
#22373=CARTESIAN_POINT ( 'NONE',  ( 11.44730853405000204, 12.38161968051000095, 1.492087993499999987 ) ) ;
#22377=DIRECTION ( 'NONE',  ( 0.000000000000000000, -0.7071067811865475727, 0.7071067811865475727 ) ) ;
#22382=CARTESIAN_POINT ( 'NONE',  ( 24.41555930013399944, -3.181808913646000381, -12.02251225967000003 ) ) ;
#22393=ORIENTED_EDGE ( 'NONE', *, *, #26671, .T. ) ;
#22399=CARTESIAN_POINT ( 'NONE',  ( 24.37816199240487691, 8.911180165120670793, -9.054574436677963689 ) ) ;
#22400=DIRECTION ( 'NONE',  ( -0.9999999999848602217, -4.443944959675825629E-06, 3.245118986823870102E-06 ) ) ;
#22403=CARTESIAN_POINT ( 'NONE',  ( 23.99447187923627567, -9.375551851464123843, -9.276312528594363727 ) ) ;
#22404=CARTESIAN_POINT ( 'NONE',  ( 12.52002425203546920, -12.10842255864623240, 3.203403679956746242 ) ) ;
#22405=CARTESIAN_POINT ( 'NONE',  ( 23.50387503050299998, 0.000000000000000000, 0.000000000000000000 ) ) ;
#22408=CARTESIAN_POINT ( 'NONE',  ( 23.95121877702899837, 3.419245466583000326, -12.90028367964000111 ) ) ;
#22409=VERTEX_POINT ( 'NONE', #4759 ) ;
#22410=FACE_OUTER_BOUND ( 'NONE', #28941, .T. ) ;
#22411=CARTESIAN_POINT ( 'NONE',  ( 17.91920925550954991, -10.80976535601232413, 4.345114692423678981 ) ) ;
#22415=CARTESIAN_POINT ( 'NONE',  ( 17.98087424867483008, -3.330341796647162234, 11.16384340189062740 ) ) ;
#22426=CARTESIAN_POINT ( 'NONE',  ( 12.38745432767040633, -10.82911002787651533, 4.296468796485326536 ) ) ;
#22438=CARTESIAN_POINT ( 'NONE',  ( 18.44383669537300108, -2.795303817231000298, 11.36579926027000020 ) ) ;
#22440=DIRECTION ( 'NONE',  ( 0.000000000000000000, -0.9989394889116069987, -0.04604234456473054599 ) ) ;
#22449=DIRECTION ( 'NONE',  ( -1.000000000000000000, 0.000000000000000000, 0.000000000000000000 ) ) ;
#22471=B_SPLINE_CURVE_WITH_KNOTS ( 'NONE', 3,
 ( #48300, #36787, #10895, #53203, #42379, #4963 ),
 .UNSPECIFIED., .F., .F.,
 ( 4, 2, 4 ),
 ( 0.000000000000000000, 0.5000000000000000000, 1.000000000000000000 ),
 .UNSPECIFIED. ) ;
#22473=ADVANCED_FACE ( 'NONE', ( #58596 ), #41399, .T. ) ;
#22486=CARTESIAN_POINT ( 'NONE',  ( 11.53926809187918856, -3.396911444218373877, 11.84566364033329400 ) ) ;
#22489=CARTESIAN_POINT ( 'NONE',  ( 11.68591862085600219, 3.663505620393999962, -12.01771987839999944 ) ) ;
#22495=CARTESIAN_POINT ( 'NONE',  ( 24.54687940532799928, -3.662828524876999836, 12.34579568540000061 ) ) ;
#22501=ORIENTED_EDGE ( 'NONE', *, *, #58555, .F. ) ;
#22502=CARTESIAN_POINT ( 'NONE',  ( 25.59994555223600088, 10.09686240769121568, -5.033199831113227773 ) ) ;
#22505=DIRECTION ( 'NONE',  ( -1.000000000000000000, 0.000000000000000000, 0.000000000000000000 ) ) ;
#22506=CARTESIAN_POINT ( 'NONE',  ( 25.59997277611800115, 2.578802611042650509E-13, -11.19994871957399241 ) ) ;
#22512=EDGE_LOOP ( 'NONE', ( #36886, #887, #45663, #4290 ) ) ;
#22516=CARTESIAN_POINT ( 'NONE',  ( 15.36937411412500154, 8.827864207275998965, 7.821779713377999599 ) ) ;
#22517=CARTESIAN_POINT ( 'NONE',  ( 15.40000000005200143, -9.187454762873001002, -8.213177997099000649 ) ) ;
#22519=AXIS2_PLACEMENT_3D ( 'NONE', #36872, #10290, #31625 ) ;
#22528=LINE ( 'NONE', #21161, #17121 ) ;
#22532=EDGE_LOOP ( 'NONE', ( #50901, #34172, #2252, #28994 ) ) ;
#22538=CARTESIAN_POINT ( 'NONE',  ( 16.42341781689399838, 3.643648243171000001, 12.02373124034999918 ) ) ;
#22545=CARTESIAN_POINT ( 'NONE',  ( 25.30000327618300204, 0.7080256801165658587, 11.56241914337144472 ) ) ;
#22551=FACE_OUTER_BOUND ( 'NONE', #62755, .T. ) ;
#22553=ORIENTED_EDGE ( 'NONE', *, *, #16658, .T. ) ;
#22556=ADVANCED_FACE ( 'NONE', ( #1252 ), #34012, .F. ) ;
#22560=CARTESIAN_POINT ( 'NONE',  ( 15.96647867633519802, 8.895858221259695497, 8.626805212950838353 ) ) ;
#22566=AXIS2_PLACEMENT_3D ( 'NONE', #2751, #61141, #7652 ) ;
#22567=CARTESIAN_POINT ( 'NONE',  ( 24.62774583285499830, -8.736962890587999908, -9.042103898172999976 ) ) ;
#22572=ORIENTED_EDGE ( 'NONE', *, *, #50968, .F. ) ;
#22576=DIRECTION ( 'NONE',  ( -1.000000000000000000, 0.000000000000000000, 0.000000000000000000 ) ) ;
#22578=CARTESIAN_POINT ( 'NONE',  ( 23.60205915885299888, 9.377218989194005871, -8.305825996818995804 ) ) ;
#22579=CIRCLE ( 'NONE', #1377, 0.6999999999999992895 ) ;
#22588=CARTESIAN_POINT ( 'NONE',  ( 23.81723327626561471, -12.99655882303040855, -3.682219191457393848 ) ) ;
#22601=CARTESIAN_POINT ( 'NONE',  ( 25.46375152665800101, -2.879425814940999917, -11.30951176145000048 ) ) ;
#22604=CARTESIAN_POINT ( 'NONE',  ( 16.06714147702597728, -8.497559733040684904, -7.969681199759283352 ) ) ;
#22608=DIRECTION ( 'NONE',  ( 0.000000000000000000, 0.000000000000000000, -1.000000000000000000 ) ) ;
#22610=ORIENTED_EDGE ( 'NONE', *, *, #7743, .T. ) ;
#22615=CARTESIAN_POINT ( 'NONE',  ( 16.08724299200000019, -9.224388201582000235, -8.529033888242999240 ) ) ;
#22629=CARTESIAN_POINT ( 'NONE',  ( 19.89999890908300273, -12.52500000000000036, 0.000000000000000000 ) ) ;
#22634=CARTESIAN_POINT ( 'NONE',  ( 23.85395532197026469, -13.23045631795083921, -3.489573210166486472 ) ) ;
#22635=CARTESIAN_POINT ( 'NONE',  ( 24.13648151864700253, 12.33467166542999927, 3.394534719267999989 ) ) ;
#22638=CARTESIAN_POINT ( 'NONE',  ( 18.35481756226800343, 2.723642650930000020, 11.47750709399999991 ) ) ;
#22644=CARTESIAN_POINT ( 'NONE',  ( 18.40429364930200151, 2.938801558760000265, -11.32979830910000096 ) ) ;
#22647=CARTESIAN_POINT ( 'NONE',  ( 23.63093901041600020, -10.04490667398999904, -9.752327919465999528 ) ) ;
#22648=CARTESIAN_POINT ( 'NONE',  ( 23.62923211109600174, -10.04860736350999950, 9.751346780839998729 ) ) ;
#22658=CIRCLE ( 'NONE', #29382, 13.92493900951000718 ) ;
#22659=CARTESIAN_POINT ( 'NONE',  ( 25.40548268214499927, 3.091940963388000174, -11.38328889108999853 ) ) ;
#22673=CYLINDRICAL_SURFACE ( 'NONE', #2027, 11.65000000000000036 ) ;
#22675=CARTESIAN_POINT ( 'NONE',  ( 12.26982956731400165, -11.56648533137999912, 4.655999611355000845 ) ) ;
#22679=CARTESIAN_POINT ( 'NONE',  ( 24.52306328725676821, 12.12196666327097638, 3.142986865081914605 ) ) ;
#22690=CARTESIAN_POINT ( 'NONE',  ( 24.33740888733500185, 12.30440757811000019, -3.219246934404999649 ) ) ;
#22693=VERTEX_POINT ( 'NONE', #34464 ) ;
#22697=CARTESIAN_POINT ( 'NONE',  ( 23.67741884366763117, 9.992396248498485178, 9.459260079125268561 ) ) ;
#22704=CARTESIAN_POINT ( 'NONE',  ( 18.13429499374400322, -12.00402196696999901, 3.371453313192000145 ) ) ;
#22706=CARTESIAN_POINT ( 'NONE',  ( 13.99967273502900156, 9.525279043350998620, 8.192384979499998110 ) ) ;
#22716=CARTESIAN_POINT ( 'NONE',  ( 16.39999999231800132, 3.216285993016000155, 11.40340220863999932 ) ) ;
#22725=EDGE_CURVE ( 'NONE', #68087, #27711, #1948, .T. ) ;
#22727=CARTESIAN_POINT ( 'NONE',  ( 24.56046482271400322, -3.658438515550000325, -12.32938606307999940 ) ) ;
#22728=CARTESIAN_POINT ( 'NONE',  ( 11.79999999684100054, 3.345264396959000130, -11.86064773189999855 ) ) ;
#22738=CARTESIAN_POINT ( 'NONE',  ( 30.60000000000000142, 0.000000000000000000, 0.000000000000000000 ) ) ;
#22739=CARTESIAN_POINT ( 'NONE',  ( 12.38745432786477529, 10.82911002781349374, -4.296468796670141366 ) ) ;
#22741=B_SPLINE_CURVE_WITH_KNOTS ( 'NONE', 3,
 ( #25430, #14603, #35923, #57236 ),
 .UNSPECIFIED., .F., .F.,
 ( 4, 4 ),
 ( 0.000000000000000000, 1.000000000000000000 ),
 .UNSPECIFIED. ) ;
#22747=CARTESIAN_POINT ( 'NONE',  ( 24.13789899383552395, -9.157240139151127778, -9.130332070236796937 ) ) ;
#22748=CARTESIAN_POINT ( 'NONE',  ( 25.59994555223599733, -8.527741194213000142, -7.260611644044000279 ) ) ;
#22751=CARTESIAN_POINT ( 'NONE',  ( 24.72545694048500309, -12.30753067676000079, 2.942917560468000460 ) ) ;
#22758=AXIS2_PLACEMENT_3D ( 'NONE', #69081, #58246, #37269 ) ;
#22765=CARTESIAN_POINT ( 'NONE',  ( 17.94368558191668939, -11.44474291118125109, 4.547324402811248056 ) ) ;
#22768=CARTESIAN_POINT ( 'NONE',  ( 25.44994989278600173, -2.258942858049999725, -12.29419282279000036 ) ) ;
#22770=CARTESIAN_POINT ( 'NONE',  ( 11.64452052416184102, 3.625675607363949116, -11.98888626465023854 ) ) ;
#22779=VERTEX_POINT ( 'NONE', #40717 ) ;
#22796=ORIENTED_EDGE ( 'NONE', *, *, #45150, .F. ) ;
#22804=CARTESIAN_POINT ( 'NONE',  ( 23.56666365135700403, -9.114812703021994977, -8.684180617873007435 ) ) ;
#22810=CARTESIAN_POINT ( 'NONE',  ( 23.68231877376700112, -3.146678492433000240, -13.35242067877000061 ) ) ;
#22816=CARTESIAN_POINT ( 'NONE',  ( 17.77423364829699892, -3.297060500158999652, 11.83473586442999981 ) ) ;
#22822=DIRECTION ( 'NONE',  ( 0.9999999999990064614, 1.235604878859008709E-06, -6.784100806884041873E-07 ) ) ;
#22840=CONICAL_SURFACE ( 'NONE', #65263, 1.150082671338000129, 0.7854605808793618804 ) ;
#22846=CARTESIAN_POINT ( 'NONE',  ( 13.50018479229797208, -9.763984779744566467, -6.782114604289273707 ) ) ;
#22851=ORIENTED_EDGE ( 'NONE', *, *, #16865, .T. ) ;
#22854=CARTESIAN_POINT ( 'NONE',  ( 13.82809631267600103, -8.844623397843001555, -7.663863542600000578 ) ) ;
#22855=CARTESIAN_POINT ( 'NONE',  ( 25.19967722607600180, -8.371103897856000842, -8.687405657236000778 ) ) ;
#22865=CARTESIAN_POINT ( 'NONE',  ( 15.62410434383600055, 8.799879896029001003, 7.715564795277000343 ) ) ;
#22868=CARTESIAN_POINT ( 'NONE',  ( 13.50006915090078152, -9.429349056561928677, -7.934633652400466808 ) ) ;
#22869=EDGE_CURVE ( 'NONE', #19259, #29376, #53613, .T. ) ;
#22873=EDGE_CURVE ( 'NONE', #28388, #40655, #66116, .T. ) ;
#22886=CARTESIAN_POINT ( 'NONE',  ( 16.13854177342199847, 3.630911166246999944, 11.92992564462999994 ) ) ;
#22887=CARTESIAN_POINT ( 'NONE',  ( 23.60205915885299888, 2.338900754103997670, 12.00073634675999834 ) ) ;
#22893=CARTESIAN_POINT ( 'NONE',  ( 18.38353273094886120, -11.69886204264012974, 4.474905155505553012 ) ) ;
#22896=CARTESIAN_POINT ( 'NONE',  ( 25.40243967972899952, 3.096345258848000270, 11.38620991970000063 ) ) ;
#22898=CARTESIAN_POINT ( 'NONE',  ( 25.19966679887500050, -3.337966940464999865, 11.59330421545000078 ) ) ;
#22899=ORIENTED_EDGE ( 'NONE', *, *, #23459, .F. ) ;
#22907=CARTESIAN_POINT ( 'NONE',  ( 25.37956771155745272, 8.342526067244204313, -8.311497089906559665 ) ) ;
#22909=CARTESIAN_POINT ( 'NONE',  ( 23.59999445750599989, -13.22316420035999940, -4.267800004853000040 ) ) ;
#22919=ORIENTED_EDGE ( 'NONE', *, *, #46261, .T. ) ;
#22932=CARTESIAN_POINT ( 'NONE',  ( 18.29991931957795259, -1.031823913341759950E-13, -12.32514597914127563 ) ) ;
#22933=CARTESIAN_POINT ( 'NONE',  ( 24.26256940594572242, -12.27508747190780625, -3.289098842859198069 ) ) ;
#22938=DIRECTION ( 'NONE',  ( 1.000000000000000000, 0.000000000000000000, 0.000000000000000000 ) ) ;
#22941=ORIENTED_EDGE ( 'NONE', *, *, #2991, .F. ) ;
#22946=CARTESIAN_POINT ( 'NONE',  ( 15.95436146409600120, 3.609635682399999546, 11.22945631340000006 ) ) ;
#22950=EDGE_CURVE ( 'NONE', #56062, #41132, #40304, .T. ) ;
#22951=CARTESIAN_POINT ( 'NONE',  ( 18.30017264560541790, 1.838307228690110540, 11.74271423064807962 ) ) ;
#22959=CARTESIAN_POINT ( 'NONE',  ( 23.52062907214899923, -13.48732121207000034, -4.206199075609999838 ) ) ;
#22966=AXIS2_PLACEMENT_3D ( 'NONE', #43908, #65210, #38653 ) ;
#22967=CARTESIAN_POINT ( 'NONE',  ( 16.09992084546400193, -8.991497430826001391, -8.719551690569000257 ) ) ;
#22970=DIRECTION ( 'NONE',  ( 1.000000000000000000, 0.000000000000000000, 0.000000000000000000 ) ) ;
#22973=ORIENTED_EDGE ( 'NONE', *, *, #18227, .F. ) ;
#22975=VERTEX_POINT ( 'NONE', #41751 ) ;
#22977=CARTESIAN_POINT ( 'NONE',  ( 11.35563386585000067, -12.29158615273999899, -1.473028240582999970 ) ) ;
#22984=CARTESIAN_POINT ( 'NONE',  ( 23.85163940690300066, 13.16376717049999989, 3.535832831874000437 ) ) ;
#22987=DIRECTION ( 'NONE',  ( 0.000000000000000000, 0.2588190451024934280, -0.9659258262890756397 ) ) ;
#22990=CARTESIAN_POINT ( 'NONE',  ( 25.59994555223599733, 8.527741194213000142, 7.260611644044000279 ) ) ;
#22996=CARTESIAN_POINT ( 'NONE',  ( 24.63807785274300244, -8.801136568184000808, -9.346917357783997460 ) ) ;
#22997=CARTESIAN_POINT ( 'NONE',  ( 23.66463366901000143, -10.00963801616000026, 9.517991018344002185 ) ) ;
#22998=CARTESIAN_POINT ( 'NONE',  ( 11.56566386073000174, -3.232480401124999680, 11.43828361194000109 ) ) ;
#23004=CARTESIAN_POINT ( 'NONE',  ( 24.35365242081699932, -3.253466243134998326, 12.21167519469000240 ) ) ;
#23015=CARTESIAN_POINT ( 'NONE',  ( 25.29995758267499895, -11.13046986584000031, -3.427500733308000314 ) ) ;
#23016=B_SPLINE_CURVE_WITH_KNOTS ( 'NONE', 3,
 ( #33596, #27659, #16463, #48979, #54213, #11911 ),
 .UNSPECIFIED., .F., .F.,
 ( 4, 2, 4 ),
 ( 0.000000000000000000, 0.5000000000000000000, 1.000000000000000000 ),
 .UNSPECIFIED. ) ;
#23023=CARTESIAN_POINT ( 'NONE',  ( 12.08926246520500136, -11.62544123506999938, 4.252388861798999997 ) ) ;
#23028=CARTESIAN_POINT ( 'NONE',  ( 23.58312595175700466, 2.942241311944000071, 13.62812806436000024 ) ) ;
#23031=CARTESIAN_POINT ( 'NONE',  ( 23.78808826920356978, -9.744861260223199650, 9.430304542841936311 ) ) ;
#23037=CARTESIAN_POINT ( 'NONE',  ( 23.55360001510700130, 13.39037920836000062, -4.197254571800000278 ) ) ;
#23042=CARTESIAN_POINT ( 'NONE',  ( 23.58888755872254706, 2.922214055433252522, 13.61647863770148703 ) ) ;
#23045=DIRECTION ( 'NONE',  ( -1.000000000000000000, 0.000000000000000000, 0.000000000000000000 ) ) ;
#23060=EDGE_CURVE ( 'NONE', #26251, #30301, #43587, .T. ) ;
#23064=CARTESIAN_POINT ( 'NONE',  ( 11.80427293869800032, 12.43391773449000048, 1.801004847141999932 ) ) ;
#23065=CARTESIAN_POINT ( 'NONE',  ( 23.55780568386700224, -3.266395970825999751, 13.70080015052999833 ) ) ;
#23070=AXIS2_PLACEMENT_3D ( 'NONE', #48047, #21467, #495 ) ;
#23079=AXIS2_PLACEMENT_3D ( 'NONE', #33776, #13490, #65915 ) ;
#23081=ORIENTED_EDGE ( 'NONE', *, *, #16865, .F. ) ;
#23091=CARTESIAN_POINT ( 'NONE',  ( 24.30001685126999789, 8.938702716825000394, -8.938676159935001309 ) ) ;
#23099=CARTESIAN_POINT ( 'NONE',  ( 24.46225079093600385, -12.39903786166000010, 3.098987673017999711 ) ) ;
#23103=CARTESIAN_POINT ( 'NONE',  ( 12.99046541331000171, -12.43411100708999939, -1.799680151465999911 ) ) ;
#23104=VERTEX_POINT ( 'NONE', #40809 ) ;
#23106=DIRECTION ( 'NONE',  ( 0.000000000000000000, 0.1862490057674050514, 0.9825025739664263735 ) ) ;
#23108=CIRCLE ( 'NONE', #2998, 1.000000000000000444 ) ;
#23109=DIRECTION ( 'NONE',  ( 0.000000000000000000, 0.000000000000000000, -1.000000000000000000 ) ) ;
#23111=ORIENTED_EDGE ( 'NONE', *, *, #47998, .F. ) ;
#23114=CARTESIAN_POINT ( 'NONE',  ( 14.70000000000000107, 9.329726667597000755, 8.204053922562998480 ) ) ;
#23119=AXIS2_PLACEMENT_3D ( 'NONE', #48963, #42353, #11894 ) ;
#23138=CARTESIAN_POINT ( 'NONE',  ( 11.71289336965100070, 3.191014699919000108, -11.45041132747999946 ) ) ;
#23147=CARTESIAN_POINT ( 'NONE',  ( 19.94999927679900154, 0.000000000000000000, -12.47499939739994979 ) ) ;
#23148=EDGE_CURVE ( 'NONE', #1641, #27849, #66986, .T. ) ;
#23160=CARTESIAN_POINT ( 'NONE',  ( 23.61807773383599951, -2.886089390029999535, -13.53865479462000110 ) ) ;
#23179=TOROIDAL_SURFACE ( 'NONE', #6449, 11.15000000000000036, 0.5000000000000000000 ) ;
#23193=FACE_OUTER_BOUND ( 'NONE', #3633, .T. ) ;
#23196=CARTESIAN_POINT ( 'NONE',  ( 24.36809152945900081, -3.197172894633000251, 12.07984101077999917 ) ) ;
#23200=CARTESIAN_POINT ( 'NONE',  ( 24.37847035506199944, -8.840951746222000196, 8.761877451061000244 ) ) ;
#23206=CARTESIAN_POINT ( 'NONE',  ( 13.78329442975000063, -8.859672882948000705, -7.785394853692999995 ) ) ;
#23209=PLANE ( 'NONE',  #11383 ) ;
#23212=CARTESIAN_POINT ( 'NONE',  ( 13.50830001818700055, 12.29143783039000049, 2.111693202397000313 ) ) ;
#23213=VERTEX_POINT ( 'NONE', #49368 ) ;
#23219=CARTESIAN_POINT ( 'NONE',  ( 25.02481001335046074, 8.536659555490478724, -8.299428667226347756 ) ) ;
#23235=ORIENTED_EDGE ( 'NONE', *, *, #43571, .F. ) ;
#23241=CARTESIAN_POINT ( 'NONE',  ( 11.29998636608000062, 3.695122995756999984, -11.25914041192000070 ) ) ;
#23254=CARTESIAN_POINT ( 'NONE',  ( 25.40550217044300041, -3.091918942015000393, 11.38326880256000173 ) ) ;
#23255=ORIENTED_EDGE ( 'NONE', *, *, #12143, .F. ) ;
#23256=ORIENTED_EDGE ( 'NONE', *, *, #31105, .T. ) ;
#23258=CARTESIAN_POINT ( 'NONE',  ( 25.29987654162099986, -8.533547851352999203, -7.925583806936000286 ) ) ;
#23261=CARTESIAN_POINT ( 'NONE',  ( 23.64966114303629041, 3.378619448667885550, -13.52224079656408229 ) ) ;
#23276=CARTESIAN_POINT ( 'NONE',  ( 19.94999927679900154, 0.000000000000000000, 5.040412531797999279E-14 ) ) ;
#23279=EDGE_CURVE ( 'NONE', #44670, #22409, #14704, .T. ) ;
#23281=PLANE ( 'NONE',  #23079 ) ;
#23284=CARTESIAN_POINT ( 'NONE',  ( 24.30001697352500045, -3.271769158411000245, -12.21048181092999840 ) ) ;
#23291=CARTESIAN_POINT ( 'NONE',  ( 24.14075163639471455, -12.48103446967273378, -3.363283332670145231 ) ) ;
#23300=EDGE_LOOP ( 'NONE', ( #55590, #6893, #24414, #53393 ) ) ;
#23314=CARTESIAN_POINT ( 'NONE',  ( 24.30001694670299983, 8.938702829764999080, 8.938676122491999720 ) ) ;
#23315=CARTESIAN_POINT ( 'NONE',  ( 23.58312609496700318, -13.27342582440000029, -4.266007375089999165 ) ) ;
#23324=CARTESIAN_POINT ( 'NONE',  ( 24.30001683570900184, 3.271769286791000209, 12.21048169671000139 ) ) ;
#23350=CARTESIAN_POINT ( 'NONE',  ( 23.62001506143800000, -10.21680080108000155, 9.338901190890000592 ) ) ;
#23353=EDGE_LOOP ( 'NONE', ( #43548, #14953, #36275, #11877 ) ) ;
#23355=B_SPLINE_CURVE_WITH_KNOTS ( 'NONE', 3,
 ( #25140, #26523, #26177, #15342 ),
 .UNSPECIFIED., .F., .F.,
 ( 4, 4 ),
 ( 0.000000000000000000, 0.4999999894681322887 ),
 .UNSPECIFIED. ) ;
#23382=CARTESIAN_POINT ( 'NONE',  ( 24.16219649940969560, -9.122613423523826981, 9.103272609183665764 ) ) ;
#23384=ORIENTED_EDGE ( 'NONE', *, *, #49921, .F. ) ;
#23390=DIRECTION ( 'NONE',  ( -1.000000000000000000, 0.000000000000000000, 0.000000000000000000 ) ) ;
#23400=VERTEX_POINT ( 'NONE', #18605 ) ;
#23401=B_SPLINE_SURFACE_WITH_KNOTS ( 'NONE', 3, 3, ( 
 ( #21160, #520, #64474, #59591 ),
 ( #48073, #21837, #32686, #10321 ),
 ( #64136, #26411, #43170, #42487 ),
 ( #10661, #64823, #16598, #177 ),
 ( #52976, #37923, #59242, #31657 ),
 ( #6101, #48762, #871, #22184 ),
 ( #43524, #16933, #31313, #16252 ),
 ( #63797, #4720, #26063, #5422 ) ),
 .UNSPECIFIED., .F., .F., .F.,
 ( 4, 1, 1, 1, 1, 4 ),
 ( 4, 4 ),
 ( 0.008355907821911999489, 0.05882352941176000050, 0.1176470588234999892, 0.1764705882353000133, 0.2352941176471000095, 0.2534671684970000172 ),
 ( -0.1830857773976999892, 1.182949828738000031 ),
 .UNSPECIFIED. ) ;
#23407=CARTESIAN_POINT ( 'NONE',  ( 17.72081995139100030, -11.49894842141999973, 4.816072468917000471 ) ) ;
#23414=B_SPLINE_CURVE_WITH_KNOTS ( 'NONE', 3,
 ( #10913, #52882, #43072, #64379 ),
 .UNSPECIFIED., .F., .F.,
 ( 4, 4 ),
 ( 0.000000000000000000, 1.000000000000000000 ),
 .UNSPECIFIED. ) ;
#23421=B_SPLINE_CURVE_WITH_KNOTS ( 'NONE', 3,
 ( #26477, #21560, #64203, #68762, #37304, #43241 ),
 .UNSPECIFIED., .F., .F.,
 ( 4, 2, 4 ),
 ( 0.000000000000000000, 0.5000000000000000000, 1.000000000000000000 ),
 .UNSPECIFIED. ) ;
#23440=EDGE_CURVE ( 'NONE', #66745, #2511, #55664, .T. ) ;
#23449=CARTESIAN_POINT ( 'NONE',  ( 24.13558482227616864, -9.160566910400561369, -9.132875783579766704 ) ) ;
#23453=CARTESIAN_POINT ( 'NONE',  ( 16.09586749610213374, 8.411110950737114678, 8.060864562931188360 ) ) ;
#23459=EDGE_CURVE ( 'NONE', #47642, #10933, #5920, .T. ) ;
#23467=DIRECTION ( 'NONE',  ( 0.000000000000000000, -0.7455306007789014311, -0.6664713972124013397 ) ) ;
#23474=ORIENTED_EDGE ( 'NONE', *, *, #7932, .F. ) ;
#23480=ORIENTED_EDGE ( 'NONE', *, *, #4808, .F. ) ;
#23483=CARTESIAN_POINT ( 'NONE',  ( 23.57792393660973573, 13.37377923847282268, -4.097348931089725532 ) ) ;
#23488=EDGE_CURVE ( 'NONE', #1641, #5569, #107, .T. ) ;
#23499=VERTEX_POINT ( 'NONE', #20 ) ;
#23505=CARTESIAN_POINT ( 'NONE',  ( 23.73665640592300363, -3.437546595577999575, -13.35043945363000084 ) ) ;
#23511=CARTESIAN_POINT ( 'NONE',  ( 20.75138802851920161, 0.000000000000000000, 0.000000000000000000 ) ) ;
#23512=CARTESIAN_POINT ( 'NONE',  ( 18.30017264560542145, 1.838307227263772159, -11.74271423084882571 ) ) ;
#23525=CIRCLE ( 'NONE', #48083, 5.000000000000000000 ) ;
#23534=ADVANCED_FACE ( 'NONE', ( #20659 ), #62609, .T. ) ;
#23543=CARTESIAN_POINT ( 'NONE',  ( 18.90826270587400160, -11.65000000000000036, 0.000000000000000000 ) ) ;
#23550=CARTESIAN_POINT ( 'NONE',  ( 24.67552801389400230, -8.698828566341001434, -9.015209094485999941 ) ) ;
#23555=CARTESIAN_POINT ( 'NONE',  ( 23.60205915885299888, 9.361474752776006270, 7.912850866691996998 ) ) ;
#23564=CIRCLE ( 'NONE', #38078, 1.300172478116999208 ) ;
#23570=VERTEX_POINT ( 'NONE', #31167 ) ;
#23575=CONICAL_SURFACE ( 'NONE', #55927, 12.71246950475999959, 0.8960553845711767273 ) ;
#23579=CARTESIAN_POINT ( 'NONE',  ( 11.80738107398800274, -11.64644714240999868, -1.863397721619000080 ) ) ;
#23590=CARTESIAN_POINT ( 'NONE',  ( 24.45998324064000329, 3.150049453514000231, 11.96533647240999976 ) ) ;
#23592=CARTESIAN_POINT ( 'NONE',  ( 25.39410189985537514, -8.421101446676589219, 8.066020039750368298 ) ) ;
#23593=VERTEX_POINT ( 'NONE', #3880 ) ;
#23606=ORIENTED_EDGE ( 'NONE', *, *, #47292, .T. ) ;
#23617=B_SPLINE_CURVE_WITH_KNOTS ( 'NONE', 3,
 ( #55819, #7922, #61060, #29610 ),
 .UNSPECIFIED., .F., .F.,
 ( 4, 4 ),
 ( 0.000000000000000000, 1.000000000000000000 ),
 .UNSPECIFIED. ) ;
#23622=EDGE_CURVE ( 'NONE', #34052, #66938, #11741, .T. ) ;
#23627=B_SPLINE_CURVE_WITH_KNOTS ( 'NONE', 3,
 ( #5416, #16592, #42821, #58549 ),
 .UNSPECIFIED., .F., .F.,
 ( 4, 4 ),
 ( 0.000000000000000000, 1.000000000000000000 ),
 .UNSPECIFIED. ) ;
#23630=CARTESIAN_POINT ( 'NONE',  ( 23.85842837956922580, -12.93469165770115481, -3.627720848801395448 ) ) ;
#23631=CARTESIAN_POINT ( 'NONE',  ( 24.56351374471499938, 3.482977112968999922, -12.16506632497999973 ) ) ;
#23635=CARTESIAN_POINT ( 'NONE',  ( 44.24148000000000280, -2.258942858049999725, -12.29419282279000036 ) ) ;
#23638=ORIENTED_EDGE ( 'NONE', *, *, #66913, .F. ) ;
#23640=ORIENTED_EDGE ( 'NONE', *, *, #43257, .T. ) ;
#23642=CARTESIAN_POINT ( 'NONE',  ( 24.76776046854388724, -8.625624972805100654, -8.557838011048463756 ) ) ;
#23645=ORIENTED_EDGE ( 'NONE', *, *, #16807, .T. ) ;
#23653=CARTESIAN_POINT ( 'NONE',  ( 23.81982929170500185, -12.91659203753999918, -3.707450659729000453 ) ) ;
#23659=CARTESIAN_POINT ( 'NONE',  ( 23.60000000000000142, -11.85420044612000012, 3.901016762742000488 ) ) ;
#23660=ADVANCED_FACE ( 'NONE', ( #6987 ), #44043, .F. ) ;
#23662=LINE ( 'NONE', #12839, #14260 ) ;
#23668=B_SPLINE_CURVE_WITH_KNOTS ( 'NONE', 3,
 ( #23994, #7225, #60707, #45329, #22951, #12825 ),
 .UNSPECIFIED., .F., .F.,
 ( 4, 2, 4 ),
 ( 0.000000000000000000, 0.5000000000000000000, 1.000000000000000000 ),
 .UNSPECIFIED. ) ;
#23669=B_SPLINE_CURVE_WITH_KNOTS ( 'NONE', 3,
 ( #8262, #33809, #45332, #29611 ),
 .UNSPECIFIED., .F., .F.,
 ( 4, 4 ),
 ( 0.000000000000000000, 1.000000000000000000 ),
 .UNSPECIFIED. ) ;
#23670=ORIENTED_EDGE ( 'NONE', *, *, #48470, .F. ) ;
#23677=DIRECTION ( 'NONE',  ( 0.000000000000000000, 0.000000000000000000, -1.000000000000000000 ) ) ;
#23680=ORIENTED_EDGE ( 'NONE', *, *, #53316, .T. ) ;
#23683=CARTESIAN_POINT ( 'NONE',  ( 18.50013789939208664, 2.065999734462983189E-14, -11.64999999999999325 ) ) ;
#23687=CONICAL_SURFACE ( 'NONE', #66101, 12.42518894556000042, 0.7854133338342391690 ) ;
#23690=DIRECTION ( 'NONE',  ( 0.000000000000000000, -1.000000000000000000, 0.000000000000000000 ) ) ;
#23694=FACE_OUTER_BOUND ( 'NONE', #4775, .T. ) ;
#23700=CARTESIAN_POINT ( 'NONE',  ( 23.56682227024313647, 2.990440059702627273, 13.66659919071918772 ) ) ;
#23705=FACE_OUTER_BOUND ( 'NONE', #65145, .T. ) ;
#23707=CARTESIAN_POINT ( 'NONE',  ( 16.10005255078199937, 3.632778330393000132, 11.06917548872000090 ) ) ;
#23714=VERTEX_POINT ( 'NONE', #363 ) ;
#23725=VERTEX_POINT ( 'NONE', #59432 ) ;
#23731=CARTESIAN_POINT ( 'NONE',  ( 24.96666885022796478, 8.756202917673951092, 7.455126455300256083 ) ) ;
#23737=TOROIDAL_SURFACE ( 'NONE', #29346, 7.720759220056000238, 1.000000000000000000 ) ;
#23738=ORIENTED_EDGE ( 'NONE', *, *, #39585, .F. ) ;
#23746=CARTESIAN_POINT ( 'NONE',  ( 17.93509931767800225, -11.57247339239000006, 4.892741173462999527 ) ) ;
#23761=CARTESIAN_POINT ( 'NONE',  ( 24.22109243572800352, -3.760953175020000039, 12.77804564811999910 ) ) ;
#23763=CARTESIAN_POINT ( 'NONE',  ( 18.23019412026599895, 3.031170125296999807, -11.90979123982999965 ) ) ;
#23766=CARTESIAN_POINT ( 'NONE',  ( 25.29987333571600061, -11.77655473258999841, -4.190794510628000680 ) ) ;
#23784=CARTESIAN_POINT ( 'NONE',  ( 24.83136329184668156, 11.65947310412830618, 3.197453827145718463 ) ) ;
#23794=CARTESIAN_POINT ( 'NONE',  ( 24.53003472522999928, -12.09081557276999952, 3.147842171698999714 ) ) ;
#23798=CARTESIAN_POINT ( 'NONE',  ( 23.60000000000000142, 11.49391741900999975, -4.090215442373000165 ) ) ;
#23814=DIRECTION ( 'NONE',  ( -0.9999999999997783995, -6.656251680840855499E-07, 7.419214651740835408E-10 ) ) ;
#23815=DIRECTION ( 'NONE',  ( 0.000000000000000000, -1.000000000000000000, 0.000000000000000000 ) ) ;
#23822=ORIENTED_EDGE ( 'NONE', *, *, #21995, .T. ) ;
#23833=CARTESIAN_POINT ( 'NONE',  ( 11.82349952450200270, 3.378095173501999948, -11.11014980558000076 ) ) ;
#23834=DIRECTION ( 'NONE',  ( -1.000000000000000000, 0.000000000000000000, 0.000000000000000000 ) ) ;
#23836=ADVANCED_FACE ( 'NONE', ( #17662 ), #39326, .F. ) ;
#23847=ORIENTED_EDGE ( 'NONE', *, *, #10819, .F. ) ;
#23854=CARTESIAN_POINT ( 'NONE',  ( 24.13646806689900259, -3.227588194705000024, -12.37943302943000035 ) ) ;
#23856=B_SPLINE_CURVE_WITH_KNOTS ( 'NONE', 3,
 ( #63159, #26120, #24747, #4436, #57235, #30680 ),
 .UNSPECIFIED., .F., .F.,
 ( 4, 1, 1, 4 ),
 ( 0.000000000000000000, 0.2305484560606776978, 0.8346924746771972048, 1.000000000000000000 ),
 .UNSPECIFIED. ) ;
#23869=CARTESIAN_POINT ( 'NONE',  ( 23.61172379773616115, -13.39866229807703313, 3.948922985516912565 ) ) ;
#23870=VERTEX_POINT ( 'NONE', #1573 ) ;
#23876=CARTESIAN_POINT ( 'NONE',  ( 24.35365242081700288, 10.90899669668998584, -3.315896191951999583 ) ) ;
#23881=B_SPLINE_CURVE_WITH_KNOTS ( 'NONE', 3,
 ( #36030, #57014, #46871, #25197 ),
 .UNSPECIFIED., .F., .F.,
 ( 4, 4 ),
 ( 0.000000000000000000, 1.000000000000000000 ),
 .UNSPECIFIED. ) ;
#23882=VECTOR ( 'NONE', #51313, 1000.000000000000227 ) ;
#23890=CARTESIAN_POINT ( 'NONE',  ( 14.46666666157666903, 8.833279249958289725, 7.896561128163720689 ) ) ;
#23892=CARTESIAN_POINT ( 'NONE',  ( 25.48370546149499916, 11.09850153045000098, 3.318332408913000187 ) ) ;
#23906=DIRECTION ( 'NONE',  ( -1.000000000000000000, 0.000000000000000000, 0.000000000000000000 ) ) ;
#23907=CARTESIAN_POINT ( 'NONE',  ( 24.72672956147405898, 3.119036157890411332, 11.78404790340006336 ) ) ;
#23909=CARTESIAN_POINT ( 'NONE',  ( 23.91429168771849945, -12.84854223911260185, 3.562185587916466556 ) ) ;
#23922=CARTESIAN_POINT ( 'NONE',  ( 25.49995889272035399, 10.64590475540159886, 3.788442452821807471 ) ) ;
#23928=CARTESIAN_POINT ( 'NONE',  ( 11.55275411606000269, -11.58372484989999940, -1.667203446842000059 ) ) ;
#23931=ORIENTED_EDGE ( 'NONE', *, *, #30100, .F. ) ;
#23935=EDGE_CURVE ( 'NONE', #67995, #18236, #41842, .T. ) ;
#23936=AXIS2_PLACEMENT_3D ( 'NONE', #58127, #15816, #63005 ) ;
#23946=ORIENTED_EDGE ( 'NONE', *, *, #53954, .F. ) ;
#23951=CARTESIAN_POINT ( 'NONE',  ( 23.61806548148500084, 10.28147268658000080, -9.269149798642001059 ) ) ;
#23952=CARTESIAN_POINT ( 'NONE',  ( 16.13895793972310599, -3.268072512451278389, -11.38828084065380608 ) ) ;
#23954=CARTESIAN_POINT ( 'NONE',  ( 23.60000000000000142, -11.85420044612000012, -3.901016762742000488 ) ) ;
#23973=ORIENTED_EDGE ( 'NONE', *, *, #24869, .T. ) ;
#23975=CARTESIAN_POINT ( 'NONE',  ( 24.67921580316900076, -12.29514843751999997, 2.979196179828000002 ) ) ;
#23978=EDGE_LOOP ( 'NONE', ( #24949, #58301, #4706, #54699 ) ) ;
#23982=CARTESIAN_POINT ( 'NONE',  ( 24.66807826147336513, -8.737531165310779002, 9.168167557060799666 ) ) ;
#23994=CARTESIAN_POINT ( 'NONE',  ( 18.30003129334700063, -2.732683817159999862, 11.53064095410000078 ) ) ;
#24002=CARTESIAN_POINT ( 'NONE',  ( 23.51693423744300304, -13.43920603419999971, -4.372108587443999994 ) ) ;
#24003=DIRECTION ( 'NONE',  ( -1.000000000000000000, 0.000000000000000000, 0.000000000000000000 ) ) ;
#24007=EDGE_LOOP ( 'NONE', ( #25311, #66312, #13071 ) ) ;
#24015=ORIENTED_EDGE ( 'NONE', *, *, #50968, .T. ) ;
#24021=EDGE_CURVE ( 'NONE', #23213, #14147, #27602, .T. ) ;
#24023=LINE ( 'NONE', #45358, #64020 ) ;
#24025=CARTESIAN_POINT ( 'NONE',  ( 23.68234916609000251, 13.13683194047999869, 3.951035445327000240 ) ) ;
#24030=CARTESIAN_POINT ( 'NONE',  ( 18.50003594170800270, -2.686563649653999963, 11.33603604535000109 ) ) ;
#24044=CARTESIAN_POINT ( 'NONE',  ( 23.58926396079670340, 3.186602112811154797, 13.61293272293995571 ) ) ;
#24045=CARTESIAN_POINT ( 'NONE',  ( 24.30000560748793959, -8.853233204563331071, -8.853233204563331071 ) ) ;
#24052=ORIENTED_EDGE ( 'NONE', *, *, #43405, .F. ) ;
#24075=CYLINDRICAL_SURFACE ( 'NONE', #14744, 11.79499999999999993 ) ;
#24085=ORIENTED_EDGE ( 'NONE', *, *, #32740, .F. ) ;
#24087=CARTESIAN_POINT ( 'NONE',  ( 24.13227430146345043, 9.165337429710305628, 9.136502937412682712 ) ) ;
#24095=CARTESIAN_POINT ( 'NONE',  ( 24.46275371595800152, -8.882876216795999369, 9.187943390076000583 ) ) ;
#24103=CARTESIAN_POINT ( 'NONE',  ( 12.22252627658614976, -11.15475449693722076, 3.361665977429223684 ) ) ;
#24105=CARTESIAN_POINT ( 'NONE',  ( 23.68333487548100180, -3.148023544630999648, 13.34998892770999923 ) ) ;
#24108=CARTESIAN_POINT ( 'NONE',  ( 18.17677363193000062, 3.419785592864999835, -11.99291007725999947 ) ) ;
#24119=VECTOR ( 'NONE', #31194, 1000.000000000000000 ) ;
#24127=DIRECTION ( 'NONE',  ( -1.000000000000000000, 0.000000000000000000, 0.000000000000000000 ) ) ;
#24131=ORIENTED_EDGE ( 'NONE', *, *, #53705, .F. ) ;
#24139=ADVANCED_FACE ( 'NONE', ( #26691 ), #67525, .F. ) ;
#24149=LINE ( 'NONE', #18218, #53081 ) ;
#24154=CARTESIAN_POINT ( 'NONE',  ( 24.30000000000000071, 10.83443035398000021, 3.855530949778000149 ) ) ;
#24160=CARTESIAN_POINT ( 'NONE',  ( 16.03331929146652257, -3.865558715575581505, -11.84348844988198834 ) ) ;
#24166=CARTESIAN_POINT ( 'NONE',  ( 25.29996559941400136, -2.596925179230000325, -11.35302181744000016 ) ) ;
#24167=ORIENTED_EDGE ( 'NONE', *, *, #36236, .F. ) ;
#24169=CARTESIAN_POINT ( 'NONE',  ( 18.49996808500599954, 1.807259461993230287, 11.54438823538759351 ) ) ;
#24190=ORIENTED_EDGE ( 'NONE', *, *, #63956, .T. ) ;
#24194=ORIENTED_EDGE ( 'NONE', *, *, #1974, .T. ) ;
#24197=CARTESIAN_POINT ( 'NONE',  ( 23.81893538673600119, -3.247264533092999894, -13.04177392601999941 ) ) ;
#24199=CARTESIAN_POINT ( 'NONE',  ( 15.96663488596630742, -8.445622082970141165, -8.216900471613381995 ) ) ;
#24205=FACE_OUTER_BOUND ( 'NONE', #12567, .T. ) ;
#24208=FACE_OUTER_BOUND ( 'NONE', #49471, .T. ) ;
#24212=AXIS2_PLACEMENT_3D ( 'NONE', #41289, #46192, #29791 ) ;
#24217=EDGE_CURVE ( 'NONE', #54214, #62492, #45532, .T. ) ;
#24219=AXIS2_PLACEMENT_3D ( 'NONE', #30942, #62062, #15198 ) ;
#24224=EDGE_CURVE ( 'NONE', #47324, #27393, #31821, .T. ) ;
#24236=ORIENTED_EDGE ( 'NONE', *, *, #29547, .T. ) ;
#24242=EDGE_CURVE ( 'NONE', #15717, #3814, #1911, .T. ) ;
#24248=VERTEX_POINT ( 'NONE', #24543 ) ;
#24262=AXIS2_PLACEMENT_3D ( 'NONE', #57299, #42606, #58334 ) ;
#24285=CARTESIAN_POINT ( 'NONE',  ( 25.29995737991200144, -8.533537546129998930, 7.925519566782000425 ) ) ;
#24286=ORIENTED_EDGE ( 'NONE', *, *, #68270, .T. ) ;
#24291=CARTESIAN_POINT ( 'NONE',  ( 25.59036983458399916, 8.351023420428999700, -7.983780165365000236 ) ) ;
#24292=CARTESIAN_POINT ( 'NONE',  ( 23.58312598483500011, 10.33118764019999958, -9.362116027220000802 ) ) ;
#24293=CARTESIAN_POINT ( 'NONE',  ( 18.26001156276199922, -2.811979134698999960, -11.55266638147999991 ) ) ;
#24302=DIRECTION ( 'NONE',  ( -1.000000000000000000, 0.000000000000000000, 0.000000000000000000 ) ) ;
#24309=ADVANCED_FACE ( 'NONE', ( #14059, #40616 ), #35385, .T. ) ;
#24312=CARTESIAN_POINT ( 'NONE',  ( 13.63350196149396609, -9.056970873722326232, -7.433404858428114714 ) ) ;
#24313=AXIS2_PLACEMENT_3D ( 'NONE', #1607, #28535, #49498 ) ;
#24321=CARTESIAN_POINT ( 'NONE',  ( 24.25374608244500152, 3.234182954713999969, -12.21793987376999979 ) ) ;
#24322=FACE_OUTER_BOUND ( 'NONE', #47549, .T. ) ;
#24329=AXIS2_PLACEMENT_3D ( 'NONE', #62996, #9522, #15471 ) ;
#24334=DIRECTION ( 'NONE',  ( 1.000000000000000000, 0.000000000000000000, 0.000000000000000000 ) ) ;
#24337=ORIENTED_EDGE ( 'NONE', *, *, #60529, .T. ) ;
#24340=AXIS2_PLACEMENT_3D ( 'NONE', #53130, #332, #5230 ) ;
#24344=ORIENTED_EDGE ( 'NONE', *, *, #13975, .F. ) ;
#24364=DIRECTION ( 'NONE',  ( 0.000000000000000000, 0.000000000000000000, -1.000000000000000000 ) ) ;
#24380=DIRECTION ( 'NONE',  ( 0.000000000000000000, -0.2588190451024934835, 0.9659258262890757507 ) ) ;
#24385=DIRECTION ( 'NONE',  ( -1.000000000000000000, 0.000000000000000000, 0.000000000000000000 ) ) ;
#24388=EDGE_CURVE ( 'NONE', #40252, #67674, #26703, .T. ) ;
#24400=CARTESIAN_POINT ( 'NONE',  ( 11.79999999497874796, 3.261294161473140107, -11.32146851427815193 ) ) ;
#24409=ADVANCED_FACE ( 'NONE', ( #18614 ), #60805, .F. ) ;
#24414=ORIENTED_EDGE ( 'NONE', *, *, #49391, .F. ) ;
#24425=AXIS2_PLACEMENT_3D ( 'NONE', #52326, #4421, #43125 ) ;
#24432=DIRECTION ( 'NONE',  ( 0.000000000000000000, 0.000000000000000000, 1.000000000000000000 ) ) ;
#24440=CARTESIAN_POINT ( 'NONE',  ( 17.75481218032700070, -12.16597452523000022, 3.139308580624999845 ) ) ;
#24452=CARTESIAN_POINT ( 'NONE',  ( 23.52038360246099913, -3.100182920209999970, 13.78394459507999947 ) ) ;
#24453=CARTESIAN_POINT ( 'NONE',  ( 13.50018479229300006, 11.60142623882999935, 2.415183939829000259 ) ) ;
#24455=EDGE_CURVE ( 'NONE', #27357, #42427, #23355, .T. ) ;
#24476=DIRECTION ( 'NONE',  ( -1.000000000000000000, 0.000000000000000000, 0.000000000000000000 ) ) ;
#24486=CARTESIAN_POINT ( 'NONE',  ( 15.86376629110799996, -3.753680978508000088, -11.28125155222999787 ) ) ;
#24510=CARTESIAN_POINT ( 'NONE',  ( 18.46577960220267300, 3.126461091534826320, -12.12859619074303552 ) ) ;
#24532=CARTESIAN_POINT ( 'NONE',  ( 24.71803171219655582, 8.650025487060094775, 8.600693273006482897 ) ) ;
#24537=ADVANCED_FACE ( 'NONE', ( #4752 ), #35403, .T. ) ;
#24543=CARTESIAN_POINT ( 'NONE',  ( 24.30000000000000071, -12.03537377768999939, -3.224868684338999980 ) ) ;
#24544=DIRECTION ( 'NONE',  ( -1.000000000000000000, 0.000000000000000000, 0.000000000000000000 ) ) ;
#24548=B_SPLINE_CURVE_WITH_KNOTS ( 'NONE', 3,
 ( #35375, #30467, #67511, #25559 ),
 .UNSPECIFIED., .F., .F.,
 ( 4, 4 ),
 ( 0.5000000026798849806, 1.000000000000000000 ),
 .UNSPECIFIED. ) ;
#24561=DIRECTION ( 'NONE',  ( 0.000000000000000000, -0.2714570858282905341, -0.9624505444715651947 ) ) ;
#24562=CARTESIAN_POINT ( 'NONE',  ( 23.59542428366313871, -13.38815799942825180, 4.017037056778253401 ) ) ;
#24564=EDGE_CURVE ( 'NONE', #66838, #49580, #34305, .T. ) ;
#24572=CARTESIAN_POINT ( 'NONE',  ( 23.58885226882633290, 2.922211860835754127, -13.61647608845786372 ) ) ;
#24575=CARTESIAN_POINT ( 'NONE',  ( 24.30000000000000071, 8.810505093353000916, 8.810505093353000916 ) ) ;
#24594=ORIENTED_EDGE ( 'NONE', *, *, #39900, .T. ) ;
#24595=B_SPLINE_CURVE_WITH_KNOTS ( 'NONE', 3,
 ( #56576, #13597, #56233, #8341, #30027, #7999 ),
 .UNSPECIFIED., .F., .F.,
 ( 4, 2, 4 ),
 ( 0.000000000000000000, 0.5000000000000000000, 1.000000000000000000 ),
 .UNSPECIFIED. ) ;
#24602=CARTESIAN_POINT ( 'NONE',  ( 15.89979320885400327, 3.824231472901999496, 11.71686814605000038 ) ) ;
#24613=ORIENTED_EDGE ( 'NONE', *, *, #62349, .T. ) ;
#24616=CARTESIAN_POINT ( 'NONE',  ( 23.56665676678700194, 3.767123864185000533E-06, -13.98989063586000015 ) ) ;
#24617=EDGE_CURVE ( 'NONE', #56214, #18715, #46579, .T. ) ;
#24621=EDGE_CURVE ( 'NONE', #38467, #48923, #13095, .T. ) ;
#24632=DIRECTION ( 'NONE',  ( 0.000000000000000000, 0.000000000000000000, 1.000000000000000000 ) ) ;
#24639=CARTESIAN_POINT ( 'NONE',  ( 24.26256944702610241, 3.289100563212026263, 12.27508693394269734 ) ) ;
#24640=CARTESIAN_POINT ( 'NONE',  ( 24.45284658036600334, 8.898487387712000540, -9.226082598753000852 ) ) ;
#24641=CARTESIAN_POINT ( 'NONE',  ( 11.49977531252999974, 12.52500000000000213, 0.5112815185527809225 ) ) ;
#24659=ORIENTED_EDGE ( 'NONE', *, *, #52896, .F. ) ;
#24665=CARTESIAN_POINT ( 'NONE',  ( 17.80000000009400196, -3.216307036143000175, -11.40341376487999980 ) ) ;
#24671=CARTESIAN_POINT ( 'NONE',  ( 13.36715644869600084, -11.69666705770999826, -2.137627928029000035 ) ) ;
#24698=CARTESIAN_POINT ( 'NONE',  ( 24.67921569845699992, 12.29514839105000057, -2.979196030862000022 ) ) ;
#24700=B_SPLINE_CURVE_WITH_KNOTS ( 'NONE', 3,
 ( #16099, #63643, #10172, #4919 ),
 .UNSPECIFIED., .F., .F.,
 ( 4, 4 ),
 ( 0.000000000000000000, 1.000000000000000000 ),
 .UNSPECIFIED. ) ;
#24709=DIRECTION ( 'NONE',  ( -1.000000000000000000, 0.000000000000000000, 0.000000000000000000 ) ) ;
#24714=CARTESIAN_POINT ( 'NONE',  ( 23.58679329660199997, 13.29300756424000163, 4.188721108045000641 ) ) ;
#24718=CARTESIAN_POINT ( 'NONE',  ( 15.83043922992600017, 9.441080823466998950, 8.288885697152998944 ) ) ;
#24719=EDGE_CURVE ( 'NONE', #61548, #63587, #33198, .T. ) ;
#24730=CARTESIAN_POINT ( 'NONE',  ( 23.61813716456500245, 10.28283487008000030, 9.267309039017000316 ) ) ;
#24733=DIRECTION ( 'NONE',  ( -5.668025694556021242E-06, 0.2588381829991006078, -0.9659206980853023428 ) ) ;
#24742=EDGE_LOOP ( 'NONE', ( #56549, #16910, #37975, #19444, #61976 ) ) ;
#24743=CARTESIAN_POINT ( 'NONE',  ( 24.44496483130000186, -3.224879855413000040, 12.03535978074999946 ) ) ;
#24747=CARTESIAN_POINT ( 'NONE',  ( 24.62769666311906036, 8.773247286767267283, -9.203857928692515955 ) ) ;
#24750=CARTESIAN_POINT ( 'NONE',  ( 11.26489721861000248, -3.710193004830000252, 11.71182445734000055 ) ) ;
#24760=VERTEX_POINT ( 'NONE', #22126 ) ;
#24778=CYLINDRICAL_SURFACE ( 'NONE', #13194, 0.5000000000000004441 ) ;
#24779=CARTESIAN_POINT ( 'NONE',  ( 18.26005557146100244, -2.925549590147000334, -11.93525498079000080 ) ) ;
#24780=CARTESIAN_POINT ( 'NONE',  ( 24.25375554908000097, -8.963946465867000057, 8.909846166044999904 ) ) ;
#24794=CARTESIAN_POINT ( 'NONE',  ( 15.90000000000000036, 0.000000000000000000, 0.000000000000000000 ) ) ;
#24797=CARTESIAN_POINT ( 'NONE',  ( 25.46375345652300126, 2.879422156700999658, -11.30951020355999859 ) ) ;
#24808=EDGE_CURVE ( 'NONE', #54071, #13468, #43423, .T. ) ;
#24825=CARTESIAN_POINT ( 'NONE',  ( 21.00000012402660232, -1.355091984497000173E-13, 1.088018564133000035E-14 ) ) ;
#24827=CARTESIAN_POINT ( 'NONE',  ( 13.99967273502900156, -9.525279043350998620, -8.192384979499998110 ) ) ;
#24830=CARTESIAN_POINT ( 'NONE',  ( 15.71007343404014200, 8.769519461636436475, 7.669310999670703843 ) ) ;
#24832=CARTESIAN_POINT ( 'NONE',  ( 24.68357798603522113, -11.80735008096011285, 3.191230140235593371 ) ) ;
#24834=ORIENTED_EDGE ( 'NONE', *, *, #59699, .F. ) ;
#24837=CARTESIAN_POINT ( 'NONE',  ( 13.12913653430045002, -11.69120254989815599, -1.923246422712994397 ) ) ;
#24842=ORIENTED_EDGE ( 'NONE', *, *, #4719, .F. ) ;
#24849=CARTESIAN_POINT ( 'NONE',  ( 24.04053350272573653, -3.344386409696779694, 12.67226691567676866 ) ) ;
#24856=CARTESIAN_POINT ( 'NONE',  ( 15.40000000009400161, -8.833277835210999740, -7.896561221812000930 ) ) ;
#24860=CARTESIAN_POINT ( 'NONE',  ( 17.80000000001300009, 3.351264566333000072, -11.15757590352999884 ) ) ;
#24869=EDGE_CURVE ( 'NONE', #43147, #38133, #42548, .T. ) ;
#24888=CIRCLE ( 'NONE', #39411, 1.000000000000000222 ) ;
#24889=EDGE_CURVE ( 'NONE', #42930, #36918, #41317, .T. ) ;
#24890=CARTESIAN_POINT ( 'NONE',  ( 23.60000000000000142, 10.96648613208696688, -8.588734463056562518 ) ) ;
#24894=CARTESIAN_POINT ( 'NONE',  ( 17.80000000009400196, -3.216307036143000175, 11.40341376487999980 ) ) ;
#24899=CARTESIAN_POINT ( 'NONE',  ( 16.13959992722299930, -8.325816698831998153, -8.094004264449001340 ) ) ;
#24901=CARTESIAN_POINT ( 'NONE',  ( 23.56734670131549336, -13.32877617996445352, 4.249149195638875831 ) ) ;
#24910=ORIENTED_EDGE ( 'NONE', *, *, #40926, .T. ) ;
#24913=FACE_OUTER_BOUND ( 'NONE', #46459, .T. ) ;
#24918=CARTESIAN_POINT ( 'NONE',  ( 24.43232361759900328, -3.176382763002000509, 12.00226528444000174 ) ) ;
#24919=EDGE_CURVE ( 'NONE', #47463, #20699, #23108, .T. ) ;
#24929=CARTESIAN_POINT ( 'NONE',  ( 23.59999467231800097, -10.30760443253999981, -9.317695455237998914 ) ) ;
#24938=AXIS2_PLACEMENT_3D ( 'NONE', #50159, #39321, #41639 ) ;
#24939=CARTESIAN_POINT ( 'NONE',  ( 17.80000000001300009, 3.351264566333000072, -11.15757590352999884 ) ) ;
#24945=CARTESIAN_POINT ( 'NONE',  ( 25.30000327618300204, 1.393126554761430436, -11.43653827017141111 ) ) ;
#24948=EDGE_CURVE ( 'NONE', #22779, #47838, #26271, .T. ) ;
#24949=ORIENTED_EDGE ( 'NONE', *, *, #14370, .T. ) ;
#24952=ORIENTED_EDGE ( 'NONE', *, *, #52036, .T. ) ;
#24956=B_SPLINE_CURVE_WITH_KNOTS ( 'NONE', 3,
 ( #12183, #6231, #54829, #11478 ),
 .UNSPECIFIED., .F., .F.,
 ( 4, 4 ),
 ( 0.000000000000000000, 1.000000000000000000 ),
 .UNSPECIFIED. ) ;
#24957=CARTESIAN_POINT ( 'NONE',  ( 24.43231275843400141, -11.98247113617999915, -3.250307990934000024 ) ) ;
#24958=B_SPLINE_CURVE_WITH_KNOTS ( 'NONE', 3,
 ( #48650, #9864, #32240, #16483, #752, #64021, #58107, #64709 ),
 .UNSPECIFIED., .F., .F.,
 ( 4, 2, 2, 4 ),
 ( 0.000000000000000000, 0.5000000000000045519, 0.7500000000000022204, 1.000000000000000000 ),
 .UNSPECIFIED. ) ;
#24959=CARTESIAN_POINT ( 'NONE',  ( 25.55262180961353380, 2.866482437163034636, 11.19816644711434606 ) ) ;
#24976=CARTESIAN_POINT ( 'NONE',  ( 23.55381026917600096, 10.32939677816000135, -9.498137881527000559 ) ) ;
#24977=CARTESIAN_POINT ( 'NONE',  ( 18.18404792230800382, -3.205001206845999651, -11.25648540289999922 ) ) ;
#24980=AXIS2_PLACEMENT_3D ( 'NONE', #46337, #19068, #67298 ) ;
#24982=ORIENTED_EDGE ( 'NONE', *, *, #17439, .F. ) ;
#24984=CIRCLE ( 'NONE', #33929, 0.2000000000000009270 ) ;
#25003=CARTESIAN_POINT ( 'NONE',  ( 23.60000000000000142, 9.305479840184000651, 8.315530346521999405 ) ) ;
#25005=VERTEX_POINT ( 'NONE', #9834 ) ;
#25010=CARTESIAN_POINT ( 'NONE',  ( 13.27439970770000066, -11.71097706365999969, -2.049245155247000127 ) ) ;
#25013=EDGE_LOOP ( 'NONE', ( #30889, #61661, #63882, #2744, #30175 ) ) ;
#25014=TOROIDAL_SURFACE ( 'NONE', #11571, 13.79999999999999893, 0.2000000000000000111 ) ;
#25018=CARTESIAN_POINT ( 'NONE',  ( 15.95563472374800185, 3.716697538693999991, 11.19594450203000058 ) ) ;
#25022=CARTESIAN_POINT ( 'NONE',  ( 23.64705884711741035, 10.02690164441486687, 9.685979275716718462 ) ) ;
#25034=CARTESIAN_POINT ( 'NONE',  ( 24.13225289473700386, 12.49514845794176843, -3.369178721750599070 ) ) ;
#25042=VERTEX_POINT ( 'NONE', #68130 ) ;
#25052=CARTESIAN_POINT ( 'NONE',  ( 25.29987261391899978, -8.756202924575998026, 7.455126447192999883 ) ) ;
#25054=ADVANCED_FACE ( 'NONE', ( #41574 ), #54398, .T. ) ;
#25057=CARTESIAN_POINT ( 'NONE',  ( 15.86122879894100102, 8.802595411723000751, 8.571496522999998646 ) ) ;
#25060=FACE_OUTER_BOUND ( 'NONE', #36950, .T. ) ;
#25065=CARTESIAN_POINT ( 'NONE',  ( 25.30000327618300204, -10.83443035398000021, 3.855530949778000149 ) ) ;
#25067=CARTESIAN_POINT ( 'NONE',  ( 23.73415186908400187, 9.844559812508000718, 9.786437184986999327 ) ) ;
#25072=CARTESIAN_POINT ( 'NONE',  ( 24.30001121497594596, -8.895961315773666556, -8.895961315773666556 ) ) ;
#25075=CARTESIAN_POINT ( 'NONE',  ( 18.31587707750999883, 3.089759977613000252, 11.98885651319999823 ) ) ;
#25084=CARTESIAN_POINT ( 'NONE',  ( 13.84418086765596811, -9.492976300313964444, -8.170822042159171517 ) ) ;
#25088=B_SPLINE_CURVE_WITH_KNOTS ( 'NONE', 3,
 ( #14891, #68703, #63802, #63105 ),
 .UNSPECIFIED., .F., .F.,
 ( 4, 4 ),
 ( 0.000000000000000000, 1.000000000000000000 ),
 .UNSPECIFIED. ) ;
#25090=ADVANCED_FACE ( 'NONE', ( #647 ), #60230, .F. ) ;
#25092=COLOUR_RGB ( '', 0.66274510, 0.83137255, 0.94901961) ;
#25095=ORIENTED_EDGE ( 'NONE', *, *, #41759, .F. ) ;
#25099=DIRECTION ( 'NONE',  ( 0.000000000000000000, -0.9925108176925444559, -0.1221567712543053241 ) ) ;
#25114=B_SPLINE_SURFACE_WITH_KNOTS ( 'NONE', 3, 3, ( 
 ( #44048, #50667, #28304, #2089 ),
 ( #39836, #64996, #29356, #60465 ),
 ( #17472, #23407, #29017, #61158 ),
 ( #23746, #34250, #44401, #33554 ),
 ( #60810, #12573, #13276, #22362 ),
 ( #33209, #66042, #17111, #55570 ),
 ( #38445, #55220, #49627, #7320 ),
 ( #59768, #65701, #1732, #11869 ),
 ( #39138, #17824, #54874, #49974 ),
 ( #1388, #54527, #18166, #33903 ),
 ( #7671, #28661, #39488, #12923 ),
 ( #6629, #22704, #50324, #2422 ),
 ( #61498, #41206, #19536, #67751 ),
 ( #24440, #36294, #62516, #45427 ),
 ( #19187, #3782, #13616, #9035 ),
 ( #45766, #30713, #61836, #9717 ) ),
 .UNSPECIFIED., .F., .F., .F.,
 ( 4, 1, 1, 1, 1, 1, 1, 1, 1, 1, 1, 1, 1, 4 ),
 ( 4, 4 ),
 ( 0.02893036654739999936, 0.07692307692307999434, 0.1538461538461999845, 0.2307692307692000011, 0.3076923076922999933, 0.3846153846154000133, 0.4615384615385000333, 0.5384615384614999112, 0.6153846153845999867, 0.6923076923076999512, 0.7692307692308000266, 0.8461538461537999600, 0.9230769230769000355, 0.9829517739831000744 ),
 ( -0.1837382356070000056, 1.183731649722000068 ),
 .UNSPECIFIED. ) ;
#25120=CARTESIAN_POINT ( 'NONE',  ( 17.79284288850699980, -3.413161633892000335, -11.89755489758000095 ) ) ;
#25121=CARTESIAN_POINT ( 'NONE',  ( 24.50549018619200226, -8.845081872398999678, 9.150167881427000438 ) ) ;
#25129=FACE_OUTER_BOUND ( 'NONE', #65231, .T. ) ;
#25133=CIRCLE ( 'NONE', #3909, 1.300177795737000874 ) ;
#25135=CARTESIAN_POINT ( 'NONE',  ( 18.01722669115800102, 3.499390932422000056, -11.96939125376999868 ) ) ;
#25140=CARTESIAN_POINT ( 'NONE',  ( 18.29995268966800026, -2.861739928647000220, -11.98821236628000086 ) ) ;
#25152=ORIENTED_EDGE ( 'NONE', *, *, #57794, .T. ) ;
#25155=AXIS2_PLACEMENT_3D ( 'NONE', #62367, #68982, #63386 ) ;
#25185=TOROIDAL_SURFACE ( 'NONE', #33021, 11.15000000000000036, 0.5000000000000000000 ) ;
#25187=CARTESIAN_POINT ( 'NONE',  ( 11.50029455687000102, -11.65000000000000036, 0.000000000000000000 ) ) ;
#25188=CARTESIAN_POINT ( 'NONE',  ( 15.89979320885400327, -3.824231472901999496, -11.71686814605000038 ) ) ;
#25190=EDGE_CURVE ( 'NONE', #58690, #47043, #25088, .T. ) ;
#25196=ADVANCED_FACE ( 'NONE', ( #58222 ), #42834, .F. ) ;
#25197=CARTESIAN_POINT ( 'NONE',  ( 23.56664311700400205, 13.31365802054999925, 4.296923094388999331 ) ) ;
#25206=CARTESIAN_POINT ( 'NONE',  ( 24.30001122408866721, -12.15210915335040909, -3.256147833976223538 ) ) ;
#25214=AXIS2_PLACEMENT_3D ( 'NONE', #22050, #64346, #38132 ) ;
#25217=CARTESIAN_POINT ( 'NONE',  ( 13.69997185827399733, 10.91304490500502666, 4.183762365652748727 ) ) ;
#25219=EDGE_CURVE ( 'NONE', #31587, #47463, #34267, .T. ) ;
#25223=ORIENTED_EDGE ( 'NONE', *, *, #4999, .T. ) ;
#25224=CARTESIAN_POINT ( 'NONE',  ( 23.66004879239100234, 13.39256445865000167, -3.813547382634999483 ) ) ;
#25236=CARTESIAN_POINT ( 'NONE',  ( 21.60000000000000142, 0.000000000000000000, 0.000000000000000000 ) ) ;
#25246=CARTESIAN_POINT ( 'NONE',  ( 23.51508327619200145, -2.987169178960999982, 13.81528548245999843 ) ) ;
#25250=CARTESIAN_POINT ( 'NONE',  ( 23.51511192986600207, 2.985795376826999803, -13.81554990515000014 ) ) ;
#25268=CARTESIAN_POINT ( 'NONE',  ( 23.59510617619071482, 13.38784577629162342, 4.018474608037379880 ) ) ;
#25273=EDGE_CURVE ( 'NONE', #16735, #16938, #65059, .T. ) ;
#25276=ORIENTED_EDGE ( 'NONE', *, *, #56357, .T. ) ;
#25292=VERTEX_POINT ( 'NONE', #60258 ) ;
#25299=CARTESIAN_POINT ( 'NONE',  ( 24.72544608131600086, -12.30754379070000049, -2.942921080080999729 ) ) ;
#25304=DIRECTION ( 'NONE',  ( 0.000000000000000000, 1.000000000000000000, 0.000000000000000000 ) ) ;
#25311=ORIENTED_EDGE ( 'NONE', *, *, #35969, .T. ) ;
#25314=CIRCLE ( 'NONE', #14149, 0.3000000000000000444 ) ;
#25317=CARTESIAN_POINT ( 'NONE',  ( 25.19550552243000041, 8.372893704327999842, -8.693236786278001560 ) ) ;
#25319=CARTESIAN_POINT ( 'NONE',  ( 18.31386961183700279, -3.086648833569000328, -11.29009770192999973 ) ) ;
#25328=DIRECTION ( 'NONE',  ( 0.000000000000000000, -0.9624505444715651947, -0.2714570858282905341 ) ) ;
#25331=ADVANCED_FACE ( 'NONE', ( #23193 ), #59939, .T. ) ;
#25332=EDGE_CURVE ( 'NONE', #26903, #4716, #58838, .T. ) ;
#25333=FACE_OUTER_BOUND ( 'NONE', #7511, .T. ) ;
#25338=CARTESIAN_POINT ( 'NONE',  ( 18.50005573548403959, -2.729642361723122246, -11.32578974454799337 ) ) ;
#25349=CARTESIAN_POINT ( 'NONE',  ( 13.73573769406200107, -11.39043216638999922, -2.256426478477000064 ) ) ;
#25352=EDGE_LOOP ( 'NONE', ( #36971, #34218, #17367, #37095 ) ) ;
#25356=EDGE_CURVE ( 'NONE', #27849, #49580, #63329, .T. ) ;
#25358=CARTESIAN_POINT ( 'NONE',  ( 16.04514873068900016, 3.655338946640000142, 11.11851555082999887 ) ) ;
#25364=VECTOR ( 'NONE', #49912, 999.9999999999998863 ) ;
#25371=EDGE_LOOP ( 'NONE', ( #9551, #38873, #25634, #15035, #39562 ) ) ;
#25375=EDGE_LOOP ( 'NONE', ( #44478, #32103, #33803, #62153, #30118, #15670, #22337, #50860, #23738, #57822 ) ) ;
#25379=CARTESIAN_POINT ( 'NONE',  ( 11.72003495742762169, 3.351648276371850699, -11.15746180793245657 ) ) ;
#25395=ORIENTED_EDGE ( 'NONE', *, *, #46597, .F. ) ;
#25412=CONICAL_SURFACE ( 'NONE', #37691, 12.71246950475999959, 0.8960553845711767273 ) ;
#25413=FACE_OUTER_BOUND ( 'NONE', #55418, .T. ) ;
#25419=CONICAL_SURFACE ( 'NONE', #26529, 1.150090567076000214, 0.7854665416972951286 ) ;
#25426=CIRCLE ( 'NONE', #10623, 1.300160336740999734 ) ;
#25430=CARTESIAN_POINT ( 'NONE',  ( 13.99999999347100044, 9.187456302440001110, 8.213201953411001455 ) ) ;
#25432=CARTESIAN_POINT ( 'NONE',  ( 24.67921310950000091, -12.29514723793999842, -2.979192343402000009 ) ) ;
#25436=ORIENTED_EDGE ( 'NONE', *, *, #40314, .T. ) ;
#25439=ORIENTED_EDGE ( 'NONE', *, *, #57207, .T. ) ;
#25441=CARTESIAN_POINT ( 'NONE',  ( 11.50029455687000102, -11.65000000000000213, -0.4692429848744596455 ) ) ;
#25455=ORIENTED_EDGE ( 'NONE', *, *, #58642, .T. ) ;
#25460=CARTESIAN_POINT ( 'NONE',  ( 18.31587707750999883, -3.089759977613000252, -11.98885651319999823 ) ) ;
#25468=ORIENTED_EDGE ( 'NONE', *, *, #69045, .T. ) ;
#25469=LINE ( 'NONE', #46803, #19390 ) ;
#25472=CARTESIAN_POINT ( 'NONE',  ( 24.30000000000000071, -8.756202924575998026, 7.455126447192999883 ) ) ;
#25477=CARTESIAN_POINT ( 'NONE',  ( 23.58665831531100210, -13.29306600526000004, 4.189265998478999720 ) ) ;
#25488=CARTESIAN_POINT ( 'NONE',  ( 13.50003721581400029, 9.159934378815998812, 7.517910889891000537 ) ) ;
#25503=CARTESIAN_POINT ( 'NONE',  ( 24.44496356299600137, 12.03536643057000077, 3.224849944858999784 ) ) ;
#25504=CARTESIAN_POINT ( 'NONE',  ( 24.62620337099106749, 8.774568046559906520, 9.205177742000389074 ) ) ;
#25512=CARTESIAN_POINT ( 'NONE',  ( 11.35641146476999985, 3.755935701663000170, -11.79446980948000068 ) ) ;
#25514=ORIENTED_EDGE ( 'NONE', *, *, #4999, .F. ) ;
#25515=CARTESIAN_POINT ( 'NONE',  ( 16.03331929146651902, 3.865558715575580617, 11.84348844988198479 ) ) ;
#25524=DIRECTION ( 'NONE',  ( -1.000000000000000000, 0.000000000000000000, 0.000000000000000000 ) ) ;
#25526=FACE_OUTER_BOUND ( 'NONE', #49998, .T. ) ;
#25529=DIRECTION ( 'NONE',  ( -1.000000000000000000, 0.000000000000000000, 0.000000000000000000 ) ) ;
#25532=CARTESIAN_POINT ( 'NONE',  ( 11.64440230172174928, 12.39501812775040612, 1.800675216608106366 ) ) ;
#25533=ADVANCED_FACE ( 'NONE', ( #24913 ), #30854, .F. ) ;
#25536=CARTESIAN_POINT ( 'NONE',  ( 23.91426360277828067, -3.339322956494537920, 12.90830990133917133 ) ) ;
#25538=DIRECTION ( 'NONE',  ( -1.000000000000000000, 0.000000000000000000, 0.000000000000000000 ) ) ;
#25539=CARTESIAN_POINT ( 'NONE',  ( 24.32158596962418073, -3.683026248290266036, -12.56966772971727409 ) ) ;
#25540=CARTESIAN_POINT ( 'NONE',  ( 24.52306329364123982, -12.12196665553936192, -3.142986863021403732 ) ) ;
#25542=CARTESIAN_POINT ( 'NONE',  ( 24.22025154479399944, -12.17221585034999976, -3.346030442038999908 ) ) ;
#25545=CARTESIAN_POINT ( 'NONE',  ( 16.03045494250125458, -9.206206171697960627, -8.492540761685251738 ) ) ;
#25559=CARTESIAN_POINT ( 'NONE',  ( 18.50001572531400029, 2.908166856580999937, -12.18270046149000052 ) ) ;
#25561=CARTESIAN_POINT ( 'NONE',  ( 24.92738733624293346, -2.996191037697414128, 11.61850378784546933 ) ) ;
#25562=CARTESIAN_POINT ( 'NONE',  ( 25.22251638624031855, 11.23359187701061757, -3.340255986890024786 ) ) ;
#25573=VERTEX_POINT ( 'NONE', #24575 ) ;
#25574=CARTESIAN_POINT ( 'NONE',  ( 24.54687940532799928, 8.860358431052000938, 9.345000394951000544 ) ) ;
#25579=DIRECTION ( 'NONE',  ( 0.000000000000000000, -0.9659258262890756397, 0.2588190451024932059 ) ) ;
#25589=CARTESIAN_POINT ( 'NONE',  ( 17.94577624695061502, -11.84175277259534731, 3.381006001198936683 ) ) ;
#25590=CARTESIAN_POINT ( 'NONE',  ( 17.80000000000000071, 14.76315775485999993, 50.50083396221000243 ) ) ;
#25599=CARTESIAN_POINT ( 'NONE',  ( 23.63992230472121747, -3.364525824305894197, -13.53833436019511360 ) ) ;
#25602=CARTESIAN_POINT ( 'NONE',  ( 23.58305236527900206, 2.939621645348999834, -13.62877849538000063 ) ) ;
#25620=ORIENTED_EDGE ( 'NONE', *, *, #57743, .F. ) ;
#25623=ORIENTED_EDGE ( 'NONE', *, *, #60693, .F. ) ;
#25634=ORIENTED_EDGE ( 'NONE', *, *, #63516, .T. ) ;
#25637=VERTEX_POINT ( 'NONE', #45566 ) ;
#25645=ADVANCED_FACE ( 'NONE', ( #8495 ), #14089, .F. ) ;
#25649=CARTESIAN_POINT ( 'NONE',  ( 12.24011731813700088, 12.12177778538999995, -3.303327906653999779 ) ) ;
#25654=CARTESIAN_POINT ( 'NONE',  ( 18.31386961183700279, 3.086648833569000328, 11.29009770192999973 ) ) ;
#25660=DIRECTION ( 'NONE',  ( 0.000000000000000000, 1.000000000000000000, 4.343333852297002239E-12 ) ) ;
#25667=CARTESIAN_POINT ( 'NONE',  ( 23.58334011193800350, 0.000000000000000000, -13.94232983116038227 ) ) ;
#25672=FACE_OUTER_BOUND ( 'NONE', #5407, .T. ) ;
#25677=CARTESIAN_POINT ( 'NONE',  ( 13.99947726215000188, 8.835099311859000437, 7.952110511812001015 ) ) ;
#25685=B_SPLINE_CURVE_WITH_KNOTS ( 'NONE', 3,
 ( #47162, #68462, #20585, #41911, #292, #21952 ),
 .UNSPECIFIED., .F., .F.,
 ( 4, 2, 4 ),
 ( 0.000000000000000000, 0.5000000000000000000, 1.000000000000000000 ),
 .UNSPECIFIED. ) ;
#25687=CARTESIAN_POINT ( 'NONE',  ( 13.56648734862639571, 12.13584047101458374, 2.505837749223091215 ) ) ;
#25692=B_SPLINE_CURVE_WITH_KNOTS ( 'NONE', 3,
 ( #66113, #38869, #33969, #18580, #44811, #22426, #1804, #7044, #43768, #44122 ),
 .UNSPECIFIED., .F., .F.,
 ( 4, 2, 2, 2, 4 ),
 ( 0.4999999997123705242, 0.6249999997842778932, 0.7499999998561852621, 0.8749999999280926311, 1.000000000000000000 ),
 .UNSPECIFIED. ) ;
#25703=CARTESIAN_POINT ( 'NONE',  ( 16.04504292973000190, 8.364028678926000993, 8.186631590245999845 ) ) ;
#25704=EDGE_CURVE ( 'NONE', #62492, #19870, #24958, .T. ) ;
#25709=FACE_OUTER_BOUND ( 'NONE', #45445, .T. ) ;
#25737=FACE_OUTER_BOUND ( 'NONE', #1635, .T. ) ;
#25739=ADVANCED_FACE ( 'NONE', ( #47623 ), #15382, .F. ) ;
#25744=EDGE_LOOP ( 'NONE', ( #58313, #68768, #5076, #24085 ) ) ;
#25745=CARTESIAN_POINT ( 'NONE',  ( 19.89999890908300273, 12.52500000000000036, 0.000000000000000000 ) ) ;
#25749=CARTESIAN_POINT ( 'NONE',  ( 15.86281931570199966, 8.823480018325001950, 8.551042465543998716 ) ) ;
#25754=EDGE_CURVE ( 'NONE', #12209, #9710, #22471, .T. ) ;
#25760=CARTESIAN_POINT ( 'NONE',  ( 24.30000000000000071, -2.078227429405999693, -11.31065739696999906 ) ) ;
#25766=CARTESIAN_POINT ( 'NONE',  ( 18.44331666222400301, 2.998518551215999750, 12.10579027554000042 ) ) ;
#25783=CARTESIAN_POINT ( 'NONE',  ( 16.13899430609699692, -3.920333201250000066, -11.93553532998999955 ) ) ;
#25785=ORIENTED_EDGE ( 'NONE', *, *, #1590, .F. ) ;
#25786=CARTESIAN_POINT ( 'NONE',  ( 16.09997386696500143, -8.350085070477001992, -8.123950967096998710 ) ) ;
#25788=VERTEX_POINT ( 'NONE', #26984 ) ;
#25801=CARTESIAN_POINT ( 'NONE',  ( 25.46372189163300348, -2.879475976718999686, 11.30953721564000070 ) ) ;
#25806=CARTESIAN_POINT ( 'NONE',  ( 23.56967113362556177, -13.34588780157434051, -4.192937399727497016 ) ) ;
#25810=CARTESIAN_POINT ( 'NONE',  ( 24.30000000000000071, -3.224868684338999980, -12.03537377768999939 ) ) ;
#25817=CARTESIAN_POINT ( 'NONE',  ( 11.79999999471800010, -3.216299622513999701, 11.40340969442000052 ) ) ;
#25822=CARTESIAN_POINT ( 'NONE',  ( 24.51193677669900239, -12.36181969389999935, 3.074607925011999754 ) ) ;
#25844=FACE_OUTER_BOUND ( 'NONE', #62649, .T. ) ;
#25846=CARTESIAN_POINT ( 'NONE',  ( 24.53429010490700080, 8.855930189872001534, 9.286429716155000236 ) ) ;
#25852=CARTESIAN_POINT ( 'NONE',  ( 13.46268444654400298, -9.428250749343998649, -7.876929641374000646 ) ) ;
#25858=CARTESIAN_POINT ( 'NONE',  ( 23.60000000000000142, -2.204728229456999866, 11.99913219504999873 ) ) ;
#25860=ORIENTED_EDGE ( 'NONE', *, *, #56320, .T. ) ;
#25865=CARTESIAN_POINT ( 'NONE',  ( 24.30000000000000071, -50.08530474119000075, 49.09535524753000146 ) ) ;
#25873=EDGE_LOOP ( 'NONE', ( #56977, #19093, #67373, #3128 ) ) ;
#25877=DIRECTION ( 'NONE',  ( 0.000000000000000000, 0.7071067811865475727, 0.7071067811865475727 ) ) ;
#25885=EDGE_LOOP ( 'NONE', ( #28447, #20517, #59913 ) ) ;
#25887=CARTESIAN_POINT ( 'NONE',  ( 13.39991752512747247, -12.13029446165151803, -2.190571078338873878 ) ) ;
#25907=B_SPLINE_CURVE_WITH_KNOTS ( 'NONE', 3,
 ( #42459, #26383, #47709, #839, #15879, #33002 ),
 .UNSPECIFIED., .F., .F.,
 ( 4, 2, 4 ),
 ( 0.000000000000000000, 0.5000000000000000000, 1.000000000000000000 ),
 .UNSPECIFIED. ) ;
#25912=CARTESIAN_POINT ( 'NONE',  ( 24.56351374471499938, 8.793767919668001198, 9.098879823118998900 ) ) ;
#25922=ADVANCED_FACE ( 'NONE', ( #41949 ), #17227, .F. ) ;
#25926=CARTESIAN_POINT ( 'NONE',  ( 25.50736953685058594, 8.309690528669074538, 8.116381377235668992 ) ) ;
#25929=CARTESIAN_POINT ( 'NONE',  ( 15.39229341877100232, -8.812225371893999792, -7.562487140343000291 ) ) ;
#25931=DIRECTION ( 'NONE',  ( 1.000000000000000000, 0.000000000000000000, 0.000000000000000000 ) ) ;
#25935=DIRECTION ( 'NONE',  ( -1.000000000000000000, 0.000000000000000000, 0.000000000000000000 ) ) ;
#25936=AXIS2_PLACEMENT_3D ( 'NONE', #4923, #58407, #53167 ) ;
#25941=CARTESIAN_POINT ( 'NONE',  ( 23.63922860583116403, -3.363517752404959538, 13.53948175984613123 ) ) ;
#25942=CARTESIAN_POINT ( 'NONE',  ( 24.30000561190290043, 3.240508259137445446, 12.09374146544330486 ) ) ;
#25962=CARTESIAN_POINT ( 'NONE',  ( 23.54905712943500262, 13.36550135992999877, -4.294179668706000541 ) ) ;
#25963=B_SPLINE_CURVE_WITH_KNOTS ( 'NONE', 3,
 ( #46187, #2499, #67497, #34330, #45505, #51426, #19615, #33979, #56334, #2166, #66818, #61917, #55300, #7395, #40593, #8438, #28742, #61235, #13351, #7749, #3521, #34676 ),
 .UNSPECIFIED., .F., .F.,
 ( 4, 2, 2, 1, 2, 2, 2, 1, 1, 1, 2, 2, 4 ),
 ( 0.000000000000000000, 0.2499999999999992228, 0.3749999999999970024, 0.4374999999999989453, 0.4687499999999975575, 0.4999999999999961142, 0.6250000000000044409, 0.6875000000000058842, 0.7187500000000067724, 0.7343750000000085487, 0.7421875000000084377, 0.7500000000000083267, 1.000000000000000000 ),
 .UNSPECIFIED. ) ;
#25967=VERTEX_POINT ( 'NONE', #22336 ) ;
#25969=CARTESIAN_POINT ( 'NONE',  ( 12.99999999998900080, 12.39025855408000076, 1.832244667012999928 ) ) ;
#25978=CARTESIAN_POINT ( 'NONE',  ( 13.43887202961200167, 11.47449689335000045, 1.782105406474000064 ) ) ;
#25994=CARTESIAN_POINT ( 'NONE',  ( 12.70688507812400125, 11.81408563393000044, -3.326099274546999940 ) ) ;
#25995=CARTESIAN_POINT ( 'NONE',  ( 17.99644948955100077, 11.78614875273999907, -3.442261952866000119 ) ) ;
#25999=CARTESIAN_POINT ( 'NONE',  ( 18.38069952315600020, -3.381269036354999979, 12.09968217836000015 ) ) ;
#26002=ORIENTED_EDGE ( 'NONE', *, *, #68605, .T. ) ;
#26005=DIRECTION ( 'NONE',  ( -1.000000000000000000, 0.000000000000000000, 0.000000000000000000 ) ) ;
#26009=B_SPLINE_CURVE_WITH_KNOTS ( 'NONE', 3,
 ( #40688, #8535, #35795, #51863, #68276, #36132 ),
 .UNSPECIFIED., .F., .F.,
 ( 4, 2, 4 ),
 ( 0.000000000000000000, 0.5000000000000000000, 1.000000000000000000 ),
 .UNSPECIFIED. ) ;
#26022=CARTESIAN_POINT ( 'NONE',  ( 16.39965637475000193, -3.313349101483999970, -11.22428178643999885 ) ) ;
#26023=CARTESIAN_POINT ( 'NONE',  ( 13.89314246895800231, 8.838637615320999785, 7.948101024408999571 ) ) ;
#26029=CONICAL_SURFACE ( 'NONE', #11546, 11.75017108327000059, 0.7854127224616339609 ) ;
#26031=CARTESIAN_POINT ( 'NONE',  ( 18.46714228073847863, -2.893782244577476792, -11.28496185859584067 ) ) ;
#26033=B_SPLINE_CURVE_WITH_KNOTS ( 'NONE', 3,
 ( #34539, #68041, #35221, #46389, #14915, #36237 ),
 .UNSPECIFIED., .F., .F.,
 ( 4, 2, 4 ),
 ( 0.000000000000000000, 0.5000000000000000000, 1.000000000000000000 ),
 .UNSPECIFIED. ) ;
#26036=CARTESIAN_POINT ( 'NONE',  ( 25.60000000000000142, 0.000000000000000000, 0.000000000000000000 ) ) ;
#26037=CARTESIAN_POINT ( 'NONE',  ( 24.62774583285499830, 3.462210234181999802, -12.08748376425999993 ) ) ;
#26046=CARTESIAN_POINT ( 'NONE',  ( 12.95917414208900098, -11.49387908994000007, -1.654391991822000030 ) ) ;
#26047=CARTESIAN_POINT ( 'NONE',  ( 11.49999672495000169, -10.14910021683508390, 5.848045769722698850 ) ) ;
#26050=DIRECTION ( 'NONE',  ( 0.000000000000000000, -0.7614089499631909730, 0.6482718649732925886 ) ) ;
#26054=CARTESIAN_POINT ( 'NONE',  ( 15.84051303026600266, 8.692957937327999929, 7.975472622866001338 ) ) ;
#26055=VERTEX_POINT ( 'NONE', #8164 ) ;
#26063=CARTESIAN_POINT ( 'NONE',  ( 25.48313547908499999, 11.09945010898000106, -3.317479108978999669 ) ) ;
#26065=ORIENTED_EDGE ( 'NONE', *, *, #39009, .T. ) ;
#26067=AXIS2_PLACEMENT_3D ( 'NONE', #29301, #3730, #61782 ) ;
#26070=CARTESIAN_POINT ( 'NONE',  ( 23.64563777841849301, -10.02996334016318514, 9.685372740697550498 ) ) ;
#26077=EDGE_LOOP ( 'NONE', ( #8698, #46529, #5043, #37841, #56706, #68972 ) ) ;
#26085=DIRECTION ( 'NONE',  ( -1.000000000000000000, 0.000000000000000000, 0.000000000000000000 ) ) ;
#26090=VERTEX_POINT ( 'NONE', #18657 ) ;
#26092=B_SPLINE_CURVE_WITH_KNOTS ( 'NONE', 3,
 ( #9706, #26144, #57957, #31052 ),
 .UNSPECIFIED., .F., .F.,
 ( 4, 4 ),
 ( 0.000000000000000000, 1.000000000000000000 ),
 .UNSPECIFIED. ) ;
#26095=CARTESIAN_POINT ( 'NONE',  ( 15.66944243593800046, 9.081775842407999733, 8.276637282895999093 ) ) ;
#26103=B_SPLINE_SURFACE_WITH_KNOTS ( 'NONE', 3, 3, ( 
 ( #64047, #37492, #2849, #7403 ),
 ( #50753, #34338, #50406, #60549 ),
 ( #66474, #28748, #33642, #34684 ),
 ( #12656, #44827, #39224, #1471 ),
 ( #39924, #49712, #50064, #54609 ),
 ( #18598, #65435, #11955, #38883 ),
 ( #66130, #12309, #17906, #23138 ),
 ( #18249, #33987, #44489, #60205 ),
 ( #23833, #17557, #61243, #39571 ) ),
 .UNSPECIFIED., .F., .F., .F.,
 ( 4, 1, 1, 1, 1, 1, 4 ),
 ( 4, 4 ),
 ( 0.02166927333700999908, 0.1666666666667000196, 0.3333333333333000081, 0.5000000000000000000, 0.6666666666667000474, 0.8333333333333000637, 0.9489586827378000411 ),
 ( -0.1917159053268999991, 1.191863452461999984 ),
 .UNSPECIFIED. ) ;
#26105=CARTESIAN_POINT ( 'NONE',  ( 18.50001572531400029, -2.908166856580999937, 12.18270046149000052 ) ) ;
#26109=CARTESIAN_POINT ( 'NONE',  ( 23.60000000000000142, 2.548720605937000006, -12.21654710926000220 ) ) ;
#26113=CARTESIAN_POINT ( 'NONE',  ( 18.12310803393399894, 3.320912951897000198, 11.92519506916999994 ) ) ;
#26120=CARTESIAN_POINT ( 'NONE',  ( 24.66807826070334286, 8.737531166019467221, -9.168167557861536920 ) ) ;
#26131=CARTESIAN_POINT ( 'NONE',  ( 16.13732479921000262, -3.901986904155000158, -11.94169104666999992 ) ) ;
#26132=CARTESIAN_POINT ( 'NONE',  ( 11.40156680346000151, 11.68030187645999973, 1.636056047313999784 ) ) ;
#26144=CARTESIAN_POINT ( 'NONE',  ( 24.39664795055900015, -12.09373373542098840, -3.240506187884208522 ) ) ;
#26149=DIRECTION ( 'NONE',  ( 1.000000000000000000, 0.000000000000000000, 0.000000000000000000 ) ) ;
#26151=CARTESIAN_POINT ( 'NONE',  ( 11.79999999116810727, 3.511856242852833265, -11.95218832016636945 ) ) ;
#26154=ADVANCED_FACE ( 'NONE', ( #50128 ), #39990, .F. ) ;
#26157=CARTESIAN_POINT ( 'NONE',  ( 23.89320776801300283, -8.862674798062995407, 7.304122743114001004 ) ) ;
#26168=CARTESIAN_POINT ( 'NONE',  ( 11.79999999523987420, -3.306280043674564517, 11.23952258183352093 ) ) ;
#26177=CARTESIAN_POINT ( 'NONE',  ( 18.29983863915590447, -0.9627070671913217081, -12.32514597913991850 ) ) ;
#26182=TOROIDAL_SURFACE ( 'NONE', #66399, 12.20000000000000107, 0.6999999999999999556 ) ;
#26187=EDGE_CURVE ( 'NONE', #64377, #29725, #64460, .T. ) ;
#26188=EDGE_CURVE ( 'NONE', #49285, #22409, #44889, .T. ) ;
#26192=VERTEX_POINT ( 'NONE', #1889 ) ;
#26196=CARTESIAN_POINT ( 'NONE',  ( 17.66658675203003881, 10.78295181803898295, -4.410266442050934543 ) ) ;
#26197=CARTESIAN_POINT ( 'NONE',  ( 24.57788509281022016, 8.817303531626452084, 9.247882801663969587 ) ) ;
#26204=CARTESIAN_POINT ( 'NONE',  ( 14.03164332880499998, -9.396061154353999356, -8.198822423776999102 ) ) ;
#26206=EDGE_LOOP ( 'NONE', ( #15136, #38903, #65003, #6607 ) ) ;
#26218=DIRECTION ( 'NONE',  ( 1.000000000000000000, 0.000000000000000000, 0.000000000000000000 ) ) ;
#26219=CARTESIAN_POINT ( 'NONE',  ( 23.73802576740300196, 3.438769318319999879, 13.34821028306000024 ) ) ;
#26236=CARTESIAN_POINT ( 'NONE',  ( 13.48771849468881534, -12.09748862696537763, -2.366366213948142949 ) ) ;
#26237=VERTEX_POINT ( 'NONE', #28464 ) ;
#26239=ADVANCED_FACE ( 'NONE', ( #65499 ), #39594, .F. ) ;
#26242=CARTESIAN_POINT ( 'NONE',  ( 27.09999999999999787, -4.026362576680999827E-13, -10.75000000000000000 ) ) ;
#26251=VERTEX_POINT ( 'NONE', #13757 ) ;
#26271=LINE ( 'NONE', #63657, #27604 ) ;
#26275=EDGE_CURVE ( 'NONE', #27371, #56572, #56670, .T. ) ;
#26277=CARTESIAN_POINT ( 'NONE',  ( 12.79999998712400178, 11.53033693765999779, -4.891431908114999949 ) ) ;
#26282=DIRECTION ( 'NONE',  ( 0.000000000000000000, 0.000000000000000000, -1.000000000000000000 ) ) ;
#26287=CARTESIAN_POINT ( 'NONE',  ( 14.80000000000000071, 3.283787102340999464, -11.28049554847999936 ) ) ;
#26289=CARTESIAN_POINT ( 'NONE',  ( 23.57795415946532458, -3.116628345736323968, -13.63414192076861831 ) ) ;
#26301=B_SPLINE_CURVE_WITH_KNOTS ( 'NONE', 3,
 ( #3500, #8416, #29759, #61894, #66795, #19594, #24837, #18567 ),
 .UNSPECIFIED., .F., .F.,
 ( 4, 2, 2, 4 ),
 ( 0.000000000000000000, 0.2500000000000013323, 0.5000000000000026645, 1.000000000000000000 ),
 .UNSPECIFIED. ) ;
#26304=CARTESIAN_POINT ( 'NONE',  ( 24.59181005845499968, 12.25104096035999923, 3.053504809259000030 ) ) ;
#26305=CARTESIAN_POINT ( 'NONE',  ( 23.60000000000000142, 2.548720605937000006, -12.21654710926000220 ) ) ;
#26306=CARTESIAN_POINT ( 'NONE',  ( 11.50001544674999820, -8.431319371640864091, 9.354420476383705108 ) ) ;
#26309=CARTESIAN_POINT ( 'NONE',  ( 24.25970694110000281, 12.09491440691000008, -3.326705949661999728 ) ) ;
#26313=ORIENTED_EDGE ( 'NONE', *, *, #67081, .T. ) ;
#26320=CARTESIAN_POINT ( 'NONE',  ( 18.15531827655737018, 3.266808065264576566, -11.18265383028565196 ) ) ;
#26321=CIRCLE ( 'NONE', #19633, 0.6999999999999992895 ) ;
#26327=ORIENTED_EDGE ( 'NONE', *, *, #11208, .F. ) ;
#26332=SURFACE_SIDE_STYLE ('',( #9549 ) ) ;
#26333=B_SPLINE_CURVE_WITH_KNOTS ( 'NONE', 3,
 ( #9002, #62144, #15287, #56561 ),
 .UNSPECIFIED., .F., .F.,
 ( 4, 4 ),
 ( 0.000000000000000000, 1.000000000000000000 ),
 .UNSPECIFIED. ) ;
#26334=ORIENTED_EDGE ( 'NONE', *, *, #29648, .T. ) ;
#26337=AXIS2_PLACEMENT_3D ( 'NONE', #23635, #34139, #66277 ) ;
#26342=CARTESIAN_POINT ( 'NONE',  ( 12.08926246520500136, 11.62544123506999938, -4.252388861798999997 ) ) ;
#26343=CARTESIAN_POINT ( 'NONE',  ( 17.86320573775099874, 11.40784081139999984, -4.532785132108998916 ) ) ;
#26346=CARTESIAN_POINT ( 'NONE',  ( 12.11873369409514112, -11.72532246831141478, 3.796278118051448658 ) ) ;
#26347=CARTESIAN_POINT ( 'NONE',  ( 18.06894639827790527, 12.08549470499584189, -3.288878289815732714 ) ) ;
#26352=ORIENTED_EDGE ( 'NONE', *, *, #62808, .F. ) ;
#26357=CARTESIAN_POINT ( 'NONE',  ( 11.36656541973662016, 12.29888939610234644, 1.513729097026024650 ) ) ;
#26364=VERTEX_POINT ( 'NONE', #46258 ) ;
#26371=CARTESIAN_POINT ( 'NONE',  ( 16.15961700471899931, -3.514971253533999640, -11.06754630474000045 ) ) ;
#26373=CARTESIAN_POINT ( 'NONE',  ( 13.99965637475000158, 8.819038952442999957, 7.693330608063000398 ) ) ;
#26383=CARTESIAN_POINT ( 'NONE',  ( 23.60000000000000142, 12.92131265950320973, 5.202871703995182173 ) ) ;
#26394=FACE_OUTER_BOUND ( 'NONE', #55296, .T. ) ;
#26398=VERTEX_POINT ( 'NONE', #63694 ) ;
#26409=ORIENTED_EDGE ( 'NONE', *, *, #37396, .T. ) ;
#26411=CARTESIAN_POINT ( 'NONE',  ( 24.74446730232600089, 11.86528397834999815, -3.111028153312999756 ) ) ;
#26423=CARTESIAN_POINT ( 'NONE',  ( 24.14647602714345709, 12.47136813241617226, 3.359330280457781814 ) ) ;
#26438=CARTESIAN_POINT ( 'NONE',  ( 12.78642148534500045, -11.38816520531000087, 4.576060180783999343 ) ) ;
#26439=EDGE_CURVE ( 'NONE', #8238, #66745, #67416, .T. ) ;
#26441=ADVANCED_FACE ( 'NONE', ( #16833 ), #39024, .F. ) ;
#26445=DIRECTION ( 'NONE',  ( 0.000000000000000000, 0.001485959642859935011, -0.9999988959613604900 ) ) ;
#26451=CARTESIAN_POINT ( 'NONE',  ( 18.49562053141630713, -2.998066116901991762, 12.16097201970263875 ) ) ;
#26459=AXIS2_PLACEMENT_3D ( 'NONE', #47419, #58245, #5104 ) ;
#26460=CARTESIAN_POINT ( 'NONE',  ( 18.53936233968600078, 2.923364741758000207, 12.21823820824000073 ) ) ;
#26466=CARTESIAN_POINT ( 'NONE',  ( 25.00269881440402386, -8.478843172797441596, 8.837112395074729676 ) ) ;
#26477=CARTESIAN_POINT ( 'NONE',  ( 11.79999999471800010, 11.69117318561000118, 1.923227876431999883 ) ) ;
#26478=CARTESIAN_POINT ( 'NONE',  ( 11.42387073792000152, 11.74429294849999827, 1.827310270344000065 ) ) ;
#26481=CARTESIAN_POINT ( 'NONE',  ( 24.68356136276056390, -8.667369894679193720, -8.629863677887273710 ) ) ;
#26482=DIRECTION ( 'NONE',  ( 0.000000000000000000, 0.000000000000000000, 1.000000000000000000 ) ) ;
#26483=EDGE_LOOP ( 'NONE', ( #4191, #64979, #42729, #30496 ) ) ;
#26499=CARTESIAN_POINT ( 'NONE',  ( 24.30000000000000071, -9.517611874540000017, -8.103398312166000039 ) ) ;
#26500=CARTESIAN_POINT ( 'NONE',  ( 15.89979320885400327, -3.824231472901999496, -11.71686814605000038 ) ) ;
#26510=DIRECTION ( 'NONE',  ( 0.000000000000000000, 0.000000000000000000, -1.000000000000000000 ) ) ;
#26511=CARTESIAN_POINT ( 'NONE',  ( 16.00017105474300294, 4.418687638008000347E-13, 6.430411758629000588E-13 ) ) ;
#26512=B_SPLINE_CURVE_WITH_KNOTS ( 'NONE', 3,
 ( #2571, #35095, #3261, #46610, #2914, #24929 ),
 .UNSPECIFIED., .F., .F.,
 ( 4, 2, 4 ),
 ( 0.000000000000000000, 0.5000000000000000000, 1.000000000000000000 ),
 .UNSPECIFIED. ) ;
#26514=CARTESIAN_POINT ( 'NONE',  ( 12.79999999975700042, -11.86189249994999884, 3.298671769835999967 ) ) ;
#26517=CARTESIAN_POINT ( 'NONE',  ( 24.42337838643000225, -12.73360400642000023, 3.018840435665000044 ) ) ;
#26523=CARTESIAN_POINT ( 'NONE',  ( 18.29983863915590447, -1.925365884025486807, -12.21183829392446540 ) ) ;
#26528=CARTESIAN_POINT ( 'NONE',  ( 18.26242787221299935, 2.744348664398000182, -11.56741553474000028 ) ) ;
#26529=AXIS2_PLACEMENT_3D ( 'NONE', #10288, #58873, #43493 ) ;
#26537=ORIENTED_EDGE ( 'NONE', *, *, #46597, .T. ) ;
#26538=CYLINDRICAL_SURFACE ( 'NONE', #38706, 0.6999999999999992895 ) ;
#26541=DIRECTION ( 'NONE',  ( -1.000000000000000000, 0.000000000000000000, 0.000000000000000000 ) ) ;
#26542=EDGE_CURVE ( 'NONE', #48552, #8563, #47778, .T. ) ;
#26568=CARTESIAN_POINT ( 'NONE',  ( 25.21375202814359540, -11.24065089990825506, -3.343241695434690630 ) ) ;
#26573=ORIENTED_EDGE ( 'NONE', *, *, #21994, .F. ) ;
#26582=ORIENTED_EDGE ( 'NONE', *, *, #53518, .T. ) ;
#26583=CARTESIAN_POINT ( 'NONE',  ( 15.82725884711995157, -9.380130419263611685, -8.300201155565218869 ) ) ;
#26589=EDGE_CURVE ( 'NONE', #20805, #48851, #25692, .T. ) ;
#26601=CARTESIAN_POINT ( 'NONE',  ( 24.91840527020981000, 8.566764005888588329, 8.413212214599523620 ) ) ;
#26620=CIRCLE ( 'NONE', #8751, 12.42499880353999941 ) ;
#26623=CARTESIAN_POINT ( 'NONE',  ( 17.97784399489637508, -3.574258648615100231, -12.00418160090810993 ) ) ;
#26626=B_SPLINE_CURVE_WITH_KNOTS ( 'NONE', 3,
 ( #47483, #10409, #25806, #47139, #32098, #36295, #57969, #9718, #4467, #4125 ),
 .UNSPECIFIED., .F., .F.,
 ( 4, 2, 2, 2, 4 ),
 ( 0.000000000000000000, 0.2499999999999997780, 0.3750000000000005551, 0.5000000000000013323, 1.000000000000000000 ),
 .UNSPECIFIED. ) ;
#26629=CARTESIAN_POINT ( 'NONE',  ( 15.39518154839200115, -8.837017240434999366, -7.949877004991000362 ) ) ;
#26631=LINE ( 'NONE', #21032, #24119 ) ;
#26636=CARTESIAN_POINT ( 'NONE',  ( 24.53429014662800256, -8.855930250654999725, 9.286429702500999639 ) ) ;
#26641=CARTESIAN_POINT ( 'NONE',  ( 23.66004879239100234, -3.393653467490999720, 13.50507469661999949 ) ) ;
#26647=B_SPLINE_CURVE_WITH_KNOTS ( 'NONE', 3,
 ( #46361, #63453, #31314, #62086, #4722, #4379, #57877, #67662 ),
 .UNSPECIFIED., .F., .F.,
 ( 4, 2, 2, 4 ),
 ( 0.4992598756075863897, 0.7496299378037931671, 0.8748149689018966946, 1.000000000000000000 ),
 .UNSPECIFIED. ) ;
#26648=CARTESIAN_POINT ( 'NONE',  ( 17.80000000001300009, -3.351264566333000072, 11.15757590352999884 ) ) ;
#26656=CARTESIAN_POINT ( 'NONE',  ( 18.29983863916000075, 2.861762957209999847, -11.98830831200999825 ) ) ;
#26657=CARTESIAN_POINT ( 'NONE',  ( 24.00507652701418237, 9.358504537843028714, -9.266396259472484687 ) ) ;
#26659=CARTESIAN_POINT ( 'NONE',  ( 23.99192795366400333, 13.00768256589000060, -3.383863472243999748 ) ) ;
#26665=PLANE ( 'NONE',  #23936 ) ;
#26669=CARTESIAN_POINT ( 'NONE',  ( 17.60000000000000142, 11.23412379136000006, -3.084957477885999833 ) ) ;
#26671=EDGE_CURVE ( 'NONE', #57964, #28289, #17406, .T. ) ;
#26672=CARTESIAN_POINT ( 'NONE',  ( 18.23176382712000176, -2.916721637292999603, 11.52766586543999949 ) ) ;
#26673=ADVANCED_FACE ( 'NONE', ( #30783 ), #19724, .F. ) ;
#26683=EDGE_LOOP ( 'NONE', ( #27088, #59221, #23384, #32607 ) ) ;
#26687=B_SPLINE_SURFACE_WITH_KNOTS ( 'NONE', 3, 3, ( 
 ( #68821, #63579, #46827, #69168 ),
 ( #67790, #20593, #63227, #37025 ),
 ( #19911, #42609, #14331, #41236 ),
 ( #68132, #35654, #56968, #51719 ),
 ( #20250, #41576, #62884, #15005 ),
 ( #54474, #49225, #21617, #22998 ),
 ( #27219, #37360, #32809, #64944 ),
 ( #38043, #16030, #28252, #17416 ),
 ( #27915, #53444, #32469, #16374 ) ),
 .UNSPECIFIED., .F., .F., .F.,
 ( 4, 1, 1, 1, 1, 1, 4 ),
 ( 4, 4 ),
 ( 0.02166927333703000044, 0.1666666666667000196, 0.3333333333333000081, 0.5000000000000000000, 0.6666666666667000474, 0.8333333333333000637, 0.9489586827378000411 ),
 ( -0.1917159053268999991, 1.191863452461999984 ),
 .UNSPECIFIED. ) ;
#26691=FACE_OUTER_BOUND ( 'NONE', #38183, .T. ) ;
#26692=CARTESIAN_POINT ( 'NONE',  ( 17.61332066134400165, 11.38815944871000063, -4.576072459028000416 ) ) ;
#26694=CARTESIAN_POINT ( 'NONE',  ( 18.30000000000000071, -2.775715947008034146, 11.68320807311170917 ) ) ;
#26695=ADVANCED_FACE ( 'NONE', ( #18921 ), #46177, .T. ) ;
#26697=CARTESIAN_POINT ( 'NONE',  ( 17.75883778089099962, -3.641526152925000037, 12.02434993381999995 ) ) ;
#26703=B_SPLINE_CURVE_WITH_KNOTS ( 'NONE', 3,
 ( #25224, #39589, #34356, #61260, #55676, #50421 ),
 .UNSPECIFIED., .F., .F.,
 ( 4, 2, 4 ),
 ( 0.000000000000000000, 0.5000000000000000000, 1.000000000000000000 ),
 .UNSPECIFIED. ) ;
#26714=ADVANCED_FACE ( 'NONE', ( #68171 ), #2948, .F. ) ;
#26715=DIRECTION ( 'NONE',  ( 0.000000000000000000, 1.000000000000000000, 0.000000000000000000 ) ) ;
#26717=CARTESIAN_POINT ( 'NONE',  ( 11.79999999684100054, -3.345264396959000130, 11.86064773189999855 ) ) ;
#26721=CARTESIAN_POINT ( 'NONE',  ( 16.34806348789000197, -3.378436248652000096, -11.11006988061000023 ) ) ;
#26722=CARTESIAN_POINT ( 'NONE',  ( 13.73494720760600174, -12.32760134815999997, -2.421442066891999811 ) ) ;
#26728=ORIENTED_EDGE ( 'NONE', *, *, #53122, .F. ) ;
#26731=FACE_OUTER_BOUND ( 'NONE', #22512, .T. ) ;
#26735=CARTESIAN_POINT ( 'NONE',  ( 25.37703116084200161, -11.10735239355999937, -3.396338630210000264 ) ) ;
#26741=CARTESIAN_POINT ( 'NONE',  ( 11.49999672495000169, -3.632761979779000061, 11.06912554803999882 ) ) ;
#26749=DIRECTION ( 'NONE',  ( 0.000000000000000000, 0.000000000000000000, -1.000000000000000000 ) ) ;
#26753=EDGE_CURVE ( 'NONE', #35889, #15208, #44905, .T. ) ;
#26756=EDGE_CURVE ( 'NONE', #12493, #19330, #35732, .T. ) ;
#26766=CARTESIAN_POINT ( 'NONE',  ( 15.96683822361929295, 3.674392175451481446, 11.19597380828297517 ) ) ;
#26773=CARTESIAN_POINT ( 'NONE',  ( 25.30000327618300204, -2.078227429405999693, 11.31065739696999906 ) ) ;
#26775=CARTESIAN_POINT ( 'NONE',  ( 23.78808814531843296, 13.03931410352375941, 3.724145320519536728 ) ) ;
#26781=CARTESIAN_POINT ( 'NONE',  ( 18.06885190415285081, -12.08553577211657348, 3.288727606363090139 ) ) ;
#26802=EDGE_CURVE ( 'NONE', #8614, #65865, #41546, .T. ) ;
#26808=DIRECTION ( 'NONE',  ( 1.000000000000000000, 0.000000000000000000, 0.000000000000000000 ) ) ;
#26815=CARTESIAN_POINT ( 'NONE',  ( 18.50003594170800270, -2.686563649653999963, 11.33603604535000109 ) ) ;
#26819=EDGE_LOOP ( 'NONE', ( #23645, #43720, #31257, #58559 ) ) ;
#26820=CARTESIAN_POINT ( 'NONE',  ( 11.50001496185000427, 10.90724927937048783, -6.294778943961341078 ) ) ;
#26828=CARTESIAN_POINT ( 'NONE',  ( 24.70908039369507492, 3.127826627798298897, -11.79915521905276243 ) ) ;
#26829=CARTESIAN_POINT ( 'NONE',  ( 24.71766312773793217, -8.650208672895015383, -8.601007095493814703 ) ) ;
#26832=CARTESIAN_POINT ( 'NONE',  ( 15.75262483093033516, -8.754898706354207860, -7.686019545157542154 ) ) ;
#26834=CARTESIAN_POINT ( 'NONE',  ( 24.53428988874600236, -8.855929874993998752, -9.286429786912000495 ) ) ;
#26837=EDGE_CURVE ( 'NONE', #27228, #20236, #38192, .T. ) ;
#26839=EDGE_LOOP ( 'NONE', ( #16770, #33479, #60011, #29656, #61474, #45007, #28086, #42820, #12877, #31374, #11350, #28741, #27564, #47406, #42438, #15317, #55776, #42890, #53707, #10726 ) ) ;
#26846=CARTESIAN_POINT ( 'NONE',  ( 15.90830001818700090, -9.238654026387999707, -8.377706362734000933 ) ) ;
#26848=EDGE_LOOP ( 'NONE', ( #32687, #44428, #66703, #32392 ) ) ;
#26849=B_SPLINE_SURFACE_WITH_KNOTS ( 'NONE', 3, 3, ( 
 ( #1190, #12370, #33004, #27413 ),
 ( #49419, #59219, #22156, #11663 ),
 ( #49773, #37547, #28106, #49077 ),
 ( #65494, #65843, #64796, #33700 ),
 ( #1531, #5731, #54318, #6076 ),
 ( #6418, #27072, #65143, #55020 ),
 ( #43843, #1884, #17264, #11320 ),
 ( #23200, #44200, #53971, #16908 ) ),
 .UNSPECIFIED., .F., .F., .F.,
 ( 4, 1, 1, 1, 1, 4 ),
 ( 4, 4 ),
 ( 0.7453056706973000267, 0.7647058823529000460, 0.8235294117646999590, 0.8823529411764999830, 0.9411764705882000870, 0.9905827404250000523 ),
 ( -0.1830915227417000135, 1.182948991274999972 ),
 .UNSPECIFIED. ) ;
#26852=CARTESIAN_POINT ( 'NONE',  ( 23.60205915885299888, -9.230633470682002795, 8.204162215359994903 ) ) ;
#26856=CARTESIAN_POINT ( 'NONE',  ( 18.35676500242969666, 3.328522075977830230, 12.07468831867923242 ) ) ;
#26867=CARTESIAN_POINT ( 'NONE',  ( 23.64714572502700207, -13.35826560361000048, 3.867671150794999679 ) ) ;
#26868=CARTESIAN_POINT ( 'NONE',  ( 21.05000072320139992, -1.355183834107999921E-13, 1.088018564133000035E-14 ) ) ;
#26881=EDGE_CURVE ( 'NONE', #65865, #1379, #7372, .T. ) ;
#26896=B_SPLINE_CURVE_WITH_KNOTS ( 'NONE', 3,
 ( #53764, #64238, #17039, #17749 ),
 .UNSPECIFIED., .F., .F.,
 ( 4, 4 ),
 ( 0.000000000000000000, 1.000000000000000000 ),
 .UNSPECIFIED. ) ;
#26903=VERTEX_POINT ( 'NONE', #41527 ) ;
#26910=ORIENTED_EDGE ( 'NONE', *, *, #31881, .F. ) ;
#26911=CARTESIAN_POINT ( 'NONE',  ( 24.14474040618317474, 12.92575721420310764, 3.214624011666622483 ) ) ;
#26923=CARTESIAN_POINT ( 'NONE',  ( 23.60205915885299888, 11.56239291746998710, 3.974820703396001242 ) ) ;
#26931=CARTESIAN_POINT ( 'NONE',  ( 25.59994555223600088, 1.356777910713891977, -11.13814279612289226 ) ) ;
#26938=ORIENTED_EDGE ( 'NONE', *, *, #47404, .F. ) ;
#26943=CARTESIAN_POINT ( 'NONE',  ( 11.68591862085600219, 12.43715917573999974, 1.778745665763999950 ) ) ;
#26944=EDGE_CURVE ( 'NONE', #50878, #30666, #26092, .T. ) ;
#26950=CARTESIAN_POINT ( 'NONE',  ( 25.59997125372800042, -2.856414944279999979, 11.13959160109000024 ) ) ;
#26954=DIRECTION ( 'NONE',  ( -1.000000000000000000, 0.000000000000000000, 0.000000000000000000 ) ) ;
#26965=CARTESIAN_POINT ( 'NONE',  ( 12.60217350508001743, 12.11433231916786823, -3.180975838886203277 ) ) ;
#26967=CARTESIAN_POINT ( 'NONE',  ( 25.29986734212600297, -2.258942858049999725, 12.29419282279000036 ) ) ;
#26971=ORIENTED_EDGE ( 'NONE', *, *, #67942, .F. ) ;
#26984=CARTESIAN_POINT ( 'NONE',  ( 19.39373726536100051, 11.26964301940000013, 0.000000000000000000 ) ) ;
#26989=AXIS2_PLACEMENT_3D ( 'NONE', #61932, #4223, #14046 ) ;
#26993=CARTESIAN_POINT ( 'NONE',  ( 11.50001544674999998, -6.312855374644978035, 10.89679704382941061 ) ) ;
#26994=CARTESIAN_POINT ( 'NONE',  ( 24.14113557808980204, 9.152656354384584247, -9.126826426531142289 ) ) ;
#26996=CARTESIAN_POINT ( 'NONE',  ( 24.30000000000000071, -2.548720605937000006, -12.21654710926000220 ) ) ;
#26998=ORIENTED_EDGE ( 'NONE', *, *, #44761, .T. ) ;
#27001=ORIENTED_EDGE ( 'NONE', *, *, #23935, .F. ) ;
#27008=CARTESIAN_POINT ( 'NONE',  ( 17.99211270977099986, -3.227071166021000082, 11.34499727797000013 ) ) ;
#27013=CARTESIAN_POINT ( 'NONE',  ( 13.25609597789999938, 11.48890257311000163, 1.688129671228999928 ) ) ;
#27017=ORIENTED_EDGE ( 'NONE', *, *, #29648, .F. ) ;
#27032=CARTESIAN_POINT ( 'NONE',  ( 12.38412398422500083, 11.44428158143999852, -4.450268217599000486 ) ) ;
#27033=CARTESIAN_POINT ( 'NONE',  ( 18.48246976263299857, 11.77475711121000224, -4.379243463657999769 ) ) ;
#27034=CARTESIAN_POINT ( 'NONE',  ( 18.30003129334700063, 2.732683817159999862, -11.53064095410000078 ) ) ;
#27038=CARTESIAN_POINT ( 'NONE',  ( 18.23590051321700400, -3.219096189435000088, 11.95421454054999977 ) ) ;
#27041=EDGE_LOOP ( 'NONE', ( #65422, #10830, #25439, #37481 ) ) ;
#27042=ORIENTED_EDGE ( 'NONE', *, *, #18008, .F. ) ;
#27057=ADVANCED_FACE ( 'NONE', ( #33808 ), #68815, .T. ) ;
#27062=CARTESIAN_POINT ( 'NONE',  ( 16.13849254682300227, -3.245716968028000249, -11.43439984646999896 ) ) ;
#27072=CARTESIAN_POINT ( 'NONE',  ( 24.74075940428600262, -8.629078674936000226, 8.723342079101000124 ) ) ;
#27075=CARTESIAN_POINT ( 'NONE',  ( 13.50000000000000178, -11.91410841793407194, -2.466613755756923876 ) ) ;
#27088=ORIENTED_EDGE ( 'NONE', *, *, #36972, .T. ) ;
#27089=DIRECTION ( 'NONE',  ( -3.790984134576917995E-06, 0.9659310420591794566, -0.2587995787710943851 ) ) ;
#27091=CARTESIAN_POINT ( 'NONE',  ( 15.59211270977100128, 8.811013545169000594, 7.841491685545999069 ) ) ;
#27093=CARTESIAN_POINT ( 'NONE',  ( 14.46666666233133469, -9.187454791078211613, -8.213178404136472821 ) ) ;
#27097=ORIENTED_EDGE ( 'NONE', *, *, #57646, .F. ) ;
#27101=VERTEX_POINT ( 'NONE', #27518 ) ;
#27102=B_SPLINE_CURVE_WITH_KNOTS ( 'NONE', 3,
 ( #49935, #2383, #55527, #18818, #29665, #23707 ),
 .UNSPECIFIED., .F., .F.,
 ( 4, 2, 4 ),
 ( 0.000000000000000000, 0.5000000000000000000, 1.000000000000000000 ),
 .UNSPECIFIED. ) ;
#27104=CARTESIAN_POINT ( 'NONE',  ( 21.70000039307920048, -13.99999960683000033, -1.736066577384000004E-09 ) ) ;
#27111=CARTESIAN_POINT ( 'NONE',  ( 16.32966272177200295, 3.529531741950000079, 11.96032165934999902 ) ) ;
#27120=DIRECTION ( 'NONE',  ( 1.000000000000000000, 0.000000000000000000, 0.000000000000000000 ) ) ;
#27124=CARTESIAN_POINT ( 'NONE',  ( 25.59037064052600030, 2.738643240522000255, 11.22408785382000040 ) ) ;
#27127=ORIENTED_EDGE ( 'NONE', *, *, #41790, .T. ) ;
#27134=DIRECTION ( 'NONE',  ( -1.000000000000000000, 0.000000000000000000, 0.000000000000000000 ) ) ;
#27142=DIRECTION ( 'NONE',  ( -1.000000000000000000, 0.000000000000000000, 0.000000000000000000 ) ) ;
#27143=ORIENTED_EDGE ( 'NONE', *, *, #15530, .F. ) ;
#27149=B_SPLINE_CURVE_WITH_KNOTS ( 'NONE', 3,
 ( #27713, #53584, #43446, #53920, #11608, #6021 ),
 .UNSPECIFIED., .F., .F.,
 ( 4, 1, 1, 4 ),
 ( 0.000000000000000000, 0.1550125385928093902, 0.7488612291951105560, 1.000000000000000000 ),
 .UNSPECIFIED. ) ;
#27165=CARTESIAN_POINT ( 'NONE',  ( 16.07057712374000147, -3.541973289920000045, -11.85942491664999920 ) ) ;
#27166=CARTESIAN_POINT ( 'NONE',  ( 11.55275411606000269, 11.58372484989999940, 1.667203446842000059 ) ) ;
#27172=ORIENTED_EDGE ( 'NONE', *, *, #60389, .F. ) ;
#27173=CARTESIAN_POINT ( 'NONE',  ( 16.10006098462790902, -8.380959734829355412, -8.092216891312066451 ) ) ;
#27190=CARTESIAN_POINT ( 'NONE',  ( 24.35365242081699932, -8.885108761826009172, 7.331500822316997734 ) ) ;
#27206=DIRECTION ( 'NONE',  ( 1.000000000000000000, 0.000000000000000000, 0.000000000000000000 ) ) ;
#27208=CARTESIAN_POINT ( 'NONE',  ( 18.35192027319500241, 2.803655468537999962, 11.45922931039000048 ) ) ;
#27212=CARTESIAN_POINT ( 'NONE',  ( 18.53711938375299795, 2.638714702496000264, -11.30796021345999947 ) ) ;
#27219=CARTESIAN_POINT ( 'NONE',  ( 11.75766493321900086, -3.377423597792000187, 11.11036430104999972 ) ) ;
#27226=CARTESIAN_POINT ( 'NONE',  ( 24.25375554908000097, 8.963946465867000057, -8.909846166044999904 ) ) ;
#27228=VERTEX_POINT ( 'NONE', #11771 ) ;
#27231=AXIS2_PLACEMENT_3D ( 'NONE', #6902, #2354, #23677 ) ;
#27233=DIRECTION ( 'NONE',  ( 0.000000000000000000, -1.000000000000000000, 0.000000000000000000 ) ) ;
#27249=CARTESIAN_POINT ( 'NONE',  ( 23.61341080715499885, 3.134550972388999934, 13.53707874230000030 ) ) ;
#27252=CARTESIAN_POINT ( 'NONE',  ( 24.97034696419939337, -11.51453382931811475, -3.225688335446051269 ) ) ;
#27264=VERTEX_POINT ( 'NONE', #35185 ) ;
#27270=EDGE_CURVE ( 'NONE', #47324, #1148, #23617, .T. ) ;
#27275=CARTESIAN_POINT ( 'NONE',  ( 14.02341781689399980, 9.526752659074999130, 8.190681853965998016 ) ) ;
#27284=CARTESIAN_POINT ( 'NONE',  ( 25.29989948031900227, 2.596966625103000137, -11.35305524894999962 ) ) ;
#27285=CARTESIAN_POINT ( 'NONE',  ( 24.57788509281863298, -8.817303531637588065, -9.247882801739393699 ) ) ;
#27286=CARTESIAN_POINT ( 'NONE',  ( 11.61689913334100055, 12.44392429648999965, 1.730928413625999918 ) ) ;
#27287=AXIS2_PLACEMENT_3D ( 'NONE', #62157, #14952, #25099 ) ;
#27296=CARTESIAN_POINT ( 'NONE',  ( 15.99981196018700125, -1.620925615952999665E-13, 0.000000000000000000 ) ) ;
#27301=FACE_OUTER_BOUND ( 'NONE', #57009, .T. ) ;
#27305=CARTESIAN_POINT ( 'NONE',  ( 11.89965592520902327, 11.89526654130151329, -3.923396420608070922 ) ) ;
#27316=CARTESIAN_POINT ( 'NONE',  ( 12.01640417260427007, -11.69872868927379272, 4.475294149990396875 ) ) ;
#27317=CYLINDRICAL_SURFACE ( 'NONE', #62554, 0.5000000000000004441 ) ;
#27324=CARTESIAN_POINT ( 'NONE',  ( 13.50000000000000178, 0.000000000000000000, 0.000000000000000000 ) ) ;
#27326=CARTESIAN_POINT ( 'NONE',  ( 18.48326398027718653, -2.855662837647996888, 11.29488646771354787 ) ) ;
#27327=EDGE_CURVE ( 'NONE', #6268, #57158, #16054, .T. ) ;
#27336=CARTESIAN_POINT ( 'NONE',  ( 23.95413598829442492, 9.440340059428892872, -9.313978351785300092 ) ) ;
#27350=CARTESIAN_POINT ( 'NONE',  ( 18.26242787221299935, -2.744348664398000182, 11.56741553474000028 ) ) ;
#27356=CARTESIAN_POINT ( 'NONE',  ( 13.51386961183700031, 11.53357255609999932, 1.992589078083000009 ) ) ;
#27357=VERTEX_POINT ( 'NONE', #3684 ) ;
#27365=CARTESIAN_POINT ( 'NONE',  ( 24.76117173203458677, -8.629364107770223669, 8.563007708072372992 ) ) ;
#27369=CARTESIAN_POINT ( 'NONE',  ( 23.60205915885299888, -9.377218989177011466, -8.305825996807000067 ) ) ;
#27371=VERTEX_POINT ( 'NONE', #46356 ) ;
#27373=CARTESIAN_POINT ( 'NONE',  ( 17.83742117717700282, 11.80639483233000142, -3.358960109135999961 ) ) ;
#27377=AXIS2_PLACEMENT_3D ( 'NONE', #35120, #30549, #46973 ) ;
#27378=CARTESIAN_POINT ( 'NONE',  ( 18.53682820967700451, -2.877067450793000081, 12.22924281482000097 ) ) ;
#27380=ORIENTED_EDGE ( 'NONE', *, *, #61488, .T. ) ;
#27382=FACE_OUTER_BOUND ( 'NONE', #11028, .T. ) ;
#27384=CARTESIAN_POINT ( 'NONE',  ( 11.79999999471800010, 3.216299622513999701, -11.40340969442000052 ) ) ;
#27385=CARTESIAN_POINT ( 'NONE',  ( 24.37846342710900061, 8.840949306909999805, -8.761878624573000707 ) ) ;
#27393=VERTEX_POINT ( 'NONE', #66979 ) ;
#27400=DIRECTION ( 'NONE',  ( 0.000000000000000000, 0.1807154286440006141, -0.9835354258236025382 ) ) ;
#27401=AXIS2_PLACEMENT_3D ( 'NONE', #197, #6814, #54715 ) ;
#27409=CARTESIAN_POINT ( 'NONE',  ( 24.30857393632600250, -3.216436940933999900, 12.15172254432999921 ) ) ;
#27412=DIRECTION ( 'NONE',  ( -1.000000000000000000, 0.000000000000000000, 0.000000000000000000 ) ) ;
#27413=CARTESIAN_POINT ( 'NONE',  ( 25.59037455770100422, -8.351027012765998236, 7.983767442140998760 ) ) ;
#27416=CARTESIAN_POINT ( 'NONE',  ( 25.59994555223599733, 10.55174472786000095, -3.754934689065000164 ) ) ;
#27419=CARTESIAN_POINT ( 'NONE',  ( 24.37808884344924465, -3.385972260544573231, 12.24452378150168563 ) ) ;
#27428=CARTESIAN_POINT ( 'NONE',  ( 13.00000000001300116, 11.52577654661000039, 1.696746661728000038 ) ) ;
#27430=AXIS2_PLACEMENT_3D ( 'NONE', #52840, #4935, #9840 ) ;
#27431=CARTESIAN_POINT ( 'NONE',  ( 15.37447410014400084, 8.836271409840000146, 7.950749727554001112 ) ) ;
#27433=CARTESIAN_POINT ( 'NONE',  ( 13.99999999347100044, -9.187456302440001110, -8.213201953411001455 ) ) ;
#27438=ORIENTED_EDGE ( 'NONE', *, *, #9160, .F. ) ;
#27441=DIRECTION ( 'NONE',  ( -0.9709491189738370664, 0.000000000000000000, -0.2392860387986094628 ) ) ;
#27442=EDGE_LOOP ( 'NONE', ( #55862, #17391, #62860 ) ) ;
#27443=CARTESIAN_POINT ( 'NONE',  ( 11.29997960521318312, -3.569935952926194478, 11.29784959202356021 ) ) ;
#27444=CARTESIAN_POINT ( 'NONE',  ( 11.50029455687000102, 11.62161504194025063, 0.9384843090728728354 ) ) ;
#27451=CARTESIAN_POINT ( 'NONE',  ( 24.76774735605714284, 11.72413114164001513, -3.191091186273769864 ) ) ;
#27457=CARTESIAN_POINT ( 'NONE',  ( 25.59997036749100374, 2.856417224717999748, 11.13959153667999935 ) ) ;
#27459=DIRECTION ( 'NONE',  ( -1.000000000000000000, -9.912705577010336396E-15, -5.699805706780943546E-14 ) ) ;
#27463=CARTESIAN_POINT ( 'NONE',  ( 25.26979641699100299, -2.550139818953999882, 11.36439134171999932 ) ) ;
#27470=EDGE_CURVE ( 'NONE', #22975, #28283, #14463, .T. ) ;
#27475=CARTESIAN_POINT ( 'NONE',  ( 17.66658663920548733, 11.23412379135927530, -3.084957477888136790 ) ) ;
#27479=CARTESIAN_POINT ( 'NONE',  ( 24.50399615158200106, -8.846403136021999458, -9.151488484734001005 ) ) ;
#27480=CARTESIAN_POINT ( 'NONE',  ( 23.66004879239100234, 9.998910715289998308, -9.691527791130999603 ) ) ;
#27483=CARTESIAN_POINT ( 'NONE',  ( 18.22497476945055439, -3.457026130723240609, 12.03849088744245499 ) ) ;
#27487=B_SPLINE_CURVE_WITH_KNOTS ( 'NONE', 3,
 ( #61600, #45533, #62288, #41310 ),
 .UNSPECIFIED., .F., .F.,
 ( 4, 4 ),
 ( 0.000000000000000000, 1.000000000000000000 ),
 .UNSPECIFIED. ) ;
#27488=DIRECTION ( 'NONE',  ( 0.000000000000000000, 0.9421243786071880066, -0.3352635608502960163 ) ) ;
#27504=CARTESIAN_POINT ( 'NONE',  ( 13.73125687462010447, 9.567603210582007023, 8.083310008147687853 ) ) ;
#27505=ORIENTED_EDGE ( 'NONE', *, *, #68605, .F. ) ;
#27506=CARTESIAN_POINT ( 'NONE',  ( 17.60000000000000142, -11.23412379136000006, 3.084957477885999833 ) ) ;
#27510=CARTESIAN_POINT ( 'NONE',  ( 24.71768487731727859, 3.123575521103121755, -11.79178543996698991 ) ) ;
#27511=CARTESIAN_POINT ( 'NONE',  ( 16.32975648157900039, 3.316681689484000106, 11.22330675696999869 ) ) ;
#27518=CARTESIAN_POINT ( 'NONE',  ( 18.49985170088394426, -7.837663500889314729E-14, -12.52499999999998792 ) ) ;
#27519=CARTESIAN_POINT ( 'NONE',  ( 16.09997386696500143, -8.350085070477001992, -8.123950967096998710 ) ) ;
#27520=ORIENTED_EDGE ( 'NONE', *, *, #59755, .F. ) ;
#27523=ORIENTED_EDGE ( 'NONE', *, *, #8467, .F. ) ;
#27524=FILL_AREA_STYLE ('',( #54086 ) ) ;
#27526=CARTESIAN_POINT ( 'NONE',  ( 16.04495723965300158, -8.927588545536998765, -8.707532029612000457 ) ) ;
#27533=DIRECTION ( 'NONE',  ( 1.000000000000000000, 0.000000000000000000, 0.000000000000000000 ) ) ;
#27542=CARTESIAN_POINT ( 'NONE',  ( 13.00000000009400303, 11.69118001589999878, 1.923222888683999932 ) ) ;
#27546=CARTESIAN_POINT ( 'NONE',  ( 24.32154984244752072, -12.72720806567605578, -3.095248367017349178 ) ) ;
#27547=CARTESIAN_POINT ( 'NONE',  ( 24.42277064782400231, 12.73424796067999942, 3.019164715476000183 ) ) ;
#27560=CARTESIAN_POINT ( 'NONE',  ( 23.68331123634199997, -9.987482016315999189, -9.401264431477001082 ) ) ;
#27562=DIRECTION ( 'NONE',  ( 0.000000000000000000, 0.000000000000000000, 1.000000000000000000 ) ) ;
#27563=AXIS2_PLACEMENT_3D ( 'NONE', #28644, #18491, #66022 ) ;
#27564=ORIENTED_EDGE ( 'NONE', *, *, #58433, .T. ) ;
#27568=CARTESIAN_POINT ( 'NONE',  ( 24.66271477989500127, 8.757902662406001681, -9.242626227026999430 ) ) ;
#27572=CARTESIAN_POINT ( 'NONE',  ( 24.46225899603300036, 3.149515489371000232, -11.96334157380999841 ) ) ;
#27576=CARTESIAN_POINT ( 'NONE',  ( 25.59997821859199973, 2.856411258734000036, -11.13959759756999901 ) ) ;
#27580=AXIS2_PLACEMENT_3D ( 'NONE', #26996, #48312, #418 ) ;
#27587=CARTESIAN_POINT ( 'NONE',  ( 12.49732881085200020, -12.03818693049999844, 3.242368311117000079 ) ) ;
#27592=ORIENTED_EDGE ( 'NONE', *, *, #53924, .F. ) ;
#27602=B_SPLINE_CURVE_WITH_KNOTS ( 'NONE', 3,
 ( #40027, #61339, #14136, #45611, #62363, #46293 ),
 .UNSPECIFIED., .F., .F.,
 ( 4, 1, 1, 4 ),
 ( 0.000000000000000000, 0.1550125199349672578, 0.7488612387844387763, 1.000000000000000000 ),
 .UNSPECIFIED. ) ;
#27604=VECTOR ( 'NONE', #16453, 1000.000000000000114 ) ;
#27615=EDGE_CURVE ( 'NONE', #12730, #8953, #9674, .T. ) ;
#27616=DIRECTION ( 'NONE',  ( 1.000000000000000000, 0.000000000000000000, 0.000000000000000000 ) ) ;
#27617=CARTESIAN_POINT ( 'NONE',  ( 13.46268444654400298, 9.428250749343998649, 7.876929641374000646 ) ) ;
#27618=ADVANCED_FACE ( 'NONE', ( #25709 ), #20462, .F. ) ;
#27620=VECTOR ( 'NONE', #63818, 1000.000000000000114 ) ;
#27625=B_SPLINE_CURVE_WITH_KNOTS ( 'NONE', 3,
 ( #25969, #10570, #68953, #46952, #63704, #9531, #47981, #37482, #53566, #52533, #52188, #16159, #47643, #21066 ),
 .UNSPECIFIED., .F., .F.,
 ( 4, 2, 2, 2, 2, 2, 4 ),
 ( 0.000000000000000000, 0.1249999999999996392, 0.2499999999999992784, 0.5000000000000024425, 0.6250000000000019984, 0.7500000000000014433, 1.000000000000000000 ),
 .UNSPECIFIED. ) ;
#27630=LINE ( 'NONE', #33218, #60408 ) ;
#27643=EDGE_CURVE ( 'NONE', #7930, #22245, #35354, .T. ) ;
#27655=SHAPE_REPRESENTATION ( 'Drip Tip - Airflow Cap', ( #9676 ), #42081 ) ;
#27659=CARTESIAN_POINT ( 'NONE',  ( 11.29997394301484093, 12.21464834955394352, 1.635338263058603303 ) ) ;
#27660=ORIENTED_EDGE ( 'NONE', *, *, #22129, .F. ) ;
#27669=AXIS2_PLACEMENT_3D ( 'NONE', #13565, #34885, #24385 ) ;
#27672=CARTESIAN_POINT ( 'NONE',  ( 24.57009630585800153, 3.716770706295000171, -12.37072133406000063 ) ) ;
#27675=CARTESIAN_POINT ( 'NONE',  ( 17.60000000000000142, -10.78295181803999903, 4.410266442048000002 ) ) ;
#27676=AXIS2_PLACEMENT_3D ( 'NONE', #40731, #45979, #35498 ) ;
#27679=DIRECTION ( 'NONE',  ( 0.000000000000000000, 0.000000000000000000, -1.000000000000000000 ) ) ;
#27684=CARTESIAN_POINT ( 'NONE',  ( 23.56664309646999911, -10.37807348783000094, 9.381504613656002078 ) ) ;
#27689=CARTESIAN_POINT ( 'NONE',  ( 24.05251143665766733, 9.284066128425779496, -9.220293913675572384 ) ) ;
#27691=ORIENTED_EDGE ( 'NONE', *, *, #47101, .T. ) ;
#27700=CARTESIAN_POINT ( 'NONE',  ( 23.96072736199457154, 3.344687141702650912, -12.82061042838967779 ) ) ;
#27701=CARTESIAN_POINT ( 'NONE',  ( 18.49055856039300139, -2.949841519493000330, 11.23086453091999992 ) ) ;
#27706=CARTESIAN_POINT ( 'NONE',  ( 21.00000012402660232, -1.355183834107999921E-13, -12.42499880353998876 ) ) ;
#27708=EDGE_CURVE ( 'NONE', #68740, #12282, #1957, .T. ) ;
#27711=VERTEX_POINT ( 'NONE', #63448 ) ;
#27713=CARTESIAN_POINT ( 'NONE',  ( 24.53429010005800137, -12.47024913742999885, 3.026245653581999928 ) ) ;
#27718=CARTESIAN_POINT ( 'NONE',  ( 25.26126798770998505, -8.521553306829913410, 7.991940928116512133 ) ) ;
#27725=ORIENTED_EDGE ( 'NONE', *, *, #68875, .T. ) ;
#27739=PLANE ( 'NONE',  #54511 ) ;
#27755=EDGE_CURVE ( 'NONE', #28289, #40442, #45300, .T. ) ;
#27757=CARTESIAN_POINT ( 'NONE',  ( 11.31944011432000075, 3.562654288336999819, -11.75631193234000094 ) ) ;
#27772=CARTESIAN_POINT ( 'NONE',  ( 13.50018479229300006, -11.60142623882999935, -2.415183939829000259 ) ) ;
#27776=CARTESIAN_POINT ( 'NONE',  ( 16.00000002095532992, -12.11988194449493506, 3.159760537119275181 ) ) ;
#27778=CARTESIAN_POINT ( 'NONE',  ( 13.58069952315600126, 12.39169461668999972, 2.069104550346000160 ) ) ;
#27780=CARTESIAN_POINT ( 'NONE',  ( 24.35365242081700288, 8.355077740067001102, 8.511587483820997946 ) ) ;
#27790=CARTESIAN_POINT ( 'NONE',  ( 11.30000000000000071, 4.368599826607999503, 15.48886178036999972 ) ) ;
#27799=VECTOR ( 'NONE', #32448, 1000.000000000000000 ) ;
#27801=CARTESIAN_POINT ( 'NONE',  ( 11.50029455687000102, 11.65000000000000213, 0.4692429876170854386 ) ) ;
#27807=DIRECTION ( 'NONE',  ( -1.000000000000000000, 0.000000000000000000, 0.000000000000000000 ) ) ;
#27808=CARTESIAN_POINT ( 'NONE',  ( 24.30001694391200218, -12.21047201246000036, 3.271805662802000025 ) ) ;
#27822=ORIENTED_EDGE ( 'NONE', *, *, #26671, .F. ) ;
#27823=EDGE_LOOP ( 'NONE', ( #49127, #19804, #2164, #68702 ) ) ;
#27824=VECTOR ( 'NONE', #15276, 999.9999999999998863 ) ;
#27833=CARTESIAN_POINT ( 'NONE',  ( 18.29999330150736014, 11.02846243710159868, -3.754394858750199848 ) ) ;
#27836=CARTESIAN_POINT ( 'NONE',  ( 18.22495619086188512, 11.54180252136524487, -4.316564229370158934 ) ) ;
#27838=B_SPLINE_SURFACE_WITH_KNOTS ( 'NONE', 3, 3, ( 
 ( #48729, #36860, #58180, #21453 ),
 ( #21799, #26022, #15868, #10282 ),
 ( #26721, #53960, #64098, #6063 ),
 ( #5719, #48033, #37200, #27062 ),
 ( #43133, #64437, #16559, #52937 ),
 ( #26371, #20429, #53281, #47698 ),
 ( #57831, #5382, #41758, #36510 ),
 ( #139, #63059, #31276, #4681 ),
 ( #47351, #69009, #35327, #24486 ) ),
 .UNSPECIFIED., .F., .F., .F.,
 ( 4, 1, 1, 1, 1, 1, 4 ),
 ( 4, 4 ),
 ( 0.02209653170519000273, 0.1666666666667000196, 0.3333333333333000081, 0.5000000000000000000, 0.6666666666667000474, 0.8333333333333000637, 0.9492823795161999811 ),
 ( -0.1916656884162999952, 1.191851428473000185 ),
 .UNSPECIFIED. ) ;
#27842=DIRECTION ( 'NONE',  ( 1.000000000000000000, 0.000000000000000000, 0.000000000000000000 ) ) ;
#27845=FACE_OUTER_BOUND ( 'NONE', #25371, .T. ) ;
#27849=VERTEX_POINT ( 'NONE', #11687 ) ;
#27867=CARTESIAN_POINT ( 'NONE',  ( 24.44496482743900145, 12.03536723905999928, -3.224852005146999989 ) ) ;
#27878=ADVANCED_FACE ( 'NONE', ( #54339 ), #6097, .F. ) ;
#27881=CARTESIAN_POINT ( 'NONE',  ( 15.35870478550200069, -9.525289020731998235, -8.192348383776000276 ) ) ;
#27893=B_SPLINE_CURVE_WITH_KNOTS ( 'NONE', 3,
 ( #41959, #52794, #47557, #46521, #46176, #10141, #62921, #57680, #41273, #4886, #40925, #68168, #3511, #67484, #25536, #9790, #31142, #20979, #42315, #52443, #37061, #24849, #14368, #15733, #9440, #36022, #63617, #4198, #58374, #62248, #57337, #4538 ),
 .UNSPECIFIED., .F., .F.,
 ( 4, 2, 2, 2, 2, 2, 2, 2, 1, 2, 2, 2, 1, 1, 1, 2, 2, 4 ),
 ( 0.000000000000000000, 0.2500000000000091593, 0.3750000000000153211, 0.4375000000000198175, 0.4687500000000232592, 0.5000000000000267564, 0.6250000000000375255, 0.6875000000000405231, 0.7187500000000419664, 0.7343750000000426326, 0.7500000000000434097, 0.8125000000000432987, 0.8437500000000421885, 0.8593750000000426326, 0.8671875000000418554, 0.8710937500000396350, 0.8750000000000375255, 1.000000000000000000 ),
 .UNSPECIFIED. ) ;
#27895=AXIS2_PLACEMENT_3D ( 'NONE', #22768, #54592, #6688 ) ;
#27896=CARTESIAN_POINT ( 'NONE',  ( 11.83966971788800215, -12.22235437154000159, -1.953272420501999784 ) ) ;
#27899=ADVANCED_FACE ( 'NONE', ( #8443, #35025 ), #35364, .F. ) ;
#27909=CARTESIAN_POINT ( 'NONE',  ( 17.99211270977099986, 3.227071166021000082, -11.34499727797000013 ) ) ;
#27914=CARTESIAN_POINT ( 'NONE',  ( 23.86794696826499873, -9.630643803976999706, 9.781828974359999762 ) ) ;
#27915=CARTESIAN_POINT ( 'NONE',  ( 11.82349952450200270, -3.378095173501999948, 11.11014980558000076 ) ) ;
#27920=DIRECTION ( 'NONE',  ( 0.000000000000000000, -0.5393439587572765870, 0.8420855622512650740 ) ) ;
#27923=CARTESIAN_POINT ( 'NONE',  ( 24.74447889200699890, 3.238408025005999669, -11.83114124653999966 ) ) ;
#27937=CARTESIAN_POINT ( 'NONE',  ( 24.41456973790700147, 12.00390065640000081, -3.256048965793000516 ) ) ;
#27938=CARTESIAN_POINT ( 'NONE',  ( 12.05989062672900047, -12.07342271643000053, 3.473919584753000223 ) ) ;
#27945=CARTESIAN_POINT ( 'NONE',  ( 24.00938322038199857, -9.351644529155782593, 9.262332192104681283 ) ) ;
#27951=CARTESIAN_POINT ( 'NONE',  ( 23.61814130164600201, 13.16711982218999921, -4.271579012135999776 ) ) ;
#27954=ADVANCED_FACE ( 'NONE', ( #63968 ), #37755, .T. ) ;
#27958=ADVANCED_FACE ( 'NONE', ( #31835 ), #279, .F. ) ;
#27960=CARTESIAN_POINT ( 'NONE',  ( 23.56666365135700403, 12.07812737769999245, 3.551569042642998664 ) ) ;
#27961=CARTESIAN_POINT ( 'NONE',  ( 23.97711684283312294, 9.403743244523731448, 9.292184203824568556 ) ) ;
#27976=FACE_OUTER_BOUND ( 'NONE', #8650, .T. ) ;
#27978=CARTESIAN_POINT ( 'NONE',  ( 11.53944595909000270, 12.46266292589999836, 1.587625155185000025 ) ) ;
#27991=AXIS2_PLACEMENT_3D ( 'NONE', #36345, #4862, #46500 ) ;
#28000=CARTESIAN_POINT ( 'NONE',  ( 18.22725926605928848, -3.461153921119815902, -12.03746648326404589 ) ) ;
#28004=CARTESIAN_POINT ( 'NONE',  ( 25.02478270113282832, 11.45587418384018896, 3.243239995978246526 ) ) ;
#28006=CYLINDRICAL_SURFACE ( 'NONE', #49768, 0.5000000000000002220 ) ;
#28011=CARTESIAN_POINT ( 'NONE',  ( 24.30001697352500045, -3.271769158411000245, -12.21048181092999840 ) ) ;
#28012=EDGE_CURVE ( 'NONE', #27393, #52892, #42676, .T. ) ;
#28017=CARTESIAN_POINT ( 'NONE',  ( 24.21996587171000215, 3.760918895062999923, -12.77941170050999986 ) ) ;
#28018=CARTESIAN_POINT ( 'NONE',  ( 23.59999176271200128, 13.22318677037999812, 4.267778497637999102 ) ) ;
#28020=EDGE_CURVE ( 'NONE', #43628, #9687, #33779, .T. ) ;
#28022=CARTESIAN_POINT ( 'NONE',  ( 12.73341324573692290, 11.23412379136182260, -3.084957477880623689 ) ) ;
#28035=DIRECTION ( 'NONE',  ( -1.901299611514599864E-27, -1.000000000000000000, 3.733732073519000081E-14 ) ) ;
#28038=ORIENTED_EDGE ( 'NONE', *, *, #55257, .T. ) ;
#28044=CARTESIAN_POINT ( 'NONE',  ( 24.12729511379000513, 3.330893262555046697, -12.51461353060619786 ) ) ;
#28067=CARTESIAN_POINT ( 'NONE',  ( 12.67430611818100061, 11.44505085583999993, -4.692779640757001047 ) ) ;
#28068=CARTESIAN_POINT ( 'NONE',  ( 13.56663524094155804, -11.53596571847203300, -2.401556225329832817 ) ) ;
#28074=DIRECTION ( 'NONE',  ( 0.000000000000000000, 2.657874803301998965E-08, -0.9999999999999996669 ) ) ;
#28076=CARTESIAN_POINT ( 'NONE',  ( 18.30008632280270930, 2.887848135250621385E-14, -11.85014035451981762 ) ) ;
#28086=ORIENTED_EDGE ( 'NONE', *, *, #19487, .T. ) ;
#28091=ADVANCED_FACE ( 'NONE', ( #12227 ), #25114, .F. ) ;
#28094=CARTESIAN_POINT ( 'NONE',  ( 12.10000000000000142, -43.96540072520999587, 14.96704326274999985 ) ) ;
#28096=ADVANCED_FACE ( 'NONE', ( #13955 ), #6624, .F. ) ;
#28102=CARTESIAN_POINT ( 'NONE',  ( 24.30001680216799897, -3.271769318036999774, 12.21048166890999909 ) ) ;
#28103=CARTESIAN_POINT ( 'NONE',  ( 13.50018479229797208, -11.40740214419244225, -3.347185923349857095 ) ) ;
#28106=CARTESIAN_POINT ( 'NONE',  ( 25.41677598325400211, -8.397334373648000394, 8.092712133474000424 ) ) ;
#28114=DIRECTION ( 'NONE',  ( 1.000000000000000000, 0.000000000000000000, 0.000000000000000000 ) ) ;
#28136=LINE ( 'NONE', #27104, #55465 ) ;
#28142=CARTESIAN_POINT ( 'NONE',  ( 15.86268444654400156, 3.728894906265999509, 11.70612128528000007 ) ) ;
#28143=CARTESIAN_POINT ( 'NONE',  ( 11.30000000000000071, 3.738146901528993205, -11.41167910143314579 ) ) ;
#28144=EDGE_CURVE ( 'NONE', #64677, #23593, #13471, .T. ) ;
#28150=DIRECTION ( 'NONE',  ( 0.000000000000000000, 0.7071067811865475727, 0.7071067811865475727 ) ) ;
#28153=CARTESIAN_POINT ( 'NONE',  ( 25.08242994833700124, 2.794105277247000085, 11.47833782540000058 ) ) ;
#28155=CARTESIAN_POINT ( 'NONE',  ( 24.56892027611100460, -3.303734510344000341, 12.00214753008000024 ) ) ;
#28162=CARTESIAN_POINT ( 'NONE',  ( 23.60707278462106373, 3.266495719822134713, -13.58453502575737026 ) ) ;
#28164=CARTESIAN_POINT ( 'NONE',  ( 23.58334011193800350, 0.000000000000000000, -3.819167204710999951E-13 ) ) ;
#28172=B_SPLINE_CURVE_WITH_KNOTS ( 'NONE', 3,
 ( #34865, #50941, #54802, #3037 ),
 .UNSPECIFIED., .F., .F.,
 ( 4, 4 ),
 ( 0.000000000000000000, 1.000000000000000000 ),
 .UNSPECIFIED. ) ;
#28175=VERTEX_POINT ( 'NONE', #21584 ) ;
#28177=CARTESIAN_POINT ( 'NONE',  ( 18.22958240948263509, 10.92137759501686034, -4.055351289589740560 ) ) ;
#28190=CARTESIAN_POINT ( 'NONE',  ( 24.14113398102592711, -12.48039438772169873, -3.363020802264193421 ) ) ;
#28192=EDGE_LOOP ( 'NONE', ( #50544, #3822, #14159, #35773, #35123 ) ) ;
#28199=ORIENTED_EDGE ( 'NONE', *, *, #67100, .T. ) ;
#28201=CARTESIAN_POINT ( 'NONE',  ( 12.79999999202000005, -11.41069016990000051, 4.623987642516999230 ) ) ;
#28205=CARTESIAN_POINT ( 'NONE',  ( 16.13862479881500178, 3.581551568669000041, 11.04584923442999944 ) ) ;
#28210=CARTESIAN_POINT ( 'NONE',  ( 23.66004879239100234, -13.39256420742000131, 3.813548264891000183 ) ) ;
#28213=EDGE_LOOP ( 'NONE', ( #26334, #49268, #67851, #40176, #59152 ) ) ;
#28216=B_SPLINE_CURVE_WITH_KNOTS ( 'NONE', 3,
 ( #56017, #41316, #4239, #30827 ),
 .UNSPECIFIED., .F., .F.,
 ( 4, 4 ),
 ( 0.000000000000000000, 1.000000000000000000 ),
 .UNSPECIFIED. ) ;
#28219=CARTESIAN_POINT ( 'NONE',  ( 16.13682146000800088, -8.990085112443999549, -8.775549782916998609 ) ) ;
#28231=VERTEX_POINT ( 'NONE', #36992 ) ;
#28233=CARTESIAN_POINT ( 'NONE',  ( 11.35194613850999978, -12.28618680900000015, -1.513058913260000082 ) ) ;
#28238=CARTESIAN_POINT ( 'NONE',  ( 24.08683856445600213, 12.68564027046999954, 3.367487813839999955 ) ) ;
#28246=CARTESIAN_POINT ( 'NONE',  ( 25.60000000000000142, 2.258942858049999725, 10.99401502705231515 ) ) ;
#28248=DIRECTION ( 'NONE',  ( -1.000000000000000000, 0.000000000000000000, 0.000000000000000000 ) ) ;
#28250=CARTESIAN_POINT ( 'NONE',  ( 24.57033794412999939, -8.854779233076000011, -9.403977091059999793 ) ) ;
#28251=CARTESIAN_POINT ( 'NONE',  ( 23.55653128217999992, -10.23594516573000135, 9.677208546218999174 ) ) ;
#28252=CARTESIAN_POINT ( 'NONE',  ( 11.80756411264299999, -3.251511910489000012, 11.33753290789000090 ) ) ;
#28257=ADVANCED_FACE ( 'NONE', ( #617 ), #54395, .F. ) ;
#28259=CARTESIAN_POINT ( 'NONE',  ( 15.90018573812067970, -7.829696748392007244, -8.945859267997793296 ) ) ;
#28263=CARTESIAN_POINT ( 'NONE',  ( 25.31133064153000234, 2.728868305775999925, -11.35932564715999860 ) ) ;
#28275=CARTESIAN_POINT ( 'NONE',  ( 24.35145719007200071, 12.30648751194999946, -3.205655321895999776 ) ) ;
#28276=CARTESIAN_POINT ( 'NONE',  ( 12.04183425709900135, -11.69157926155999938, 4.070931047779999368 ) ) ;
#28283=VERTEX_POINT ( 'NONE', #5850 ) ;
#28284=CARTESIAN_POINT ( 'NONE',  ( 24.00507834543561003, -9.358513022419435501, 9.266405905701180501 ) ) ;
#28289=VERTEX_POINT ( 'NONE', #26500 ) ;
#28291=CARTESIAN_POINT ( 'NONE',  ( 23.73581876812099978, 13.39628736436000089, -3.629848242966999816 ) ) ;
#28297=CARTESIAN_POINT ( 'NONE',  ( 23.60205915885299888, 11.72032963060998867, 3.891881970952999481 ) ) ;
#28298=CARTESIAN_POINT ( 'NONE',  ( 23.65871351072082618, 10.04305333474976081, 9.454472293059238197 ) ) ;
#28302=CARTESIAN_POINT ( 'NONE',  ( 23.56666365135700403, 2.920993777334001340, -11.72568747145000145 ) ) ;
#28304=CARTESIAN_POINT ( 'NONE',  ( 17.56873934038800300, -11.44357731092999941, 4.696002633125000436 ) ) ;
#28313=AXIS2_PLACEMENT_3D ( 'NONE', #6222, #43297, #55513 ) ;
#28317=CARTESIAN_POINT ( 'NONE',  ( 11.53898320224999985, 12.47165320829000024, 1.511147746418000093 ) ) ;
#28321=CARTESIAN_POINT ( 'NONE',  ( 18.35499787466299892, 2.879071536379000040, -12.03968120189999880 ) ) ;
#28322=ADVANCED_FACE ( 'NONE', ( #63191 ), #15320, .F. ) ;
#28343=EDGE_CURVE ( 'NONE', #4716, #67055, #39403, .T. ) ;
#28351=CARTESIAN_POINT ( 'NONE',  ( 18.30000077768849565, 11.66744147158535405, -3.971919865264926575 ) ) ;
#28355=CARTESIAN_POINT ( 'NONE',  ( 24.13225745270770517, -9.165361937195044106, -9.136521564051420796 ) ) ;
#28358=CARTESIAN_POINT ( 'NONE',  ( 21.65000086032551252, 3.970157536060000036E-13, 1.776356839399999796E-13 ) ) ;
#28362=CARTESIAN_POINT ( 'NONE',  ( 13.36350100824700071, -12.09092425779999935, -2.196870506499999820 ) ) ;
#28363=ORIENTED_EDGE ( 'NONE', *, *, #27327, .T. ) ;
#28381=VERTEX_POINT ( 'NONE', #60723 ) ;
#28383=AXIS2_PLACEMENT_3D ( 'NONE', #52963, #6087, #26050 ) ;
#28384=ORIENTED_EDGE ( 'NONE', *, *, #49752, .F. ) ;
#28388=VERTEX_POINT ( 'NONE', #65614 ) ;
#28401=LINE ( 'NONE', #7408, #1329 ) ;
#28403=ORIENTED_EDGE ( 'NONE', *, *, #55010, .F. ) ;
#28405=CARTESIAN_POINT ( 'NONE',  ( 25.05003896993082435, -8.531459344605563544, 8.270378173953636392 ) ) ;
#28414=ADVANCED_FACE ( 'NONE', ( #50237 ), #10355, .F. ) ;
#28417=CARTESIAN_POINT ( 'NONE',  ( 12.68949153424100196, 11.39033517652999983, -4.571431300619999583 ) ) ;
#28419=CARTESIAN_POINT ( 'NONE',  ( 24.08681017553700343, -3.426492766728000294, -12.66987775218999879 ) ) ;
#28422=B_SPLINE_SURFACE_WITH_KNOTS ( 'NONE', 3, 3, ( 
 ( #17779, #12528, #49233, #39097 ),
 ( #27572, #54482, #44702, #2042 ),
 ( #6583, #27923, #1343, #65657 ),
 ( #44003, #43658, #6928, #60422 ),
 ( #38400, #48899, #11826, #22659 ),
 ( #33859, #28263, #54134, #55174 ),
 ( #49581, #38753, #65310, #7278 ),
 ( #17424, #18122, #28617, #65997 ) ),
 .UNSPECIFIED., .F., .F., .F.,
 ( 4, 1, 1, 1, 1, 4 ),
 ( 4, 4 ),
 ( 0.008355529829647000833, 0.05882352941176000050, 0.1176470588234999892, 0.1764705882353000133, 0.2352941176471000095, 0.2534842851975999678 ),
 ( -0.1830816906711000003, 1.182949851103000105 ),
 .UNSPECIFIED. ) ;
#28447=ORIENTED_EDGE ( 'NONE', *, *, #5533, .F. ) ;
#28462=CARTESIAN_POINT ( 'NONE',  ( 24.59180953954000159, -12.25104150531999991, -3.053504439888000022 ) ) ;
#28464=CARTESIAN_POINT ( 'NONE',  ( 16.10005255078199937, 3.632778330393000132, 11.06917548872000090 ) ) ;
#28467=DIRECTION ( 'NONE',  ( 1.000000000000000000, 0.000000000000000000, 0.000000000000000000 ) ) ;
#28470=CARTESIAN_POINT ( 'NONE',  ( 23.89320776801300283, 8.862674798131001452, 7.304122743059000555 ) ) ;
#28474=CARTESIAN_POINT ( 'NONE',  ( 24.83137806176560503, 8.598806517310384478, -8.498658647712348468 ) ) ;
#28475=CARTESIAN_POINT ( 'NONE',  ( 23.50387503050299998, 0.01734707287875719012, -13.99998925281954065 ) ) ;
#28477=CARTESIAN_POINT ( 'NONE',  ( 24.13560165858060813, -12.48955752925216167, 3.366833954017129482 ) ) ;
#28484=CARTESIAN_POINT ( 'NONE',  ( 23.66004879239100234, 6.960835523577999950, -12.06029416026999890 ) ) ;
#28485=EDGE_LOOP ( 'NONE', ( #66017, #21864, #11155, #51791 ) ) ;
#28487=ORIENTED_EDGE ( 'NONE', *, *, #44622, .F. ) ;
#28492=CARTESIAN_POINT ( 'NONE',  ( 15.95279538704000366, 3.847565940079000324, 11.76597731123000123 ) ) ;
#28493=CARTESIAN_POINT ( 'NONE',  ( 11.64596081258699911, -11.57456368445000017, -1.729631387595999881 ) ) ;
#28503=FACE_OUTER_BOUND ( 'NONE', #59316, .T. ) ;
#28506=CARTESIAN_POINT ( 'NONE',  ( 24.67332306156800215, 3.458640006525999677, 12.04351266709000079 ) ) ;
#28508=CARTESIAN_POINT ( 'NONE',  ( 24.98632790797000069, -3.086020258067999844, 11.61344380798999865 ) ) ;
#28523=FACE_OUTER_BOUND ( 'NONE', #53200, .T. ) ;
#28530=ORIENTED_EDGE ( 'NONE', *, *, #53401, .T. ) ;
#28534=CARTESIAN_POINT ( 'NONE',  ( 24.96658445227665979, 10.83443034554823825, 3.855530973479976531 ) ) ;
#28535=DIRECTION ( 'NONE',  ( -1.000000000000000000, 0.000000000000000000, 0.000000000000000000 ) ) ;
#28538=AXIS2_PLACEMENT_3D ( 'NONE', #65744, #55955, #66089 ) ;
#28542=ORIENTED_EDGE ( 'NONE', *, *, #1760, .F. ) ;
#28546=DIRECTION ( 'NONE',  ( -1.000000000000000000, 0.000000000000000000, 0.000000000000000000 ) ) ;
#28558=CARTESIAN_POINT ( 'NONE',  ( 16.13849254682300227, 3.245716968028000249, 11.43439984646999896 ) ) ;
#28562=CARTESIAN_POINT ( 'NONE',  ( 25.39993151917486713, -2.060147809147888420, -11.21226007647768874 ) ) ;
#28569=CARTESIAN_POINT ( 'NONE',  ( 16.10004050617000004, 3.886235259787000018, 11.90683839252000098 ) ) ;
#28574=AXIS2_PLACEMENT_3D ( 'NONE', #41912, #47163, #12682 ) ;
#28578=CARTESIAN_POINT ( 'NONE',  ( 24.39664325339802176, 8.810500106973549350, 8.810500106973549350 ) ) ;
#28587=CARTESIAN_POINT ( 'NONE',  ( 11.50001544675000176, -12.52500000000000036, 0.000000000000000000 ) ) ;
#28592=AXIS2_PLACEMENT_3D ( 'NONE', #53754, #27533, #11103 ) ;
#28600=DIRECTION ( 'NONE',  ( -8.953094821931283005E-11, -0.9867385579967302700, -0.1623176458754050089 ) ) ;
#28607=CARTESIAN_POINT ( 'NONE',  ( 23.54916673983900210, -10.40118575069000073, 9.428023239853999371 ) ) ;
#28614=CARTESIAN_POINT ( 'NONE',  ( 23.58131316884520245, 3.140314540300665591, 13.62732133062536377 ) ) ;
#28616=ORIENTED_EDGE ( 'NONE', *, *, #57765, .F. ) ;
#28617=CARTESIAN_POINT ( 'NONE',  ( 25.48313700195200227, 2.676699651352000053, -11.27114471784999949 ) ) ;
#28620=DIRECTION ( 'NONE',  ( -1.000000000000000000, 0.000000000000000000, 0.000000000000000000 ) ) ;
#28636=VECTOR ( 'NONE', #30440, 1000.000000000000114 ) ;
#28637=CARTESIAN_POINT ( 'NONE',  ( 23.58435506825300010, 2.902136918182999903, 13.63397704980999947 ) ) ;
#28639=VERTEX_POINT ( 'NONE', #38588 ) ;
#28640=CARTESIAN_POINT ( 'NONE',  ( 23.61469341836961533, -10.17936131679624445, 9.423452332300746193 ) ) ;
#28641=B_SPLINE_CURVE_WITH_KNOTS ( 'NONE', 3,
 ( #57289, #10429, #9391, #30737, #52045, #25488 ),
 .UNSPECIFIED., .F., .F.,
 ( 4, 2, 4 ),
 ( 0.000000000000000000, 0.4999999999999991118, 1.000000000000000000 ),
 .UNSPECIFIED. ) ;
#28644=CARTESIAN_POINT ( 'NONE',  ( 23.66004879239100234, 0.000000000000000000, 0.000000000000000000 ) ) ;
#28653=VERTEX_POINT ( 'NONE', #44552 ) ;
#28655=CARTESIAN_POINT ( 'NONE',  ( 24.04055934518150650, 9.302271743222915390, 9.232431401971632923 ) ) ;
#28656=ORIENTED_EDGE ( 'NONE', *, *, #6687, .T. ) ;
#28661=CARTESIAN_POINT ( 'NONE',  ( 18.29014736449600420, -11.95934322008999828, 3.530971945262000311 ) ) ;
#28670=ORIENTED_EDGE ( 'NONE', *, *, #68357, .T. ) ;
#28672=CARTESIAN_POINT ( 'NONE',  ( 24.35365242081700288, -10.90899669668998584, 3.315896191951999583 ) ) ;
#28674=CARTESIAN_POINT ( 'NONE',  ( 23.73581744296999929, -3.554601233002000260, 13.41645131342000141 ) ) ;
#28684=CARTESIAN_POINT ( 'NONE',  ( 24.61098151538899970, -3.467630292425999627, -12.10773253045999986 ) ) ;
#28695=ORIENTED_EDGE ( 'NONE', *, *, #31325, .T. ) ;
#28705=CARTESIAN_POINT ( 'NONE',  ( 18.29983863915590803, -1.925365984851983070, 12.21183827962646085 ) ) ;
#28708=FACE_OUTER_BOUND ( 'NONE', #43567, .T. ) ;
#28711=DIRECTION ( 'NONE',  ( -1.000000000000000000, 0.000000000000000000, 0.000000000000000000 ) ) ;
#28712=CARTESIAN_POINT ( 'NONE',  ( 13.32310803393400178, -12.20807901729000022, -2.049767542799999731 ) ) ;
#28721=CARTESIAN_POINT ( 'NONE',  ( 14.39999999971666789, 12.11987147417543298, -3.159800697744812314 ) ) ;
#28730=VECTOR ( 'NONE', #44687, 1000.000000000000000 ) ;
#28736=ORIENTED_EDGE ( 'NONE', *, *, #57433, .T. ) ;
#28737=AXIS2_PLACEMENT_3D ( 'NONE', #42447, #32312, #27400 ) ;
#28740=ORIENTED_EDGE ( 'NONE', *, *, #11814, .F. ) ;
#28741=ORIENTED_EDGE ( 'NONE', *, *, #8608, .T. ) ;
#28742=CARTESIAN_POINT ( 'NONE',  ( 24.73255430586192816, -3.116067653016331818, -11.77907593398745867 ) ) ;
#28744=CARTESIAN_POINT ( 'NONE',  ( 23.59999462723899910, 13.22316330987000121, -4.267799687262000319 ) ) ;
#28747=CARTESIAN_POINT ( 'NONE',  ( 24.30000000000000071, -11.49391741900999975, -4.090215442373000165 ) ) ;
#28748=CARTESIAN_POINT ( 'NONE',  ( 11.44795901272999927, 3.583381594953999549, -11.14153199795000049 ) ) ;
#28752=ADVANCED_FACE ( 'NONE', ( #22157 ), #23737, .T. ) ;
#28765=ORIENTED_EDGE ( 'NONE', *, *, #66623, .F. ) ;
#28768=EDGE_LOOP ( 'NONE', ( #61034, #35616, #11289, #2932 ) ) ;
#28769=CARTESIAN_POINT ( 'NONE',  ( 12.83143828159500188, 11.44347076768000093, -4.696252053897000067 ) ) ;
#28771=CARTESIAN_POINT ( 'NONE',  ( 23.99048274734800046, -3.573011467988000067, -12.95903152520000035 ) ) ;
#28778=B_SPLINE_CURVE_WITH_KNOTS ( 'NONE', 3,
 ( #62585, #25539, #3852, #67831, #14372, #14026 ),
 .UNSPECIFIED., .F., .F.,
 ( 4, 2, 4 ),
 ( 0.000000000000000000, 0.5000000000000000000, 1.000000000000000000 ),
 .UNSPECIFIED. ) ;
#28788=CARTESIAN_POINT ( 'NONE',  ( 16.00429364930199938, -8.559608311085998622, -7.983357056237001537 ) ) ;
#28791=ORIENTED_EDGE ( 'NONE', *, *, #58026, .F. ) ;
#28798=VECTOR ( 'NONE', #11024, 1000.000000000000227 ) ;
#28802=CARTESIAN_POINT ( 'NONE',  ( 11.61689913334100055, 3.709679022145000005, -12.00356807880999988 ) ) ;
#28815=ORIENTED_EDGE ( 'NONE', *, *, #44054, .F. ) ;
#28817=VECTOR ( 'NONE', #63190, 1000.000000000000000 ) ;
#28821=CARTESIAN_POINT ( 'NONE',  ( 13.31007343199765813, -11.51543253752115525, -1.765677284072121989 ) ) ;
#28825=CARTESIAN_POINT ( 'NONE',  ( 24.30000000000000071, -9.289189189551001036, 7.908916752675001050 ) ) ;
#28829=CARTESIAN_POINT ( 'NONE',  ( 24.44496264144000364, 8.810483598181999554, -8.810508341310001157 ) ) ;
#28830=AXIS2_PLACEMENT_3D ( 'NONE', #13326, #28711, #39190 ) ;
#28832=CARTESIAN_POINT ( 'NONE',  ( 24.52306339378907296, 8.782889706257643425, -8.926437547059927979 ) ) ;
#28846=ORIENTED_EDGE ( 'NONE', *, *, #57706, .F. ) ;
#28850=CARTESIAN_POINT ( 'NONE',  ( 24.54223752889256360, -3.611770689511173860, -12.30300795109232581 ) ) ;
#28851=CARTESIAN_POINT ( 'NONE',  ( 11.80585503023100102, -11.57020517019000039, -1.758699328329000222 ) ) ;
#28873=DIRECTION ( 'NONE',  ( 0.000000000000000000, 0.000000000000000000, -1.000000000000000000 ) ) ;
#28883=CIRCLE ( 'NONE', #63479, 1.000000000000001332 ) ;
#28894=VERTEX_POINT ( 'NONE', #56399 ) ;
#28900=CARTESIAN_POINT ( 'NONE',  ( 23.61456421552348672, -13.25068299535432459, -4.104339497028676398 ) ) ;
#28901=CARTESIAN_POINT ( 'NONE',  ( 24.30857393632600250, 3.216436940933999900, -12.15172254432999921 ) ) ;
#28904=EDGE_CURVE ( 'NONE', #23570, #23499, #14808, .T. ) ;
#28905=ADVANCED_FACE ( 'NONE', ( #45227 ), #40730, .F. ) ;
#28912=CARTESIAN_POINT ( 'NONE',  ( 12.79999998875598344, -11.49049412642037460, 4.802266170000438983 ) ) ;
#28915=CARTESIAN_POINT ( 'NONE',  ( 24.92743226742850382, -8.563809462501300374, -8.403983636214338304 ) ) ;
#28925=CARTESIAN_POINT ( 'NONE',  ( 23.95204486579200420, -12.88042262741999977, -3.488172014188000158 ) ) ;
#28927=CARTESIAN_POINT ( 'NONE',  ( 16.10004050617000004, 4.849232186851351933, 11.59252887645442343 ) ) ;
#28930=DIRECTION ( 'NONE',  ( 0.000000000000000000, 0.000000000000000000, -1.000000000000000000 ) ) ;
#28933=CARTESIAN_POINT ( 'NONE',  ( 23.61469341658364840, -3.071268921750722303, -13.52731160624835027 ) ) ;
#28934=CARTESIAN_POINT ( 'NONE',  ( 25.29989727901499919, -2.258942858049999725, -12.29419282279000036 ) ) ;
#28941=EDGE_LOOP ( 'NONE', ( #59305, #6230, #62510, #28736 ) ) ;
#28942=DIRECTION ( 'NONE',  ( -1.000000000000000000, 0.000000000000000000, 0.000000000000000000 ) ) ;
#28946=EDGE_CURVE ( 'NONE', #67995, #23400, #40384, .T. ) ;
#28950=VERTEX_POINT ( 'NONE', #68 ) ;
#28952=CARTESIAN_POINT ( 'NONE',  ( 17.96012107570599881, 3.168891391480999520, 11.45723209283999999 ) ) ;
#28959=CARTESIAN_POINT ( 'NONE',  ( 24.69899873138500013, -12.37166880149999848, 2.942311212846000057 ) ) ;
#28962=CARTESIAN_POINT ( 'NONE',  ( 24.46729256464000457, 3.339593025236999857, 12.12065414616999881 ) ) ;
#28968=CARTESIAN_POINT ( 'NONE',  ( 15.89979320885400327, -3.824231472901999496, -11.71686814605000038 ) ) ;
#28971=CARTESIAN_POINT ( 'NONE',  ( 17.79403162610499933, 3.298115360370000193, 11.83441368098000090 ) ) ;
#28978=CARTESIAN_POINT ( 'NONE',  ( 13.63331750507211559, -9.617283495289667528, -7.919506078536236338 ) ) ;
#28992=DIRECTION ( 'NONE',  ( 1.000000000000000000, 0.000000000000000000, 0.000000000000000000 ) ) ;
#28994=ORIENTED_EDGE ( 'NONE', *, *, #7137, .F. ) ;
#28996=ORIENTED_EDGE ( 'NONE', *, *, #22873, .T. ) ;
#28999=DIRECTION ( 'NONE',  ( 0.000000000000000000, 1.000000000000000000, 0.000000000000000000 ) ) ;
#29004=EDGE_CURVE ( 'NONE', #63987, #27357, #9543, .T. ) ;
#29008=ORIENTED_EDGE ( 'NONE', *, *, #17439, .T. ) ;
#29010=CARTESIAN_POINT ( 'NONE',  ( 25.49995753756256178, -8.603837101910434271, 7.325400450397203223 ) ) ;
#29012=B_SPLINE_SURFACE_WITH_KNOTS ( 'NONE', 3, 3, ( 
 ( #45128, #55957, #33603, #49321 ),
 ( #49674, #34296, #23099, #7367 ),
 ( #61543, #55618, #7718, #33948 ),
 ( #29059, #61205, #54922, #29408 ),
 ( #8064, #50715, #2469, #39186 ),
 ( #50369, #23794, #66438, #22751 ) ),
 .UNSPECIFIED., .F., .F., .F.,
 ( 4, 1, 1, 4 ),
 ( 4, 4 ),
 ( 0.1811037439853999953, 0.3333333333333000081, 0.6666666666667000474, 0.8725156478927998949 ),
 ( -0.1256563615239000009, 1.125656361510000147 ),
 .UNSPECIFIED. ) ;
#29017=CARTESIAN_POINT ( 'NONE',  ( 17.70779401564400146, -11.44429775961999951, 4.694470971454999919 ) ) ;
#29027=CARTESIAN_POINT ( 'NONE',  ( 23.86982303804800054, -3.657043654406999966, 13.22876065065999818 ) ) ;
#29045=CARTESIAN_POINT ( 'NONE',  ( 25.58980649241400229, 8.350730680791999205, 7.985153332161000428 ) ) ;
#29053=VERTEX_POINT ( 'NONE', #29426 ) ;
#29056=CARTESIAN_POINT ( 'NONE',  ( 24.84557271449745741, 12.09420847694864065, 2.925015109421550186 ) ) ;
#29057=DIRECTION ( 'NONE',  ( 0.000000000000000000, 0.000000000000000000, -1.000000000000000000 ) ) ;
#29059=CARTESIAN_POINT ( 'NONE',  ( 24.36809152995600058, -12.06003563572999937, 3.271087558185000077 ) ) ;
#29063=CARTESIAN_POINT ( 'NONE',  ( 23.61469345536201558, 13.25062970456771083, 4.103859225642715103 ) ) ;
#29079=CARTESIAN_POINT ( 'NONE',  ( 11.50002653705205446, 3.809920415104828262, -11.93174655290500574 ) ) ;
#29103=CIRCLE ( 'NONE', #14565, 12.52500000000000036 ) ;
#29106=CARTESIAN_POINT ( 'NONE',  ( 23.59999441188499958, 10.30760541648000128, -9.317696302454001156 ) ) ;
#29115=CARTESIAN_POINT ( 'NONE',  ( 21.00000000000000000, 0.000000000000000000, 0.000000000000000000 ) ) ;
#29116=CARTESIAN_POINT ( 'NONE',  ( 18.43329219593509194, 2.701919656448346529, 11.40083085748005054 ) ) ;
#29132=CARTESIAN_POINT ( 'NONE',  ( 23.59959168357080017, -13.39165867665727205, 3.997819989704973764 ) ) ;
#29139=CIRCLE ( 'NONE', #116, 5.760713961201000544 ) ;
#29149=DIRECTION ( 'NONE',  ( 1.000000000000000000, 0.000000000000000000, 0.000000000000000000 ) ) ;
#29159=DIRECTION ( 'NONE',  ( 0.000000000000000000, -0.5895247755844827964, -0.8077502949377767250 ) ) ;
#29169=CARTESIAN_POINT ( 'NONE',  ( 24.92845940784351555, 2.996118283957757811, 11.61748718301992156 ) ) ;
#29171=CARTESIAN_POINT ( 'NONE',  ( 24.01911655981654548, -12.68156841354276310, 3.458532931849343850 ) ) ;
#29187=CARTESIAN_POINT ( 'NONE',  ( 11.61719580513100247, -11.50344080059000085, -1.587150035090999722 ) ) ;
#29201=EDGE_CURVE ( 'NONE', #57124, #6268, #35448, .T. ) ;
#29202=EDGE_CURVE ( 'NONE', #23593, #52535, #27893, .T. ) ;
#29203=ORIENTED_EDGE ( 'NONE', *, *, #11281, .F. ) ;
#29209=CARTESIAN_POINT ( 'NONE',  ( 24.56914376165800107, 8.855803919881999775, -9.404908024782999476 ) ) ;
#29210=CARTESIAN_POINT ( 'NONE',  ( 18.07439970769999960, -3.110573872314000177, -11.47478625844000177 ) ) ;
#29214=VERTEX_POINT ( 'NONE', #25187 ) ;
#29217=CARTESIAN_POINT ( 'NONE',  ( 24.35365242081700288, -11.54878985765998500, -2.979915831562000239 ) ) ;
#29221=ORIENTED_EDGE ( 'NONE', *, *, #10420, .F. ) ;
#29226=DIRECTION ( 'NONE',  ( 1.000000000000000000, 0.000000000000000000, 0.000000000000000000 ) ) ;
#29239=CARTESIAN_POINT ( 'NONE',  ( 18.30003129332100187, -2.732683818840999646, -11.53064095373000164 ) ) ;
#29242=B_SPLINE_CURVE_WITH_KNOTS ( 'NONE', 3,
 ( #51114, #56014, #30820, #30479 ),
 .UNSPECIFIED., .F., .F.,
 ( 4, 4 ),
 ( 0.000000000000000000, 1.000000000000000000 ),
 .UNSPECIFIED. ) ;
#29249=CARTESIAN_POINT ( 'NONE',  ( 12.79999999038796688, -11.45060587895086002, 4.713120762395663910 ) ) ;
#29251=EDGE_CURVE ( 'NONE', #47653, #10995, #54983, .T. ) ;
#29252=CARTESIAN_POINT ( 'NONE',  ( 16.39999999393279140, -3.428567374516922506, -11.90640519000895559 ) ) ;
#29257=CARTESIAN_POINT ( 'NONE',  ( 18.90826270587400160, -11.15000000000000036, -4.842665157767000124E-11 ) ) ;
#29263=CARTESIAN_POINT ( 'NONE',  ( 23.55381274576900097, -13.39033134663000091, -4.196426638631999495 ) ) ;
#29271=CARTESIAN_POINT ( 'NONE',  ( 23.78808895316426231, -3.294453063347192234, -13.15444831767801759 ) ) ;
#29272=CARTESIAN_POINT ( 'NONE',  ( 24.30000000000000071, -9.305479840184000651, 8.315530346521999405 ) ) ;
#29280=CIRCLE ( 'NONE', #53811, 0.2999999999999993228 ) ;
#29291=CARTESIAN_POINT ( 'NONE',  ( 25.30000327618300204, -9.659335867304680079, -6.394377797198711910 ) ) ;
#29298=CIRCLE ( 'NONE', #67199, 12.52500000000000036 ) ;
#29301=CARTESIAN_POINT ( 'NONE',  ( 24.30000000000000071, 9.240454295252998662, 8.250504801592001058 ) ) ;
#29307=CARTESIAN_POINT ( 'NONE',  ( 15.90003771078200145, -3.695138809391000034, -11.25918926437999978 ) ) ;
#29323=B_SPLINE_CURVE_WITH_KNOTS ( 'NONE', 3,
 ( #34414, #8175, #46271, #18667, #67574, #55731, #66893, #39999, #41019, #19005, #29169, #8517, #62341, #50477, #29865, #2579, #3268, #23907, #61313, #13434, #34755, #50826 ),
 .UNSPECIFIED., .F., .F.,
 ( 4, 2, 2, 1, 2, 2, 2, 1, 1, 1, 2, 2, 4 ),
 ( 0.000000000000000000, 0.2499999999999572564, 0.3749999999999340528, 0.4374999999999227840, 0.4687499999999181211, 0.4999999999999135136, 0.6249999999999101830, 0.6874999999999068523, 0.7187499999999039657, 0.7343749999999026334, 0.7421874999999006350, 0.7499999999998986366, 1.000000000000000000 ),
 .UNSPECIFIED. ) ;
#29330=CARTESIAN_POINT ( 'NONE',  ( 24.15455566405240617, -9.133426265715067771, 9.111863915754568666 ) ) ;
#29334=DIRECTION ( 'NONE',  ( 0.000000000000000000, -0.7071067811865475727, -0.7071067811865475727 ) ) ;
#29346=AXIS2_PLACEMENT_3D ( 'NONE', #38238, #53637, #11321 ) ;
#29347=VERTEX_POINT ( 'NONE', #13938 ) ;
#29349=B_SPLINE_CURVE_WITH_KNOTS ( 'NONE', 3,
 ( #61625, #66866, #67893, #13403 ),
 .UNSPECIFIED., .F., .F.,
 ( 4, 4 ),
 ( 0.000000000000000000, 1.000000000000000000 ),
 .UNSPECIFIED. ) ;
#29354=FACE_OUTER_BOUND ( 'NONE', #8350, .T. ) ;
#29356=CARTESIAN_POINT ( 'NONE',  ( 17.60718180634500030, -11.44293104347999979, 4.697469793150999884 ) ) ;
#29376=VERTEX_POINT ( 'NONE', #14281 ) ;
#29378=B_SPLINE_CURVE_WITH_KNOTS ( 'NONE', 3,
 ( #30093, #40906, #8408, #67805 ),
 .UNSPECIFIED., .F., .F.,
 ( 4, 4 ),
 ( 0.000000000000000000, 1.000000000000000000 ),
 .UNSPECIFIED. ) ;
#29382=AXIS2_PLACEMENT_3D ( 'NONE', #50359, #67449, #7353 ) ;
#29386=B_SPLINE_CURVE_WITH_KNOTS ( 'NONE', 3,
 ( #64160, #5444, #43541, #54364, #59956, #38988, #37941, #49462 ),
 .UNSPECIFIED., .F., .F.,
 ( 4, 2, 2, 4 ),
 ( 0.000000000000000000, 0.4999999999999995559, 0.7499999999999997780, 1.000000000000000000 ),
 .UNSPECIFIED. ) ;
#29390=ORIENTED_EDGE ( 'NONE', *, *, #33538, .F. ) ;
#29407=B_SPLINE_CURVE_WITH_KNOTS ( 'NONE', 3,
 ( #16696, #37343, #53427, #42257 ),
 .UNSPECIFIED., .F., .F.,
 ( 4, 4 ),
 ( 0.000000000000000000, 1.000000000000000000 ),
 .UNSPECIFIED. ) ;
#29408=CARTESIAN_POINT ( 'NONE',  ( 24.66122485283899834, -12.38509973019000121, 2.963735973451999683 ) ) ;
#29410=CARTESIAN_POINT ( 'NONE',  ( 11.50001436749000128, -11.64999275565999959, -4.104694901035999596E-10 ) ) ;
#29415=CARTESIAN_POINT ( 'NONE',  ( 24.72675064436329606, -8.645756478877553164, 8.593170189962409111 ) ) ;
#29423=EDGE_CURVE ( 'NONE', #30301, #40828, #45478, .T. ) ;
#29426=CARTESIAN_POINT ( 'NONE',  ( 18.29983863916000075, 2.861762957209999847, -11.98830831200999825 ) ) ;
#29428=CARTESIAN_POINT ( 'NONE',  ( 11.66883611461859971, 3.345349279800629905, -11.86065815404513479 ) ) ;
#29438=DIRECTION ( 'NONE',  ( 1.000000000000000000, 0.000000000000000000, -4.770489558936215471E-13 ) ) ;
#29440=CARTESIAN_POINT ( 'NONE',  ( 24.44496356232399847, -3.224881240379999792, -12.03535804424000055 ) ) ;
#29454=CARTESIAN_POINT ( 'NONE',  ( 24.65659314676950231, 8.681452214508958320, 8.652166108174951020 ) ) ;
#29466=ORIENTED_EDGE ( 'NONE', *, *, #24224, .F. ) ;
#29483=CARTESIAN_POINT ( 'NONE',  ( 17.80000000009400196, 3.216307036143000175, 11.40341376487999980 ) ) ;
#29494=CARTESIAN_POINT ( 'NONE',  ( 23.60205915885299888, 11.56239291744999065, -3.974820703413998846 ) ) ;
#29495=CARTESIAN_POINT ( 'NONE',  ( 13.50018479229797208, 11.40740214419261278, 3.347185923349937031 ) ) ;
#29502=AXIS2_PLACEMENT_3D ( 'NONE', #44826, #49019, #22440 ) ;
#29503=CARTESIAN_POINT ( 'NONE',  ( 21.60000012424471194, -13.89999856298999958, 0.000000000000000000 ) ) ;
#29515=CARTESIAN_POINT ( 'NONE',  ( 25.41798597150000205, -8.397682312107999536, -8.090308797361000615 ) ) ;
#29522=ORIENTED_EDGE ( 'NONE', *, *, #50997, .F. ) ;
#29524=DIRECTION ( 'NONE',  ( -1.000000000000000000, 0.000000000000000000, 0.000000000000000000 ) ) ;
#29526=CARTESIAN_POINT ( 'NONE',  ( 23.80820397230190011, -13.01045451829668842, 3.693343721330374141 ) ) ;
#29543=B_SPLINE_CURVE_WITH_KNOTS ( 'NONE', 3,
 ( #50014, #18547, #17860, #65737, #61534, #7354 ),
 .UNSPECIFIED., .F., .F.,
 ( 4, 2, 4 ),
 ( 0.000000000000000000, 0.5000000000000000000, 1.000000000000000000 ),
 .UNSPECIFIED. ) ;
#29544=CARTESIAN_POINT ( 'NONE',  ( 24.31006797060300073, -12.13011445653000031, -3.289861759914999517 ) ) ;
#29547=EDGE_CURVE ( 'NONE', #68281, #54071, #48811, .T. ) ;
#29562=CARTESIAN_POINT ( 'NONE',  ( 23.61719497714241101, 3.300271013483454308, -13.56984003092980196 ) ) ;
#29563=CARTESIAN_POINT ( 'NONE',  ( 23.95204244535300120, 9.461060432932999475, -9.410689202680000420 ) ) ;
#29565=CARTESIAN_POINT ( 'NONE',  ( 17.77447410014400120, -3.189754565392000085, -11.45074580414000032 ) ) ;
#29569=ORIENTED_EDGE ( 'NONE', *, *, #2828, .F. ) ;
#29570=EDGE_CURVE ( 'NONE', #68067, #49685, #57976, .T. ) ;
#29585=ORIENTED_EDGE ( 'NONE', *, *, #32281, .F. ) ;
#29587=CARTESIAN_POINT ( 'NONE',  ( 24.44496488041000148, -12.03536727282999941, 3.224852091355999928 ) ) ;
#29588=CARTESIAN_POINT ( 'NONE',  ( 23.67309896701788219, -13.19585400017914267, -3.926555274927371553 ) ) ;
#29589=CARTESIAN_POINT ( 'NONE',  ( 24.46225079000999969, 3.515716880278999756, -12.28737560831000053 ) ) ;
#29600=ORIENTED_EDGE ( 'NONE', *, *, #28144, .F. ) ;
#29603=VECTOR ( 'NONE', #18762, 1000.000000000000000 ) ;
#29610=CARTESIAN_POINT ( 'NONE',  ( 24.30000000000000071, 2.078227429405999693, -11.31065739696999906 ) ) ;
#29611=CARTESIAN_POINT ( 'NONE',  ( 25.46373154986600085, 8.354608910739999672, 8.148450287869000164 ) ) ;
#29637=CARTESIAN_POINT ( 'NONE',  ( 25.60000000000000142, 8.131727983644998048, -8.131727983644998048 ) ) ;
#29640=EDGE_LOOP ( 'NONE', ( #14124, #57440, #67291, #4364, #46096 ) ) ;
#29648=EDGE_CURVE ( 'NONE', #19263, #40828, #42125, .T. ) ;
#29649=CARTESIAN_POINT ( 'NONE',  ( 23.66004879239100234, 0.000000000000000000, 0.000000000000000000 ) ) ;
#29653=CARTESIAN_POINT ( 'NONE',  ( 24.72544608131600086, 3.605127478668999963, 12.13010612098000074 ) ) ;
#29656=ORIENTED_EDGE ( 'NONE', *, *, #17610, .T. ) ;
#29659=DIRECTION ( 'NONE',  ( -0.000000000000000000, 0.8765967884314782577, 0.4812255921203881792 ) ) ;
#29665=CARTESIAN_POINT ( 'NONE',  ( 16.10009593531633243, 3.558564495895859991, 11.09347632393068928 ) ) ;
#29666=ORIENTED_EDGE ( 'NONE', *, *, #29202, .F. ) ;
#29668=CARTESIAN_POINT ( 'NONE',  ( 18.39984528086700166, -1.003641614260999896E-13, -12.42515511467992440 ) ) ;
#29673=ORIENTED_EDGE ( 'NONE', *, *, #38220, .F. ) ;
#29674=CARTESIAN_POINT ( 'NONE',  ( 11.48828127163000268, -3.524947629324000076, 11.86450458095000116 ) ) ;
#29685=CARTESIAN_POINT ( 'NONE',  ( 24.30000000000000071, 11.49391741900999975, 4.090215442373000165 ) ) ;
#29698=AXIS2_PLACEMENT_3D ( 'NONE', #23276, #39703, #44956 ) ;
#29700=CARTESIAN_POINT ( 'NONE',  ( 14.80000000000000071, -3.470217030164000072, 11.92928724693999953 ) ) ;
#29707=CARTESIAN_POINT ( 'NONE',  ( 17.88701341325399952, -3.642483061606999861, -12.02409215997000125 ) ) ;
#29715=ORIENTED_EDGE ( 'NONE', *, *, #45197, .T. ) ;
#29718=EDGE_CURVE ( 'NONE', #19870, #68412, #23668, .T. ) ;
#29719=CARTESIAN_POINT ( 'NONE',  ( 24.51195298297300340, -3.518215509121000117, 12.24293180497000044 ) ) ;
#29725=VERTEX_POINT ( 'NONE', #61400 ) ;
#29736=B_SPLINE_CURVE_WITH_KNOTS ( 'NONE', 3,
 ( #8126, #9746, #18276, #2875 ),
 .UNSPECIFIED., .F., .F.,
 ( 4, 4 ),
 ( 0.000000000000000000, 1.000000000000000000 ),
 .UNSPECIFIED. ) ;
#29738=EDGE_LOOP ( 'NONE', ( #13208, #11353, #42712 ) ) ;
#29747=AXIS2_PLACEMENT_3D ( 'NONE', #23114, #33271, #44113 ) ;
#29751=CARTESIAN_POINT ( 'NONE',  ( 21.60000012424459825, -2.247091401841000284E-13, 4.272138198758000206E-13 ) ) ;
#29754=LINE ( 'NONE', #56985, #14109 ) ;
#29757=ORIENTED_EDGE ( 'NONE', *, *, #46900, .F. ) ;
#29759=CARTESIAN_POINT ( 'NONE',  ( 13.48832048419380314, -11.62805077016393618, -2.291814632468948343 ) ) ;
#29763=EDGE_LOOP ( 'NONE', ( #31228, #45458, #17461, #45897, #14258, #8515 ) ) ;
#29766=CARTESIAN_POINT ( 'NONE',  ( 23.60000000000000142, 0.000000000000000000, 0.000000000000000000 ) ) ;
#29770=EDGE_CURVE ( 'NONE', #57373, #53930, #45008, .T. ) ;
#29776=CARTESIAN_POINT ( 'NONE',  ( 18.14797787938944751, 3.506662021213152514, -12.02412632936462522 ) ) ;
#29783=EDGE_LOOP ( 'NONE', ( #4222, #58811, #57346, #10319 ) ) ;
#29791=DIRECTION ( 'NONE',  ( 0.000000000000000000, 0.000000000000000000, 1.000000000000000000 ) ) ;
#29794=CARTESIAN_POINT ( 'NONE',  ( 11.50001544675000176, -12.52500000000000036, 0.000000000000000000 ) ) ;
#29804=B_SPLINE_CURVE_WITH_KNOTS ( 'NONE', 3,
 ( #21773, #32626, #31593, #16535 ),
 .UNSPECIFIED., .F., .F.,
 ( 4, 4 ),
 ( 0.000000000000000000, 1.000000000000000000 ),
 .UNSPECIFIED. ) ;
#29811=CYLINDRICAL_SURFACE ( 'NONE', #10257, 0.6999999999999992895 ) ;
#29812=CARTESIAN_POINT ( 'NONE',  ( 24.22012277176100170, -3.188429784449000159, -12.21471352112000019 ) ) ;
#29816=CARTESIAN_POINT ( 'NONE',  ( 17.60000001298399397, -11.65261404859787930, 3.227423182320804163 ) ) ;
#29820=CARTESIAN_POINT ( 'NONE',  ( 25.59994555223599733, 10.55174472786000095, -3.754934689065000164 ) ) ;
#29825=LINE ( 'NONE', #29483, #39763 ) ;
#29828=ORIENTED_EDGE ( 'NONE', *, *, #24224, .T. ) ;
#29829=AXIS2_PLACEMENT_3D ( 'NONE', #44877, #12011, #12710 ) ;
#29840=B_SPLINE_CURVE_WITH_KNOTS ( 'NONE', 3,
 ( #43110, #68987, #31594, #63391 ),
 .UNSPECIFIED., .F., .F.,
 ( 4, 4 ),
 ( 0.000000000000000000, 1.000000000000000000 ),
 .UNSPECIFIED. ) ;
#29843=CARTESIAN_POINT ( 'NONE',  ( 13.00000000000000178, -49.86679564220000316, -7.696464862566000598 ) ) ;
#29846=CARTESIAN_POINT ( 'NONE',  ( 23.66004879239100234, -13.39256464007999980, -3.813546745462999876 ) ) ;
#29853=DIRECTION ( 'NONE',  ( 0.000000000000000000, 0.7614089499631913061, 0.6482718649732923666 ) ) ;
#29855=CARTESIAN_POINT ( 'NONE',  ( 13.64514873068900158, -9.050862583665999495, -7.420564490681000436 ) ) ;
#29857=DIRECTION ( 'NONE',  ( 0.7071068187612229439, 0.000000000000000000, -0.7071067436118699812 ) ) ;
#29865=CARTESIAN_POINT ( 'NONE',  ( 24.76115083069733203, 3.101111505761503295, 11.75477011280721840 ) ) ;
#29867=CARTESIAN_POINT ( 'NONE',  ( 18.20279897579441197, 3.027817980922571817, -11.45825916412429457 ) ) ;
#29871=ORIENTED_EDGE ( 'NONE', *, *, #25704, .F. ) ;
#29872=CARTESIAN_POINT ( 'NONE',  ( 25.30000327618300204, 2.078227429405999693, -11.31065739696999906 ) ) ;
#29876=EDGE_CURVE ( 'NONE', #33943, #37994, #24888, .T. ) ;
#29884=DIRECTION ( 'NONE',  ( 0.000000000000000000, -0.1807154286440003366, -0.9835354258236024272 ) ) ;
#29885=AXIS2_PLACEMENT_3D ( 'NONE', #18106, #66326, #13214 ) ;
#29886=CARTESIAN_POINT ( 'NONE',  ( 24.46275371508600216, -12.39843049379000028, -3.098824767661999768 ) ) ;
#29904=CARTESIAN_POINT ( 'NONE',  ( 25.41675762280700113, 8.397332536106999257, -8.092742924401999716 ) ) ;
#29905=CARTESIAN_POINT ( 'NONE',  ( 25.00271319629458944, -3.413733088963054385, -11.76143375765198407 ) ) ;
#29906=CARTESIAN_POINT ( 'NONE',  ( 18.24051303026600124, -3.055556278716000218, -11.39470302754000031 ) ) ;
#29917=CYLINDRICAL_SURFACE ( 'NONE', #28737, 1.000000000000000222 ) ;
#29926=B_SPLINE_CURVE_WITH_KNOTS ( 'NONE', 3,
 ( #38025, #27546, #32794, #22634, #54109, #21263 ),
 .UNSPECIFIED., .F., .F.,
 ( 4, 2, 4 ),
 ( 0.000000000000000000, 0.5000000000000000000, 1.000000000000000000 ),
 .UNSPECIFIED. ) ;
#29930=CARTESIAN_POINT ( 'NONE',  ( 24.36453968238300050, 3.372832729159999765, -12.24475767785000002 ) ) ;
#29931=CARTESIAN_POINT ( 'NONE',  ( 18.20279897513207246, -3.027817981728709640, -11.45825916391119037 ) ) ;
#29940=CIRCLE ( 'NONE', #24329, 1.000000000000000888 ) ;
#29961=EDGE_LOOP ( 'NONE', ( #34204, #23640, #45784, #27520, #53168, #18337, #48480, #57310 ) ) ;
#29966=CARTESIAN_POINT ( 'NONE',  ( 24.05220244970136179, -3.343001867506199432, -12.65093409602237529 ) ) ;
#29972=ORIENTED_EDGE ( 'NONE', *, *, #40833, .F. ) ;
#29986=CARTESIAN_POINT ( 'NONE',  ( 15.95500032369699994, 8.890098389148999303, 8.614471248541999415 ) ) ;
#29990=TOROIDAL_SURFACE ( 'NONE', #33317, 12.20000000000000107, 0.6999999999999999556 ) ;
#29995=FACE_OUTER_BOUND ( 'NONE', #10363, .T. ) ;
#29997=CARTESIAN_POINT ( 'NONE',  ( 24.63329909277253194, -2.078227420229220357, -11.31065739865757536 ) ) ;
#30003=VERTEX_POINT ( 'NONE', #63093 ) ;
#30008=ORIENTED_EDGE ( 'NONE', *, *, #24455, .T. ) ;
#30013=CARTESIAN_POINT ( 'NONE',  ( 24.30001129594134568, -12.15210919218037233, 3.256147844378488809 ) ) ;
#30014=DIRECTION ( 'NONE',  ( 1.000000000000000000, 0.000000000000000000, 0.000000000000000000 ) ) ;
#30027=CARTESIAN_POINT ( 'NONE',  ( 16.10009593531634664, -3.558564495883423273, -11.09347632393477134 ) ) ;
#30047=CARTESIAN_POINT ( 'NONE',  ( 18.53682146000800302, -2.876943948391000205, -12.22927217127999988 ) ) ;
#30062=CARTESIAN_POINT ( 'NONE',  ( 17.87620400591499958, 3.527529948368999690, -11.96092454128000071 ) ) ;
#30082=CARTESIAN_POINT ( 'NONE',  ( 25.29989948031900227, 2.258942858049999725, -12.29419282279000036 ) ) ;
#30093=CARTESIAN_POINT ( 'NONE',  ( 13.70005190196300227, 9.005348107749998832, 7.391036106496999381 ) ) ;
#30094=CARTESIAN_POINT ( 'NONE',  ( 16.06714147702547635, 8.497559733041605057, 7.969681199758297474 ) ) ;
#30098=VERTEX_POINT ( 'NONE', #24860 ) ;
#30100=EDGE_CURVE ( 'NONE', #15615, #21235, #62779, .T. ) ;
#30101=CARTESIAN_POINT ( 'NONE',  ( 24.57709886597293547, -8.720615828874477060, 8.720613681126877736 ) ) ;
#30113=CARTESIAN_POINT ( 'NONE',  ( 11.79999999684100054, 12.15995044155999949, 2.000340912084999978 ) ) ;
#30114=CARTESIAN_POINT ( 'NONE',  ( 24.30001120070703990, 12.15210914071406734, -3.256147830588134173 ) ) ;
#30118=ORIENTED_EDGE ( 'NONE', *, *, #16250, .F. ) ;
#30121=EDGE_LOOP ( 'NONE', ( #39466, #14794, #2400, #28815 ) ) ;
#30123=CARTESIAN_POINT ( 'NONE',  ( 18.50003594170800270, -2.686563649653999963, 11.33603604535000109 ) ) ;
#30144=DIRECTION ( 'NONE',  ( 0.000000000000000000, 0.000000000000000000, -1.000000000000000000 ) ) ;
#30147=FACE_OUTER_BOUND ( 'NONE', #1038, .T. ) ;
#30153=ADVANCED_FACE ( 'NONE', ( #50059 ), #40937, .F. ) ;
#30155=CARTESIAN_POINT ( 'NONE',  ( 24.30000000000000071, 2.258942858049999725, 12.29419282279000036 ) ) ;
#30166=CARTESIAN_POINT ( 'NONE',  ( 23.59642540973940683, -13.38915559410792078, 4.012079637628372275 ) ) ;
#30171=CARTESIAN_POINT ( 'NONE',  ( 23.61700615888999977, -2.917315259571999775, 13.53528614794999996 ) ) ;
#30173=CARTESIAN_POINT ( 'NONE',  ( 13.50018479229797208, 10.27880801399748734, 5.973155204427849974 ) ) ;
#30175=ORIENTED_EDGE ( 'NONE', *, *, #26275, .T. ) ;
#30180=CARTESIAN_POINT ( 'NONE',  ( 24.30000000000000071, 9.289189189551001036, -7.908916752675001050 ) ) ;
#30181=DIRECTION ( 'NONE',  ( 0.000000000000000000, 0.000000000000000000, -1.000000000000000000 ) ) ;
#30217=CARTESIAN_POINT ( 'NONE',  ( 24.36504260745899941, -12.29008018610999819, -3.201257196435000285 ) ) ;
#30218=CARTESIAN_POINT ( 'NONE',  ( 25.50719570236825362, 2.874190748112039895, 11.25480690672102746 ) ) ;
#30223=CYLINDRICAL_SURFACE ( 'NONE', #48460, 11.50000000000000000 ) ;
#30225=AXIS2_PLACEMENT_3D ( 'NONE', #7256, #22987, #38379 ) ;
#30237=CARTESIAN_POINT ( 'NONE',  ( 24.87549197752000296, 8.587510512484001879, -8.379258482743999537 ) ) ;
#30238=CARTESIAN_POINT ( 'NONE',  ( 23.66565514010100202, 10.00711324362000099, -9.518238975075000496 ) ) ;
#30239=CARTESIAN_POINT ( 'NONE',  ( 17.88018231457700224, -3.314507696643999690, -11.22393832560999982 ) ) ;
#30244=ORIENTED_EDGE ( 'NONE', *, *, #31402, .F. ) ;
#30256=CARTESIAN_POINT ( 'NONE',  ( 24.84571067577687842, -3.513925179492865425, 11.93623758569678728 ) ) ;
#30268=CARTESIAN_POINT ( 'NONE',  ( 13.55481756226799916, -11.54935041389000006, -2.400813070608000199 ) ) ;
#30271=ORIENTED_EDGE ( 'NONE', *, *, #20371, .T. ) ;
#30281=CARTESIAN_POINT ( 'NONE',  ( 23.56673047179102909, 10.35362056585002755, 9.408487697651425563 ) ) ;
#30283=AXIS2_PLACEMENT_3D ( 'NONE', #37276, #57214, #9316 ) ;
#30285=ADVANCED_FACE ( 'NONE', ( #46533 ), #10491, .T. ) ;
#30294=VERTEX_POINT ( 'NONE', #36732 ) ;
#30296=CARTESIAN_POINT ( 'NONE',  ( 18.50003594167399967, 2.686563651857999613, 11.33603604486000016 ) ) ;
#30301=VERTEX_POINT ( 'NONE', #58051 ) ;
#30303=EDGE_LOOP ( 'NONE', ( #3342, #14292, #29715, #33681 ) ) ;
#30310=CARTESIAN_POINT ( 'NONE',  ( 23.52034478825299857, 13.48676252767000072, 4.209100417191000254 ) ) ;
#30311=ORIENTED_EDGE ( 'NONE', *, *, #55884, .F. ) ;
#30316=CARTESIAN_POINT ( 'NONE',  ( 15.95168611684299975, 8.949867560646000086, 8.553740745252000011 ) ) ;
#30317=CARTESIAN_POINT ( 'NONE',  ( 18.29983863916000075, 2.861762957209999847, -11.98830831200999825 ) ) ;
#30324=CYLINDRICAL_SURFACE ( 'NONE', #26067, 0.6999999999999992895 ) ;
#30328=CARTESIAN_POINT ( 'NONE',  ( 23.55669233645500071, 10.23544483926000126, 9.677465815984000130 ) ) ;
#30331=FACE_OUTER_BOUND ( 'NONE', #45981, .T. ) ;
#30337=CARTESIAN_POINT ( 'NONE',  ( 18.48724299199999876, 3.206939682244000167, 12.14698705996000072 ) ) ;
#30348=CARTESIAN_POINT ( 'NONE',  ( 11.40162633574000139, -3.633188743968999823, 11.83198634993999931 ) ) ;
#30371=ORIENTED_EDGE ( 'NONE', *, *, #58555, .T. ) ;
#30376=CARTESIAN_POINT ( 'NONE',  ( 17.77415039705200073, -3.297056071606000227, -11.83473721697999892 ) ) ;
#30377=CARTESIAN_POINT ( 'NONE',  ( 24.70869262248000098, -8.717234922876000880, 9.201991545054999833 ) ) ;
#30382=ORIENTED_EDGE ( 'NONE', *, *, #15946, .T. ) ;
#30383=ORIENTED_EDGE ( 'NONE', *, *, #16042, .F. ) ;
#30386=CARTESIAN_POINT ( 'NONE',  ( 12.38752622490241784, -11.20128320855829607, 3.203207420542418138 ) ) ;
#30392=CARTESIAN_POINT ( 'NONE',  ( 17.79055474012400140, 3.643253463509999790, -12.02383756773999934 ) ) ;
#30395=ADVANCED_FACE ( 'NONE', ( #22357 ), #60117, .F. ) ;
#30403=FACE_OUTER_BOUND ( 'NONE', #40278, .T. ) ;
#30411=CARTESIAN_POINT ( 'NONE',  ( 23.50387503050299998, 0.000000000000000000, 0.000000000000000000 ) ) ;
#30417=AXIS2_PLACEMENT_3D ( 'NONE', #64356, #65406, #16480 ) ;
#30423=CARTESIAN_POINT ( 'NONE',  ( 14.03986884071600016, -9.265369649631999494, -8.206962993589000277 ) ) ;
#30424=CARTESIAN_POINT ( 'NONE',  ( 15.89979320884932612, 5.681736459260974037, 10.98277228430208474 ) ) ;
#30430=EDGE_LOOP ( 'NONE', ( #3012, #13170, #63554, #34489 ) ) ;
#30440=DIRECTION ( 'NONE',  ( 0.9999999999777403614, 3.933702048292161083E-06, 5.389360667264221932E-06 ) ) ;
#30444=CARTESIAN_POINT ( 'NONE',  ( 18.10505187282181794, 3.528432543146514000, -12.01774066417131870 ) ) ;
#30455=CARTESIAN_POINT ( 'NONE',  ( 15.90018573812067260, 7.829696748392686700, 8.945859267998583775 ) ) ;
#30462=B_SPLINE_CURVE_WITH_KNOTS ( 'NONE', 3,
 ( #11107, #14975, #9721, #25810 ),
 .UNSPECIFIED., .F., .F.,
 ( 4, 4 ),
 ( 0.000000000000000000, 1.000000000000000000 ),
 .UNSPECIFIED. ) ;
#30466=ORIENTED_EDGE ( 'NONE', *, *, #54091, .T. ) ;
#30467=CARTESIAN_POINT ( 'NONE',  ( 18.50001572531400029, 0.9783175424405120557, -12.52500000000000568 ) ) ;
#30472=CARTESIAN_POINT ( 'NONE',  ( 11.30000000000000071, 7.371880883511000048E-13, 4.000966224993000022E-14 ) ) ;
#30476=EDGE_CURVE ( 'NONE', #38805, #10241, #2007, .T. ) ;
#30479=CARTESIAN_POINT ( 'NONE',  ( 24.30000000000000071, 12.03537377768999939, -3.224868684338999980 ) ) ;
#30485=DIRECTION ( 'NONE',  ( 0.7070584287740061535, 0.000000000000000000, -0.7071551302929461880 ) ) ;
#30495=CARTESIAN_POINT ( 'NONE',  ( 23.57017933877721916, -13.34347207735601160, 4.199491041959400484 ) ) ;
#30496=ORIENTED_EDGE ( 'NONE', *, *, #68640, .F. ) ;
#30504=CARTESIAN_POINT ( 'NONE',  ( 25.44993786153400350, -9.517611874540000017, 8.103398312166000039 ) ) ;
#30507=ORIENTED_EDGE ( 'NONE', *, *, #4071, .T. ) ;
#30508=VECTOR ( 'NONE', #51935, 1000.000000000000227 ) ;
#30519=CARTESIAN_POINT ( 'NONE',  ( 24.69847990089700218, 12.37231928222000121, 2.942482175274999889 ) ) ;
#30522=CARTESIAN_POINT ( 'NONE',  ( 13.73763077846600034, -8.978479145825000174, -7.363267546620999582 ) ) ;
#30534=CARTESIAN_POINT ( 'NONE',  ( 18.50003594170800270, 2.686563649653999963, -11.33603604535000109 ) ) ;
#30535=ADVANCED_FACE ( 'NONE', ( #45341 ), #11543, .F. ) ;
#30549=DIRECTION ( 'NONE',  ( 1.000000000000000000, 0.000000000000000000, 0.000000000000000000 ) ) ;
#30556=CARTESIAN_POINT ( 'NONE',  ( 23.56665657345700282, 3.286260152889999888E-13, -3.641531520771000148E-13 ) ) ;
#30557=AXIS2_PLACEMENT_3D ( 'NONE', #29637, #61430, #13547 ) ;
#30558=EDGE_CURVE ( 'NONE', #4322, #12209, #39521, .T. ) ;
#30559=CARTESIAN_POINT ( 'NONE',  ( 12.79999999975700042, -11.86189249994999884, 3.298671769835999967 ) ) ;
#30560=DIRECTION ( 'NONE',  ( -1.000000000000000000, 0.000000000000000000, 0.000000000000000000 ) ) ;
#30563=ORIENTED_EDGE ( 'NONE', *, *, #45197, .F. ) ;
#30567=CARTESIAN_POINT ( 'NONE',  ( 24.45991766033800019, 8.787291314975000489, -8.710735419493000009 ) ) ;
#30568=CARTESIAN_POINT ( 'NONE',  ( 23.73546195074399989, 9.842300901745000274, -9.786565046940999935 ) ) ;
#30569=CARTESIAN_POINT ( 'NONE',  ( 17.85728973496400229, -3.190139087762999814, -11.45065787240999988 ) ) ;
#30574=ORIENTED_EDGE ( 'NONE', *, *, #44248, .T. ) ;
#30581=B_SPLINE_CURVE_WITH_KNOTS ( 'NONE', 3,
 ( #65367, #38462, #17837, #33917 ),
 .UNSPECIFIED., .F., .F.,
 ( 4, 4 ),
 ( 0.000000000000000000, 1.000000000000000000 ),
 .UNSPECIFIED. ) ;
#30585=CARTESIAN_POINT ( 'NONE',  ( 13.78329442975000063, 8.859672882948000705, 7.785394853692999995 ) ) ;
#30594=CARTESIAN_POINT ( 'NONE',  ( 24.67921321800200118, -8.727630028894999725, 9.158313644156001132 ) ) ;
#30595=CARTESIAN_POINT ( 'NONE',  ( 24.67921580188599862, 3.567514645466999923, -12.13750897870000145 ) ) ;
#30601=CARTESIAN_POINT ( 'NONE',  ( 12.99229341877100019, -11.49414526569999850, -1.652619848542000058 ) ) ;
#30607=VERTEX_POINT ( 'NONE', #61414 ) ;
#30612=ORIENTED_EDGE ( 'NONE', *, *, #2298, .T. ) ;
#30613=CARTESIAN_POINT ( 'NONE',  ( 23.56664318980499928, 10.37807351222000030, 9.381504534996999212 ) ) ;
#30615=CARTESIAN_POINT ( 'NONE',  ( 25.29987517282700082, -11.77655473258999841, 4.190794510628000680 ) ) ;
#30617=CARTESIAN_POINT ( 'NONE',  ( 24.30000000000000071, -11.76537389984999926, 3.877215761401999750 ) ) ;
#30620=ORIENTED_EDGE ( 'NONE', *, *, #24617, .F. ) ;
#30622=EDGE_CURVE ( 'NONE', #47384, #15208, #41130, .T. ) ;
#30624=LINE ( 'NONE', #68011, #30508 ) ;
#30631=AXIS2_PLACEMENT_3D ( 'NONE', #50904, #24334, #19080 ) ;
#30646=CARTESIAN_POINT ( 'NONE',  ( 15.90000000000000036, 8.611670352361814551, 8.369116320313937152 ) ) ;
#30647=CARTESIAN_POINT ( 'NONE',  ( 23.61267528292200168, 13.29118196436999888, 4.056509241667999532 ) ) ;
#30666=VERTEX_POINT ( 'NONE', #54006 ) ;
#30672=CARTESIAN_POINT ( 'NONE',  ( 18.35500032369700207, 2.879010252073999521, 12.03969535450000095 ) ) ;
#30678=CARTESIAN_POINT ( 'NONE',  ( 24.30001694968100168, 3.271769180623000040, -12.21048179117000032 ) ) ;
#30680=CARTESIAN_POINT ( 'NONE',  ( 24.53428993882599940, 8.855929947951999281, -9.286429770520999938 ) ) ;
#30683=CARTESIAN_POINT ( 'NONE',  ( 11.44437913529000106, -3.868861692926000462, 11.85573592760000139 ) ) ;
#30685=VECTOR ( 'NONE', #9027, 1000.000000000000000 ) ;
#30693=ORIENTED_EDGE ( 'NONE', *, *, #62895, .T. ) ;
#30703=ORIENTED_EDGE ( 'NONE', *, *, #35769, .F. ) ;
#30712=CARTESIAN_POINT ( 'NONE',  ( 17.60000000000000142, 11.23412379136000006, -3.084957477885999833 ) ) ;
#30713=CARTESIAN_POINT ( 'NONE',  ( 17.56428618385299956, -12.04952459351999927, 3.198091602616999651 ) ) ;
#30714=CARTESIAN_POINT ( 'NONE',  ( 13.69992376746900042, 12.26631831379999937, 2.532779022035999805 ) ) ;
#30719=EDGE_LOOP ( 'NONE', ( #44813, #33897, #26971, #25623 ) ) ;
#30728=CARTESIAN_POINT ( 'NONE',  ( 13.40279821320923581, 11.66091458874561582, 2.117181037223689000 ) ) ;
#30731=CARTESIAN_POINT ( 'NONE',  ( 23.58305315713300132, -13.27270145722000017, 4.268532316603000254 ) ) ;
#30737=CARTESIAN_POINT ( 'NONE',  ( 13.55377458794190382, 8.990344585381031095, 7.716059257659970250 ) ) ;
#30747=EDGE_CURVE ( 'NONE', #12746, #34641, #22106, .T. ) ;
#30751=CIRCLE ( 'NONE', #25155, 12.52500000000000036 ) ;
#30752=CARTESIAN_POINT ( 'NONE',  ( 24.45617574031838615, -12.38364418572106018, 3.108063453459867453 ) ) ;
#30760=FACE_OUTER_BOUND ( 'NONE', #45417, .T. ) ;
#30773=CARTESIAN_POINT ( 'NONE',  ( 24.30000000000000071, 0.000000000000000000, 0.000000000000000000 ) ) ;
#30780=AXIS2_PLACEMENT_3D ( 'NONE', #16542, #32633, #50431 ) ;
#30783=FACE_OUTER_BOUND ( 'NONE', #33772, .T. ) ;
#30787=CARTESIAN_POINT ( 'NONE',  ( 24.45999011096800047, -3.150047400517000273, -11.96533092960999944 ) ) ;
#30788=FACE_OUTER_BOUND ( 'NONE', #12593, .T. ) ;
#30790=EDGE_LOOP ( 'NONE', ( #28363, #784, #19369, #28846 ) ) ;
#30791=CARTESIAN_POINT ( 'NONE',  ( 15.75060268747966319, -9.413968701432777308, -8.261605506243164143 ) ) ;
#30807=CARTESIAN_POINT ( 'NONE',  ( 24.90037356005226954, -3.015686408853957889, 11.63997006242029819 ) ) ;
#30818=ORIENTED_EDGE ( 'NONE', *, *, #22129, .T. ) ;
#30819=CARTESIAN_POINT ( 'NONE',  ( 24.46225079000999969, 8.883320982495000351, 9.188387934989000527 ) ) ;
#30820=CARTESIAN_POINT ( 'NONE',  ( 24.34832160914637456, 12.03537035475460115, -3.224867767164909083 ) ) ;
#30827=CARTESIAN_POINT ( 'NONE',  ( 24.30000000000000071, -12.03537377768999939, -3.224868684338999980 ) ) ;
#30838=DIRECTION ( 'NONE',  ( 1.000000000000000000, 0.000000000000000000, 0.000000000000000000 ) ) ;
#30847=FACE_OUTER_BOUND ( 'NONE', #68750, .T. ) ;
#30854=CYLINDRICAL_SURFACE ( 'NONE', #5291, 0.5000000000000004441 ) ;
#30858=AXIS2_PLACEMENT_3D ( 'NONE', #8505, #30865, #29853 ) ;
#30865=DIRECTION ( 'NONE',  ( -1.000000000000000000, 0.000000000000000000, 0.000000000000000000 ) ) ;
#30867=EDGE_CURVE ( 'NONE', #56058, #26192, #25469, .T. ) ;
#30868=DIRECTION ( 'NONE',  ( -1.000000000000000000, 0.000000000000000000, 0.000000000000000000 ) ) ;
#30873=ORIENTED_EDGE ( 'NONE', *, *, #50235, .T. ) ;
#30887=CARTESIAN_POINT ( 'NONE',  ( 13.73837349797500096, 9.670565172354999461, 8.019813433522999802 ) ) ;
#30889=ORIENTED_EDGE ( 'NONE', *, *, #17841, .F. ) ;
#30898=DIRECTION ( 'NONE',  ( -8.953281780977936028E-11, 0.7455324205424948003, 0.6664693615763958023 ) ) ;
#30899=ORIENTED_EDGE ( 'NONE', *, *, #46031, .F. ) ;
#30906=CARTESIAN_POINT ( 'NONE',  ( 17.79518154839200150, 3.190852234727000081, 11.45040960482999814 ) ) ;
#30912=CARTESIAN_POINT ( 'NONE',  ( 11.53144126044203688, 11.54570453903531480, 1.556370816894309783 ) ) ;
#30915=CARTESIAN_POINT ( 'NONE',  ( 24.17809239055575077, 3.317955234501958728, 12.42377263001247201 ) ) ;
#30922=AXIS2_PLACEMENT_3D ( 'NONE', #30504, #29226, #34475 ) ;
#30933=CARTESIAN_POINT ( 'NONE',  ( 13.64649313145500109, 9.010717346174999420, 7.468773375841999851 ) ) ;
#30936=CARTESIAN_POINT ( 'NONE',  ( 25.26996942120215905, -3.169757571932660944, 11.48332646995987005 ) ) ;
#30942=CARTESIAN_POINT ( 'NONE',  ( 12.40000000000000213, 11.60847947989999973, 1.809983899806999919 ) ) ;
#30958=DIRECTION ( 'NONE',  ( 0.000000000000000000, 1.000000000000000000, 0.000000000000000000 ) ) ;
#30963=DIRECTION ( 'NONE',  ( 0.000000000000000000, 0.2098314828218890149, -0.9777375664342490280 ) ) ;
#30976=AXIS2_PLACEMENT_3D ( 'NONE', #59044, #31794, #60082 ) ;
#30984=DIRECTION ( 'NONE',  ( 0.000000000000000000, 0.9999606858717338120, -0.008867170401640298016 ) ) ;
#30988=DIRECTION ( 'NONE',  ( 0.000000000000000000, 0.000000000000000000, -1.000000000000000000 ) ) ;
#30998=CARTESIAN_POINT ( 'NONE',  ( 13.70003001321900449, -11.73562684670656431, -4.491863874615365404 ) ) ;
#30999=B_SPLINE_CURVE_WITH_KNOTS ( 'NONE', 3,
 ( #14003, #8752, #23453, #51057, #30094, #55958, #18560, #44790, #19586, #34989, #24830, #67123, #51398, #61544 ),
 .UNSPECIFIED., .F., .F.,
 ( 4, 2, 2, 2, 2, 2, 4 ),
 ( 0.000000000000000000, 0.1250000000000024702, 0.2500000000000049405, 0.5000000000000068834, 0.6250000000000041078, 0.7500000000000013323, 1.000000000000000000 ),
 .UNSPECIFIED. ) ;
#31003=FACE_OUTER_BOUND ( 'NONE', #51356, .T. ) ;
#31013=ADVANCED_FACE ( 'NONE', ( #24322 ), #53961, .F. ) ;
#31022=DIRECTION ( 'NONE',  ( 0.000000000000000000, 0.9659258262890757507, -0.2588190451024934835 ) ) ;
#31024=ORIENTED_EDGE ( 'NONE', *, *, #3302, .F. ) ;
#31025=VECTOR ( 'NONE', #2149, 1000.000000000000114 ) ;
#31034=PLANE ( 'NONE',  #65628 ) ;
#31038=CARTESIAN_POINT ( 'NONE',  ( 15.52913652543167267, 8.833284221180715434, 7.896593172538426408 ) ) ;
#31046=CARTESIAN_POINT ( 'NONE',  ( 24.30000000000000071, 11.77655473258999841, -4.190794510628000680 ) ) ;
#31052=CARTESIAN_POINT ( 'NONE',  ( 24.30001683613300045, -12.21047198529999989, -3.271805531187999883 ) ) ;
#31055=EDGE_LOOP ( 'NONE', ( #53750, #9956, #20473, #35444, #43186, #53225, #56437, #37910, #50164, #17813 ) ) ;
#31056=DIRECTION ( 'NONE',  ( 0.000000000000000000, -0.2483836997597965168, 0.9686617251102859205 ) ) ;
#31061=EDGE_CURVE ( 'NONE', #63987, #46963, #60192, .T. ) ;
#31063=CARTESIAN_POINT ( 'NONE',  ( 18.49586274151939236, 2.771911498364446391, 11.31551287271585160 ) ) ;
#31064=CARTESIAN_POINT ( 'NONE',  ( 18.48724299199999876, -3.206939682244000167, -12.14698705996000072 ) ) ;
#31067=EDGE_CURVE ( 'NONE', #60364, #22975, #54016, .T. ) ;
#31070=CARTESIAN_POINT ( 'NONE',  ( 18.49997192701553317, 2.999031289807200906, 12.16100995559787812 ) ) ;
#31075=AXIS2_PLACEMENT_3D ( 'NONE', #38155, #43766, #11938 ) ;
#31082=CARTESIAN_POINT ( 'NONE',  ( 24.32786205753600228, -12.60040638205000008, 3.143984624925999949 ) ) ;
#31085=ORIENTED_EDGE ( 'NONE', *, *, #19091, .T. ) ;
#31104=EDGE_CURVE ( 'NONE', #65237, #39410, #16835, .T. ) ;
#31105=EDGE_CURVE ( 'NONE', #58276, #68518, #54359, .T. ) ;
#31113=AXIS2_PLACEMENT_3D ( 'NONE', #62776, #38190, #30988 ) ;
#31115=CARTESIAN_POINT ( 'NONE',  ( 13.64647714749800045, -9.589793698018000967, -7.972185502806999224 ) ) ;
#31118=VERTEX_POINT ( 'NONE', #36347 ) ;
#31122=CARTESIAN_POINT ( 'NONE',  ( 24.56711857111956832, -11.92025347580062800, 3.200166735598448664 ) ) ;
#31132=CARTESIAN_POINT ( 'NONE',  ( 23.86947959890900250, 3.656851216063000010, 13.22922481556000029 ) ) ;
#31134=CARTESIAN_POINT ( 'NONE',  ( 11.79999999684100054, 3.345264396959000130, -11.86064773189999855 ) ) ;
#31140=CIRCLE ( 'NONE', #69041, 1.000000000000000000 ) ;
#31141=B_SPLINE_CURVE_WITH_KNOTS ( 'NONE', 3,
 ( #48989, #28022, #60178, #5984, #65754, #32571, #32913, #17165, #749, #54226 ),
 .UNSPECIFIED., .F., .F.,
 ( 4, 2, 2, 2, 4 ),
 ( 0.000000000000000000, 0.1249999999280923674, 0.2499999998561847347, 0.3749999997842771160, 0.4999999997123694695 ),
 .UNSPECIFIED. ) ;
#31142=CARTESIAN_POINT ( 'NONE',  ( 23.96071373372425839, -3.344686053530380399, 12.82063560515832812 ) ) ;
#31145=CARTESIAN_POINT ( 'NONE',  ( 25.37703408795700355, -2.612353912486999885, -11.31741720513000082 ) ) ;
#31152=ORIENTED_EDGE ( 'NONE', *, *, #38831, .T. ) ;
#31165=CARTESIAN_POINT ( 'NONE',  ( 24.56710006383056211, -3.188707335874072957, 11.92334242227752483 ) ) ;
#31166=CARTESIAN_POINT ( 'NONE',  ( 24.44496488009700030, 8.810487470433001178, 8.810507756548000557 ) ) ;
#31167=CARTESIAN_POINT ( 'NONE',  ( 29.60000000000000142, 0.000000000000000000, -9.250000000000000000 ) ) ;
#31187=CARTESIAN_POINT ( 'NONE',  ( 12.01640417260608729, 11.69872868927256349, -4.475294149993699122 ) ) ;
#31188=EDGE_CURVE ( 'NONE', #45386, #63789, #29378, .T. ) ;
#31193=B_SPLINE_CURVE_WITH_KNOTS ( 'NONE', 3,
 ( #46022, #19797, #4391, #19105, #25379, #61753 ),
 .UNSPECIFIED., .F., .F.,
 ( 4, 2, 4 ),
 ( 0.000000000000000000, 0.5000000000000000000, 1.000000000000000000 ),
 .UNSPECIFIED. ) ;
#31194=DIRECTION ( 'NONE',  ( 2.186536431443105034E-10, 0.8764392776392420092, 0.4815124013057229813 ) ) ;
#31204=ORIENTED_EDGE ( 'NONE', *, *, #64544, .T. ) ;
#31205=EDGE_CURVE ( 'NONE', #252, #36754, #1872, .T. ) ;
#31216=CARTESIAN_POINT ( 'NONE',  ( 24.37847037357300195, 12.00848431662999971, 3.275550077227999957 ) ) ;
#31228=ORIENTED_EDGE ( 'NONE', *, *, #27615, .T. ) ;
#31237=CARTESIAN_POINT ( 'NONE',  ( 13.73854177342199989, 9.465667024606000624, 8.118361260918998568 ) ) ;
#31240=VECTOR ( 'NONE', #50892, 1000.000000000000227 ) ;
#31242=VERTEX_POINT ( 'NONE', #36003 ) ;
#31249=CARTESIAN_POINT ( 'NONE',  ( 12.20391894010300149, 11.86124369401000145, -3.532130569927999897 ) ) ;
#31250=CARTESIAN_POINT ( 'NONE',  ( 17.56043522961499903, 11.55259058373999892, -4.939852154758999525 ) ) ;
#31253=CARTESIAN_POINT ( 'NONE',  ( 12.45488131765416284, -11.84188428343376032, 3.380847681380453551 ) ) ;
#31254=CARTESIAN_POINT ( 'NONE',  ( 18.04310822451204999, 12.08952385220933756, -3.274024637468825993 ) ) ;
#31257=ORIENTED_EDGE ( 'NONE', *, *, #31932, .F. ) ;
#31259=CARTESIAN_POINT ( 'NONE',  ( 11.72006719377404593, 11.52583591983466071, 1.696350940370162652 ) ) ;
#31261=CARTESIAN_POINT ( 'NONE',  ( 23.79452334243675438, 3.298030808557463445, 13.14157935970629687 ) ) ;
#31264=CARTESIAN_POINT ( 'NONE',  ( 24.67921321731900264, -3.567517257907000250, -12.13750614118000115 ) ) ;
#31272=DIRECTION ( 'NONE',  ( 0.000000000000000000, 0.000000000000000000, 1.000000000000000000 ) ) ;
#31273=DIRECTION ( 'NONE',  ( 0.000000000000000000, -0.007439385635797960035, -0.9999723273877941798 ) ) ;
#31276=CARTESIAN_POINT ( 'NONE',  ( 15.95266668291200141, -3.685671355860000276, -11.20570641515999988 ) ) ;
#31277=CARTESIAN_POINT ( 'NONE',  ( 15.88771848669684061, -8.938332686943013528, -8.488529254939264135 ) ) ;
#31290=DIRECTION ( 'NONE',  ( 1.000000000000000000, 0.000000000000000000, 0.000000000000000000 ) ) ;
#31293=VERTEX_POINT ( 'NONE', #23015 ) ;
#31297=CARTESIAN_POINT ( 'NONE',  ( 13.19211270977099915, -11.64284154253999937, -1.888701237101999997 ) ) ;
#31299=CARTESIAN_POINT ( 'NONE',  ( 12.96900185986900134, 12.22197440418000092, 1.955830866674999946 ) ) ;
#31302=ORIENTED_EDGE ( 'NONE', *, *, #17719, .F. ) ;
#31313=CARTESIAN_POINT ( 'NONE',  ( 25.47133129397800033, 11.11904401118000152, -3.299919292445999908 ) ) ;
#31314=CARTESIAN_POINT ( 'NONE',  ( 12.17504389532245845, 11.54180247361012412, -4.316564347524264988 ) ) ;
#31315=ORIENTED_EDGE ( 'NONE', *, *, #11260, .T. ) ;
#31318=CARTESIAN_POINT ( 'NONE',  ( 23.56677800383048194, -10.34876416779365726, 9.413867714140970122 ) ) ;
#31319=CARTESIAN_POINT ( 'NONE',  ( 23.94495438039136559, 12.80028382019095368, -3.529837795375663667 ) ) ;
#31324=CARTESIAN_POINT ( 'NONE',  ( 23.91319602772269093, 12.85058282302694899, 3.562133635490558614 ) ) ;
#31325=EDGE_CURVE ( 'NONE', #42427, #27101, #41171, .T. ) ;
#31328=ORIENTED_EDGE ( 'NONE', *, *, #49164, .T. ) ;
#31335=CARTESIAN_POINT ( 'NONE',  ( 24.53428991268900106, -12.47024905405999995, -3.026245386525999947 ) ) ;
#31340=CARTESIAN_POINT ( 'NONE',  ( 24.34832088047999932, 8.810502052204325807, -8.810502052203421641 ) ) ;
#31343=CARTESIAN_POINT ( 'NONE',  ( 15.46531638133300035, 9.264179323101998875, 8.208366262023000459 ) ) ;
#31350=CARTESIAN_POINT ( 'NONE',  ( 25.08547621458700050, -11.33429752798000045, 3.320990893601000415 ) ) ;
#31355=CARTESIAN_POINT ( 'NONE',  ( 12.79999999202000005, 11.41069016990000051, -4.623987642516999230 ) ) ;
#31361=CARTESIAN_POINT ( 'NONE',  ( 25.60000000000000142, -11.10814700232000085, -2.976419018679000050 ) ) ;
#31364=CONICAL_SURFACE ( 'NONE', #10152, 12.47499939740000130, 0.7853981102588313279 ) ;
#31365=EDGE_CURVE ( 'NONE', #36843, #1716, #9332, .T. ) ;
#31374=ORIENTED_EDGE ( 'NONE', *, *, #9650, .T. ) ;
#31375=CARTESIAN_POINT ( 'NONE',  ( 11.35564217374000329, -3.878722322503999731, 11.75620894677000017 ) ) ;
#31379=VERTEX_POINT ( 'NONE', #24743 ) ;
#31380=CARTESIAN_POINT ( 'NONE',  ( 16.31137892731300099, -3.415016125706999972, -11.89702177947000017 ) ) ;
#31381=CARTESIAN_POINT ( 'NONE',  ( 11.80432898647400108, 11.49396319796999855, 1.654000935039000142 ) ) ;
#31401=DIRECTION ( 'NONE',  ( 1.000000000000000000, 0.000000000000000000, 0.000000000000000000 ) ) ;
#31402=EDGE_CURVE ( 'NONE', #2551, #1379, #35189, .T. ) ;
#31405=EDGE_CURVE ( 'NONE', #60460, #64287, #68062, .T. ) ;
#31408=DIRECTION ( 'NONE',  ( 1.000000000000000000, 0.000000000000000000, 0.000000000000000000 ) ) ;
#31414=CARTESIAN_POINT ( 'NONE',  ( 11.79999999550100220, -3.351258778187000242, 11.15757272551999968 ) ) ;
#31419=CARTESIAN_POINT ( 'NONE',  ( 23.85184979680500206, -13.16354065916999971, 3.535578269679999774 ) ) ;
#31422=EDGE_LOOP ( 'NONE', ( #19119, #2047, #17020, #20667 ) ) ;
#31431=CARTESIAN_POINT ( 'NONE',  ( 24.74447938189800311, 8.626864566307999027, 8.720113821614001282 ) ) ;
#31444=ORIENTED_EDGE ( 'NONE', *, *, #47101, .F. ) ;
#31445=CARTESIAN_POINT ( 'NONE',  ( 15.89994436294300151, -8.847904542234999781, -8.580301953175000662 ) ) ;
#31449=CARTESIAN_POINT ( 'NONE',  ( 13.59022209853100094, -9.429754002912000388, -8.017367994085999428 ) ) ;
#31451=ORIENTED_EDGE ( 'NONE', *, *, #24621, .T. ) ;
#31456=CARTESIAN_POINT ( 'NONE',  ( 24.71431109946687243, -11.77711172499810210, 3.190793255218363544 ) ) ;
#31466=CARTESIAN_POINT ( 'NONE',  ( 25.29995758267499895, -11.13046986584000031, -3.427500733308000314 ) ) ;
#31486=DIRECTION ( 'NONE',  ( 1.000000000000000000, 0.000000000000000000, 0.000000000000000000 ) ) ;
#31500=FACE_OUTER_BOUND ( 'NONE', #49239, .T. ) ;
#31504=CARTESIAN_POINT ( 'NONE',  ( 24.30000000000000071, 3.224868684338999980, -12.03537377768999939 ) ) ;
#31509=EDGE_CURVE ( 'NONE', #49843, #7211, #6810, .T. ) ;
#31512=AXIS2_PLACEMENT_3D ( 'NONE', #48744, #22505, #58886 ) ;
#31523=CARTESIAN_POINT ( 'NONE',  ( 15.39999999998900293, 9.471998555523999386, 8.194929586088999685 ) ) ;
#31529=CARTESIAN_POINT ( 'NONE',  ( 15.89979320885400327, 3.824231472901999496, 11.71686814605000038 ) ) ;
#31531=CIRCLE ( 'NONE', #19250, 1.000000000000000000 ) ;
#31534=FACE_OUTER_BOUND ( 'NONE', #15403, .T. ) ;
#31538=CARTESIAN_POINT ( 'NONE',  ( 23.52014407070900148, 3.097444545157999940, -13.78484368444999930 ) ) ;
#31544=B_SPLINE_CURVE_WITH_KNOTS ( 'NONE', 3,
 ( #66278, #23982, #45319, #65589, #55110, #18402 ),
 .UNSPECIFIED., .F., .F.,
 ( 4, 1, 1, 4 ),
 ( 0.000000000000000000, 0.2305484780870906414, 0.8346924593416191751, 1.000000000000000000 ),
 .UNSPECIFIED. ) ;
#31550=CARTESIAN_POINT ( 'NONE',  ( 24.95409956869000112, 12.04587931301000125, 2.875990604036999798 ) ) ;
#31553=CARTESIAN_POINT ( 'NONE',  ( 24.14324603874189279, 9.149633372423830124, -9.124494086798831560 ) ) ;
#31555=CARTESIAN_POINT ( 'NONE',  ( 23.83662696556500293, 13.03915312176000008, -3.620547879630999777 ) ) ;
#31562=AXIS2_PLACEMENT_3D ( 'NONE', #22738, #48976, #54565 ) ;
#31568=CARTESIAN_POINT ( 'NONE',  ( 17.79514046837899954, -3.190852705101999920, 11.45040944101999969 ) ) ;
#31572=CARTESIAN_POINT ( 'NONE',  ( 13.06873602477000063, 11.64657800763999873, 1.862567138450999860 ) ) ;
#31574=CARTESIAN_POINT ( 'NONE',  ( 13.46395943152100116, 9.515552291263999152, 7.774702642439999423 ) ) ;
#31576=EDGE_CURVE ( 'NONE', #10089, #55299, #52756, .T. ) ;
#31579=AXIS2_PLACEMENT_3D ( 'NONE', #36645, #57968, #31401 ) ;
#31587=VERTEX_POINT ( 'NONE', #54667 ) ;
#31588=CARTESIAN_POINT ( 'NONE',  ( 12.00339635128600158, 11.70009917314000170, -4.315816162729000816 ) ) ;
#31593=CARTESIAN_POINT ( 'NONE',  ( 25.59994555223600088, 0.6895522877779571846, 11.26073925913301288 ) ) ;
#31594=CARTESIAN_POINT ( 'NONE',  ( 14.40000000633000177, -11.86188960395448788, 3.298666394459744300 ) ) ;
#31608=VECTOR ( 'NONE', #53711, 1000.000000000000114 ) ;
#31617=CARTESIAN_POINT ( 'NONE',  ( 13.99956681845000084, 8.827069132150999309, 7.822720559936999329 ) ) ;
#31625=DIRECTION ( 'NONE',  ( 0.000000000000000000, 0.007439385635797960035, 0.9999723273877941798 ) ) ;
#31626=VERTEX_POINT ( 'NONE', #62491 ) ;
#31636=DIRECTION ( 'NONE',  ( -8.147729033647319588E-21, 0.9999999999999638067, 2.692747184958149612E-07 ) ) ;
#31638=CARTESIAN_POINT ( 'NONE',  ( 12.96385332268500079, 12.32790784140999918, 1.878650414825000059 ) ) ;
#31643=CARTESIAN_POINT ( 'NONE',  ( 13.42968832854115391, 11.50414049279873829, 1.837906235098867302 ) ) ;
#31645=CARTESIAN_POINT ( 'NONE',  ( 16.04720874474600123, 8.391565830097999168, 8.158729932893001191 ) ) ;
#31648=B_SPLINE_CURVE_WITH_KNOTS ( 'NONE', 3,
 ( #10186, #16454, #32549, #53862 ),
 .UNSPECIFIED., .F., .F.,
 ( 4, 4 ),
 ( 0.000000000000000000, 1.000000000000000000 ),
 .UNSPECIFIED. ) ;
#31654=EDGE_CURVE ( 'NONE', #1910, #31995, #59611, .T. ) ;
#31657=CARTESIAN_POINT ( 'NONE',  ( 25.40550542876300000, 11.40415454737000012, -3.013955980041000071 ) ) ;
#31666=FACE_OUTER_BOUND ( 'NONE', #41184, .T. ) ;
#31668=CARTESIAN_POINT ( 'NONE',  ( 24.11212143908326055, 12.52880557495846503, 3.383090514263496384 ) ) ;
#31670=ORIENTED_EDGE ( 'NONE', *, *, #6885, .T. ) ;
#31675=EDGE_CURVE ( 'NONE', #25788, #53930, #56281, .T. ) ;
#31680=CARTESIAN_POINT ( 'NONE',  ( 25.36445294295100084, 2.635917447299000127, 11.32519224169999994 ) ) ;
#31684=CARTESIAN_POINT ( 'NONE',  ( 11.50001496185000249, 12.52500000000000036, 0.000000000000000000 ) ) ;
#31690=CARTESIAN_POINT ( 'NONE',  ( 12.45594992591624361, -11.44468663792873642, 4.547234112432998465 ) ) ;
#31692=CARTESIAN_POINT ( 'NONE',  ( 25.41800046775599853, -11.20523436166000053, 3.227464342313000056 ) ) ;
#31697=CARTESIAN_POINT ( 'NONE',  ( 24.33723497696300342, 8.940350178607999965, 9.046507324144998918 ) ) ;
#31701=AXIS2_PLACEMENT_3D ( 'NONE', #64169, #43205, #6480 ) ;
#31707=CARTESIAN_POINT ( 'NONE',  ( 18.40156003475500057, 3.148349829928000165, 12.06792178657999948 ) ) ;
#31712=CARTESIAN_POINT ( 'NONE',  ( 23.60000000000000142, -0.9826167936418868099, -13.89473236361234676 ) ) ;
#31724=CARTESIAN_POINT ( 'NONE',  ( 15.95563772304700301, -3.878390400849000219, -11.75631652949000205 ) ) ;
#31725=CARTESIAN_POINT ( 'NONE',  ( 11.44794916906000104, 11.60968724315999978, 1.479704744065999833 ) ) ;
#31730=FACE_OUTER_BOUND ( 'NONE', #42816, .T. ) ;
#31741=ADVANCED_FACE ( 'NONE', ( #58283 ), #8356, .F. ) ;
#31742=EDGE_LOOP ( 'NONE', ( #14277, #50678, #33406, #4474, #31935 ) ) ;
#31749=CARTESIAN_POINT ( 'NONE',  ( 17.98179591661069665, 3.334516285427552518, 11.16264808783946805 ) ) ;
#31750=CARTESIAN_POINT ( 'NONE',  ( 23.60205915885299888, -9.361474752760003071, 7.912850866705011477 ) ) ;
#31754=CARTESIAN_POINT ( 'NONE',  ( 18.49993212792200126, 2.908182645667999999, 12.18276646858999968 ) ) ;
#31760=CARTESIAN_POINT ( 'NONE',  ( 23.66004879239100234, 3.393653897912999984, 13.50507458845999942 ) ) ;
#31764=CARTESIAN_POINT ( 'NONE',  ( 17.80000000005199823, 3.345268251980999974, -11.86064071431999878 ) ) ;
#31785=CARTESIAN_POINT ( 'NONE',  ( 25.46373329105799854, 11.23406619596999967, -3.161081784610999978 ) ) ;
#31786=CARTESIAN_POINT ( 'NONE',  ( 24.36504260745899941, 8.917410149216999926, -9.042893057505001053 ) ) ;
#31794=DIRECTION ( 'NONE',  ( 1.000000000000000000, 0.000000000000000000, 0.000000000000000000 ) ) ;
#31804=EDGE_LOOP ( 'NONE', ( #1657, #58980, #64089, #54843 ) ) ;
#31810=CARTESIAN_POINT ( 'NONE',  ( 24.42335568937500057, 3.752333166337999959, 12.53709289204000044 ) ) ;
#31812=CARTESIAN_POINT ( 'NONE',  ( 23.73953410686057452, 13.33634109980698845, 3.648241387586184103 ) ) ;
#31818=CARTESIAN_POINT ( 'NONE',  ( 16.39999999379500295, -3.351248059343999941, -11.15756683833000018 ) ) ;
#31821=B_SPLINE_CURVE_WITH_KNOTS ( 'NONE', 3,
 ( #19291, #35722, #62287, #40965 ),
 .UNSPECIFIED., .F., .F.,
 ( 4, 4 ),
 ( 0.000000000000000000, 1.000000000000000000 ),
 .UNSPECIFIED. ) ;
#31825=ADVANCED_FACE ( 'NONE', ( #55810 ), #18406, .T. ) ;
#31835=FACE_OUTER_BOUND ( 'NONE', #31422, .T. ) ;
#31841=ORIENTED_EDGE ( 'NONE', *, *, #66706, .F. ) ;
#31849=DIRECTION ( 'NONE',  ( -1.000000000000000000, 0.000000000000000000, 0.000000000000000000 ) ) ;
#31853=EDGE_LOOP ( 'NONE', ( #50125, #21238, #47960, #9326 ) ) ;
#31854=CARTESIAN_POINT ( 'NONE',  ( 24.66122485234200212, 8.759220508654999904, 9.243943008462998989 ) ) ;
#31856=DIRECTION ( 'NONE',  ( 0.000000000000000000, 0.000000000000000000, 1.000000000000000000 ) ) ;
#31871=CARTESIAN_POINT ( 'NONE',  ( 17.68432968562860808, -11.86180690035067187, 3.298554102281288980 ) ) ;
#31874=EDGE_LOOP ( 'NONE', ( #62058, #37226, #65347, #9419 ) ) ;
#31878=AXIS2_PLACEMENT_3D ( 'NONE', #22131, #53942, #11988 ) ;
#31881=EDGE_CURVE ( 'NONE', #252, #19259, #39259, .T. ) ;
#31883=CARTESIAN_POINT ( 'NONE',  ( 23.61761589919547433, -3.310052744450573847, -13.56819651954416628 ) ) ;
#31887=VERTEX_POINT ( 'NONE', #54764 ) ;
#31889=EDGE_CURVE ( 'NONE', #44668, #9687, #51780, .T. ) ;
#31893=CARTESIAN_POINT ( 'NONE',  ( 23.56665676678700194, 2.935519496638999914, -13.67844162499000049 ) ) ;
#31897=DIRECTION ( 'NONE',  ( 0.7071060218674898312, 0.7071075405047898554, -8.464222916703876687E-10 ) ) ;
#31900=CARTESIAN_POINT ( 'NONE',  ( 24.30000000000000071, 8.810505093353000916, 8.810505093353000916 ) ) ;
#31903=FACE_OUTER_BOUND ( 'NONE', #49192, .T. ) ;
#31907=ORIENTED_EDGE ( 'NONE', *, *, #8608, .F. ) ;
#31913=CARTESIAN_POINT ( 'NONE',  ( 23.89491988614704709, 3.335475672761040844, -12.94525074951522647 ) ) ;
#31919=CARTESIAN_POINT ( 'NONE',  ( 12.96937411412500119, 11.64648275985999959, 1.863025408066000033 ) ) ;
#31932=EDGE_CURVE ( 'NONE', #53410, #10995, #7163, .T. ) ;
#31935=ORIENTED_EDGE ( 'NONE', *, *, #11821, .F. ) ;
#31936=CARTESIAN_POINT ( 'NONE',  ( 12.46470380486700158, 12.15408297959000095, -3.184072412108000183 ) ) ;
#31937=CARTESIAN_POINT ( 'NONE',  ( 18.35475438412399996, 11.75582082520000071, -3.881266971570000113 ) ) ;
#31941=CARTESIAN_POINT ( 'NONE',  ( 17.79290994143500271, -3.413161104324000217, 11.89755508104000015 ) ) ;
#31946=DIRECTION ( 'NONE',  ( -0.000000000000000000, 0.7071067811865475727, 0.7071067811865475727 ) ) ;
#31947=LINE ( 'NONE', #65111, #21827 ) ;
#31969=CARTESIAN_POINT ( 'NONE',  ( 17.80000000001300009, 3.351264566333000072, 11.15757590352999884 ) ) ;
#31973=B_SPLINE_CURVE_WITH_KNOTS ( 'NONE', 3,
 ( #44686, #29291, #61435, #34538 ),
 .UNSPECIFIED., .F., .F.,
 ( 4, 4 ),
 ( 0.000000000000000000, 1.000000000000000000 ),
 .UNSPECIFIED. ) ;
#31980=DIRECTION ( 'NONE',  ( -3.667764737047155134E-10, -0.9466472399347399813, 0.3222716294121134584 ) ) ;
#31983=EDGE_LOOP ( 'NONE', ( #38206, #52338, #29972, #59312, #36432, #42166, #63428, #24659, #48050, #55558, #55254 ) ) ;
#31984=CARTESIAN_POINT ( 'NONE',  ( 25.48370107584300470, -11.09850929439999945, -3.318324248302000345 ) ) ;
#31987=ADVANCED_FACE ( 'NONE', ( #22170 ), #11110, .F. ) ;
#31988=DIRECTION ( 'NONE',  ( -1.000000000000000000, 0.000000000000000000, 0.000000000000000000 ) ) ;
#31995=VERTEX_POINT ( 'NONE', #17276 ) ;
#31996=CARTESIAN_POINT ( 'NONE',  ( 13.70006033574439108, 11.41449502534878491, 2.331043471729913108 ) ) ;
#31998=CARTESIAN_POINT ( 'NONE',  ( 15.95481756226799952, 8.457314961363000094, 8.223455601337001042 ) ) ;
#31999=VERTEX_POINT ( 'NONE', #38959 ) ;
#32002=B_SPLINE_CURVE_WITH_KNOTS ( 'NONE', 3,
 ( #49335, #7381, #38149, #22765, #17171, #22067, #43417, #11931 ),
 .UNSPECIFIED., .F., .F.,
 ( 4, 2, 2, 4 ),
 ( 0.000000000000000000, 0.1253882094777247769, 0.2507764189554495537, 0.5015528379108959989 ),
 .UNSPECIFIED. ) ;
#32009=CARTESIAN_POINT ( 'NONE',  ( 25.59997239626699894, 8.218962773316999204, -8.043525096612999192 ) ) ;
#32015=CARTESIAN_POINT ( 'NONE',  ( 23.56860850335619162, -10.31977020530763944, 9.444771763729463032 ) ) ;
#32018=AXIS2_PLACEMENT_3D ( 'NONE', #22009, #16761, #16079 ) ;
#32022=CARTESIAN_POINT ( 'NONE',  ( 23.79457312070770669, 13.02989123031758645, 3.714539862624964162 ) ) ;
#32025=CARTESIAN_POINT ( 'NONE',  ( 13.17784398560648995, -12.38705052588331412, -1.853828488290533816 ) ) ;
#32029=CARTESIAN_POINT ( 'NONE',  ( 18.14404865540673129, -11.59829761222289690, 4.728902891304503697 ) ) ;
#32032=CARTESIAN_POINT ( 'NONE',  ( 24.62769666370824950, -12.35739842162390367, -2.995926059522363794 ) ) ;
#32038=CARTESIAN_POINT ( 'NONE',  ( 16.09992084546400193, 8.991497430826001391, 8.719551690569000257 ) ) ;
#32040=CARTESIAN_POINT ( 'NONE',  ( 13.99999999347100044, 9.187456302440001110, 8.213201953411001455 ) ) ;
#32073=CARTESIAN_POINT ( 'NONE',  ( 11.64440219406983523, -12.39501813438487154, -1.800675169423894273 ) ) ;
#32076=CARTESIAN_POINT ( 'NONE',  ( 11.60581233665799950, 11.65209074823999913, 1.826497490784000144 ) ) ;
#32077=VERTEX_POINT ( 'NONE', #45916 ) ;
#32092=CARTESIAN_POINT ( 'NONE',  ( 15.37415039705200215, -9.132871822554998076, -8.217191491449000296 ) ) ;
#32097=CARTESIAN_POINT ( 'NONE',  ( 23.59999468372399889, -2.915558691838999739, 13.58549495651999983 ) ) ;
#32098=CARTESIAN_POINT ( 'NONE',  ( 23.58110596194431352, -13.37140776802827880, -4.095521627281163646 ) ) ;
#32103=ORIENTED_EDGE ( 'NONE', *, *, #2220, .F. ) ;
#32108=CARTESIAN_POINT ( 'NONE',  ( 25.60000000000000142, -10.55163788719000095, -3.754896668835000284 ) ) ;
#32111=CARTESIAN_POINT ( 'NONE',  ( 12.79999999838119606, -11.94789761932849181, 3.252399792653988708 ) ) ;
#32114=CARTESIAN_POINT ( 'NONE',  ( 24.25969244708700145, -12.09494195645999959, 3.326713950767999695 ) ) ;
#32123=CIRCLE ( 'NONE', #34378, 12.20000000000000284 ) ;
#32133=CARTESIAN_POINT ( 'NONE',  ( 17.60000000000000142, 48.67241131317999958, -16.56944037379999912 ) ) ;
#32135=ADVANCED_FACE ( 'NONE', ( #36111 ), #33974, .T. ) ;
#32141=CARTESIAN_POINT ( 'NONE',  ( 25.59997327719300131, 11.07537871057999901, 3.096068926251000164 ) ) ;
#32145=CARTESIAN_POINT ( 'NONE',  ( 25.46373329105799854, 11.23406619596999967, -3.161081784610999978 ) ) ;
#32158=CARTESIAN_POINT ( 'NONE',  ( 24.32784272479599963, 3.577368779004999944, 12.48430931087000140 ) ) ;
#32160=CARTESIAN_POINT ( 'NONE',  ( 24.53429014209899961, 12.47024915613999951, 3.026245713505000268 ) ) ;
#32161=B_SPLINE_CURVE_WITH_KNOTS ( 'NONE', 3,
 ( #41508, #10033, #30013, #40474 ),
 .UNSPECIFIED., .F., .F.,
 ( 4, 4 ),
 ( 0.000000000000000000, 1.000000000000000000 ),
 .UNSPECIFIED. ) ;
#32163=EDGE_CURVE ( 'NONE', #60460, #62750, #27625, .T. ) ;
#32164=VECTOR ( 'NONE', #61627, 1000.000000000000114 ) ;
#32171=CARTESIAN_POINT ( 'NONE',  ( 25.08240820202400201, -2.794122706165999670, -11.47835358574999987 ) ) ;
#32192=CARTESIAN_POINT ( 'NONE',  ( 24.65657813088902017, -3.152276120826353445, 11.84445435621313969 ) ) ;
#32206=PLANE ( 'NONE',  #41552 ) ;
#32218=CARTESIAN_POINT ( 'NONE',  ( 25.46373154986600085, 8.354608910739999672, 8.148450287869000164 ) ) ;
#32222=CARTESIAN_POINT ( 'NONE',  ( 12.79999999914999975, 12.11987927271999865, -3.159802730921999814 ) ) ;
#32224=FACE_OUTER_BOUND ( 'NONE', #51978, .T. ) ;
#32227=ADVANCED_FACE ( 'NONE', ( #53223 ), #6053, .F. ) ;
#32229=CARTESIAN_POINT ( 'NONE',  ( 15.90003771078200145, 3.695138809391000034, 11.25918926437999978 ) ) ;
#32230=CARTESIAN_POINT ( 'NONE',  ( 12.57461732485516670, -12.11259905827365913, 3.187575261699951312 ) ) ;
#32234=CARTESIAN_POINT ( 'NONE',  ( 24.32784070168699841, 3.577437594875000126, -12.48429269957000010 ) ) ;
#32236=B_SPLINE_CURVE_WITH_KNOTS ( 'NONE', 3,
 ( #46605, #57418, #4621, #15124, #40656, #10219 ),
 .UNSPECIFIED., .F., .F.,
 ( 4, 2, 4 ),
 ( 0.000000000000000000, 0.5000000000000000000, 1.000000000000000000 ),
 .UNSPECIFIED. ) ;
#32240=CARTESIAN_POINT ( 'NONE',  ( 18.06247470497385876, -3.164801830445712394, 11.41978211466257243 ) ) ;
#32243=ADVANCED_FACE ( 'NONE', ( #83 ), #26665, .F. ) ;
#32250=CARTESIAN_POINT ( 'NONE',  ( 21.10000109091659937, -1.355183834107999921E-13, -12.52499975980128966 ) ) ;
#32251=CARTESIAN_POINT ( 'NONE',  ( 24.61098151538899970, 12.21941909980999874, 3.050810341055000041 ) ) ;
#32263=CARTESIAN_POINT ( 'NONE',  ( 18.53711938375299795, -2.638714702496000264, 11.30796021345999947 ) ) ;
#32270=CARTESIAN_POINT ( 'NONE',  ( 13.55296092448800138, 11.54193659611999934, 2.433871908353000268 ) ) ;
#32276=CARTESIAN_POINT ( 'NONE',  ( 11.64459552687324262, -11.53034370678229514, -1.666360532292795904 ) ) ;
#32278=CARTESIAN_POINT ( 'NONE',  ( 24.98034467287493854, -8.548010802276017728, 8.348296163080446419 ) ) ;
#32281=EDGE_CURVE ( 'NONE', #44907, #41132, #23414, .T. ) ;
#32286=ORIENTED_EDGE ( 'NONE', *, *, #5613, .T. ) ;
#32287=CARTESIAN_POINT ( 'NONE',  ( 12.34907277967800177, 11.89802509695999966, -3.395950604129000183 ) ) ;
#32291=CARTESIAN_POINT ( 'NONE',  ( 12.18965064077726623, -11.77436608085473857, 3.633175706309820008 ) ) ;
#32292=CARTESIAN_POINT ( 'NONE',  ( 18.50035835255887307, 11.89543982599948535, -3.922887695644379669 ) ) ;
#32297=CARTESIAN_POINT ( 'NONE',  ( 11.80000000000000071, -14.76315775485999993, 50.50083396221000243 ) ) ;
#32300=PLANE ( 'NONE',  #10967 ) ;
#32306=VERTEX_POINT ( 'NONE', #36455 ) ;
#32312=DIRECTION ( 'NONE',  ( -1.000000000000000000, 0.000000000000000000, 0.000000000000000000 ) ) ;
#32327=CARTESIAN_POINT ( 'NONE',  ( 13.49994651945300284, -12.07042783918999795, -2.492331243371999960 ) ) ;
#32332=CARTESIAN_POINT ( 'NONE',  ( 14.40000001005266661, -12.11987670936007078, 3.159780617438794792 ) ) ;
#32333=CARTESIAN_POINT ( 'NONE',  ( 11.50029455687000102, -11.65000000000000036, 0.000000000000000000 ) ) ;
#32336=B_SPLINE_CURVE_WITH_KNOTS ( 'NONE', 3,
 ( #32333, #5404, #10992, #15557, #26047, #68679, #53643, #20797, #42811, #26741 ),
 .UNSPECIFIED., .F., .F.,
 ( 4, 2, 2, 2, 4 ),
 ( 0.000000000000000000, 0.2499999999999999445, 0.4999999999999998335, 0.7499999999999997780, 1.000000000000000000 ),
 .UNSPECIFIED. ) ;
#32342=CARTESIAN_POINT ( 'NONE',  ( 15.49162860438300271, 8.811474098792000831, 7.563394002770000846 ) ) ;
#32343=ORIENTED_EDGE ( 'NONE', *, *, #48470, .T. ) ;
#32355=CARTESIAN_POINT ( 'NONE',  ( 24.44496351116800170, 3.224881296174999967, 12.03535797436000010 ) ) ;
#32359=CARTESIAN_POINT ( 'NONE',  ( 16.00261247405899923, 3.453035413593999792, 11.78892418867000025 ) ) ;
#32362=ADVANCED_FACE ( 'NONE', ( #30788 ), #66952, .F. ) ;
#32364=EDGE_CURVE ( 'NONE', #33733, #47838, #46296, .T. ) ;
#32366=CARTESIAN_POINT ( 'NONE',  ( 13.35060253487350401, -12.37707099949019174, -1.919647290784824545 ) ) ;
#32370=CARTESIAN_POINT ( 'NONE',  ( 25.30000327618300204, -2.078227429405999693, 11.31065739696999906 ) ) ;
#32373=CARTESIAN_POINT ( 'NONE',  ( 25.27036090913500033, 2.549220333827999951, 11.36408438533999998 ) ) ;
#32375=CARTESIAN_POINT ( 'NONE',  ( 13.70003001321900271, -10.86123379505843189, -6.319444516909303644 ) ) ;
#32385=CARTESIAN_POINT ( 'NONE',  ( 12.17504389532412645, -11.54180247360918621, 4.316564347526565371 ) ) ;
#32387=CARTESIAN_POINT ( 'NONE',  ( 24.70770306079000278, -8.718110200638999885, -9.202866107698000064 ) ) ;
#32391=CARTESIAN_POINT ( 'NONE',  ( 23.99069334398700093, 9.436054250658999720, 9.573720703848998426 ) ) ;
#32392=ORIENTED_EDGE ( 'NONE', *, *, #66517, .F. ) ;
#32396=CARTESIAN_POINT ( 'NONE',  ( 18.30000000000000071, 48.67241131317999958, -16.56944037379999912 ) ) ;
#32407=CARTESIAN_POINT ( 'NONE',  ( 13.99999997324030510, -8.827177816329490057, -7.803278505680545152 ) ) ;
#32408=ORIENTED_EDGE ( 'NONE', *, *, #12818, .F. ) ;
#32414=DIRECTION ( 'NONE',  ( 0.000000000000000000, 0.2588190451024932059, -0.9659258262890756397 ) ) ;
#32416=CARTESIAN_POINT ( 'NONE',  ( 11.72772918458500158, 11.64671933177000085, 1.861692232596000141 ) ) ;
#32419=CARTESIAN_POINT ( 'NONE',  ( 24.44496412535000118, -8.810486166165000910, -8.810507954003998776 ) ) ;
#32434=B_SPLINE_SURFACE_WITH_KNOTS ( 'NONE', 3, 3, ( 
 ( #32760, #6170, #17009, #54073 ),
 ( #43598, #65249, #38338, #49177 ),
 ( #64895, #27511, #12124, #6868 ),
 ( #7561, #59667, #50220, #28558 ),
 ( #2322, #43945, #65597, #17365 ),
 ( #60014, #33453, #54768, #39044 ),
 ( #28205, #49519, #22946, #12467 ),
 ( #55118, #25358, #3676, #7915 ),
 ( #56491, #19081, #25018, #14537 ) ),
 .UNSPECIFIED., .F., .F., .F.,
 ( 4, 1, 1, 1, 1, 1, 4 ),
 ( 4, 4 ),
 ( 0.02209653170519000273, 0.1666666666667000196, 0.3333333333333000081, 0.5000000000000000000, 0.6666666666667000474, 0.8333333333333000637, 0.9492823795161999811 ),
 ( -0.1916656884162999952, 1.191851428473000185 ),
 .UNSPECIFIED. ) ;
#32441=CARTESIAN_POINT ( 'NONE',  ( 18.43044927002210542, 3.211191212926777450, 12.10643352320258970 ) ) ;
#32448=DIRECTION ( 'NONE',  ( -0.9999999999751629787, -5.691912098208790371E-06, 4.156456142935844641E-06 ) ) ;
#32450=CARTESIAN_POINT ( 'NONE',  ( 15.40000000009400161, 8.833277835210999740, 7.896561221812000930 ) ) ;
#32452=DIRECTION ( 'NONE',  ( -1.000000000000000000, 0.000000000000000000, 0.000000000000000000 ) ) ;
#32453=CARTESIAN_POINT ( 'NONE',  ( 23.66481111098300261, -13.24745896931000111, 3.909204073637000398 ) ) ;
#32459=ADVANCED_FACE ( 'NONE', ( #58908 ), #23401, .F. ) ;
#32461=CARTESIAN_POINT ( 'NONE',  ( 17.79222771582700346, 3.377813322129000095, -11.11021622646999951 ) ) ;
#32463=EDGE_CURVE ( 'NONE', #14810, #22779, #16140, .T. ) ;
#32466=CARTESIAN_POINT ( 'NONE',  ( 24.23278707828200140, -9.064214965309000505, -9.161880861702000445 ) ) ;
#32468=CIRCLE ( 'NONE', #52568, 13.92493900951000363 ) ;
#32469=CARTESIAN_POINT ( 'NONE',  ( 11.84006751466700180, -3.254324250158000087, 11.33670592834999979 ) ) ;
#32477=ORIENTED_EDGE ( 'NONE', *, *, #31654, .T. ) ;
#32491=CARTESIAN_POINT ( 'NONE',  ( 24.57937622054542715, 12.41575245047435416, 3.011584258239457412 ) ) ;
#32492=CARTESIAN_POINT ( 'NONE',  ( 12.79484580939900162, -11.81466332729999991, 3.323431527667999763 ) ) ;
#32508=DIRECTION ( 'NONE',  ( 0.000000000000000000, 0.000000000000000000, -1.000000000000000000 ) ) ;
#32509=EDGE_LOOP ( 'NONE', ( #52639, #39659, #57166, #12315, #41772 ) ) ;
#32510=CARTESIAN_POINT ( 'NONE',  ( 23.60205915885299888, 11.88166580726000454, 3.967996863081999948 ) ) ;
#32541=CARTESIAN_POINT ( 'NONE',  ( 13.99999999379500082, 8.815218614167999789, 7.616697584347000394 ) ) ;
#32542=EDGE_CURVE ( 'NONE', #43802, #32077, #57406, .T. ) ;
#32544=B_SPLINE_CURVE_WITH_KNOTS ( 'NONE', 3,
 ( #59201, #57565, #62804, #35903 ),
 .UNSPECIFIED., .F., .F.,
 ( 4, 4 ),
 ( 0.000000000000000000, 1.000000000000000000 ),
 .UNSPECIFIED. ) ;
#32549=CARTESIAN_POINT ( 'NONE',  ( 24.63329111161720419, -10.83443034947476136, -3.855530962446055643 ) ) ;
#32551=CARTESIAN_POINT ( 'NONE',  ( 17.89019624313940326, -3.590943193543576495, -11.99920113072214534 ) ) ;
#32562=CARTESIAN_POINT ( 'NONE',  ( 23.84019040512217913, -9.641975614964733765, -9.401257029815200283 ) ) ;
#32569=ORIENTED_EDGE ( 'NONE', *, *, #11820, .T. ) ;
#32571=CARTESIAN_POINT ( 'NONE',  ( 12.22252627677945291, 11.15475449699942523, -3.361665977246885095 ) ) ;
#32574=CARTESIAN_POINT ( 'NONE',  ( 18.33131097850136371, -3.122881743056324488, 11.22368843778173364 ) ) ;
#32583=CARTESIAN_POINT ( 'NONE',  ( 11.50001544675000176, -11.50879548944698527, 5.112724829059166254 ) ) ;
#32584=CARTESIAN_POINT ( 'NONE',  ( 24.23036450625643923, 9.028689804025722410, -9.024522586024058768 ) ) ;
#32596=CARTESIAN_POINT ( 'NONE',  ( 18.40429364930200151, -2.938801558760000265, 11.32979830910000096 ) ) ;
#32600=DIRECTION ( 'NONE',  ( 1.000000000000000000, 0.000000000000000000, 0.000000000000000000 ) ) ;
#32607=ORIENTED_EDGE ( 'NONE', *, *, #58862, .F. ) ;
#32621=CARTESIAN_POINT ( 'NONE',  ( 18.34010937327100166, 12.07342271643000053, -3.473919584753000223 ) ) ;
#32625=EDGE_CURVE ( 'NONE', #51578, #30294, #35908, .T. ) ;
#32626=CARTESIAN_POINT ( 'NONE',  ( 25.59994555223600088, -0.6895522877783650806, 11.26073925913298801 ) ) ;
#32627=CARTESIAN_POINT ( 'NONE',  ( 18.38411421680242341, 11.69918008064787074, -4.474081357806680259 ) ) ;
#32628=CIRCLE ( 'NONE', #25936, 5.000000000000000000 ) ;
#32633=DIRECTION ( 'NONE',  ( 0.000000000000000000, -0.3222656952305000266, -0.9466492601157001641 ) ) ;
#32635=DIRECTION ( 'NONE',  ( 0.000000000000000000, 0.000000000000000000, 1.000000000000000000 ) ) ;
#32651=AXIS2_PLACEMENT_3D ( 'NONE', #28164, #1248, #28873 ) ;
#32654=FACE_OUTER_BOUND ( 'NONE', #52030, .T. ) ;
#32655=ORIENTED_EDGE ( 'NONE', *, *, #39900, .F. ) ;
#32657=ADVANCED_FACE ( 'NONE', ( #13323 ), #11641, .T. ) ;
#32664=CARTESIAN_POINT ( 'NONE',  ( 25.19548857725200008, -11.71503324258999967, -2.904521392034999927 ) ) ;
#32668=FACE_OUTER_BOUND ( 'NONE', #34130, .T. ) ;
#32669=DIRECTION ( 'NONE',  ( 0.000000000000000000, 0.000000000000000000, -1.000000000000000000 ) ) ;
#32679=ORIENTED_EDGE ( 'NONE', *, *, #15057, .F. ) ;
#32680=CARTESIAN_POINT ( 'NONE',  ( 23.61437304120291358, -13.25092132859138339, 4.104831388036656037 ) ) ;
#32686=CARTESIAN_POINT ( 'NONE',  ( 24.67558927346200193, 12.15674323158999925, -3.025799392731000292 ) ) ;
#32687=ORIENTED_EDGE ( 'NONE', *, *, #66377, .F. ) ;
#32691=EDGE_LOOP ( 'NONE', ( #52784, #39737, #22572, #6159 ) ) ;
#32696=CARTESIAN_POINT ( 'NONE',  ( 16.44809435262699893, 3.299700711820999555, 11.83394467541999973 ) ) ;
#32701=ORIENTED_EDGE ( 'NONE', *, *, #38169, .T. ) ;
#32704=CARTESIAN_POINT ( 'NONE',  ( 18.04463993611876660, -11.57310880395660746, 4.789662202686257864 ) ) ;
#32714=EDGE_LOOP ( 'NONE', ( #9920, #8524, #21854, #23638 ) ) ;
#32720=DIRECTION ( 'NONE',  ( 0.2392860387991979920, 0.9709491189736919603, 1.627359028554984806E-14 ) ) ;
#32729=CARTESIAN_POINT ( 'NONE',  ( 18.47825479160223239, -3.085175724103950579, 12.13916519603823119 ) ) ;
#32738=ORIENTED_EDGE ( 'NONE', *, *, #11302, .F. ) ;
#32740=EDGE_CURVE ( 'NONE', #18501, #54794, #122, .T. ) ;
#32748=ADVANCED_FACE ( 'NONE', ( #28708 ), #29012, .F. ) ;
#32750=AXIS2_PLACEMENT_3D ( 'NONE', #48933, #24003, #56504 ) ;
#32756=B_SPLINE_CURVE_WITH_KNOTS ( 'NONE', 3,
 ( #13180, #17372, #34509, #38700, #2330, #7923, #56154, #55820 ),
 .UNSPECIFIED., .F., .F.,
 ( 4, 2, 2, 4 ),
 ( 0.000000000000000000, 0.2500000000000002776, 0.5000000000000005551, 1.000000000000000000 ),
 .UNSPECIFIED. ) ;
#32759=CARTESIAN_POINT ( 'NONE',  ( 25.10989042599555177, 2.855873493246296579, -11.47557929325230930 ) ) ;
#32760=CARTESIAN_POINT ( 'NONE',  ( 16.42348875342600323, 3.378076265369000186, 11.11016813414000204 ) ) ;
#32762=ORIENTED_EDGE ( 'NONE', *, *, #54091, .F. ) ;
#32767=CARTESIAN_POINT ( 'NONE',  ( 24.60000000000000142, 0.000000000000000000, 0.000000000000000000 ) ) ;
#32788=ORIENTED_EDGE ( 'NONE', *, *, #52896, .T. ) ;
#32789=CARTESIAN_POINT ( 'NONE',  ( 11.61689913334100055, -12.44392429648999965, -1.730928413625999918 ) ) ;
#32794=CARTESIAN_POINT ( 'NONE',  ( 24.14469595025496318, -12.92580541902093216, -3.214657694676578803 ) ) ;
#32795=CARTESIAN_POINT ( 'NONE',  ( 24.45266148221099911, 12.43950837972999857, 3.093335738978999938 ) ) ;
#32796=CARTESIAN_POINT ( 'NONE',  ( 16.86666666323366925, 3.595157417865990634, 11.99793599502776154 ) ) ;
#32803=CARTESIAN_POINT ( 'NONE',  ( 18.16715644869600155, 3.024463723863999753, -11.49930835314999911 ) ) ;
#32807=CARTESIAN_POINT ( 'NONE',  ( 23.99190355937800234, -9.434386195893999627, -9.573065527095000249 ) ) ;
#32809=CARTESIAN_POINT ( 'NONE',  ( 11.72781722417300188, -3.253150999210000283, 11.33706231867000014 ) ) ;
#32814=CARTESIAN_POINT ( 'NONE',  ( 24.35146665670700017, 8.929414329884000523, -9.054894786836999998 ) ) ;
#32817=FACE_OUTER_BOUND ( 'NONE', #63117, .T. ) ;
#32831=CARTESIAN_POINT ( 'NONE',  ( 24.25374608244500152, 12.19813778996000053, -3.308085337617999944 ) ) ;
#32836=CARTESIAN_POINT ( 'NONE',  ( 12.68129448069100107, -12.04903608036000051, 3.200077553391999619 ) ) ;
#32840=CARTESIAN_POINT ( 'NONE',  ( 23.51521485843800008, 2.989497430995999849, 13.81461181470000099 ) ) ;
#32847=B_SPLINE_SURFACE_WITH_KNOTS ( 'NONE', 3, 3, ( 
 ( #52615, #25703, #52968, #63787 ),
 ( #4021, #31645, #31998, #41445 ),
 ( #68339, #53311, #62754, #41102 ),
 ( #20804, #4710, #57865, #62417 ),
 ( #14538, #35855, #26054, #14873 ),
 ( #36195, #9616, #20457, #41785 ),
 ( #16923, #22865, #27091, #38254 ),
 ( #32342, #53651, #65512, #16589 ),
 ( #64466, #53991, #5747, #48406 ),
 ( #512, #49436, #22516, #27431 ) ),
 .UNSPECIFIED., .F., .F., .F.,
 ( 4, 1, 1, 1, 1, 1, 1, 4 ),
 ( 4, 4 ),
 ( 0.04183311431307000505, 0.1428571428570999946, 0.2857142857143000203, 0.4285714285713999594, 0.5714285714286000406, 0.7142857142856999797, 0.8571428571429000609, 0.9292981235707000742 ),
 ( -0.1917799910644999994, 1.191756862851000021 ),
 .UNSPECIFIED. ) ;
#32863=CARTESIAN_POINT ( 'NONE',  ( 12.79999998712400178, 11.53033693765999779, -4.891431908114999949 ) ) ;
#32871=CARTESIAN_POINT ( 'NONE',  ( 23.89320776801300283, -11.54071136931999852, 2.936967729253997295 ) ) ;
#32873=CARTESIAN_POINT ( 'NONE',  ( 11.55259020248000112, 12.34178403982000205, 1.785089783152000065 ) ) ;
#32878=ADVANCED_FACE ( 'NONE', ( #16270 ), #26182, .F. ) ;
#32899=CARTESIAN_POINT ( 'NONE',  ( 25.21376063843823445, 11.24064175245759678, 3.343247825242493754 ) ) ;
#32901=ORIENTED_EDGE ( 'NONE', *, *, #18399, .T. ) ;
#32902=CIRCLE ( 'NONE', #8352, 11.26964301940000013 ) ;
#32904=CARTESIAN_POINT ( 'NONE',  ( 23.96071917867679346, -9.430644054855381597, -9.306896137895602550 ) ) ;
#32909=CARTESIAN_POINT ( 'NONE',  ( 23.86816321758700354, 3.656111997911000167, -13.23100399352999901 ) ) ;
#32913=CARTESIAN_POINT ( 'NONE',  ( 12.17041389168972643, 11.12724491010661332, -3.450620876805502668 ) ) ;
#32914=CARTESIAN_POINT ( 'NONE',  ( 18.29999330150736014, -11.02846243710336616, 3.754394858745019103 ) ) ;
#32915=CARTESIAN_POINT ( 'NONE',  ( 18.49586274151939591, -2.771911498359158621, -11.31551287271714656 ) ) ;
#32926=CARTESIAN_POINT ( 'NONE',  ( 24.36958145701300182, 12.05823614978999991, 3.270605474396000023 ) ) ;
#32940=CARTESIAN_POINT ( 'NONE',  ( 23.76527109147985328, 3.280149080713666176, -13.20035194756249020 ) ) ;
#32941=CARTESIAN_POINT ( 'NONE',  ( 17.76930066282600151, -3.251864118589000263, 11.33740735155000046 ) ) ;
#32942=CARTESIAN_POINT ( 'NONE',  ( 24.34833292274466743, -12.15210578639278793, 3.256146931800457001 ) ) ;
#32947=VERTEX_POINT ( 'NONE', #41044 ) ;
#32950=CARTESIAN_POINT ( 'NONE',  ( 15.96663488596630742, 8.445622082970144717, 8.216900471613380219 ) ) ;
#32972=CARTESIAN_POINT ( 'NONE',  ( 23.60000000000000142, -2.258942858049999725, 12.29419282279000036 ) ) ;
#32975=CARTESIAN_POINT ( 'NONE',  ( 29.60000000000000142, 2.052090884164000168E-07, -7.720759220056000238 ) ) ;
#32989=CARTESIAN_POINT ( 'NONE',  ( 24.37816251333097028, 12.29708173412044481, 3.190021852498594601 ) ) ;
#32990=DIRECTION ( 'NONE',  ( 0.000000000000000000, 0.9466492601157001641, -0.3222656952305000266 ) ) ;
#32991=CIRCLE ( 'NONE', #46372, 11.50000000000000178 ) ;
#33000=CARTESIAN_POINT ( 'NONE',  ( 25.49994615399576148, 8.603880941064447896, 7.325437794649206857 ) ) ;
#33002=CARTESIAN_POINT ( 'NONE',  ( 23.59999192078999997, 10.30759737717999869, 9.317725909430999209 ) ) ;
#33004=CARTESIAN_POINT ( 'NONE',  ( 25.48370471471800158, -8.423010586709999359, 7.952419693825000024 ) ) ;
#33007=CARTESIAN_POINT ( 'NONE',  ( 25.40244255529000128, -11.40891536676000051, -3.011592991499000060 ) ) ;
#33010=CARTESIAN_POINT ( 'NONE',  ( 25.60000000000000142, -2.023988666086999899, -11.01546541709000060 ) ) ;
#33012=CARTESIAN_POINT ( 'NONE',  ( 24.30000000000000071, -3.224868684338999980, 12.03537377768999939 ) ) ;
#33015=CARTESIAN_POINT ( 'NONE',  ( 23.60205915885299888, 9.223492163368996799, 8.025915643339997629 ) ) ;
#33018=ADVANCED_FACE ( 'NONE', ( #16185 ), #3324, .F. ) ;
#33019=CARTESIAN_POINT ( 'NONE',  ( 13.35262485425079326, 11.51206127779273203, 1.787622147829904362 ) ) ;
#33021=AXIS2_PLACEMENT_3D ( 'NONE', #45040, #28620, #49933 ) ;
#33023=ORIENTED_EDGE ( 'NONE', *, *, #2827, .T. ) ;
#33029=ORIENTED_EDGE ( 'NONE', *, *, #45255, .T. ) ;
#33033=ORIENTED_EDGE ( 'NONE', *, *, #62093, .F. ) ;
#33054=CARTESIAN_POINT ( 'NONE',  ( 24.67558972156300001, -3.457952286748999793, 12.04094770214000043 ) ) ;
#33067=CARTESIAN_POINT ( 'NONE',  ( 23.50387503050299998, -0.02050624307146717284, 13.79998476426676923 ) ) ;
#33071=CARTESIAN_POINT ( 'NONE',  ( 24.43232361759900328, -8.806075257782000065, -8.751960807121999864 ) ) ;
#33073=CARTESIAN_POINT ( 'NONE',  ( 17.77436674347223189, 11.41733448236052517, -4.609296047865278467 ) ) ;
#33082=CARTESIAN_POINT ( 'NONE',  ( 17.60000000024299993, 11.86189249994999884, -3.298671769835999967 ) ) ;
#33083=CARTESIAN_POINT ( 'NONE',  ( 24.35365242081699932, 8.885108761826009172, -7.331500822316997734 ) ) ;
#33088=EDGE_LOOP ( 'NONE', ( #45466, #11852, #40862, #47501, #27691 ) ) ;
#33100=ORIENTED_EDGE ( 'NONE', *, *, #51566, .T. ) ;
#33101=CARTESIAN_POINT ( 'NONE',  ( 16.44809435262699893, -3.299700711820999555, -11.83394467541999973 ) ) ;
#33120=CARTESIAN_POINT ( 'NONE',  ( 15.36900185986900169, -9.263677555280001030, -8.208910455558001473 ) ) ;
#33128=B_SPLINE_CURVE_WITH_KNOTS ( 'NONE', 3,
 ( #63125, #30646, #51956, #13884 ),
 .UNSPECIFIED., .F., .F.,
 ( 4, 4 ),
 ( 0.000000000000000000, 1.000000000000000000 ),
 .UNSPECIFIED. ) ;
#33133=ORIENTED_EDGE ( 'NONE', *, *, #35909, .F. ) ;
#33136=CARTESIAN_POINT ( 'NONE',  ( 11.80577368593200305, -12.32791529894999982, -1.878576500660000148 ) ) ;
#33142=EDGE_CURVE ( 'NONE', #33910, #55299, #43343, .T. ) ;
#33144=EDGE_CURVE ( 'NONE', #10227, #68412, #55849, .T. ) ;
#33149=CARTESIAN_POINT ( 'NONE',  ( 25.29995737991200144, -8.533537546129998930, 7.925519566782000425 ) ) ;
#33151=CARTESIAN_POINT ( 'NONE',  ( 17.86871151025999893, 3.252328409732000214, -11.33729656921000029 ) ) ;
#33153=AXIS2_PLACEMENT_3D ( 'NONE', #41482, #36933, #62113 ) ;
#33154=CARTESIAN_POINT ( 'NONE',  ( 23.56665676678100141, 1.475264355121999897E-12, 7.429612480791998923E-13 ) ) ;
#33155=CARTESIAN_POINT ( 'NONE',  ( 23.51508444987500113, -10.47082793957999947, -9.494578343657000374 ) ) ;
#33156=CARTESIAN_POINT ( 'NONE',  ( 23.91165634958499808, -9.488820091758000785, 9.248970464519000956 ) ) ;
#33162=CARTESIAN_POINT ( 'NONE',  ( 24.46729256464000457, 8.826997888453998797, -8.952499471243999807 ) ) ;
#33169=CARTESIAN_POINT ( 'NONE',  ( 21.10000109091659937, 0.000000000000000000, 0.000000000000000000 ) ) ;
#33178=CARTESIAN_POINT ( 'NONE',  ( 24.46580263708699832, 12.16839033447999974, -3.168637030101999930 ) ) ;
#33179=CARTESIAN_POINT ( 'NONE',  ( 12.13642952379600004, -11.66478987891999886, 3.865847705614000152 ) ) ;
#33184=ORIENTED_EDGE ( 'NONE', *, *, #17947, .T. ) ;
#33185=CARTESIAN_POINT ( 'NONE',  ( 24.05220196936242161, -9.284530115100020353, 9.220592073794886545 ) ) ;
#33190=ORIENTED_EDGE ( 'NONE', *, *, #62895, .F. ) ;
#33193=CARTESIAN_POINT ( 'NONE',  ( 24.38583233132600014, 12.22835294837999953, -3.200653174729999773 ) ) ;
#33197=CARTESIAN_POINT ( 'NONE',  ( 23.57777265339244721, 2.928868628335262514, 13.64745830326427800 ) ) ;
#33198=CIRCLE ( 'NONE', #19771, 5.760713961201000544 ) ;
#33201=FACE_OUTER_BOUND ( 'NONE', #51888, .T. ) ;
#33209=CARTESIAN_POINT ( 'NONE',  ( 18.33872945691700096, -11.68442479034000137, 4.616443127689999315 ) ) ;
#33211=CARTESIAN_POINT ( 'NONE',  ( 13.60261247405900242, 9.239907047945001395, 8.094831983377998696 ) ) ;
#33218=CARTESIAN_POINT ( 'NONE',  ( 11.79999999684100054, 12.15995044155999949, 2.000340912084999978 ) ) ;
#33220=CARTESIAN_POINT ( 'NONE',  ( 11.56599877858000092, 12.45298756855999933, 1.663864064400000009 ) ) ;
#33233=CARTESIAN_POINT ( 'NONE',  ( 24.26733149983100191, -3.229785797570000394, -12.20153234936999986 ) ) ;
#33244=TOROIDAL_SURFACE ( 'NONE', #8687, 6.000000000000000000, 1.000000000000000000 ) ;
#33246=CYLINDRICAL_SURFACE ( 'NONE', #31562, 5.000000000000000000 ) ;
#33247=CARTESIAN_POINT ( 'NONE',  ( 24.59999999957999961, -2.749830041232999947E-09, 4.999999999859999988 ) ) ;
#33248=CARTESIAN_POINT ( 'NONE',  ( 24.89163422318532426, 11.59758331541865672, 3.206058750856457529 ) ) ;
#33251=ORIENTED_EDGE ( 'NONE', *, *, #9291, .T. ) ;
#33254=CARTESIAN_POINT ( 'NONE',  ( 23.76527261957394188, -9.791761873676088967, -9.440867193121368572 ) ) ;
#33257=CARTESIAN_POINT ( 'NONE',  ( 12.08335418496243463, -11.66230666314274345, 4.568774126648690093 ) ) ;
#33258=CARTESIAN_POINT ( 'NONE',  ( 24.53429015151300163, -3.614318902553999902, -12.31267542782000035 ) ) ;
#33263=CARTESIAN_POINT ( 'NONE',  ( 13.18628609634500215, -12.21854424350999935, -1.979874043355999813 ) ) ;
#33271=DIRECTION ( 'NONE',  ( -0.000000000000000000, 0.06400262754466103099, 0.9979497300302152540 ) ) ;
#33274=AXIS2_PLACEMENT_3D ( 'NONE', #61900, #45823, #67819 ) ;
#33275=CARTESIAN_POINT ( 'NONE',  ( 11.49999035076000276, -3.886252136122000156, 11.90689009355000039 ) ) ;
#33286=B_SPLINE_CURVE_WITH_KNOTS ( 'NONE', 3,
 ( #36868, #20093, #58184, #35832 ),
 .UNSPECIFIED., .F., .F.,
 ( 4, 4 ),
 ( 0.000000000000000000, 1.000000000000000000 ),
 .UNSPECIFIED. ) ;
#33308=CIRCLE ( 'NONE', #36648, 11.79499999999999993 ) ;
#33309=CARTESIAN_POINT ( 'NONE',  ( 23.60205915885299888, -9.223492163368996799, -8.025915643339997629 ) ) ;
#33317=AXIS2_PLACEMENT_3D ( 'NONE', #40595, #50060, #33983 ) ;
#33330=EDGE_CURVE ( 'NONE', #49843, #18862, #34703, .T. ) ;
#33336=B_SPLINE_CURVE_WITH_KNOTS ( 'NONE', 3,
 ( #66903, #34075, #56423, #8184 ),
 .UNSPECIFIED., .F., .F.,
 ( 4, 4 ),
 ( 0.000000000000000000, 1.000000000000000000 ),
 .UNSPECIFIED. ) ;
#33344=CARTESIAN_POINT ( 'NONE',  ( 11.80852891948700290, 3.296364302329999774, -11.83491796280999964 ) ) ;
#33351=CARTESIAN_POINT ( 'NONE',  ( 24.60999195316300003, -3.467950226999999774, 12.10892777233999951 ) ) ;
#33354=CARTESIAN_POINT ( 'NONE',  ( 15.40000000009400161, 8.833277835210999740, 7.896561221812000930 ) ) ;
#33358=ORIENTED_EDGE ( 'NONE', *, *, #63903, .F. ) ;
#33361=CARTESIAN_POINT ( 'NONE',  ( 13.99965637475000158, -8.819038952442999957, -7.693330608063000398 ) ) ;
#33363=FACE_OUTER_BOUND ( 'NONE', #69183, .T. ) ;
#33366=ORIENTED_EDGE ( 'NONE', *, *, #63903, .T. ) ;
#33371=CARTESIAN_POINT ( 'NONE',  ( 24.81044895848265952, 8.607468258889918289, -8.518276782355464150 ) ) ;
#33376=CARTESIAN_POINT ( 'NONE',  ( 15.95370777310256294, -3.574818104395616647, -11.79277689209176749 ) ) ;
#33382=ORIENTED_EDGE ( 'NONE', *, *, #868, .T. ) ;
#33391=CARTESIAN_POINT ( 'NONE',  ( 30.60000000000000142, 0.000000000000000000, -8.250000000000000000 ) ) ;
#33393=EDGE_CURVE ( 'NONE', #31379, #14147, #10021, .T. ) ;
#33395=EDGE_CURVE ( 'NONE', #38268, #35889, #29242, .T. ) ;
#33396=ORIENTED_EDGE ( 'NONE', *, *, #30476, .F. ) ;
#33397=DIRECTION ( 'NONE',  ( -1.000000000000000000, 0.000000000000000000, 0.000000000000000000 ) ) ;
#33399=CARTESIAN_POINT ( 'NONE',  ( 25.29986325275000070, 2.078227429405999693, 11.31065739696999906 ) ) ;
#33406=ORIENTED_EDGE ( 'NONE', *, *, #48052, .T. ) ;
#33432=B_SPLINE_SURFACE_WITH_KNOTS ( 'NONE', 3, 3, ( 
 ( #27378, #16192, #43466, #58840 ),
 ( #59186, #9916, #53937, #21100 ),
 ( #48350, #15513, #47330, #52564 ),
 ( #6040, #64413, #42425, #64073 ),
 ( #25999, #48704, #27038, #37515 ),
 ( #68633, #52915, #20754, #22123 ),
 ( #53600, #37176, #457, #4660 ),
 ( #42082, #36838, #58157, #10259 ),
 ( #63733, #15845, #31941, #5358 ),
 ( #26697, #50088, #2197, #22816 ) ),
 .UNSPECIFIED., .F., .F., .F.,
 ( 4, 1, 1, 1, 1, 1, 1, 4 ),
 ( 4, 4 ),
 ( 0.04111222701783000255, 0.1428571428570999946, 0.2857142857143000203, 0.4285714285713999594, 0.5714285714286000406, 0.7142857142856999797, 0.8571428571429000609, 0.9278613184711000939 ),
 ( -0.1900620218102000158, 1.190128522698000069 ),
 .UNSPECIFIED. ) ;
#33442=B_SPLINE_CURVE_WITH_KNOTS ( 'NONE', 3,
 ( #19229, #2808, #40556, #39884 ),
 .UNSPECIFIED., .F., .F.,
 ( 4, 4 ),
 ( 0.000000000000000000, 1.000000000000000000 ),
 .UNSPECIFIED. ) ;
#33452=DIRECTION ( 'NONE',  ( 0.000000000000000000, -0.9999606858717338120, 0.008867170401640298016 ) ) ;
#33453=CARTESIAN_POINT ( 'NONE',  ( 16.07488484168399978, 3.504106430365000246, 11.16639795596000084 ) ) ;
#33455=ADVANCED_FACE ( 'NONE', ( #30147 ), #29811, .F. ) ;
#33459=CARTESIAN_POINT ( 'NONE',  ( 24.53428988874600236, -8.855929874993998752, -9.286429786912000495 ) ) ;
#33462=CARTESIAN_POINT ( 'NONE',  ( 24.54223752884104925, 3.611770689525808375, 12.30300795115269175 ) ) ;
#33467=CARTESIAN_POINT ( 'NONE',  ( 15.95168611684299975, -8.949867560646000086, -8.553740745252000011 ) ) ;
#33473=DIRECTION ( 'NONE',  ( 0.000000000000000000, -0.7614089499631908620, 0.6482718649732929217 ) ) ;
#33474=CARTESIAN_POINT ( 'NONE',  ( 11.49978667957999967, -12.52500000000000213, -0.5112815185527788131 ) ) ;
#33475=B_SPLINE_CURVE_WITH_KNOTS ( 'NONE', 3,
 ( #7183, #22907, #65207, #38650, #12083, #17680 ),
 .UNSPECIFIED., .F., .F.,
 ( 4, 2, 4 ),
 ( 0.000000000000000000, 0.5000000000000000000, 1.000000000000000000 ),
 .UNSPECIFIED. ) ;
#33479=ORIENTED_EDGE ( 'NONE', *, *, #7796, .T. ) ;
#33481=EDGE_CURVE ( 'NONE', #6782, #43577, #27487, .T. ) ;
#33492=VERTEX_POINT ( 'NONE', #14741 ) ;
#33498=CARTESIAN_POINT ( 'NONE',  ( 18.44721083353000068, 2.702837639295000205, -11.38762126772000016 ) ) ;
#33503=CARTESIAN_POINT ( 'NONE',  ( 23.74330720574500120, -9.836545709669998416, -9.383277561883000217 ) ) ;
#33504=CARTESIAN_POINT ( 'NONE',  ( 24.15332041333400070, -9.223082443678000786, 9.474599958732000005 ) ) ;
#33505=CARTESIAN_POINT ( 'NONE',  ( 11.50029455687000102, 11.65000000000000036, 0.000000000000000000 ) ) ;
#33510=CARTESIAN_POINT ( 'NONE',  ( 24.60000000000000142, 0.000000000000000000, -5.000000000000000000 ) ) ;
#33518=ORIENTED_EDGE ( 'NONE', *, *, #28946, .T. ) ;
#33525=CARTESIAN_POINT ( 'NONE',  ( 24.60999195316300003, 12.22061417693999985, -3.051130890528999995 ) ) ;
#33526=CARTESIAN_POINT ( 'NONE',  ( 12.13190478341600098, -11.96733320521999921, 3.503025077341000326 ) ) ;
#33530=CARTESIAN_POINT ( 'NONE',  ( 23.54917040509700144, 2.965869371470000182, 13.72136993952999973 ) ) ;
#33533=CARTESIAN_POINT ( 'NONE',  ( 23.84134149042290574, -9.640897496743738415, 9.399424730200435008 ) ) ;
#33536=CARTESIAN_POINT ( 'NONE',  ( 17.60000000000000142, 10.78295181803999903, -4.410266442048000002 ) ) ;
#33538=EDGE_CURVE ( 'NONE', #63477, #7350, #63382, .T. ) ;
#33539=EDGE_CURVE ( 'NONE', #52478, #65259, #68202, .T. ) ;
#33541=CARTESIAN_POINT ( 'NONE',  ( 23.85322625602900004, 13.16205774920000060, -3.533916265924000211 ) ) ;
#33546=ORIENTED_EDGE ( 'NONE', *, *, #15417, .T. ) ;
#33548=CARTESIAN_POINT ( 'NONE',  ( 16.39999999347100257, 3.345256695718999751, 11.86066175541999890 ) ) ;
#33549=VERTEX_POINT ( 'NONE', #42681 ) ;
#33552=CARTESIAN_POINT ( 'NONE',  ( 24.35365242081700288, 3.193712117489998281, -11.49150331539999215 ) ) ;
#33554=CARTESIAN_POINT ( 'NONE',  ( 17.83726331522299802, -11.40363207186999972, 4.542070182500999920 ) ) ;
#33555=CARTESIAN_POINT ( 'NONE',  ( 12.79999998875598344, 11.49049412642037460, -4.802266170000438983 ) ) ;
#33564=CARTESIAN_POINT ( 'NONE',  ( 23.89320776801300283, -10.87822567731000234, 3.284864823438000236 ) ) ;
#33567=CARTESIAN_POINT ( 'NONE',  ( 24.13718786373500080, -3.227326363975000056, 12.37799336445999998 ) ) ;
#33577=CARTESIAN_POINT ( 'NONE',  ( 24.54688887196200042, -3.662825465818000392, -12.34578425079000041 ) ) ;
#33586=DIRECTION ( 'NONE',  ( 0.000000000000000000, 0.000000000000000000, -1.000000000000000000 ) ) ;
#33596=CARTESIAN_POINT ( 'NONE',  ( 11.29996849689000271, 12.23272706294999956, 1.505586356912999912 ) ) ;
#33599=CARTESIAN_POINT ( 'NONE',  ( 23.98814404780929621, -9.385780080724808627, -9.282153661438828252 ) ) ;
#33603=CARTESIAN_POINT ( 'NONE',  ( 24.44916829770000177, -12.41483723393999838, 3.103225306172999964 ) ) ;
#33606=CARTESIAN_POINT ( 'NONE',  ( 24.13681546429500102, 3.227485322444999749, -12.37873180773000215 ) ) ;
#33607=CARTESIAN_POINT ( 'NONE',  ( 13.46281931570200108, -12.03411875281000043, -2.480748420245000307 ) ) ;
#33612=CARTESIAN_POINT ( 'NONE',  ( 17.74638838757924120, -10.78680295286659074, 4.401676307955865397 ) ) ;
#33613=CARTESIAN_POINT ( 'NONE',  ( 18.41451919223733213, -3.018310540773369688, -11.25254019301576669 ) ) ;
#33615=FACE_OUTER_BOUND ( 'NONE', #50512, .T. ) ;
#33642=CARTESIAN_POINT ( 'NONE',  ( 11.35620373058000077, 3.594096350588000366, -11.23428177897000069 ) ) ;
#33649=VERTEX_POINT ( 'NONE', #32541 ) ;
#33660=CARTESIAN_POINT ( 'NONE',  ( 12.78268972790800184, 11.49710380946999955, -4.820178426657999005 ) ) ;
#33662=B_SPLINE_CURVE_WITH_KNOTS ( 'NONE', 3,
 ( #2343, #28578, #2001, #65616 ),
 .UNSPECIFIED., .F., .F.,
 ( 4, 4 ),
 ( 0.000000000000000000, 1.000000000000000000 ),
 .UNSPECIFIED. ) ;
#33666=EDGE_CURVE ( 'NONE', #31242, #9579, #38381, .T. ) ;
#33681=ORIENTED_EDGE ( 'NONE', *, *, #10811, .T. ) ;
#33688=CARTESIAN_POINT ( 'NONE',  ( 23.57773632097178407, -13.28348942634863583, 4.287207044979979287 ) ) ;
#33700=CARTESIAN_POINT ( 'NONE',  ( 25.40241821196899963, -8.312581368709999197, 8.374650789474999968 ) ) ;
#33704=ADVANCED_FACE ( 'NONE', ( #21015 ), #32206, .T. ) ;
#33708=CARTESIAN_POINT ( 'NONE',  ( 25.26979265321100243, -8.566783789541000615, -7.890681328063000599 ) ) ;
#33709=CARTESIAN_POINT ( 'NONE',  ( 13.18179592085193974, -11.52326738618029012, -1.714065324703454740 ) ) ;
#33717=EDGE_LOOP ( 'NONE', ( #35593, #27001, #58935, #36998, #43669 ) ) ;
#33719=CARTESIAN_POINT ( 'NONE',  ( 24.72673738265526922, 8.645762772944534547, -8.593181399093179351 ) ) ;
#33725=ORIENTED_EDGE ( 'NONE', *, *, #30100, .T. ) ;
#33733=VERTEX_POINT ( 'NONE', #43024 ) ;
#33738=CARTESIAN_POINT ( 'NONE',  ( 15.86053068095500151, 3.820355458042000052, 11.67812044351000011 ) ) ;
#33739=CARTESIAN_POINT ( 'NONE',  ( 11.29998658800000122, 3.824194713071000340, -11.71675648045999907 ) ) ;
#33741=B_SPLINE_CURVE_WITH_KNOTS ( 'NONE', 3,
 ( #45799, #56635, #50360, #45462 ),
 .UNSPECIFIED., .F., .F.,
 ( 4, 4 ),
 ( 0.000000000000000000, 1.000000000000000000 ),
 .UNSPECIFIED. ) ;
#33750=CARTESIAN_POINT ( 'NONE',  ( 24.84741859043700174, 3.386183434052000063, 11.85236409072000008 ) ) ;
#33754=ORIENTED_EDGE ( 'NONE', *, *, #18095, .T. ) ;
#33760=CARTESIAN_POINT ( 'NONE',  ( 23.56665676678700194, 2.935519496638999914, -13.67844162499000049 ) ) ;
#33768=CARTESIAN_POINT ( 'NONE',  ( 23.56960665000709909, 10.30499699461899610, -9.460494264439814671 ) ) ;
#33772=EDGE_LOOP ( 'NONE', ( #9286, #58360, #65424, #48904, #43663 ) ) ;
#33776=CARTESIAN_POINT ( 'NONE',  ( 25.60000000000000142, 0.000000000000000000, 0.000000000000000000 ) ) ;
#33777=LINE ( 'NONE', #40307, #32164 ) ;
#33779=CIRCLE ( 'NONE', #8124, 11.49999999999999467 ) ;
#33782=AXIS2_PLACEMENT_3D ( 'NONE', #47078, #68379, #47771 ) ;
#33787=CARTESIAN_POINT ( 'NONE',  ( 23.95413516103606000, -12.78631318506285020, -3.518586055979009863 ) ) ;
#33799=ORIENTED_EDGE ( 'NONE', *, *, #33481, .F. ) ;
#33801=CARTESIAN_POINT ( 'NONE',  ( 25.39408680342049252, -2.774728762786359493, -11.32588899302948882 ) ) ;
#33803=ORIENTED_EDGE ( 'NONE', *, *, #45969, .F. ) ;
#33806=B_SPLINE_CURVE_WITH_KNOTS ( 'NONE', 3,
 ( #20221, #16348, #57618, #5171, #5854, #53757 ),
 .UNSPECIFIED., .F., .F.,
 ( 4, 2, 4 ),
 ( 0.000000000000000000, 0.5000000000000000000, 1.000000000000000000 ),
 .UNSPECIFIED. ) ;
#33808=FACE_OUTER_BOUND ( 'NONE', #3000, .T. ) ;
#33809=CARTESIAN_POINT ( 'NONE',  ( 25.34480302439135713, 8.474813402932349859, 7.997915580558633941 ) ) ;
#33812=CARTESIAN_POINT ( 'NONE',  ( 23.55064466279999991, -13.34882249087999995, -4.337886341278000657 ) ) ;
#33813=ADVANCED_FACE ( 'NONE', ( #18187 ), #65228, .F. ) ;
#33814=CARTESIAN_POINT ( 'NONE',  ( 16.10004050617000004, 7.492404338401442487, 10.08789649943575029 ) ) ;
#33830=CARTESIAN_POINT ( 'NONE',  ( 11.48381255716000027, -12.35454260995000020, -1.695649549036999826 ) ) ;
#33834=CARTESIAN_POINT ( 'NONE',  ( 24.45625562564337585, 3.500080689026665581, 12.27866752497065761 ) ) ;
#33837=VERTEX_POINT ( 'NONE', #38819 ) ;
#33838=CARTESIAN_POINT ( 'NONE',  ( 18.26242637978999994, 2.744390477411999818, 11.56740641610000075 ) ) ;
#33846=ADVANCED_FACE ( 'NONE', ( #12251 ), #23687, .T. ) ;
#33849=CARTESIAN_POINT ( 'NONE',  ( 23.61707917866500139, -10.26292876439000068, 9.294242752039000521 ) ) ;
#33855=CARTESIAN_POINT ( 'NONE',  ( 23.56971388309658266, 3.042564011621391895, 13.65415468161493706 ) ) ;
#33858=CONICAL_SURFACE ( 'NONE', #20471, 11.75015521449999945, 0.7854113701714536822 ) ;
#33859=CARTESIAN_POINT ( 'NONE',  ( 25.20466149916200038, 2.650184388215000020, -11.40090097795000013 ) ) ;
#33864=VERTEX_POINT ( 'NONE', #1242 ) ;
#33877=CARTESIAN_POINT ( 'NONE',  ( 23.58699566483300103, 3.020915523320000240, 13.60570109925000004 ) ) ;
#33880=CARTESIAN_POINT ( 'NONE',  ( 24.73253179669367086, -11.75903539564235523, -3.190943823743348950 ) ) ;
#33888=CARTESIAN_POINT ( 'NONE',  ( 23.51706673858500096, 13.43779730422000007, -4.375994916149999803 ) ) ;
#33894=ORIENTED_EDGE ( 'NONE', *, *, #13156, .F. ) ;
#33896=CARTESIAN_POINT ( 'NONE',  ( 24.30001694670299983, 8.938702829764999080, 8.938676122491999720 ) ) ;
#33897=ORIENTED_EDGE ( 'NONE', *, *, #48928, .F. ) ;
#33903=CARTESIAN_POINT ( 'NONE',  ( 18.22523891024100351, -11.70723067604000001, 3.729442327036999849 ) ) ;
#33910=VERTEX_POINT ( 'NONE', #16882 ) ;
#33915=CARTESIAN_POINT ( 'NONE',  ( 24.32839855075200219, -3.577297860116000372, 12.48354892467999910 ) ) ;
#33917=CARTESIAN_POINT ( 'NONE',  ( 13.50003721581400029, -9.159934378815998812, -7.517910889891000537 ) ) ;
#33921=ORIENTED_EDGE ( 'NONE', *, *, #35969, .F. ) ;
#33924=CARTESIAN_POINT ( 'NONE',  ( 24.43231275843400141, -3.176386277817000003, -12.00227839950999886 ) ) ;
#33929=AXIS2_PLACEMENT_3D ( 'NONE', #58241, #21182, #57902 ) ;
#33936=CARTESIAN_POINT ( 'NONE',  ( 25.52466926685099935, 8.322335989133000211, 8.137640611811999491 ) ) ;
#33943=VERTEX_POINT ( 'NONE', #16540 ) ;
#33945=CARTESIAN_POINT ( 'NONE',  ( 23.59999467231800097, -10.30760443253999981, -9.317695455237998914 ) ) ;
#33948=CARTESIAN_POINT ( 'NONE',  ( 24.60170725970500172, -12.45697516994999887, 2.983025822335999777 ) ) ;
#33958=CARTESIAN_POINT ( 'NONE',  ( 17.98179591661178023, -3.334516285427086668, -11.16264808783960305 ) ) ;
#33961=CARTESIAN_POINT ( 'NONE',  ( 12.79999999914999975, 12.11987927271999865, -3.159802730921999814 ) ) ;
#33966=CARTESIAN_POINT ( 'NONE',  ( 18.50001572531399674, -0.9783175319534245240, 12.52500000122871526 ) ) ;
#33968=CARTESIAN_POINT ( 'NONE',  ( 11.29998901737826955, 3.699024971382844029, -11.75540534549141825 ) ) ;
#33969=CARTESIAN_POINT ( 'NONE',  ( 12.10941530413763445, -10.98038939419360815, 3.892884065153699336 ) ) ;
#33971=B_SPLINE_CURVE_WITH_KNOTS ( 'NONE', 3,
 ( #54325, #27776, #32332, #43151 ),
 .UNSPECIFIED., .F., .F.,
 ( 4, 4 ),
 ( 0.000000000000000000, 1.000000000000000000 ),
 .UNSPECIFIED. ) ;
#33974=TOROIDAL_SURFACE ( 'NONE', #49635, 13.79999999999999893, 0.2000000000000000111 ) ;
#33979=CARTESIAN_POINT ( 'NONE',  ( 24.99828677809757238, -2.941260336786404306, -11.56306762256811105 ) ) ;
#33981=ADVANCED_FACE ( 'NONE', ( #27382 ), #53940, .T. ) ;
#33983=DIRECTION ( 'NONE',  ( 0.000000000000000000, 0.9439966912222074180, 0.3299549165591025846 ) ) ;
#33986=DIRECTION ( 'NONE',  ( -1.000000000000000000, 4.460717509654651142E-14, 1.610814656264179684E-14 ) ) ;
#33987=CARTESIAN_POINT ( 'NONE',  ( 11.80600022547799988, 3.313997181012000137, -11.22408540768999963 ) ) ;
#34002=B_SPLINE_CURVE_WITH_KNOTS ( 'NONE', 3,
 ( #21340, #16436, #27285, #42670, #43012, #37421 ),
 .UNSPECIFIED., .F., .F.,
 ( 4, 1, 1, 4 ),
 ( 0.000000000000000000, 0.1550125217837789171, 0.7488612475957610037, 1.000000000000000000 ),
 .UNSPECIFIED. ) ;
#34003=ORIENTED_EDGE ( 'NONE', *, *, #31405, .T. ) ;
#34009=CARTESIAN_POINT ( 'NONE',  ( 24.33638798420900073, -3.364639815177999704, -12.26716122899000005 ) ) ;
#34012=B_SPLINE_SURFACE_WITH_KNOTS ( 'NONE', 3, 3, ( 
 ( #38655, #37961, #6487, #60328 ),
 ( #21533, #22224, #48803, #16289 ),
 ( #65211, #38304, #27479, #43210 ),
 ( #21875, #7188, #54737, #58944 ),
 ( #59281, #48456, #565, #32387 ),
 ( #33071, #53700, #22567, #12435 ) ),
 .UNSPECIFIED., .F., .F., .F.,
 ( 4, 1, 1, 4 ),
 ( 4, 4 ),
 ( 0.1811037619699999990, 0.3333333333333000081, 0.6666666666667000474, 0.8725156331704999602 ),
 ( -0.1256563615239000009, 1.125656361510000147 ),
 .UNSPECIFIED. ) ;
#34017=ADVANCED_FACE ( 'NONE', ( #47680 ), #44167, .F. ) ;
#34019=CARTESIAN_POINT ( 'NONE',  ( 18.30017264560542145, 0.9191760154459583942, -11.85014035451979630 ) ) ;
#34020=DIRECTION ( 'NONE',  ( 0.000000000000000000, -0.9659258262890756397, 0.2588190451024934280 ) ) ;
#34023=EDGE_CURVE ( 'NONE', #37068, #11162, #47500, .T. ) ;
#34034=AXIS2_PLACEMENT_3D ( 'NONE', #32767, #54081, #6177 ) ;
#34039=CARTESIAN_POINT ( 'NONE',  ( 24.30001696810800027, 12.21047201856000086, 3.271805692349999628 ) ) ;
#34042=B_SPLINE_CURVE_WITH_KNOTS ( 'NONE', 3,
 ( #44690, #5876, #17054, #59712 ),
 .UNSPECIFIED., .F., .F.,
 ( 4, 4 ),
 ( 0.000000000000000000, 1.000000000000000000 ),
 .UNSPECIFIED. ) ;
#34047=CARTESIAN_POINT ( 'NONE',  ( 24.39664882158933423, -3.240506423573137784, 12.09373461503223091 ) ) ;
#34051=CARTESIAN_POINT ( 'NONE',  ( 25.52344634951100133, 11.21071681617999971, 3.136836603414999924 ) ) ;
#34052=VERTEX_POINT ( 'NONE', #34709 ) ;
#34056=CARTESIAN_POINT ( 'NONE',  ( 24.46218697145600274, -8.785835042869001299, -8.709278711906000225 ) ) ;
#34059=CARTESIAN_POINT ( 'NONE',  ( 13.46005557146100173, 12.04952288628000012, 2.412084176363999966 ) ) ;
#34067=CARTESIAN_POINT ( 'NONE',  ( 13.55370778485685435, -9.344737785247383854, -8.032732227356667920 ) ) ;
#34075=CARTESIAN_POINT ( 'NONE',  ( 25.59994555223700274, -10.09686240769118903, 5.033199831113347678 ) ) ;
#34084=DIRECTION ( 'NONE',  ( 1.000000000000000000, 0.000000000000000000, 0.000000000000000000 ) ) ;
#34094=CARTESIAN_POINT ( 'NONE',  ( 25.19548756823600399, 3.342128045641000078, 11.59777824541000157 ) ) ;
#34096=CARTESIAN_POINT ( 'NONE',  ( 24.63779836814899937, -3.092549035221999976, 11.81391394322000110 ) ) ;
#34102=EDGE_CURVE ( 'NONE', #12282, #12604, #63252, .T. ) ;
#34126=CARTESIAN_POINT ( 'NONE',  ( 13.56683625432858342, -9.108504156368539384, -7.475700167246311700 ) ) ;
#34130=EDGE_LOOP ( 'NONE', ( #2481, #1726, #18444, #15356 ) ) ;
#34139=DIRECTION ( 'NONE',  ( -1.000000000000000000, 0.000000000000000000, 0.000000000000000000 ) ) ;
#34142=ORIENTED_EDGE ( 'NONE', *, *, #9887, .T. ) ;
#34144=ORIENTED_EDGE ( 'NONE', *, *, #19336, .F. ) ;
#34157=CARTESIAN_POINT ( 'NONE',  ( 23.64816398247700135, -13.35748263717000128, -3.865423979300999680 ) ) ;
#34166=CARTESIAN_POINT ( 'NONE',  ( 24.54174074851610143, 12.46120270712776090, -3.023779783529694676 ) ) ;
#34172=ORIENTED_EDGE ( 'NONE', *, *, #24948, .T. ) ;
#34181=CARTESIAN_POINT ( 'NONE',  ( 24.21983515806600096, 12.94789048768999962, 3.132737188682000351 ) ) ;
#34183=VERTEX_POINT ( 'NONE', #56021 ) ;
#34190=CARTESIAN_POINT ( 'NONE',  ( 18.36682228790375859, -2.717338739979838547, 11.46589211741050285 ) ) ;
#34193=CARTESIAN_POINT ( 'NONE',  ( 25.55305567154783475, -2.866385917523393001, -11.19763132080514367 ) ) ;
#34195=CARTESIAN_POINT ( 'NONE',  ( 23.51695514933100029, -10.50652978964999917, 9.451976498271999816 ) ) ;
#34198=ORIENTED_EDGE ( 'NONE', *, *, #65365, .T. ) ;
#34202=CARTESIAN_POINT ( 'NONE',  ( 24.35365242081700288, -2.582848009804000533, 11.10541636511000085 ) ) ;
#34204=ORIENTED_EDGE ( 'NONE', *, *, #10811, .F. ) ;
#34218=ORIENTED_EDGE ( 'NONE', *, *, #56516, .F. ) ;
#34227=CARTESIAN_POINT ( 'NONE',  ( 24.57709178557182383, -11.91258736157513098, -3.191969742968967516 ) ) ;
#34231=ORIENTED_EDGE ( 'NONE', *, *, #41790, .F. ) ;
#34241=ORIENTED_EDGE ( 'NONE', *, *, #27708, .F. ) ;
#34250=CARTESIAN_POINT ( 'NONE',  ( 17.90248731685900196, -11.51619295222000083, 4.775850843141999924 ) ) ;
#34258=DIRECTION ( 'NONE',  ( -1.000000000000000000, 0.000000000000000000, 0.000000000000000000 ) ) ;
#34259=CARTESIAN_POINT ( 'NONE',  ( 18.30003129332100187, -2.732683818840999646, -11.53064095373000164 ) ) ;
#34260=CARTESIAN_POINT ( 'NONE',  ( 23.74082840454099852, -3.323468775169000189, 13.27900164760999857 ) ) ;
#34267=B_SPLINE_CURVE_WITH_KNOTS ( 'NONE', 3,
 ( #32355, #53671, #21165, #48422 ),
 .UNSPECIFIED., .F., .F.,
 ( 4, 4 ),
 ( 0.000000000000000000, 1.000000000000000000 ),
 .UNSPECIFIED. ) ;
#34287=CARTESIAN_POINT ( 'NONE',  ( 25.05003967968370304, 11.42808677591299649, 3.253271619634388045 ) ) ;
#34296=CARTESIAN_POINT ( 'NONE',  ( 24.36453968330800279, -12.29068757565999981, 3.201420012455000297 ) ) ;
#34300=FACE_OUTER_BOUND ( 'NONE', #56988, .T. ) ;
#34305=CIRCLE ( 'NONE', #33153, 11.85002173638999778 ) ;
#34308=VERTEX_POINT ( 'NONE', #45542 ) ;
#34311=LINE ( 'NONE', #38863, #31025 ) ;
#34323=ORIENTED_EDGE ( 'NONE', *, *, #56798, .F. ) ;
#34325=B_SPLINE_CURVE_WITH_KNOTS ( 'NONE', 3,
 ( #58874, #41422, #36175, #47014 ),
 .UNSPECIFIED., .F., .F.,
 ( 4, 4 ),
 ( 0.000000000000000000, 1.000000000000000000 ),
 .UNSPECIFIED. ) ;
#34330=CARTESIAN_POINT ( 'NONE',  ( 25.12927302627635484, -2.819697932548927533, -11.46537540841081615 ) ) ;
#34338=CARTESIAN_POINT ( 'NONE',  ( 11.44446797630000034, 3.649424658612000272, -11.12042579671999931 ) ) ;
#34342=FACE_OUTER_BOUND ( 'NONE', #60495, .T. ) ;
#34356=CARTESIAN_POINT ( 'NONE',  ( 23.85395881716046773, 13.23045290494460247, -3.489568871745106549 ) ) ;
#34359=CARTESIAN_POINT ( 'NONE',  ( 24.63625149985600160, -3.694707171958000025, -12.29749030356000006 ) ) ;
#34368=DIRECTION ( 'NONE',  ( -1.000000000000000000, 0.000000000000000000, 0.000000000000000000 ) ) ;
#34376=CARTESIAN_POINT ( 'NONE',  ( 23.58690406892612756, -13.37933363478873794, 4.060878750407953319 ) ) ;
#34378=AXIS2_PLACEMENT_3D ( 'NONE', #60602, #29149, #50457 ) ;
#34379=EDGE_CURVE ( 'NONE', #4046, #32306, #22579, .T. ) ;
#34390=DIRECTION ( 'NONE',  ( -1.000000000000000000, 0.000000000000000000, 0.000000000000000000 ) ) ;
#34397=CARTESIAN_POINT ( 'NONE',  ( 14.93333333083533532, 8.833279250037010755, 7.896561129384958910 ) ) ;
#34399=CARTESIAN_POINT ( 'NONE',  ( 24.98214587845099999, 11.60529653845999931, 3.133087885915999848 ) ) ;
#34408=CARTESIAN_POINT ( 'NONE',  ( 18.30000000002852900, -11.04996330604345722, 3.691231741008185629 ) ) ;
#34410=ORIENTED_EDGE ( 'NONE', *, *, #66570, .F. ) ;
#34412=ORIENTED_EDGE ( 'NONE', *, *, #37952, .F. ) ;
#34414=CARTESIAN_POINT ( 'NONE',  ( 25.29995422340600086, 2.596935224161999844, 11.35301931920000129 ) ) ;
#34434=B_SPLINE_CURVE_WITH_KNOTS ( 'NONE', 3,
 ( #24030, #38383, #34190, #54465 ),
 .UNSPECIFIED., .F., .F.,
 ( 4, 4 ),
 ( 0.000000000000000000, 1.000000000000000000 ),
 .UNSPECIFIED. ) ;
#34437=CARTESIAN_POINT ( 'NONE',  ( 23.60205915885299888, 2.504446818062000535, 12.27382285989999566 ) ) ;
#34450=CARTESIAN_POINT ( 'NONE',  ( 25.46372797112000086, -8.354608193938998895, 8.148457429720000533 ) ) ;
#34452=ORIENTED_EDGE ( 'NONE', *, *, #17119, .T. ) ;
#34464=CARTESIAN_POINT ( 'NONE',  ( 24.67921310950000091, -12.29514723793999842, -2.979192343402000009 ) ) ;
#34475=DIRECTION ( 'NONE',  ( 0.000000000000000000, 0.000000000000000000, -1.000000000000000000 ) ) ;
#34478=CARTESIAN_POINT ( 'NONE',  ( 17.60000001947600268, -11.86186880240999919, 3.298627760718999991 ) ) ;
#34489=ORIENTED_EDGE ( 'NONE', *, *, #34102, .T. ) ;
#34504=ADVANCED_FACE ( 'NONE', ( #10868 ), #33858, .F. ) ;
#34509=CARTESIAN_POINT ( 'NONE',  ( 18.28771814374038129, -2.987295517884131169, 11.95930540589378133 ) ) ;
#34512=EDGE_CURVE ( 'NONE', #28231, #28381, #31648, .T. ) ;
#34521=CARTESIAN_POINT ( 'NONE',  ( 24.66708179677300450, 12.30983497458833931, -2.983163088688387976 ) ) ;
#34522=DIRECTION ( 'NONE',  ( 0.000000000000000000, 0.1807154286440006141, 0.9835354258236025382 ) ) ;
#34525=ORIENTED_EDGE ( 'NONE', *, *, #40499, .F. ) ;
#34528=ADVANCED_FACE ( 'NONE', ( #27301 ), #57295, .T. ) ;
#34533=CARTESIAN_POINT ( 'NONE',  ( 24.53429010005800137, -12.47024913742999885, 3.026245653581999928 ) ) ;
#34538=CARTESIAN_POINT ( 'NONE',  ( 25.29987333571600061, -10.83443035398000021, -3.855530949778000149 ) ) ;
#34539=CARTESIAN_POINT ( 'NONE',  ( 23.66004879239100234, 9.998911746292000302, 9.691526727427998367 ) ) ;
#34546=FACE_OUTER_BOUND ( 'NONE', #41950, .T. ) ;
#34555=CARTESIAN_POINT ( 'NONE',  ( 15.90018573812399971, -8.493548356068000516, -8.263529029821000904 ) ) ;
#34567=PLANE ( 'NONE',  #60019 ) ;
#34568=ORIENTED_EDGE ( 'NONE', *, *, #57044, .T. ) ;
#34576=CARTESIAN_POINT ( 'NONE',  ( 24.81041655173479299, -11.68081165545370403, -3.195144698386812809 ) ) ;
#34578=EDGE_LOOP ( 'NONE', ( #5555, #28656, #10475, #11489 ) ) ;
#34584=CYLINDRICAL_SURFACE ( 'NONE', #65646, 0.5000000000000004441 ) ;
#34602=DIRECTION ( 'NONE',  ( 0.000000000000000000, 0.2483835927444960623, -0.9686617525510834437 ) ) ;
#34617=CARTESIAN_POINT ( 'NONE',  ( 18.26004861284300063, 2.925574202914999589, -11.93524904697000011 ) ) ;
#34637=CARTESIAN_POINT ( 'NONE',  ( 24.66908053516780086, 11.82197461467616684, 3.190505267773458886 ) ) ;
#34639=CIRCLE ( 'NONE', #45802, 1.000000000000000222 ) ;
#34641=VERTEX_POINT ( 'NONE', #53783 ) ;
#34645=CYLINDRICAL_SURFACE ( 'NONE', #28538, 0.5000000000000002220 ) ;
#34649=FACE_OUTER_BOUND ( 'NONE', #58895, .T. ) ;
#34651=CARTESIAN_POINT ( 'NONE',  ( 13.51587707751000167, -12.16770442808000041, -2.286102833273000012 ) ) ;
#34674=ORIENTED_EDGE ( 'NONE', *, *, #6090, .T. ) ;
#34675=ORIENTED_EDGE ( 'NONE', *, *, #8133, .T. ) ;
#34676=CARTESIAN_POINT ( 'NONE',  ( 24.44496356232399847, -3.224881240379999792, -12.03535804424000055 ) ) ;
#34678=CIRCLE ( 'NONE', #52514, 13.89999856298999958 ) ;
#34684=CARTESIAN_POINT ( 'NONE',  ( 11.26444844843000048, 3.604811106221999850, -11.32703155999000089 ) ) ;
#34688=ORIENTED_EDGE ( 'NONE', *, *, #4563, .F. ) ;
#34689=EDGE_CURVE ( 'NONE', #25967, #63987, #67468, .T. ) ;
#34703=LINE ( 'NONE', #51793, #60519 ) ;
#34704=FACE_OUTER_BOUND ( 'NONE', #66146, .T. ) ;
#34709=CARTESIAN_POINT ( 'NONE',  ( 16.39999999347100257, 3.345256695718999751, 11.86066175541999890 ) ) ;
#34714=B_SPLINE_CURVE_WITH_KNOTS ( 'NONE', 3,
 ( #27416, #22502, #54321, #44203 ),
 .UNSPECIFIED., .F., .F.,
 ( 4, 4 ),
 ( 0.000000000000000000, 1.000000000000000000 ),
 .UNSPECIFIED. ) ;
#34717=CARTESIAN_POINT ( 'NONE',  ( 15.83887202961200025, -8.726161303169000405, -7.661206663860999910 ) ) ;
#34742=CARTESIAN_POINT ( 'NONE',  ( 13.92975648157900004, -8.821327856274999490, -7.690719526968000430 ) ) ;
#34747=CARTESIAN_POINT ( 'NONE',  ( 18.22958618736246095, -11.12724485990815282, 3.450621024319162622 ) ) ;
#34755=CARTESIAN_POINT ( 'NONE',  ( 24.57709181747383909, 3.191966789821324646, 11.91258812936151479 ) ) ;
#34770=ORIENTED_EDGE ( 'NONE', *, *, #55884, .T. ) ;
#34788=ORIENTED_EDGE ( 'NONE', *, *, #61488, .F. ) ;
#34791=DIRECTION ( 'NONE',  ( 1.000000000000000000, 0.000000000000000000, 0.000000000000000000 ) ) ;
#34794=CARTESIAN_POINT ( 'NONE',  ( 23.68315217816700269, 9.987916080909998939, -9.401273449222999901 ) ) ;
#34795=CARTESIAN_POINT ( 'NONE',  ( 17.76427412810700091, -3.313981393620000215, -11.22406656470000108 ) ) ;
#34802=ADVANCED_FACE ( 'NONE', ( #59715 ), #41314, .F. ) ;
#34803=ADVANCED_FACE ( 'NONE', ( #59368 ), #43940, .F. ) ;
#34811=( BOUNDED_SURFACE ( )  B_SPLINE_SURFACE ( 3, 3, ( 
 ( #6621, #54520, #27960, #32510 ),
 ( #49269, #11860, #65693, #28297 ),
 ( #60458, #49618, #60114, #26923 ),
 ( #44040, #65345, #21659, #64987 ) ),
 .UNSPECIFIED., .F., .F., .T. ) 
 B_SPLINE_SURFACE_WITH_KNOTS ( ( 4, 4 ),
 ( 4, 4 ),
 ( 0.000000000000000000, 1.000000000000000000 ),
 ( 0.000000000000000000, 1.000000000000000000 ),
 .UNSPECIFIED. ) 
 GEOMETRIC_REPRESENTATION_ITEM ( )  RATIONAL_B_SPLINE_SURFACE ( (
 ( 1.512182578520000042, 1.160176301760999840, 1.160176301760999840, 1.512182578520000042),
 ( 1.111288591041000196, 0.8526025270081000196, 0.8526025270081000196, 1.111288591041000196),
 ( 1.111288591041000196, 0.8526025270081000196, 0.8526025270081000196, 1.111288591041000196),
 ( 1.512182578520000042, 1.160176301760999840, 1.160176301760999840, 1.512182578520000042) ) ) 
 REPRESENTATION_ITEM ( '' )  SURFACE ( )  );
#34812=DIRECTION ( 'NONE',  ( 1.000000000000000000, 0.000000000000000000, 0.000000000000000000 ) ) ;
#34820=AXIS2_PLACEMENT_3D ( 'NONE', #38544, #59867, #11972 ) ;
#34822=CARTESIAN_POINT ( 'NONE',  ( 24.53003472522700434, 3.319296498592000155, -12.04487452434999994 ) ) ;
#34833=ORIENTED_EDGE ( 'NONE', *, *, #12499, .F. ) ;
#34834=CARTESIAN_POINT ( 'NONE',  ( 16.39999999347100257, -3.345256695718999751, -11.86066175541999890 ) ) ;
#34840=CARTESIAN_POINT ( 'NONE',  ( 23.85396356904521298, -9.637273725658499046, -9.713123508487292668 ) ) ;
#34846=CARTESIAN_POINT ( 'NONE',  ( 23.91242816463300258, -12.75285422775000121, -3.592234604002999987 ) ) ;
#34849=ORIENTED_EDGE ( 'NONE', *, *, #29570, .T. ) ;
#34858=ORIENTED_EDGE ( 'NONE', *, *, #2778, .F. ) ;
#34865=CARTESIAN_POINT ( 'NONE',  ( 25.30000327618300204, -8.756202924575998026, -7.455126447192999883 ) ) ;
#34868=B_SPLINE_CURVE_WITH_KNOTS ( 'NONE', 3,
 ( #52121, #57363, #18002, #62276, #28850, #1919 ),
 .UNSPECIFIED., .F., .F.,
 ( 4, 1, 1, 4 ),
 ( 0.000000000000000000, 0.2305484670070869491, 0.8346924774606477859, 1.000000000000000000 ),
 .UNSPECIFIED. ) ;
#34872=CARTESIAN_POINT ( 'NONE',  ( 24.44496412535000118, -8.810486166165000910, -8.810507954003998776 ) ) ;
#34881=ADVANCED_FACE ( 'NONE', ( #29995 ), #12222, .F. ) ;
#34885=DIRECTION ( 'NONE',  ( 0.000000000000000000, -0.9624505444715651947, 0.2714570858282905341 ) ) ;
#34888=ADVANCED_FACE ( 'NONE', ( #61444 ), #13563, .F. ) ;
#34889=ADVANCED_FACE ( 'NONE', ( #23694 ), #30324, .F. ) ;
#34892=ORIENTED_EDGE ( 'NONE', *, *, #24564, .F. ) ;
#34898=ORIENTED_EDGE ( 'NONE', *, *, #44475, .F. ) ;
#34904=VERTEX_POINT ( 'NONE', #7964 ) ;
#34905=CARTESIAN_POINT ( 'NONE',  ( 11.64585080655600002, -3.555558855182999967, 11.95257446901999998 ) ) ;
#34906=EDGE_CURVE ( 'NONE', #37994, #31995, #14067, .T. ) ;
#34932=CARTESIAN_POINT ( 'NONE',  ( 24.63332939992940140, -2.078227417246087505, 11.31065739920066804 ) ) ;
#34936=ADVANCED_FACE ( 'NONE', ( #62464 ), #40587, .T. ) ;
#34939=CARTESIAN_POINT ( 'NONE',  ( 17.87616489729400371, -3.527537751923000009, -11.96092219328000006 ) ) ;
#34947=ORIENTED_EDGE ( 'NONE', *, *, #41232, .F. ) ;
#34948=ORIENTED_EDGE ( 'NONE', *, *, #37253, .T. ) ;
#34950=CARTESIAN_POINT ( 'NONE',  ( 25.29987654162099986, 8.533547811387000692, 7.925584028117998336 ) ) ;
#34952=CARTESIAN_POINT ( 'NONE',  ( 23.82002623614400250, -3.247612122070000051, 13.03939220338999938 ) ) ;
#34953=CARTESIAN_POINT ( 'NONE',  ( 13.26247400726061976, 11.68416116973912366, 1.976808445614457677 ) ) ;
#34955=DIRECTION ( 'NONE',  ( 0.000000000000000000, -0.9999606858717338120, 0.008867170401640296282 ) ) ;
#34956=B_SPLINE_CURVE_WITH_KNOTS ( 'NONE', 3,
 ( #61370, #67975, #67624, #19750 ),
 .UNSPECIFIED., .F., .F.,
 ( 4, 4 ),
 ( 0.000000000000000000, 1.000000000000000000 ),
 .UNSPECIFIED. ) ;
#34971=ORIENTED_EDGE ( 'NONE', *, *, #62182, .T. ) ;
#34978=CARTESIAN_POINT ( 'NONE',  ( 24.73255498974337385, 11.75901231425727289, 3.190944228439685837 ) ) ;
#34984=CARTESIAN_POINT ( 'NONE',  ( 12.45488131765549511, 11.84188428343392552, -3.380847681379787417 ) ) ;
#34985=AXIS2_PLACEMENT_3D ( 'NONE', #10330, #27807, #65531 ) ;
#34986=CARTESIAN_POINT ( 'NONE',  ( 12.57536348658395831, -11.53887048480306632, 4.871543742293778401 ) ) ;
#34989=CARTESIAN_POINT ( 'NONE',  ( 15.75262483093262844, 8.754898706353550608, 7.686019545158286448 ) ) ;
#34990=LINE ( 'NONE', #29410, #15189 ) ;
#34993=ORIENTED_EDGE ( 'NONE', *, *, #53040, .T. ) ;
#35002=CARTESIAN_POINT ( 'NONE',  ( 13.50003721581400029, -9.159934378815998812, -7.517910889891000537 ) ) ;
#35010=CARTESIAN_POINT ( 'NONE',  ( 18.49562053141631779, 2.998066116905866441, -12.16097201970168307 ) ) ;
#35020=CARTESIAN_POINT ( 'NONE',  ( 18.50003594167399967, 2.686563651857999613, 11.33603604486000016 ) ) ;
#35021=CARTESIAN_POINT ( 'NONE',  ( 44.24148000000000280, 2.258942858049999725, 12.29419282279000036 ) ) ;
#35022=DIRECTION ( 'NONE',  ( 0.000000000000000000, 0.9421243786071877846, 0.3352635608502959608 ) ) ;
#35025=FACE_OUTER_BOUND ( 'NONE', #50989, .T. ) ;
#35041=ORIENTED_EDGE ( 'NONE', *, *, #3463, .F. ) ;
#35044=EDGE_LOOP ( 'NONE', ( #31085, #809, #35373 ) ) ;
#35048=CARTESIAN_POINT ( 'NONE',  ( 23.52033604279600354, -3.098099968686999883, -13.78446056569000078 ) ) ;
#35056=DIRECTION ( 'NONE',  ( 0.000000000000000000, -1.000000000000000000, 0.000000000000000000 ) ) ;
#35062=CARTESIAN_POINT ( 'NONE',  ( 16.13712493497300215, -8.294738329384999886, -8.125890082391000746 ) ) ;
#35065=EDGE_LOOP ( 'NONE', ( #61628, #49534, #50768, #49308, #35041, #46068, #28542, #50700, #29522, #49432 ) ) ;
#35066=VECTOR ( 'NONE', #8631, 1000.000000000000114 ) ;
#35071=CARTESIAN_POINT ( 'NONE',  ( 23.56666365135700403, 11.16210620489000327, -3.571147223011999827 ) ) ;
#35073=CARTESIAN_POINT ( 'NONE',  ( 24.35365242081699932, 8.948887819865001703, -8.923422014301001681 ) ) ;
#35082=AXIS2_PLACEMENT_3D ( 'NONE', #6783, #12734, #23906 ) ;
#35090=CIRCLE ( 'NONE', #44016, 12.42499880353999941 ) ;
#35092=CARTESIAN_POINT ( 'NONE',  ( 23.65249378741842534, 13.39790967320782045, 3.829259155508669021 ) ) ;
#35094=CARTESIAN_POINT ( 'NONE',  ( 21.05000072320139992, -1.355183834107999921E-13, -12.47499939739999064 ) ) ;
#35095=CARTESIAN_POINT ( 'NONE',  ( 23.60000000000000142, -12.92130526834925242, -5.202888421357703130 ) ) ;
#35108=VERTEX_POINT ( 'NONE', #7192 ) ;
#35119=PRODUCT_DEFINITION ( 'UNKNOWN', '', #566, #63240 ) ;
#35120=CARTESIAN_POINT ( 'NONE',  ( 21.00000000000000000, 0.000000000000000000, 0.000000000000000000 ) ) ;
#35121=CARTESIAN_POINT ( 'NONE',  ( 24.41555930013399944, -12.00270549100999951, -3.255728780632000330 ) ) ;
#35123=ORIENTED_EDGE ( 'NONE', *, *, #62427, .T. ) ;
#35138=CARTESIAN_POINT ( 'NONE',  ( 25.47110272103000028, 8.417196128994998361, -7.979950812399000171 ) ) ;
#35141=CARTESIAN_POINT ( 'NONE',  ( 23.52062617334100025, 10.38635790624000066, -9.577244370524999439 ) ) ;
#35142=CARTESIAN_POINT ( 'NONE',  ( 17.79518154839200150, -3.190852234727000081, -11.45040960482999814 ) ) ;
#35156=B_SPLINE_CURVE_WITH_KNOTS ( 'NONE', 3,
 ( #10540, #42372, #37121, #26289, #68229, #9855, #15106, #31883, #25599, #46925 ),
 .UNSPECIFIED., .F., .F.,
 ( 4, 2, 2, 2, 4 ),
 ( 0.000000000000000000, 0.2500000000000029976, 0.3750000000000044964, 0.5000000000000059952, 1.000000000000000000 ),
 .UNSPECIFIED. ) ;
#35165=FACE_OUTER_BOUND ( 'NONE', #48707, .T. ) ;
#35168=ORIENTED_EDGE ( 'NONE', *, *, #65075, .T. ) ;
#35171=CARTESIAN_POINT ( 'NONE',  ( 13.46242637979000101, -11.63956415132000011, -2.420148064723000481 ) ) ;
#35176=EDGE_LOOP ( 'NONE', ( #2954, #27143, #40111, #66696 ) ) ;
#35177=FACE_OUTER_BOUND ( 'NONE', #35044, .T. ) ;
#35185=CARTESIAN_POINT ( 'NONE',  ( 15.90003771078200145, 3.695138809391000034, 11.25918926437999978 ) ) ;
#35187=ORIENTED_EDGE ( 'NONE', *, *, #11302, .T. ) ;
#35189=B_SPLINE_CURVE_WITH_KNOTS ( 'NONE', 3,
 ( #3745, #46759, #24400, #20178 ),
 .UNSPECIFIED., .F., .F.,
 ( 4, 4 ),
 ( 0.000000000000000000, 1.000000000000000000 ),
 .UNSPECIFIED. ) ;
#35195=B_SPLINE_CURVE_WITH_KNOTS ( 'NONE', 3,
 ( #65113, #17238, #11990, #54993 ),
 .UNSPECIFIED., .F., .F.,
 ( 4, 4 ),
 ( 0.000000000000000000, 1.000000000000000000 ),
 .UNSPECIFIED. ) ;
#35197=CARTESIAN_POINT ( 'NONE',  ( 23.71152188531511129, 13.14507144390817572, -3.853799391295626542 ) ) ;
#35199=B_SPLINE_CURVE_WITH_KNOTS ( 'NONE', 3,
 ( #35388, #51455, #46217, #66027 ),
 .UNSPECIFIED., .F., .F.,
 ( 4, 4 ),
 ( 0.000000000000000000, 1.000000000000000000 ),
 .UNSPECIFIED. ) ;
#35201=CARTESIAN_POINT ( 'NONE',  ( 24.14647681242191624, -3.326418506915634676, -12.48018534518304357 ) ) ;
#35215=CARTESIAN_POINT ( 'NONE',  ( 23.64695494181500379, 13.35841243503999820, 3.868091839254999886 ) ) ;
#35219=CARTESIAN_POINT ( 'NONE',  ( 15.55534550153200080, 9.119897322331999234, 8.232476562723000768 ) ) ;
#35221=CARTESIAN_POINT ( 'NONE',  ( 23.85399089423582453, 9.637233468683378490, 9.713115584480068065 ) ) ;
#35225=ADVANCED_FACE ( 'NONE', ( #9499 ), #1512, .T. ) ;
#35231=DIRECTION ( 'NONE',  ( 0.000000000000000000, 0.000000000000000000, -1.000000000000000000 ) ) ;
#35248=CARTESIAN_POINT ( 'NONE',  ( 25.59997774154300032, -2.856411620672000051, -11.13959722905999961 ) ) ;
#35249=ORIENTED_EDGE ( 'NONE', *, *, #13156, .T. ) ;
#35265=CARTESIAN_POINT ( 'NONE',  ( 14.93333333083533532, -8.833279250037012531, -7.896561129384960687 ) ) ;
#35266=FACE_OUTER_BOUND ( 'NONE', #25352, .T. ) ;
#35275=ORIENTED_EDGE ( 'NONE', *, *, #45255, .F. ) ;
#35281=CARTESIAN_POINT ( 'NONE',  ( 18.01722669115800102, -3.499390932422000056, -11.96939125376999868 ) ) ;
#35283=CARTESIAN_POINT ( 'NONE',  ( 24.60320129381999976, -8.810542265102998982, 9.295223627185000836 ) ) ;
#35291=ORIENTED_EDGE ( 'NONE', *, *, #11260, .F. ) ;
#35292=DIRECTION ( 'NONE',  ( -1.000000000000000000, 0.000000000000000000, 0.000000000000000000 ) ) ;
#35296=CARTESIAN_POINT ( 'NONE',  ( 24.52301136554485694, -8.782808807263306150, -8.926452893334182903 ) ) ;
#35297=DIRECTION ( 'NONE',  ( 1.000000000000000000, 0.000000000000000000, 0.000000000000000000 ) ) ;
#35298=CARTESIAN_POINT ( 'NONE',  ( 23.58444451512600182, -13.25737176886000057, 4.306335449404000038 ) ) ;
#35322=CIRCLE ( 'NONE', #48731, 0.9999999999999993339 ) ;
#35325=EDGE_CURVE ( 'NONE', #2511, #10719, #55113, .T. ) ;
#35327=CARTESIAN_POINT ( 'NONE',  ( 15.95563472374800185, -3.716697538693999991, -11.19594450203000058 ) ) ;
#35329=B_SPLINE_CURVE_WITH_KNOTS ( 'NONE', 3,
 ( #56948, #50681, #45775, #18865, #30386, #24103, #45435, #39497, #3119, #45093 ),
 .UNSPECIFIED., .F., .F.,
 ( 4, 2, 2, 2, 4 ),
 ( 0.000000000000000000, 0.1249999999280926311, 0.2499999998561852621, 0.3749999997842778932, 0.4999999997123705242 ),
 .UNSPECIFIED. ) ;
#35334=FACE_OUTER_BOUND ( 'NONE', #21081, .T. ) ;
#35336=ORIENTED_EDGE ( 'NONE', *, *, #1656, .T. ) ;
#35342=VERTEX_POINT ( 'NONE', #15705 ) ;
#35349=DIRECTION ( 'NONE',  ( -1.000000000000000000, 0.000000000000000000, 0.000000000000000000 ) ) ;
#35350=CARTESIAN_POINT ( 'NONE',  ( 11.29998636608000062, 3.695122995756999984, -11.25914041192000070 ) ) ;
#35354=CIRCLE ( 'NONE', #48766, 5.760713961201000544 ) ;
#35364=PLANE ( 'NONE',  #24212 ) ;
#35368=CARTESIAN_POINT ( 'NONE',  ( 11.79999999550100220, 3.351258778187000242, -11.15757272551999968 ) ) ;
#35373=ORIENTED_EDGE ( 'NONE', *, *, #20787, .T. ) ;
#35375=CARTESIAN_POINT ( 'NONE',  ( 18.49985170088394426, -7.837663500889314729E-14, -12.52499999999998792 ) ) ;
#35380=CARTESIAN_POINT ( 'NONE',  ( 13.69997185827400088, 10.10519270881758480, 5.872265061164083200 ) ) ;
#35384=EDGE_LOOP ( 'NONE', ( #62488, #19457, #48573, #68002 ) ) ;
#35385=PLANE ( 'NONE',  #7489 ) ;
#35386=DIRECTION ( 'NONE',  ( 5.840561064144232596E-06, 0.2588571483570100695, 0.9659156157296374667 ) ) ;
#35388=CARTESIAN_POINT ( 'NONE',  ( 13.99999999347100044, 9.187456302440001110, 8.213201953411001455 ) ) ;
#35399=CARTESIAN_POINT ( 'NONE',  ( 15.62410434383600055, -8.799879896029001003, -7.715564795277000343 ) ) ;
#35403=TOROIDAL_SURFACE ( 'NONE', #26459, 6.000000000000000000, 1.000000000000000000 ) ;
#35408=CARTESIAN_POINT ( 'NONE',  ( 23.58444974876299938, -2.899236306833000043, 13.63438999212000091 ) ) ;
#35409=CARTESIAN_POINT ( 'NONE',  ( 23.56666365135700403, 11.61524011578000604, -3.333188920255001353 ) ) ;
#35421=CARTESIAN_POINT ( 'NONE',  ( 23.60000000000000142, 0.000000000000000000, 0.000000000000000000 ) ) ;
#35424=DIRECTION ( 'NONE',  ( 0.000000000000000000, 0.000000000000000000, -1.000000000000000000 ) ) ;
#35428=CARTESIAN_POINT ( 'NONE',  ( 13.50542051561400214, -9.036698429651000453, -7.720610530813999617 ) ) ;
#35433=ORIENTED_EDGE ( 'NONE', *, *, #11422, .F. ) ;
#35438=FACE_OUTER_BOUND ( 'NONE', #24742, .T. ) ;
#35444=ORIENTED_EDGE ( 'NONE', *, *, #31104, .T. ) ;
#35448=B_SPLINE_CURVE_WITH_KNOTS ( 'NONE', 3,
 ( #36368, #41614, #20633, #31818 ),
 .UNSPECIFIED., .F., .F.,
 ( 4, 4 ),
 ( 0.000000000000000000, 1.000000000000000000 ),
 .UNSPECIFIED. ) ;
#35454=ORIENTED_EDGE ( 'NONE', *, *, #44943, .T. ) ;
#35458=CARTESIAN_POINT ( 'NONE',  ( 11.31919037786000182, -11.76444917719000038, -1.692529869092999961 ) ) ;
#35460=CARTESIAN_POINT ( 'NONE',  ( 24.26733149983100191, -12.18172987844000055, -3.303689625207000269 ) ) ;
#35480=CARTESIAN_POINT ( 'NONE',  ( 25.18904416930200085, 8.466527073521000091, -8.230891403741001255 ) ) ;
#35482=CARTESIAN_POINT ( 'NONE',  ( 18.53712493497300073, -2.638811780578999677, -11.30793729956000071 ) ) ;
#35491=DIRECTION ( 'NONE',  ( 0.000000000000000000, 0.2714570858282905341, -0.9624505444715651947 ) ) ;
#35498=DIRECTION ( 'NONE',  ( 0.000000000000000000, -0.3380467785883188858, -0.9411293085894520960 ) ) ;
#35503=CARTESIAN_POINT ( 'NONE',  ( 11.79999999550100220, -3.351258778187000242, 11.15757272551999968 ) ) ;
#35506=DIRECTION ( 'NONE',  ( -1.000000000000000000, 0.000000000000000000, 0.000000000000000000 ) ) ;
#35517=VERTEX_POINT ( 'NONE', #32141 ) ;
#35518=PLANE ( 'NONE',  #54074 ) ;
#35531=EDGE_CURVE ( 'NONE', #64134, #36266, #7365, .T. ) ;
#35535=B_SPLINE_CURVE_WITH_KNOTS ( 'NONE', 3,
 ( #5035, #63413, #42108, #15537, #62726, #31277, #15869, #20776 ),
 .UNSPECIFIED., .F., .F.,
 ( 4, 2, 2, 4 ),
 ( 0.000000000000000000, 0.4999999999999937828, 0.7499999999999968914, 1.000000000000000000 ),
 .UNSPECIFIED. ) ;
#35539=CARTESIAN_POINT ( 'NONE',  ( 23.91426378890381343, 12.84858547818794250, -3.562216227305645244 ) ) ;
#35541=CARTESIAN_POINT ( 'NONE',  ( 24.15455626517813670, -3.324392337986376678, -12.46571004933703719 ) ) ;
#35546=ORIENTED_EDGE ( 'NONE', *, *, #60451, .F. ) ;
#35550=FACE_OUTER_BOUND ( 'NONE', #62099, .T. ) ;
#35553=EDGE_CURVE ( 'NONE', #57489, #47653, #24956, .T. ) ;
#35556=CARTESIAN_POINT ( 'NONE',  ( 23.51695493258000269, 13.43892003569000160, 4.372923714577000354 ) ) ;
#35558=AXIS2_PLACEMENT_3D ( 'NONE', #55514, #3392, #2715 ) ;
#35561=CARTESIAN_POINT ( 'NONE',  ( 16.13494720760600032, 9.102952917978999636, 8.658486291235998777 ) ) ;
#35571=DIRECTION ( 'NONE',  ( 0.000000000000000000, 0.9659258262890757507, -0.2588190451024934835 ) ) ;
#35573=CARTESIAN_POINT ( 'NONE',  ( 23.61990774387100345, 10.21722221107000017, 9.338757681905001107 ) ) ;
#35578=FACE_OUTER_BOUND ( 'NONE', #7148, .T. ) ;
#35585=ADVANCED_FACE ( 'NONE', ( #32817 ), #28422, .F. ) ;
#35592=CARTESIAN_POINT ( 'NONE',  ( 25.60000000000000142, 11.77655473258999841, 4.190794510628000680 ) ) ;
#35593=ORIENTED_EDGE ( 'NONE', *, *, #46572, .T. ) ;
#35599=VERTEX_POINT ( 'NONE', #39442 ) ;
#35603=CARTESIAN_POINT ( 'NONE',  ( 25.60000000000000142, 0.000000000000000000, 0.000000000000000000 ) ) ;
#35605=ORIENTED_EDGE ( 'NONE', *, *, #57123, .T. ) ;
#35616=ORIENTED_EDGE ( 'NONE', *, *, #51055, .T. ) ;
#35641=CARTESIAN_POINT ( 'NONE',  ( 23.64082968872000023, -13.18734614699999952, 4.071470701135999626 ) ) ;
#35644=ORIENTED_EDGE ( 'NONE', *, *, #29251, .F. ) ;
#35654=CARTESIAN_POINT ( 'NONE',  ( 11.48394322905000031, -3.487217528443999903, 11.17162453992000160 ) ) ;
#35655=ORIENTED_EDGE ( 'NONE', *, *, #57971, .T. ) ;
#35662=VERTEX_POINT ( 'NONE', #19283 ) ;
#35666=CARTESIAN_POINT ( 'NONE',  ( 13.73854177342199989, -9.465667024606000624, -8.118361260918998568 ) ) ;
#35672=CARTESIAN_POINT ( 'NONE',  ( 25.10992574103807229, -11.36603783439706916, 3.264548188536176010 ) ) ;
#35683=EDGE_LOOP ( 'NONE', ( #20458, #26002, #34241, #42220 ) ) ;
#35690=CARTESIAN_POINT ( 'NONE',  ( 18.49995202021990082, 2.953582884394188479, -12.17185907300008907 ) ) ;
#35693=VERTEX_POINT ( 'NONE', #50764 ) ;
#35710=ORIENTED_EDGE ( 'NONE', *, *, #3707, .F. ) ;
#35722=CARTESIAN_POINT ( 'NONE',  ( 25.39994675557665005, 2.060146035114244878, -11.21225038255773043 ) ) ;
#35724=AXIS2_PLACEMENT_3D ( 'NONE', #264, #58647, #10748 ) ;
#35728=CARTESIAN_POINT ( 'NONE',  ( 23.59999999999999787, 12.52456229676467103, -6.096442089472905224 ) ) ;
#35731=CARTESIAN_POINT ( 'NONE',  ( 19.99999987597299977, 0.000000000000000000, 5.040412531797999279E-14 ) ) ;
#35732=B_SPLINE_CURVE_WITH_KNOTS ( 'NONE', 3,
 ( #62584, #35690, #35010, #61565, #24510, #56326, #41615, #9106, #14706, #29776, #30444, #51756, #36023, #57338 ),
 .UNSPECIFIED., .F., .F.,
 ( 4, 2, 2, 2, 2, 2, 4 ),
 ( 0.000000000000000000, 0.1250000000000010270, 0.2500000000000020539, 0.5000000000000017764, 0.6250000000000012212, 0.7500000000000006661, 1.000000000000000000 ),
 .UNSPECIFIED. ) ;
#35740=CARTESIAN_POINT ( 'NONE',  ( 23.57173046905473868, -13.34896468215902843, 4.180125146958469706 ) ) ;
#35745=CARTESIAN_POINT ( 'NONE',  ( 23.58303186465700207, -2.940599899367999814, 13.62861925944999975 ) ) ;
#35746=ADVANCED_FACE ( 'NONE', ( #31500 ), #67856, .T. ) ;
#35748=CARTESIAN_POINT ( 'NONE',  ( 23.89320776801300283, 12.21745654473000542, -3.256241354580001524 ) ) ;
#35750=CARTESIAN_POINT ( 'NONE',  ( 44.24148000000000280, 11.77655473258999841, 4.190794510628000680 ) ) ;
#35755=DIRECTION ( 'NONE',  ( 0.000000000000000000, 0.9867381147929490393, 0.1623203401144079905 ) ) ;
#35763=CARTESIAN_POINT ( 'NONE',  ( 24.67333021737300314, 12.15929973297999922, 3.026485043723000423 ) ) ;
#35769=EDGE_CURVE ( 'NONE', #7194, #15848, #51760, .T. ) ;
#35771=CARTESIAN_POINT ( 'NONE',  ( 18.01256889503379099, -11.20125638878304208, 3.203298770433383513 ) ) ;
#35773=ORIENTED_EDGE ( 'NONE', *, *, #17138, .T. ) ;
#35779=CARTESIAN_POINT ( 'NONE',  ( 18.33131097849702229, 3.122881743061651783, -11.22368843778023439 ) ) ;
#35780=CARTESIAN_POINT ( 'NONE',  ( 13.50006915090078152, 9.429349056561928677, 7.934633652400466808 ) ) ;
#35790=( NAMED_UNIT ( * ) SI_UNIT ( $, .STERADIAN. ) SOLID_ANGLE_UNIT ( ) );
#35795=CARTESIAN_POINT ( 'NONE',  ( 16.13125657743222519, 3.735736757533928198, 11.95504925863862411 ) ) ;
#35798=CARTESIAN_POINT ( 'NONE',  ( 25.59997036749100374, 2.856417224717999748, 11.13959153667999935 ) ) ;
#35803=CARTESIAN_POINT ( 'NONE',  ( 18.30000000000000071, -2.818741034879777008, 11.83575128182368452 ) ) ;
#35809=ORIENTED_EDGE ( 'NONE', *, *, #17755, .T. ) ;
#35813=FACE_OUTER_BOUND ( 'NONE', #19709, .T. ) ;
#35814=CARTESIAN_POINT ( 'NONE',  ( 24.33654939907400205, 8.941170855541997753, -9.047257172721998586 ) ) ;
#35825=CARTESIAN_POINT ( 'NONE',  ( 25.39994675514505218, -2.060146016733654939, 11.21225038637377303 ) ) ;
#35827=CYLINDRICAL_SURFACE ( 'NONE', #67782, 1.000000000000000222 ) ;
#35832=CARTESIAN_POINT ( 'NONE',  ( 17.60000000798000386, 11.41069016990000051, -4.623987642516999230 ) ) ;
#35841=ORIENTED_EDGE ( 'NONE', *, *, #63645, .T. ) ;
#35846=CARTESIAN_POINT ( 'NONE',  ( 12.96937411412500119, -11.64648275985999959, -1.863025408066000033 ) ) ;
#35851=ORIENTED_EDGE ( 'NONE', *, *, #36133, .F. ) ;
#35852=CIRCLE ( 'NONE', #62636, 1.000000000000000444 ) ;
#35855=CARTESIAN_POINT ( 'NONE',  ( 15.91386961183700244, 8.663061527162000175, 7.870519177131000355 ) ) ;
#35857=CARTESIAN_POINT ( 'NONE',  ( 16.39999999439439549, 3.511866690759578802, 11.95216930658972032 ) ) ;
#35868=EDGE_LOOP ( 'NONE', ( #59982, #1985, #68637, #16935 ) ) ;
#35879=VERTEX_POINT ( 'NONE', #17043 ) ;
#35886=CARTESIAN_POINT ( 'NONE',  ( 16.86666666157666583, -3.216308280197300196, -11.40341444503674850 ) ) ;
#35887=CARTESIAN_POINT ( 'NONE',  ( 21.72233714749290101, 0.000000000000000000, 5.000000000000000000 ) ) ;
#35889=VERTEX_POINT ( 'NONE', #48525 ) ;
#35892=CARTESIAN_POINT ( 'NONE',  ( 15.39165415090800337, 9.395515400280999074, 8.199438574490999443 ) ) ;
#35898=CARTESIAN_POINT ( 'NONE',  ( 25.26979939644500206, -11.11691833729999779, 3.473712811964000391 ) ) ;
#35903=CARTESIAN_POINT ( 'NONE',  ( 24.53429014662800256, -8.855930250654999725, 9.286429702500999639 ) ) ;
#35904=CARTESIAN_POINT ( 'NONE',  ( 23.83545958851000179, 9.657130125948000909, 9.482575700297999788 ) ) ;
#35907=EDGE_CURVE ( 'NONE', #7406, #5174, #29926, .T. ) ;
#35908=B_SPLINE_CURVE_WITH_KNOTS ( 'NONE', 3,
 ( #19707, #41027, #62350, #8183 ),
 .UNSPECIFIED., .F., .F.,
 ( 4, 4 ),
 ( 0.000000000000000000, 1.000000000000000000 ),
 .UNSPECIFIED. ) ;
#35909=EDGE_CURVE ( 'NONE', #21396, #47463, #61846, .T. ) ;
#35920=CARTESIAN_POINT ( 'NONE',  ( 25.37956555325600405, -8.342521218007666661, 8.311507340610738481 ) ) ;
#35923=CARTESIAN_POINT ( 'NONE',  ( 14.93333333119166717, 9.187454790032710150, 8.213178404203523186 ) ) ;
#35930=ORIENTED_EDGE ( 'NONE', *, *, #12840, .F. ) ;
#35932=CARTESIAN_POINT ( 'NONE',  ( 25.60000000000000142, -11.77655473258999841, 4.190794510628000680 ) ) ;
#35952=LINE ( 'NONE', #30712, #28817 ) ;
#35953=CARTESIAN_POINT ( 'NONE',  ( 18.04816728597000264, -3.610133590554000182, -12.03375048192000207 ) ) ;
#35960=EDGE_LOOP ( 'NONE', ( #18363, #44617, #49824, #39337, #53397, #29008 ) ) ;
#35967=CIRCLE ( 'NONE', #43810, 0.6999999999999992895 ) ;
#35968=CARTESIAN_POINT ( 'NONE',  ( 17.77423364829699892, 3.297060500158999652, -11.83473586442999981 ) ) ;
#35969=EDGE_CURVE ( 'NONE', #20236, #16591, #11441, .T. ) ;
#35979=CARTESIAN_POINT ( 'NONE',  ( 25.08547572896300082, 8.543211284141001727, 8.155294727984999881 ) ) ;
#35995=VECTOR ( 'NONE', #32720, 1000.000000000000114 ) ;
#35996=EDGE_CURVE ( 'NONE', #26398, #5569, #39768, .T. ) ;
#35998=CARTESIAN_POINT ( 'NONE',  ( 11.43328525708585452, -3.653536053513362525, 11.13242455109463869 ) ) ;
#36003=CARTESIAN_POINT ( 'NONE',  ( 13.99999999379500082, -8.815218614167999789, -7.616697584347000394 ) ) ;
#36011=DIRECTION ( 'NONE',  ( 0.000000000000000000, 0.000000000000000000, -1.000000000000000000 ) ) ;
#36015=VERTEX_POINT ( 'NONE', #60736 ) ;
#36022=CARTESIAN_POINT ( 'NONE',  ( 24.12728201901689573, -3.330896228204782705, 12.51463748290429479 ) ) ;
#36023=CARTESIAN_POINT ( 'NONE',  ( 17.89107826690647940, 3.595094513005142822, -11.99795484439389170 ) ) ;
#36025=CARTESIAN_POINT ( 'NONE',  ( 25.41677544510499942, -2.809827979128999953, -11.31866138444999770 ) ) ;
#36030=CARTESIAN_POINT ( 'NONE',  ( 23.59999176271200128, 13.22318677037999812, 4.267778497637999102 ) ) ;
#36031=VERTEX_POINT ( 'NONE', #34533 ) ;
#36047=CARTESIAN_POINT ( 'NONE',  ( 25.10986374740704008, 11.36610807887094943, -3.264518009230023221 ) ) ;
#36064=CARTESIAN_POINT ( 'NONE',  ( 16.03328789001813703, -8.397841793663575416, -8.170414199808828215 ) ) ;
#36071=DIRECTION ( 'NONE',  ( 1.000000000000000000, 0.000000000000000000, 0.000000000000000000 ) ) ;
#36072=EDGE_CURVE ( 'NONE', #19330, #31999, #24023, .T. ) ;
#36079=ADVANCED_FACE ( 'NONE', ( #66666 ), #40116, .F. ) ;
#36088=FACE_OUTER_BOUND ( 'NONE', #38899, .T. ) ;
#36090=CIRCLE ( 'NONE', #19371, 11.50000000000000533 ) ;
#36099=DIRECTION ( 'NONE',  ( 0.000000000000000000, 0.1807154286440004198, 0.9835354258236025382 ) ) ;
#36101=CARTESIAN_POINT ( 'NONE',  ( 24.56666037493200250, 12.04830180860999889, 3.140564670074999842 ) ) ;
#36104=CARTESIAN_POINT ( 'NONE',  ( 13.75961700471900073, -8.905065757320999253, -7.452879173751000508 ) ) ;
#36105=CARTESIAN_POINT ( 'NONE',  ( 23.60000000000000142, -2.258942858049999725, -12.29419282279000036 ) ) ;
#36111=FACE_OUTER_BOUND ( 'NONE', #30303, .T. ) ;
#36122=ORIENTED_EDGE ( 'NONE', *, *, #2406, .F. ) ;
#36123=CARTESIAN_POINT ( 'NONE',  ( 13.55458079702099994, 9.509022223680998920, 7.924557572090001223 ) ) ;
#36132=CARTESIAN_POINT ( 'NONE',  ( 16.39999999485600313, 3.595156957901000094, 11.99794989424000136 ) ) ;
#36133=EDGE_CURVE ( 'NONE', #35662, #37068, #5617, .T. ) ;
#36134=EDGE_CURVE ( 'NONE', #44042, #10297, #28172, .T. ) ;
#36135=CARTESIAN_POINT ( 'NONE',  ( 24.54688887196200042, -12.52317552374000087, -3.000792222368999784 ) ) ;
#36153=CARTESIAN_POINT ( 'NONE',  ( 24.14647126608543459, 3.326442287260038988, 12.48027977927276311 ) ) ;
#36160=ORIENTED_EDGE ( 'NONE', *, *, #14993, .F. ) ;
#36164=DIRECTION ( 'NONE',  ( 1.000000000000000000, 0.000000000000000000, 0.000000000000000000 ) ) ;
#36175=CARTESIAN_POINT ( 'NONE',  ( 25.49995777816882025, -10.64590202376374251, -3.788441483803001830 ) ) ;
#36177=ORIENTED_EDGE ( 'NONE', *, *, #27327, .F. ) ;
#36180=ADVANCED_FACE ( 'NONE', ( #40440 ), #25014, .T. ) ;
#36181=CARTESIAN_POINT ( 'NONE',  ( 16.10005255078199937, 3.632778330393000132, 11.06917548872000090 ) ) ;
#36187=CARTESIAN_POINT ( 'NONE',  ( 13.69055856039300068, -11.42191202915999781, -2.091365271848000251 ) ) ;
#36190=VERTEX_POINT ( 'NONE', #35887 ) ;
#36195=CARTESIAN_POINT ( 'NONE',  ( 15.83887202961200025, 8.726161303169000405, 7.661206663860999910 ) ) ;
#36197=CARTESIAN_POINT ( 'NONE',  ( 23.58296120034879451, 10.22496133173016730, 9.539120963660936425 ) ) ;
#36202=DIRECTION ( 'NONE',  ( -1.000000000000000000, 0.000000000000000000, 0.000000000000000000 ) ) ;
#36212=CARTESIAN_POINT ( 'NONE',  ( 23.59112020737914506, -10.18869760917455736, 9.572450890279778690 ) ) ;
#36213=CARTESIAN_POINT ( 'NONE',  ( 23.97708749418018570, 12.74918579704523935, -3.497816719186660261 ) ) ;
#36217=FACE_OUTER_BOUND ( 'NONE', #44493, .T. ) ;
#36236=EDGE_CURVE ( 'NONE', #6697, #56117, #33128, .T. ) ;
#36237=CARTESIAN_POINT ( 'NONE',  ( 24.53429010490700080, 8.855930189872001534, 9.286429716155000236 ) ) ;
#36255=CARTESIAN_POINT ( 'NONE',  ( 18.53682146000800302, 2.876943948391000205, 12.22927217127999988 ) ) ;
#36261=CARTESIAN_POINT ( 'NONE',  ( 24.30001129978747443, 3.256147844935088909, -12.15210919425762803 ) ) ;
#36266=VERTEX_POINT ( 'NONE', #4056 ) ;
#36272=ORIENTED_EDGE ( 'NONE', *, *, #25190, .T. ) ;
#36275=ORIENTED_EDGE ( 'NONE', *, *, #15946, .F. ) ;
#36277=CARTESIAN_POINT ( 'NONE',  ( 25.60000000000000142, 2.023980670379999847, 11.01542190082000161 ) ) ;
#36293=CARTESIAN_POINT ( 'NONE',  ( 18.50003594167399967, 2.686563651857999613, 11.33603604486000016 ) ) ;
#36294=CARTESIAN_POINT ( 'NONE',  ( 17.73974579646600347, -12.04854797699000102, 3.202106586035000202 ) ) ;
#36295=CARTESIAN_POINT ( 'NONE',  ( 23.58894640129908993, -13.38207337446602629, -4.048532477468460122 ) ) ;
#36299=EDGE_CURVE ( 'NONE', #44907, #60364, #20612, .T. ) ;
#36302=EDGE_LOOP ( 'NONE', ( #11470, #67361, #44655, #61845 ) ) ;
#36303=B_SPLINE_CURVE_WITH_KNOTS ( 'NONE', 3,
 ( #13680, #12993, #18231, #60532, #61226, #50735 ),
 .UNSPECIFIED., .F., .F.,
 ( 4, 2, 4 ),
 ( 0.000000000000000000, 0.5000000000000000000, 1.000000000000000000 ),
 .UNSPECIFIED. ) ;
#36306=DIRECTION ( 'NONE',  ( 0.000000000000000000, -1.000000000000000000, 0.000000000000000000 ) ) ;
#36329=B_SPLINE_CURVE_WITH_KNOTS ( 'NONE', 3,
 ( #1123, #43436, #64731, #16163 ),
 .UNSPECIFIED., .F., .F.,
 ( 4, 4 ),
 ( 0.000000000000000000, 1.000000000000000000 ),
 .UNSPECIFIED. ) ;
#36331=FACE_OUTER_BOUND ( 'NONE', #35868, .T. ) ;
#36332=ORIENTED_EDGE ( 'NONE', *, *, #56829, .F. ) ;
#36337=CARTESIAN_POINT ( 'NONE',  ( 18.29999330150736014, 11.02846243710159868, -3.754394858750199848 ) ) ;
#36344=CARTESIAN_POINT ( 'NONE',  ( 11.26396921949000074, 3.857819209177999920, -11.66658462090000015 ) ) ;
#36345=CARTESIAN_POINT ( 'NONE',  ( 24.30000000000000071, -2.258942858049999725, 12.29419282279000036 ) ) ;
#36347=CARTESIAN_POINT ( 'NONE',  ( 21.72233714749290101, -4.999803429358669504, 0.04433585200820151090 ) ) ;
#36352=ORIENTED_EDGE ( 'NONE', *, *, #51855, .F. ) ;
#36358=VECTOR ( 'NONE', #68218, 1000.000000000000227 ) ;
#36359=CARTESIAN_POINT ( 'NONE',  ( 24.38453493561400265, 3.342915742751000341, 12.19240510248000042 ) ) ;
#36368=CARTESIAN_POINT ( 'NONE',  ( 17.80000000001300009, -3.351264566333000072, -11.15757590352999884 ) ) ;
#36369=CARTESIAN_POINT ( 'NONE',  ( 24.30001680106099826, 12.21047197645999915, -3.271805488357999891 ) ) ;
#36371=CARTESIAN_POINT ( 'NONE',  ( 24.44496356267099912, -8.810485190366000197, 8.810508100388000585 ) ) ;
#36374=ORIENTED_EDGE ( 'NONE', *, *, #60838, .T. ) ;
#36378=CARTESIAN_POINT ( 'NONE',  ( 12.40000000000000213, 12.27510221496999954, 1.916289661941000144 ) ) ;
#36390=ORIENTED_EDGE ( 'NONE', *, *, #53040, .F. ) ;
#36391=B_SPLINE_CURVE_WITH_KNOTS ( 'NONE', 3,
 ( #39482, #7664, #29010, #50317 ),
 .UNSPECIFIED., .F., .F.,
 ( 4, 4 ),
 ( 0.000000000000000000, 1.000000000000000000 ),
 .UNSPECIFIED. ) ;
#36392=CARTESIAN_POINT ( 'NONE',  ( 24.94498139921191893, -2.983199262474947488, 11.60459641112071871 ) ) ;
#36393=FACE_OUTER_BOUND ( 'NONE', #66661, .T. ) ;
#36394=CARTESIAN_POINT ( 'NONE',  ( 24.89076865818686812, 8.576159828362898807, 8.441116150885008551 ) ) ;
#36402=CARTESIAN_POINT ( 'NONE',  ( 24.35145719007200071, 8.929422700512001043, 9.054903155755001265 ) ) ;
#36410=TOROIDAL_SURFACE ( 'NONE', #53134, 6.000000000000000000, 1.000000000000000000 ) ;
#36417=CARTESIAN_POINT ( 'NONE',  ( 12.33432433144330354, 11.58110100107862728, -4.770114854518291203 ) ) ;
#36422=FACE_OUTER_BOUND ( 'NONE', #1828, .T. ) ;
#36431=CARTESIAN_POINT ( 'NONE',  ( 24.30000000000000071, 3.224868684338999980, 12.03537377768999939 ) ) ;
#36432=ORIENTED_EDGE ( 'NONE', *, *, #28020, .F. ) ;
#36435=DIRECTION ( 'NONE',  ( 1.000000000000000000, 0.000000000000000000, 0.000000000000000000 ) ) ;
#36438=LINE ( 'NONE', #52516, #66747 ) ;
#36441=EDGE_CURVE ( 'NONE', #48090, #15819, #3713, .T. ) ;
#36445=CARTESIAN_POINT ( 'NONE',  ( 24.44496356267099912, -8.810485190366000197, 8.810508100388000585 ) ) ;
#36453=EDGE_LOOP ( 'NONE', ( #38292, #27127, #599, #17784 ) ) ;
#36454=CONICAL_SURFACE ( 'NONE', #30922, 1.150084366273999903, 0.7854618604947302130 ) ;
#36455=CARTESIAN_POINT ( 'NONE',  ( 24.30000000000000071, 8.756202924575998026, 7.455126447192999883 ) ) ;
#36460=CARTESIAN_POINT ( 'NONE',  ( 17.92913687513144794, 3.216295279492275672, -11.40344415250779520 ) ) ;
#36465=FACE_OUTER_BOUND ( 'NONE', #26683, .T. ) ;
#36474=CARTESIAN_POINT ( 'NONE',  ( 11.35179910620000143, -11.71014626380999957, -1.422059914427000082 ) ) ;
#36477=ORIENTED_EDGE ( 'NONE', *, *, #43571, .T. ) ;
#36478=CARTESIAN_POINT ( 'NONE',  ( 11.86287780003600112, 11.93788271774999998, -3.912105503483000124 ) ) ;
#36479=CARTESIAN_POINT ( 'NONE',  ( 17.71880694038500437, 12.04903009916999856, -3.200100868470999949 ) ) ;
#36506=LINE ( 'NONE', #14843, #64869 ) ;
#36507=VECTOR ( 'NONE', #41693, 1000.000000000000000 ) ;
#36510=CARTESIAN_POINT ( 'NONE',  ( 15.86222979673600264, -3.623677739266000231, -11.32125985288999992 ) ) ;
#36512=DIRECTION ( 'NONE',  ( 0.000000000000000000, 0.000000000000000000, -1.000000000000000000 ) ) ;
#36515=CARTESIAN_POINT ( 'NONE',  ( 18.50013789939208664, 2.065999734462983189E-14, -11.64999999999999325 ) ) ;
#36518=ORIENTED_EDGE ( 'NONE', *, *, #2221, .T. ) ;
#36527=CARTESIAN_POINT ( 'NONE',  ( 18.30017264560542145, -1.838307228410961613, -11.74271423071413523 ) ) ;
#36531=CARTESIAN_POINT ( 'NONE',  ( 13.64382898362900143, -11.47858090575000034, -2.288513382665999796 ) ) ;
#36533=CARTESIAN_POINT ( 'NONE',  ( 13.06531638133300177, 12.22210578456000007, 1.955102404769999858 ) ) ;
#36538=CARTESIAN_POINT ( 'NONE',  ( 16.10004050617000004, 3.886235259787000018, 11.90683839252000098 ) ) ;
#36542=CARTESIAN_POINT ( 'NONE',  ( 23.58820312822635756, 10.20123823674837382, 9.561024946571489380 ) ) ;
#36550=CARTESIAN_POINT ( 'NONE',  ( 21.70000133425200062, 0.000000000000000000, 0.000000000000000000 ) ) ;
#36554=AXIS2_PLACEMENT_3D ( 'NONE', #48396, #36883, #15888 ) ;
#36558=CARTESIAN_POINT ( 'NONE',  ( 24.22565383484945656, 12.33873734749843187, -3.306152860255493930 ) ) ;
#36561=DIRECTION ( 'NONE',  ( -1.000000000000000000, 0.000000000000000000, 0.000000000000000000 ) ) ;
#36568=ORIENTED_EDGE ( 'NONE', *, *, #47750, .T. ) ;
#36573=CARTESIAN_POINT ( 'NONE',  ( 25.41679837370699957, 2.809785212777999863, 11.31864426913000088 ) ) ;
#36575=CARTESIAN_POINT ( 'NONE',  ( 25.30000327618300204, 10.36736154742122018, -5.168041346173460227 ) ) ;
#36578=EDGE_CURVE ( 'NONE', #16464, #35599, #46501, .T. ) ;
#36579=CARTESIAN_POINT ( 'NONE',  ( 12.83523642498299999, -11.49802605210000195, 4.818062943702999590 ) ) ;
#36585=CARTESIAN_POINT ( 'NONE',  ( 24.35365242081700288, -3.193712117558000774, -11.49150331547998860 ) ) ;
#36595=FACE_OUTER_BOUND ( 'NONE', #35065, .T. ) ;
#36596=ORIENTED_EDGE ( 'NONE', *, *, #57794, .F. ) ;
#36602=AXIS2_PLACEMENT_3D ( 'NONE', #47359, #38232, #16219 ) ;
#36607=EDGE_CURVE ( 'NONE', #12790, #16879, #29804, .T. ) ;
#36611=CARTESIAN_POINT ( 'NONE',  ( 13.73125687463581102, -9.567603210565605920, -8.083310008166920468 ) ) ;
#36614=CARTESIAN_POINT ( 'NONE',  ( 11.50001496185000249, 12.52499999999999680, -1.310230436094052653 ) ) ;
#36626=CARTESIAN_POINT ( 'NONE',  ( 25.60000000000000142, -3.623466631435000362, 13.52296156804999860 ) ) ;
#36637=ORIENTED_EDGE ( 'NONE', *, *, #50851, .T. ) ;
#36645=CARTESIAN_POINT ( 'NONE',  ( 17.80000000000000071, 13.72414332887999855, -50.50083396221000243 ) ) ;
#36648=AXIS2_PLACEMENT_3D ( 'NONE', #39255, #37869, #17936 ) ;
#36650=CARTESIAN_POINT ( 'NONE',  ( 18.01911383345317930, 3.562435417626197420, 12.00770609665305066 ) ) ;
#36654=ORIENTED_EDGE ( 'NONE', *, *, #45969, .T. ) ;
#36666=ORIENTED_EDGE ( 'NONE', *, *, #18509, .T. ) ;
#36671=CARTESIAN_POINT ( 'NONE',  ( 23.64973524161407425, -10.02113549012734417, -9.687121459438744253 ) ) ;
#36685=DIRECTION ( 'NONE',  ( 0.000000000000000000, 0.001239076634196941687, -0.9999992323442525866 ) ) ;
#36692=AXIS2_PLACEMENT_3D ( 'NONE', #8709, #8370, #13622 ) ;
#36695=CARTESIAN_POINT ( 'NONE',  ( 13.67057712374000289, -9.352787036275000077, -8.106596622149000453 ) ) ;
#36702=CARTESIAN_POINT ( 'NONE',  ( 24.71770621865795192, -11.77375252400051231, 3.190797026286958271 ) ) ;
#36708=CARTESIAN_POINT ( 'NONE',  ( 13.69992376746900042, 12.26631831379999937, 2.532779022035999805 ) ) ;
#36711=DIRECTION ( 'NONE',  ( 0.000000000000000000, -0.1807154286440004198, -0.9835354258236025382 ) ) ;
#36712=CARTESIAN_POINT ( 'NONE',  ( 23.91242875217100305, 3.265460742156999885, 12.84041179270000121 ) ) ;
#36713=EDGE_LOOP ( 'NONE', ( #24052, #46723, #8208, #50824 ) ) ;
#36714=FACE_OUTER_BOUND ( 'NONE', #59327, .T. ) ;
#36724=EDGE_CURVE ( 'NONE', #5569, #49580, #25685, .T. ) ;
#36725=CARTESIAN_POINT ( 'NONE',  ( 24.87547482180800174, -2.962908632962999889, -11.62664876782000078 ) ) ;
#36732=CARTESIAN_POINT ( 'NONE',  ( 24.30000000000000071, -12.03537377768999939, 3.224868684338999980 ) ) ;
#36749=CARTESIAN_POINT ( 'NONE',  ( 13.69997185827400266, 11.40547114375999982, 2.374390024598000082 ) ) ;
#36754=VERTEX_POINT ( 'NONE', #643 ) ;
#36755=CARTESIAN_POINT ( 'NONE',  ( 24.36809152945900081, 8.862862741694000235, 8.808753452432000586 ) ) ;
#36757=CARTESIAN_POINT ( 'NONE',  ( 13.00000000001300116, 11.52577654661000039, 1.696746661728000038 ) ) ;
#36762=CARTESIAN_POINT ( 'NONE',  ( 18.40015514469800095, 2.597921877622999464E-14, 2.051692149506999743E-13 ) ) ;
#36766=CARTESIAN_POINT ( 'NONE',  ( 12.44187590071328131, 11.55958658085554980, -4.822001495576104801 ) ) ;
#36769=CARTESIAN_POINT ( 'NONE',  ( 18.21067574918971843, -11.77411897367713323, 3.633863173939181568 ) ) ;
#36770=CARTESIAN_POINT ( 'NONE',  ( 17.80000000005199823, 3.345268251980999974, -11.86064071431999878 ) ) ;
#36771=PLANE ( 'NONE',  #5099 ) ;
#36780=CARTESIAN_POINT ( 'NONE',  ( 23.61702258298599943, 2.916534779610000072, -13.53539279049999955 ) ) ;
#36787=CARTESIAN_POINT ( 'NONE',  ( 25.37954957502917708, 3.026737125307685350, 11.38060389463865363 ) ) ;
#36798=CARTESIAN_POINT ( 'NONE',  ( 18.30003129334700063, 2.732683817159999862, -11.53064095410000078 ) ) ;
#36799=CARTESIAN_POINT ( 'NONE',  ( 23.79452173965752948, 9.731929379560703808, -9.426968994335380714 ) ) ;
#36811=ADVANCED_FACE ( 'NONE', ( #49218 ), #66386, .F. ) ;
#36813=CARTESIAN_POINT ( 'NONE',  ( 18.02331223755004785, 3.318306765095501820, -11.16743751352750991 ) ) ;
#36814=CARTESIAN_POINT ( 'NONE',  ( 17.60000000000000142, 52.95171880992000268, -18.02623547589999831 ) ) ;
#36820=CARTESIAN_POINT ( 'NONE',  ( 25.29987931604000195, 11.13052921044000065, -3.427478701325000099 ) ) ;
#36825=( NAMED_UNIT ( * ) PLANE_ANGLE_UNIT ( ) SI_UNIT ( $, .RADIAN. ) );
#36826=ORIENTED_EDGE ( 'NONE', *, *, #68833, .F. ) ;
#36827=CARTESIAN_POINT ( 'NONE',  ( 11.79999999550100220, -11.52577121388000059, -1.696750555870000010 ) ) ;
#36831=CARTESIAN_POINT ( 'NONE',  ( 13.55377458794190737, -8.990344585381047082, -7.716059257659925841 ) ) ;
#36833=CARTESIAN_POINT ( 'NONE',  ( 12.82792991967100171, 11.81434786598999942, -3.324782598720999793 ) ) ;
#36835=CARTESIAN_POINT ( 'NONE',  ( 25.60000000000000142, 0.000000000000000000, 0.000000000000000000 ) ) ;
#36838=CARTESIAN_POINT ( 'NONE',  ( 17.87620400591499958, -3.527529948368999690, 11.96092454128000071 ) ) ;
#36843=VERTEX_POINT ( 'NONE', #45708 ) ;
#36853=ORIENTED_EDGE ( 'NONE', *, *, #29876, .F. ) ;
#36854=DIRECTION ( 'NONE',  ( -1.000000000000000000, 0.000000000000000000, 0.000000000000000000 ) ) ;
#36860=CARTESIAN_POINT ( 'NONE',  ( 16.43176826122700263, -3.316188843241000050, -11.22344245815999919 ) ) ;
#36863=CARTESIAN_POINT ( 'NONE',  ( 14.04832727683000115, 8.838110522795000534, 7.948685794524999793 ) ) ;
#36868=CARTESIAN_POINT ( 'NONE',  ( 17.60000001287599858, 11.53033693765999779, -4.891431908114999949 ) ) ;
#36872=CARTESIAN_POINT ( 'NONE',  ( 29.60000000000000142, 0.000000000000000000, 0.000000000000000000 ) ) ;
#36877=CARTESIAN_POINT ( 'NONE',  ( 24.72545694048200104, 3.605123969772000336, -12.13009300416999992 ) ) ;
#36883=DIRECTION ( 'NONE',  ( 1.000000000000000000, 0.000000000000000000, 0.000000000000000000 ) ) ;
#36886=ORIENTED_EDGE ( 'NONE', *, *, #41995, .T. ) ;
#36895=ORIENTED_EDGE ( 'NONE', *, *, #59294, .T. ) ;
#36896=CARTESIAN_POINT ( 'NONE',  ( 23.56797307596834656, 10.32882671279216780, 9.435355520811883778 ) ) ;
#36898=CARTESIAN_POINT ( 'NONE',  ( 18.43348807395466338, 2.701964790437661357, -11.40102144998395062 ) ) ;
#36904=ORIENTED_EDGE ( 'NONE', *, *, #37913, .F. ) ;
#36911=CARTESIAN_POINT ( 'NONE',  ( 11.79999999684100054, -12.15995044155999949, -2.000340912084999978 ) ) ;
#36912=DIRECTION ( 'NONE',  ( 0.000000000000000000, 0.7614089499631907509, 0.6482718649732928107 ) ) ;
#36918=VERTEX_POINT ( 'NONE', #28246 ) ;
#36921=VECTOR ( 'NONE', #59882, 1000.000000000000000 ) ;
#36922=DIRECTION ( 'NONE',  ( 1.000000000000000000, 0.000000000000000000, 0.000000000000000000 ) ) ;
#36933=DIRECTION ( 'NONE',  ( 1.000000000000000000, 0.000000000000000000, 0.000000000000000000 ) ) ;
#36937=CARTESIAN_POINT ( 'NONE',  ( 12.37550370467983818, -11.46556593385705369, 4.499409319922215822 ) ) ;
#36939=CARTESIAN_POINT ( 'NONE',  ( 25.36465286085400095, -11.12555525505000098, 3.380130932433000002 ) ) ;
#36949=DIRECTION ( 'NONE',  ( -1.000000000000000000, 0.000000000000000000, 0.000000000000000000 ) ) ;
#36950=EDGE_LOOP ( 'NONE', ( #11135, #57621, #46003, #4764 ) ) ;
#36952=CARTESIAN_POINT ( 'NONE',  ( 18.26281931570200356, 2.856833007231000199, 11.95042392763000016 ) ) ;
#36963=CARTESIAN_POINT ( 'NONE',  ( 11.49999144015000319, 3.886253129992999877, -11.90689313971000018 ) ) ;
#36964=CARTESIAN_POINT ( 'NONE',  ( 15.66247398912732436, 8.798600188463543859, 7.938011626707100810 ) ) ;
#36967=EDGE_LOOP ( 'NONE', ( #32477, #2397, #36853, #68340, #34144 ) ) ;
#36968=CARTESIAN_POINT ( 'NONE',  ( 15.86053068095500151, -3.820355458042000052, -11.67812044351000011 ) ) ;
#36969=B_SPLINE_CURVE_WITH_KNOTS ( 'NONE', 3,
 ( #38252, #6433, #53989, #43513 ),
 .UNSPECIFIED., .F., .F.,
 ( 4, 4 ),
 ( 0.000000000000000000, 1.000000000000000000 ),
 .UNSPECIFIED. ) ;
#36971=ORIENTED_EDGE ( 'NONE', *, *, #15417, .F. ) ;
#36972=EDGE_CURVE ( 'NONE', #26055, #24760, #551, .T. ) ;
#36976=CARTESIAN_POINT ( 'NONE',  ( 17.80000000009400196, -3.216307036143000175, -11.40341376487999980 ) ) ;
#36978=CARTESIAN_POINT ( 'NONE',  ( 24.45617572612135504, -8.883484012707175026, -9.170518742179092797 ) ) ;
#36983=ORIENTED_EDGE ( 'NONE', *, *, #55535, .T. ) ;
#36992=CARTESIAN_POINT ( 'NONE',  ( 25.29987333571600061, -10.83443035398000021, -3.855530949778000149 ) ) ;
#36998=ORIENTED_EDGE ( 'NONE', *, *, #55658, .T. ) ;
#36999=ORIENTED_EDGE ( 'NONE', *, *, #31932, .T. ) ;
#37014=ADVANCED_FACE ( 'NONE', ( #25060 ), #61550, .F. ) ;
#37022=CONICAL_SURFACE ( 'NONE', #61619, 1.150087858351999781, 0.7854644967339313721 ) ;
#37025=CARTESIAN_POINT ( 'NONE',  ( 11.25913761803000135, -3.706864829039000053, 11.29572955805999968 ) ) ;
#37031=CARTESIAN_POINT ( 'NONE',  ( 24.31006797060300073, 8.914161087288000829, -8.860056390205999222 ) ) ;
#37037=CARTESIAN_POINT ( 'NONE',  ( 13.55279538703999975, -9.560508190731999534, -7.863756665013000635 ) ) ;
#37039=ORIENTED_EDGE ( 'NONE', *, *, #7971, .T. ) ;
#37043=CARTESIAN_POINT ( 'NONE',  ( 24.44496488041000148, -12.03536727282999941, 3.224852091355999928 ) ) ;
#37050=CARTESIAN_POINT ( 'NONE',  ( 24.44496356299600137, 12.03536643057000077, 3.224849944858999784 ) ) ;
#37054=CARTESIAN_POINT ( 'NONE',  ( 23.85399058234839487, 13.23042188477195147, 3.489531688373534557 ) ) ;
#37057=EDGE_CURVE ( 'NONE', #60421, #12823, #62795, .T. ) ;
#37061=CARTESIAN_POINT ( 'NONE',  ( 24.01908879469848301, -3.345608066011616533, 12.71187805225699030 ) ) ;
#37065=CARTESIAN_POINT ( 'NONE',  ( 25.18907804500399905, -2.894871919440999974, -11.44764655394999942 ) ) ;
#37068=VERTEX_POINT ( 'NONE', #15943 ) ;
#37069=CARTESIAN_POINT ( 'NONE',  ( 15.39999999998900293, -9.471998555523999386, -8.194929586088999685 ) ) ;
#37083=ORIENTED_EDGE ( 'NONE', *, *, #48779, .F. ) ;
#37092=EDGE_CURVE ( 'NONE', #35599, #19259, #66419, .T. ) ;
#37094=ADVANCED_FACE ( 'NONE', ( #5459 ), #54034, .F. ) ;
#37095=ORIENTED_EDGE ( 'NONE', *, *, #18487, .F. ) ;
#37098=CARTESIAN_POINT ( 'NONE',  ( 13.84412491599044159, -8.835575362389704424, -7.593298916478498306 ) ) ;
#37112=CARTESIAN_POINT ( 'NONE',  ( 18.15867081906211311, -11.79498723463443177, 3.559233470735385652 ) ) ;
#37115=VERTEX_POINT ( 'NONE', #59631 ) ;
#37121=CARTESIAN_POINT ( 'NONE',  ( 23.56971544161007159, -3.042705470371831478, -13.65412327231683243 ) ) ;
#37124=CARTESIAN_POINT ( 'NONE',  ( 23.58471847246500275, 3.197974897699999985, -13.62073867207999989 ) ) ;
#37134=CARTESIAN_POINT ( 'NONE',  ( 24.45999053249100186, 11.93730388424000033, 3.254644296425999617 ) ) ;
#37138=CARTESIAN_POINT ( 'NONE',  ( 11.50001544675000531, -12.31773593200242090, 2.620250046283704837 ) ) ;
#37141=CARTESIAN_POINT ( 'NONE',  ( 24.57034583260499971, 12.57146371045999977, -2.966472501429000097 ) ) ;
#37142=ORIENTED_EDGE ( 'NONE', *, *, #1674, .T. ) ;
#37145=ORIENTED_EDGE ( 'NONE', *, *, #31675, .T. ) ;
#37152=CARTESIAN_POINT ( 'NONE',  ( 18.16715644869600155, -3.024463723863999753, 11.49930835314999911 ) ) ;
#37156=CARTESIAN_POINT ( 'NONE',  ( 13.27439970770000066, 11.71097706365999969, 2.049245155247000127 ) ) ;
#37159=ORIENTED_EDGE ( 'NONE', *, *, #52574, .F. ) ;
#37161=CARTESIAN_POINT ( 'NONE',  ( 16.09997386696500143, 8.350085070477001992, 8.123950967096998710 ) ) ;
#37162=ORIENTED_EDGE ( 'NONE', *, *, #57971, .F. ) ;
#37165=CARTESIAN_POINT ( 'NONE',  ( 17.77392020236939985, 11.85836615397808025, -3.313854778486285291 ) ) ;
#37171=CARTESIAN_POINT ( 'NONE',  ( 12.01716035628400192, 11.91307312420999942, -3.686993282830000052 ) ) ;
#37172=CARTESIAN_POINT ( 'NONE',  ( 18.35816574290100078, 11.69157926155999938, -4.070931047779999368 ) ) ;
#37176=CARTESIAN_POINT ( 'NONE',  ( 18.01722669115800102, -3.499390932422000056, 11.96939125376999868 ) ) ;
#37178=B_SPLINE_CURVE_WITH_KNOTS ( 'NONE', 3,
 ( #23314, #50571, #39391, #60712 ),
 .UNSPECIFIED., .F., .F.,
 ( 4, 4 ),
 ( 0.000000000000000000, 1.000000000000000000 ),
 .UNSPECIFIED. ) ;
#37182=CARTESIAN_POINT ( 'NONE',  ( 11.50001258332000020, 11.56502147876000031, 1.404302031979000054 ) ) ;
#37184=DIRECTION ( 'NONE',  ( 0.000000000000000000, 0.7071067811865995312, 0.7071067811864953923 ) ) ;
#37191=ORIENTED_EDGE ( 'NONE', *, *, #19176, .F. ) ;
#37200=CARTESIAN_POINT ( 'NONE',  ( 16.18329442974999921, -3.298233714334000144, -11.32377282473999891 ) ) ;
#37209=ORIENTED_EDGE ( 'NONE', *, *, #36072, .T. ) ;
#37215=ORIENTED_EDGE ( 'NONE', *, *, #37700, .F. ) ;
#37226=ORIENTED_EDGE ( 'NONE', *, *, #29718, .F. ) ;
#37235=FACE_OUTER_BOUND ( 'NONE', #14629, .T. ) ;
#37245=DIRECTION ( 'NONE',  ( -1.000000000000000000, 0.000000000000000000, 0.000000000000000000 ) ) ;
#37253=EDGE_CURVE ( 'NONE', #23714, #3814, #49616, .T. ) ;
#37255=EDGE_CURVE ( 'NONE', #855, #16959, #18883, .T. ) ;
#37264=CIRCLE ( 'NONE', #29502, 1.300160515709999576 ) ;
#37267=CARTESIAN_POINT ( 'NONE',  ( 12.83143828159500188, -11.44347076768000093, 4.696252053897000067 ) ) ;
#37269=DIRECTION ( 'NONE',  ( 0.000000000000000000, 1.000000000000000000, 0.000000000000000000 ) ) ;
#37276=CARTESIAN_POINT ( 'NONE',  ( 15.99981196018700125, 1.318944953255000000E-13, -6.750155989720999729E-14 ) ) ;
#37281=CARTESIAN_POINT ( 'NONE',  ( 24.03014912280099935, 9.409787345911999168, 9.736160099024999681 ) ) ;
#37296=CARTESIAN_POINT ( 'NONE',  ( 23.66004879239100234, 0.000000000000000000, 0.000000000000000000 ) ) ;
#37299=CARTESIAN_POINT ( 'NONE',  ( 11.50001496185000249, 6.312855374401662445, -10.89679704397376447 ) ) ;
#37304=CARTESIAN_POINT ( 'NONE',  ( 11.29999334531184552, 11.74553346643965668, 1.558194258341519811 ) ) ;
#37305=CARTESIAN_POINT ( 'NONE',  ( 11.64596081258699911, 11.57456368445000017, 1.729631387595999881 ) ) ;
#37306=ORIENTED_EDGE ( 'NONE', *, *, #67686, .F. ) ;
#37308=CARTESIAN_POINT ( 'NONE',  ( 13.50018479229300006, 11.60142623882999935, 2.415183939829000259 ) ) ;
#37310=EDGE_CURVE ( 'NONE', #19021, #47311, #48102, .T. ) ;
#37313=CARTESIAN_POINT ( 'NONE',  ( 27.09999999999999787, -1.808321269955000243E-12, 9.250000000000000000 ) ) ;
#37319=VERTEX_POINT ( 'NONE', #23954 ) ;
#37322=CARTESIAN_POINT ( 'NONE',  ( 25.60000000000000142, -9.517611874540000017, 8.103398312166000039 ) ) ;
#37323=CARTESIAN_POINT ( 'NONE',  ( 15.83043922992600017, -9.441080823466998950, -8.288885697152998944 ) ) ;
#37325=VERTEX_POINT ( 'NONE', #44263 ) ;
#37327=DIRECTION ( 'NONE',  ( -1.000000000000000000, 0.000000000000000000, 0.000000000000000000 ) ) ;
#37328=CARTESIAN_POINT ( 'NONE',  ( 23.60000000000000142, 1.954819123156861016, 13.79162281801090195 ) ) ;
#37340=CARTESIAN_POINT ( 'NONE',  ( 11.79999999497874796, -3.261294161473140107, 11.32146851427815193 ) ) ;
#37343=CARTESIAN_POINT ( 'NONE',  ( 23.58885774780335609, -10.33110206683957877, -9.338943755861244256 ) ) ;
#37344=CARTESIAN_POINT ( 'NONE',  ( 24.30001131207184528, 12.15210920089874413, 3.256147846716761940 ) ) ;
#37345=CARTESIAN_POINT ( 'NONE',  ( 16.39999999231800132, 3.216285993016000155, 11.40340220863999932 ) ) ;
#37360=CARTESIAN_POINT ( 'NONE',  ( 11.74274107869599959, -3.315287298500999569, 11.22371330986000082 ) ) ;
#37368=AXIS2_PLACEMENT_3D ( 'NONE', #13608, #39478, #24432 ) ;
#37370=EDGE_LOOP ( 'NONE', ( #56235, #37039, #67219, #8710 ) ) ;
#37372=CARTESIAN_POINT ( 'NONE',  ( 13.73140886085690582, 8.907522817021753525, 7.508769385438491817 ) ) ;
#37373=UNCERTAINTY_MEASURE_WITH_UNIT (LENGTH_MEASURE( 1.000000000000000082E-05 ), #67587, 'distance_accuracy_value', 'NONE');
#37375=DIRECTION ( 'NONE',  ( 1.000000000000000000, 0.000000000000000000, 0.000000000000000000 ) ) ;
#37376=CARTESIAN_POINT ( 'NONE',  ( 25.26997866307398155, 11.52971827777785307, -2.996576611362720577 ) ) ;
#37396=EDGE_CURVE ( 'NONE', #34183, #37319, #2286, .T. ) ;
#37399=EDGE_CURVE ( 'NONE', #54794, #66938, #63056, .T. ) ;
#37402=CARTESIAN_POINT ( 'NONE',  ( 25.47111444092800170, -2.702220074950000051, -11.27947351919000063 ) ) ;
#37406=CARTESIAN_POINT ( 'NONE',  ( 23.98816739749597104, 9.385742420920845319, 9.282132427818025278 ) ) ;
#37420=CARTESIAN_POINT ( 'NONE',  ( 24.71800958153259842, -3.123417170972841106, 11.79150745397447153 ) ) ;
#37421=CARTESIAN_POINT ( 'NONE',  ( 24.67921430886200085, -8.727631620858000261, -9.158313288899000426 ) ) ;
#37422=CARTESIAN_POINT ( 'NONE',  ( 11.75750014570500035, 12.43407951582999971, 1.799970604841000021 ) ) ;
#37429=ORIENTED_EDGE ( 'NONE', *, *, #42192, .T. ) ;
#37430=CARTESIAN_POINT ( 'NONE',  ( 24.70770306079000278, 8.718110200638999885, 9.202866107698000064 ) ) ;
#37432=CARTESIAN_POINT ( 'NONE',  ( 13.92027728201558112, -8.815475954240428180, -7.616421984250669297 ) ) ;
#37435=B_SPLINE_SURFACE_WITH_KNOTS ( 'NONE', 3, 3, ( 
 ( #24321, #8242, #8925, #19761 ),
 ( #56478, #29930, #29589, #2987 ),
 ( #28901, #7900, #62403, #45985 ),
 ( #2309, #67297, #23631, #66273 ),
 ( #2648, #45312, #66618, #18740 ),
 ( #61382, #34822, #26037, #36877 ) ),
 .UNSPECIFIED., .F., .F., .F.,
 ( 4, 1, 1, 4 ),
 ( 4, 4 ),
 ( 0.1811037619699999990, 0.3333333333333000081, 0.6666666666667000474, 0.8725156331704999602 ),
 ( -0.1256563615239000009, 1.125656361510000147 ),
 .UNSPECIFIED. ) ;
#37476=CARTESIAN_POINT ( 'NONE',  ( 24.62773497368900166, 12.19918623920000122, 3.045383383698999857 ) ) ;
#37481=ORIENTED_EDGE ( 'NONE', *, *, #21607, .F. ) ;
#37482=CARTESIAN_POINT ( 'NONE',  ( 13.52727141073982331, 12.35275327559081582, 2.070326479558311839 ) ) ;
#37487=CARTESIAN_POINT ( 'NONE',  ( 23.99448051247391334, 3.345746474086601641, -12.75760653321332327 ) ) ;
#37492=CARTESIAN_POINT ( 'NONE',  ( 11.44749694427000186, 3.679776032594999968, -11.11060924501999914 ) ) ;
#37493=CARTESIAN_POINT ( 'NONE',  ( 13.69055856039300068, 11.42191202915999781, 2.091365271848000251 ) ) ;
#37494=VERTEX_POINT ( 'NONE', #67964 ) ;
#37505=CARTESIAN_POINT ( 'NONE',  ( 24.99828499555314565, -8.543280344662843362, 8.328740866081538741 ) ) ;
#37510=CARTESIAN_POINT ( 'NONE',  ( 12.26982956731400165, 11.56648533137999912, -4.655999611355000845 ) ) ;
#37511=CARTESIAN_POINT ( 'NONE',  ( 17.61881199949500143, 11.55156539432999985, -4.942255484049000280 ) ) ;
#37515=CARTESIAN_POINT ( 'NONE',  ( 18.16350100824700320, -3.138009765975000143, 11.88148072165000002 ) ) ;
#37546=CARTESIAN_POINT ( 'NONE',  ( 24.34832162658637600, 3.224867771844263320, -12.03537037221818728 ) ) ;
#37547=CARTESIAN_POINT ( 'NONE',  ( 25.31010614027100303, -8.472730232543000284, 8.045075953992999018 ) ) ;
#37556=CARTESIAN_POINT ( 'NONE',  ( 23.60000000000000142, 2.258942858049999725, 12.29419282279000036 ) ) ;
#37573=DIRECTION ( 'NONE',  ( 0.000000000000000000, 1.000000000000000000, -1.290201028711000169E-14 ) ) ;
#37577=AXIS2_PLACEMENT_3D ( 'NONE', #59081, #11182, #5587 ) ;
#37580=VERTEX_POINT ( 'NONE', #471 ) ;
#37586=CARTESIAN_POINT ( 'NONE',  ( 15.90567905817900218, 3.588626488247999902, 11.74852861413999960 ) ) ;
#37596=B_SPLINE_CURVE_WITH_KNOTS ( 'NONE', 3,
 ( #64811, #59927, #53990, #43159, #43857, #17280, #23219, #1899, #7475, #16588, #44567, #43514, #28474, #33371, #65859, #65158, #59580, #12037, #33719, #22174, #54333, #64465, #28829 ),
 .UNSPECIFIED., .F., .F.,
 ( 4, 2, 2, 1, 2, 2, 2, 2, 1, 1, 2, 2, 4 ),
 ( 0.000000000000000000, 0.2500000000000036082, 0.3750000000000054401, 0.4375000000000017208, 0.4687499999999983347, 0.4999999999999949485, 0.6249999999999795719, 0.6874999999999711342, 0.7187499999999680256, 0.7343749999999659162, 0.7421874999999619194, 0.7499999999999579225, 1.000000000000000000 ),
 .UNSPECIFIED. ) ;
#37597=CARTESIAN_POINT ( 'NONE',  ( 17.98957057434314066, -12.09691025065527903, 3.246626905778224881 ) ) ;
#37600=DIRECTION ( 'NONE',  ( -1.055605809059559446E-16, -0.9835354258236025382, 0.1807154286440004198 ) ) ;
#37623=ORIENTED_EDGE ( 'NONE', *, *, #15083, .T. ) ;
#37625=CARTESIAN_POINT ( 'NONE',  ( 13.49980696792483137, -11.54838492169068331, -4.420196298692892434 ) ) ;
#37646=EDGE_LOOP ( 'NONE', ( #41517, #30612, #1342, #35655, #15341 ) ) ;
#37647=CARTESIAN_POINT ( 'NONE',  ( 16.04506009312500225, -3.874776422117000241, -11.85383417895000058 ) ) ;
#37651=CARTESIAN_POINT ( 'NONE',  ( 18.29983863916000075, -2.861762957209999847, 11.98830831200999825 ) ) ;
#37653=ORIENTED_EDGE ( 'NONE', *, *, #24242, .T. ) ;
#37658=CARTESIAN_POINT ( 'NONE',  ( 11.29997960521317957, 3.569935952926198031, -11.29784959202355488 ) ) ;
#37665=CARTESIAN_POINT ( 'NONE',  ( 16.13494720760600032, -9.102952917978999636, -8.658486291235998777 ) ) ;
#37682=CARTESIAN_POINT ( 'NONE',  ( 11.42397234076999979, -12.13750352647000064, -1.893412522203000048 ) ) ;
#37683=CARTESIAN_POINT ( 'NONE',  ( 13.00000000005200107, 12.15994572112000149, 2.000334444851999738 ) ) ;
#37685=CARTESIAN_POINT ( 'NONE',  ( 12.79999999824000589, -12.03389405692475478, 3.206111686008664918 ) ) ;
#37691=AXIS2_PLACEMENT_3D ( 'NONE', #14246, #46057, #35231 ) ;
#37692=CARTESIAN_POINT ( 'NONE',  ( 18.44504292973000048, 2.664685748803000021, 11.39637496735000077 ) ) ;
#37694=CARTESIAN_POINT ( 'NONE',  ( 23.66004879239100234, 3.393652551760000247, -13.50507492672999987 ) ) ;
#37696=CARTESIAN_POINT ( 'NONE',  ( 17.89159592529800236, 3.376698609984999599, -11.11057657535000054 ) ) ;
#37700=EDGE_CURVE ( 'NONE', #52892, #37325, #38923, .T. ) ;
#37702=CARTESIAN_POINT ( 'NONE',  ( 23.73828294872599898, -9.840026834037999492, -9.652156658315000470 ) ) ;
#37705=B_SPLINE_SURFACE_WITH_KNOTS ( 'NONE', 3, 3, ( 
 ( #62007, #437, #32270, #22097 ),
 ( #92, #10237, #16511, #10926 ),
 ( #64048, #63714, #58819, #64738 ),
 ( #37493, #58137, #42744, #47652 ),
 ( #37840, #27356, #21077, #16168 ),
 ( #25978, #48678, #21751, #37156 ),
 ( #27013, #59161, #53579, #5672 ),
 ( #48330, #21410, #31572, #58475 ),
 ( #9896, #10580, #43085, #64390 ),
 ( #11265, #42060, #31919, #52891 ) ),
 .UNSPECIFIED., .F., .F., .F.,
 ( 4, 1, 1, 1, 1, 1, 1, 4 ),
 ( 4, 4 ),
 ( 0.04183311431308000400, 0.1428571428570999946, 0.2857142857143000203, 0.4285714285713999594, 0.5714285714286000406, 0.7142857142856999797, 0.8571428571429000609, 0.9292981235707000742 ),
 ( -0.1917799910644999994, 1.191756862851000021 ),
 .UNSPECIFIED. ) ;
#37710=CARTESIAN_POINT ( 'NONE',  ( 24.36958145701300182, 8.861545501478000020, -8.807436093351999062 ) ) ;
#37724=ORIENTED_EDGE ( 'NONE', *, *, #49130, .F. ) ;
#37725=CARTESIAN_POINT ( 'NONE',  ( 24.66122485234200212, 12.38509973078999948, -2.963735973613000230 ) ) ;
#37735=CARTESIAN_POINT ( 'NONE',  ( 24.99826494465212434, -11.48456307779601637, -3.234320738292375097 ) ) ;
#37736=ADVANCED_FACE ( 'NONE', ( #52148 ), #14758, .F. ) ;
#37755=CYLINDRICAL_SURFACE ( 'NONE', #37577, 11.50000000000000178 ) ;
#37764=CARTESIAN_POINT ( 'NONE',  ( 24.63609268136318420, -3.161156455721329195, 11.86232637917242627 ) ) ;
#37766=CARTESIAN_POINT ( 'NONE',  ( 16.39999999308669842, 3.302282894619416265, 11.70823727156336425 ) ) ;
#37771=DIRECTION ( 'NONE',  ( 1.000000000000000000, 0.000000000000000000, 0.000000000000000000 ) ) ;
#37788=CARTESIAN_POINT ( 'NONE',  ( 25.60000000000000142, 10.55164198324999880, 3.754898126455999741 ) ) ;
#37792=CARTESIAN_POINT ( 'NONE',  ( 24.30000000000000071, 10.83443035398000021, -3.855530949778000149 ) ) ;
#37797=AXIS2_PLACEMENT_3D ( 'NONE', #69040, #4369, #26749 ) ;
#37800=CARTESIAN_POINT ( 'NONE',  ( 11.92270903091197987, -11.93179002798757615, 3.810633631265414767 ) ) ;
#37809=AXIS2_PLACEMENT_3D ( 'NONE', #55838, #2349, #8288 ) ;
#37810=PLANE ( 'NONE',  #55330 ) ;
#37812=CARTESIAN_POINT ( 'NONE',  ( 18.23289209645828990, -3.217460216940595696, 11.19708622233677175 ) ) ;
#37820=CARTESIAN_POINT ( 'NONE',  ( 18.30000000000000071, 2.818741034879777008, -11.83575128182368452 ) ) ;
#37821=CARTESIAN_POINT ( 'NONE',  ( 24.19015592859265951, 9.083557491131649897, -9.071480578485305202 ) ) ;
#37826=VERTEX_POINT ( 'NONE', #36770 ) ;
#37838=CIRCLE ( 'NONE', #45688, 12.42499880353999941 ) ;
#37840=CARTESIAN_POINT ( 'NONE',  ( 13.58722619340700177, 11.45202530529999940, 1.920069653109999885 ) ) ;
#37841=ORIENTED_EDGE ( 'NONE', *, *, #3319, .F. ) ;
#37857=CARTESIAN_POINT ( 'NONE',  ( 17.61698155344500094, 11.49709674579000129, -4.820194475709000059 ) ) ;
#37858=B_SPLINE_CURVE_WITH_KNOTS ( 'NONE', 3,
 ( #29872, #24945, #41026, #62348 ),
 .UNSPECIFIED., .F., .F.,
 ( 4, 4 ),
 ( 0.000000000000000000, 0.5000000000000044409 ),
 .UNSPECIFIED. ) ;
#37862=CARTESIAN_POINT ( 'NONE',  ( 17.82671363066053871, 12.11440107311990211, -3.181008590938710245 ) ) ;
#37869=DIRECTION ( 'NONE',  ( 1.000000000000000000, 0.000000000000000000, 0.000000000000000000 ) ) ;
#37873=LINE ( 'NONE', #6739, #36921 ) ;
#37886=CARTESIAN_POINT ( 'NONE',  ( 23.58885196634466297, -13.25333333387674273, 4.277492436922254448 ) ) ;
#37887=CARTESIAN_POINT ( 'NONE',  ( 25.34480063931457394, 11.16380230704550591, -3.340454812006480978 ) ) ;
#37899=ORIENTED_EDGE ( 'NONE', *, *, #8989, .F. ) ;
#37903=CONICAL_SURFACE ( 'NONE', #27895, 1.150068028907000661, 0.7854495265279701766 ) ;
#37910=ORIENTED_EDGE ( 'NONE', *, *, #24021, .F. ) ;
#37912=CARTESIAN_POINT ( 'NONE',  ( 17.80000000009400196, 3.216307036143000175, 11.40341376487999980 ) ) ;
#37913=EDGE_CURVE ( 'NONE', #8238, #60967, #45513, .T. ) ;
#37921=ORIENTED_EDGE ( 'NONE', *, *, #19342, .F. ) ;
#37923=CARTESIAN_POINT ( 'NONE',  ( 25.19216650927900147, 11.35756831782000020, -3.218651103263999946 ) ) ;
#37933=CARTESIAN_POINT ( 'NONE',  ( 24.51105731435045598, 11.97394790521814301, -3.208410371361174018 ) ) ;
#37935=CARTESIAN_POINT ( 'NONE',  ( 23.95415663622134161, 12.78629371929804925, 3.518569764782334630 ) ) ;
#37936=B_SPLINE_CURVE_WITH_KNOTS ( 'NONE', 3,
 ( #6663, #65388, #32899, #66427, #12963, #34287, #28004, #17861, #50361, #65034, #2460, #33248, #23784, #49313, #1426, #44090, #38835, #34978, #19576, #8739, #34637, #8398, #25503 ),
 .UNSPECIFIED., .F., .F.,
 ( 4, 2, 2, 1, 2, 2, 2, 2, 1, 1, 2, 2, 4 ),
 ( 0.000000000000000000, 0.2500000000000463518, 0.3750000000000697775, 0.4375000000000831002, 0.4687500000000872635, 0.5000000000000913714, 0.6250000000000957012, 0.6875000000000990319, 0.7187500000001006972, 0.7343750000001003642, 0.7421875000001036948, 0.7500000000001070255, 1.000000000000000000 ),
 .UNSPECIFIED. ) ;
#37941=CARTESIAN_POINT ( 'NONE',  ( 13.49998535730551019, 12.08447166622788771, 2.429352492459241120 ) ) ;
#37946=CARTESIAN_POINT ( 'NONE',  ( 25.25799098492100114, -2.569256426743999899, 11.37081265261999974 ) ) ;
#37952=EDGE_CURVE ( 'NONE', #38805, #27228, #37936, .T. ) ;
#37956=CARTESIAN_POINT ( 'NONE',  ( 24.63781023927800007, 8.684869114355000974, 8.585175602391000638 ) ) ;
#37959=CARTESIAN_POINT ( 'NONE',  ( 17.91921746558384498, 11.21561494459062480, -3.152940210887823724 ) ) ;
#37961=CARTESIAN_POINT ( 'NONE',  ( 24.35145719007200071, -8.929422700512001043, -9.054903155755001265 ) ) ;
#37962=CARTESIAN_POINT ( 'NONE',  ( 18.30000077768849565, 11.66744147158535405, -3.971919865264926575 ) ) ;
#37965=CARTESIAN_POINT ( 'NONE',  ( 12.79999999734009464, 10.99220013531737372, -4.481500379774075782 ) ) ;
#37975=ORIENTED_EDGE ( 'NONE', *, *, #15139, .F. ) ;
#37979=CARTESIAN_POINT ( 'NONE',  ( 15.66247398912731725, -8.798600188463547411, -7.938011626707102586 ) ) ;
#37985=CARTESIAN_POINT ( 'NONE',  ( 11.50000302521714701, -12.42140736507980137, -1.609561362244301241 ) ) ;
#37988=CARTESIAN_POINT ( 'NONE',  ( 11.35563158142000262, 11.71552011691000139, 1.381878615183999903 ) ) ;
#37990=CARTESIAN_POINT ( 'NONE',  ( 24.69609986848488248, 3.134121630126239122, -11.81029131445869673 ) ) ;
#37994=VERTEX_POINT ( 'NONE', #46832 ) ;
#38006=CARTESIAN_POINT ( 'NONE',  ( 15.58628609634500073, -9.247881098673000011, -8.227358011109998870 ) ) ;
#38012=CARTESIAN_POINT ( 'NONE',  ( 23.89320776801300283, -8.928716006355012169, 8.952507060126997374 ) ) ;
#38013=CARTESIAN_POINT ( 'NONE',  ( 24.17844198652961296, -3.317834083975258253, -12.42307627910415313 ) ) ;
#38018=EDGE_LOOP ( 'NONE', ( #14481, #54125, #36332, #13398 ) ) ;
#38025=CARTESIAN_POINT ( 'NONE',  ( 24.53428991268900106, -12.47024905405999995, -3.026245386525999947 ) ) ;
#38026=CARTESIAN_POINT ( 'NONE',  ( 24.22000602247700130, -12.94771364386000201, 3.132628870380000041 ) ) ;
#38027=CARTESIAN_POINT ( 'NONE',  ( 17.33333333161133538, 3.595161661651967933, 11.99793472338499711 ) ) ;
#38029=CARTESIAN_POINT ( 'NONE',  ( 18.44720874474599981, 2.702894824448000222, 11.38760777189999907 ) ) ;
#38036=CARTESIAN_POINT ( 'NONE',  ( 17.75907622778400352, 3.376089723145999866, -11.11072845602000037 ) ) ;
#38040=CARTESIAN_POINT ( 'NONE',  ( 23.58681704922799938, -10.27308883388000105, -9.418745758480000063 ) ) ;
#38041=CARTESIAN_POINT ( 'NONE',  ( 23.55066264645300222, -10.43161032036999813, 9.390903619644999978 ) ) ;
#38043=CARTESIAN_POINT ( 'NONE',  ( 11.80443633831200145, -3.376482451534999818, 11.11063790749999924 ) ) ;
#38049=CARTESIAN_POINT ( 'NONE',  ( 24.53002386606100060, 8.771528676252001944, -8.897041952684000776 ) ) ;
#38056=DIRECTION ( 'NONE',  ( 0.000000000000000000, -0.1623203401144080182, 0.9867381147929490393 ) ) ;
#38065=FACE_BOUND ( 'NONE', #9698, .T. ) ;
#38071=ORIENTED_EDGE ( 'NONE', *, *, #61114, .F. ) ;
#38072=CARTESIAN_POINT ( 'NONE',  ( 25.05002157598449841, -11.42810647003321378, -3.253264283331835038 ) ) ;
#38078=AXIS2_PLACEMENT_3D ( 'NONE', #45891, #67202, #9164 ) ;
#38082=CARTESIAN_POINT ( 'NONE',  ( 25.59997324745700098, 8.218963665694001719, 8.043524865688999270 ) ) ;
#38086=CARTESIAN_POINT ( 'NONE',  ( 23.84021450726483238, 9.641930377286131559, 9.401241262644600027 ) ) ;
#38091=CARTESIAN_POINT ( 'NONE',  ( 25.29987261391899978, -8.756202924575998026, 7.455126447192999883 ) ) ;
#38105=CARTESIAN_POINT ( 'NONE',  ( 24.30001694670299983, 8.938702829764999080, 8.938676122491999720 ) ) ;
#38115=EDGE_CURVE ( 'NONE', #53930, #25788, #32902, .T. ) ;
#38132=DIRECTION ( 'NONE',  ( 0.000000000000000000, 0.1807154286440005586, 0.9835354258236025382 ) ) ;
#38133=VERTEX_POINT ( 'NONE', #31785 ) ;
#38136=CARTESIAN_POINT ( 'NONE',  ( 23.77343862489363602, -9.774797336595577590, -9.437290416679315896 ) ) ;
#38137=CARTESIAN_POINT ( 'NONE',  ( 12.44187590071209826, -11.55958658085556046, 4.822001495576079044 ) ) ;
#38142=CARTESIAN_POINT ( 'NONE',  ( 23.91176682606199932, 3.265437890189999859, -12.84181129811999966 ) ) ;
#38148=CARTESIAN_POINT ( 'NONE',  ( 18.50007554376851715, -2.772760791832214800, 11.31557096909616966 ) ) ;
#38149=CARTESIAN_POINT ( 'NONE',  ( 17.77409395429256023, -11.41728060638866538, 4.609654547496091936 ) ) ;
#38155=CARTESIAN_POINT ( 'NONE',  ( 25.60000000000000142, -2.258942858049999725, 12.29419282279000036 ) ) ;
#38156=CARTESIAN_POINT ( 'NONE',  ( 11.50001544675000176, -12.52500000000000036, 0.000000000000000000 ) ) ;
#38157=CARTESIAN_POINT ( 'NONE',  ( 24.66271477989500127, 12.38330044149000031, 2.963253076001000075 ) ) ;
#38168=CARTESIAN_POINT ( 'NONE',  ( 24.13226547067089101, 3.329776921202292517, -12.50568236576632764 ) ) ;
#38169=EDGE_CURVE ( 'NONE', #60441, #55462, #44649, .T. ) ;
#38177=ORIENTED_EDGE ( 'NONE', *, *, #7827, .F. ) ;
#38183=EDGE_LOOP ( 'NONE', ( #14553, #14671, #13015, #4015, #62476 ) ) ;
#38190=DIRECTION ( 'NONE',  ( 1.000000000000000000, 0.000000000000000000, 0.000000000000000000 ) ) ;
#38192=B_SPLINE_CURVE_WITH_KNOTS ( 'NONE', 3,
 ( #14371, #15395, #53818, #63618 ),
 .UNSPECIFIED., .F., .F.,
 ( 4, 4 ),
 ( 0.000000000000000000, 1.000000000000000000 ),
 .UNSPECIFIED. ) ;
#38200=VECTOR ( 'NONE', #63651, 999.9999999999998863 ) ;
#38206=ORIENTED_EDGE ( 'NONE', *, *, #40023, .F. ) ;
#38208=DIRECTION ( 'NONE',  ( 1.000000000000000000, 0.000000000000000000, 0.000000000000000000 ) ) ;
#38219=B_SPLINE_CURVE_WITH_KNOTS ( 'NONE', 3,
 ( #36708, #63253, #46851, #10812, #68847, #20274 ),
 .UNSPECIFIED., .F., .F.,
 ( 4, 2, 4 ),
 ( 0.000000000000000000, 0.5000000000000000000, 1.000000000000000000 ),
 .UNSPECIFIED. ) ;
#38220=EDGE_CURVE ( 'NONE', #40403, #19021, #6220, .T. ) ;
#38232=DIRECTION ( 'NONE',  ( 0.000000000000000000, 0.9659258262890757507, 0.2588190451024934835 ) ) ;
#38233=CARTESIAN_POINT ( 'NONE',  ( 24.56351374471499938, -3.482977112968999922, 12.16506632497999973 ) ) ;
#38238=CARTESIAN_POINT ( 'NONE',  ( 29.60000000000000142, 0.000000000000000000, 0.000000000000000000 ) ) ;
#38247=CARTESIAN_POINT ( 'NONE',  ( 13.73682146000800053, 12.29517900649999973, 2.580790095973999776 ) ) ;
#38251=ORIENTED_EDGE ( 'NONE', *, *, #2827, .F. ) ;
#38252=CARTESIAN_POINT ( 'NONE',  ( 12.79999998712400178, 11.53033693765999779, -4.891431908114999949 ) ) ;
#38254=CARTESIAN_POINT ( 'NONE',  ( 15.56012107570600023, 8.822147194309000184, 7.967418575816001436 ) ) ;
#38268=VERTEX_POINT ( 'NONE', #45298 ) ;
#38276=CARTESIAN_POINT ( 'NONE',  ( 24.67921580255100267, 8.727633792449999817, 9.158312800479000870 ) ) ;
#38278=B_SPLINE_SURFACE_WITH_KNOTS ( 'NONE', 3, 3, ( 
 ( #49126, #12422, #43199, #12770 ),
 ( #43546, #28155, #33054, #64846 ),
 ( #34096, #6473, #49469, #22209 ),
 ( #7509, #28508, #43893, #22898 ),
 ( #48789, #18018, #49822, #23254 ),
 ( #54721, #44596, #65196, #65889 ),
 ( #37946, #11714, #59268, #17315 ),
 ( #27463, #38640, #16957, #11371 ) ),
 .UNSPECIFIED., .F., .F., .F.,
 ( 4, 1, 1, 1, 1, 4 ),
 ( 4, 4 ),
 ( 0.008355857670640998852, 0.05882352941176000050, 0.1176470588234999892, 0.1764705882353000133, 0.2352941176471000095, 0.2534691232731000055 ),
 ( -0.1830855917210000017, 1.182949831419999986 ),
 .UNSPECIFIED. ) ;
#38291=ORIENTED_EDGE ( 'NONE', *, *, #44232, .F. ) ;
#38292=ORIENTED_EDGE ( 'NONE', *, *, #61788, .T. ) ;
#38297=FACE_OUTER_BOUND ( 'NONE', #56315, .T. ) ;
#38304=CARTESIAN_POINT ( 'NONE',  ( 24.40628504395400000, -8.880942544344001988, -9.006432928708999697 ) ) ;
#38310=CARTESIAN_POINT ( 'NONE',  ( 24.51193477385900010, 8.843600298101000234, 9.168347890893999264 ) ) ;
#38315=CARTESIAN_POINT ( 'NONE',  ( 23.89320776801300283, 8.313844348326997036, -8.526065359053994541 ) ) ;
#38323=DIRECTION ( 'NONE',  ( 1.000000000000000000, 0.000000000000000000, 0.000000000000000000 ) ) ;
#38332=CARTESIAN_POINT ( 'NONE',  ( 13.92020863221766902, 9.472241403191404174, 8.194648738509947350 ) ) ;
#38334=CARTESIAN_POINT ( 'NONE',  ( 17.10000000000000142, 3.283787102340999464, 11.28049554847999936 ) ) ;
#38336=EDGE_LOOP ( 'NONE', ( #26409, #17575, #2463, #47416 ) ) ;
#38337=CARTESIAN_POINT ( 'NONE',  ( 24.56711102116320689, 3.188703611083238965, -11.92333255138484560 ) ) ;
#38338=CARTESIAN_POINT ( 'NONE',  ( 16.39956681845000119, 3.250692199830000018, 11.33777344299000056 ) ) ;
#38343=CARTESIAN_POINT ( 'NONE',  ( 17.60000003185799855, -12.11983897296999935, 3.159727888982000188 ) ) ;
#38354=CARTESIAN_POINT ( 'NONE',  ( 15.47616489729399980, -9.395071224208001226, -8.199988963223999505 ) ) ;
#38368=CARTESIAN_POINT ( 'NONE',  ( 25.44993529014200107, -2.258942858049999725, 12.29419282279000036 ) ) ;
#38369=EDGE_LOOP ( 'NONE', ( #62617, #595, #65444 ) ) ;
#38371=CARTESIAN_POINT ( 'NONE',  ( 11.53944595909000270, -12.46266292589999836, -1.587625155185000025 ) ) ;
#38376=CARTESIAN_POINT ( 'NONE',  ( 24.23191122837300426, 12.46786376384999961, 3.269411384671000231 ) ) ;
#38377=CARTESIAN_POINT ( 'NONE',  ( 17.60000000024299993, 11.86189249994999884, -3.298671769835999967 ) ) ;
#38379=DIRECTION ( 'NONE',  ( -1.000000000000000000, 0.000000000000000000, 0.000000000000000000 ) ) ;
#38381=B_SPLINE_CURVE_WITH_KNOTS ( 'NONE', 3,
 ( #15079, #37432, #37098, #58754, #5607, #68548 ),
 .UNSPECIFIED., .F., .F.,
 ( 4, 2, 4 ),
 ( 0.000000000000000000, 0.5000000000000000000, 1.000000000000000000 ),
 .UNSPECIFIED. ) ;
#38383=CARTESIAN_POINT ( 'NONE',  ( 18.43348807395470956, -2.701964790437650255, 11.40102144998400213 ) ) ;
#38384=CARTESIAN_POINT ( 'NONE',  ( 17.96012107570599881, 3.168891391480999520, -11.45723209283999999 ) ) ;
#38388=CARTESIAN_POINT ( 'NONE',  ( 23.64143804138000249, -10.11749648602000029, -9.385403416437998914 ) ) ;
#38389=CARTESIAN_POINT ( 'NONE',  ( 24.51038808216000220, -8.845036404463000324, 9.169859949269000055 ) ) ;
#38390=CARTESIAN_POINT ( 'NONE',  ( 24.62620337099072998, 3.584633747643987345, -12.20158770655988789 ) ) ;
#38391=EDGE_CURVE ( 'NONE', #31887, #66938, #17128, .T. ) ;
#38392=ORIENTED_EDGE ( 'NONE', *, *, #14993, .T. ) ;
#38398=ORIENTED_EDGE ( 'NONE', *, *, #12499, .T. ) ;
#38400=CARTESIAN_POINT ( 'NONE',  ( 25.08547525503900033, 2.791087243097000403, -11.47628568378999958 ) ) ;
#38402=AXIS2_PLACEMENT_3D ( 'NONE', #61729, #12466, #33452 ) ;
#38404=CARTESIAN_POINT ( 'NONE',  ( 11.30000000000000071, -18.88101580703000337, -3.105963843451999828 ) ) ;
#38415=CARTESIAN_POINT ( 'NONE',  ( 12.79342929296800158, -12.04986812289999953, 3.196648259943000170 ) ) ;
#38425=ORIENTED_EDGE ( 'NONE', *, *, #13886, .F. ) ;
#38428=CARTESIAN_POINT ( 'NONE',  ( 23.68333479628300253, 13.13544135902000143, -3.948726516682999677 ) ) ;
#38433=ORIENTED_EDGE ( 'NONE', *, *, #65999, .T. ) ;
#38437=ORIENTED_EDGE ( 'NONE', *, *, #55010, .T. ) ;
#38445=CARTESIAN_POINT ( 'NONE',  ( 18.46719854810600125, -11.76170593772999950, 4.414464320434000832 ) ) ;
#38447=CARTESIAN_POINT ( 'NONE',  ( 13.82798078375900275, 9.420238147574000465, 8.170996254510999535 ) ) ;
#38452=ORIENTED_EDGE ( 'NONE', *, *, #52920, .T. ) ;
#38453=EDGE_CURVE ( 'NONE', #2543, #46546, #47102, .T. ) ;
#38454=AXIS2_PLACEMENT_3D ( 'NONE', #4630, #58809, #68601 ) ;
#38458=CARTESIAN_POINT ( 'NONE',  ( 11.35563386585000067, 12.29158615273999899, 1.473028240582999970 ) ) ;
#38462=CARTESIAN_POINT ( 'NONE',  ( 13.50000000000339639, -9.396284335645857411, -7.729197028970922645 ) ) ;
#38467=VERTEX_POINT ( 'NONE', #60865 ) ;
#38470=CARTESIAN_POINT ( 'NONE',  ( 24.36504260745899941, -3.372670036896999513, -12.24415025393999912 ) ) ;
#38489=CARTESIAN_POINT ( 'NONE',  ( 18.29995268966800026, 2.861739928647000220, 11.98821236628000086 ) ) ;
#38490=CARTESIAN_POINT ( 'NONE',  ( 12.25178171628779111, -12.07365382811727628, 3.333154641342844116 ) ) ;
#38491=DIRECTION ( 'NONE',  ( 0.000000000000000000, 0.4998826579293299543, -0.8660931406618508355 ) ) ;
#38494=CARTESIAN_POINT ( 'NONE',  ( 23.85180091069500108, 3.519844699246999831, -13.16782481969999807 ) ) ;
#38495=CARTESIAN_POINT ( 'NONE',  ( 13.43590051321700152, -12.19118104410000036, -2.154281854449000555 ) ) ;
#38499=FACE_OUTER_BOUND ( 'NONE', #50019, .T. ) ;
#38501=CARTESIAN_POINT ( 'NONE',  ( 13.99999999308669629, -9.069400206872137105, -8.107642827045808076 ) ) ;
#38511=EDGE_CURVE ( 'NONE', #33492, #47043, #51064, .T. ) ;
#38515=ORIENTED_EDGE ( 'NONE', *, *, #10088, .F. ) ;
#38523=CARTESIAN_POINT ( 'NONE',  ( 23.65869700875494885, 3.166258104914992266, -13.42481195133845162 ) ) ;
#38525=CARTESIAN_POINT ( 'NONE',  ( 17.79222771582700346, -3.377813322129000095, 11.11021622646999951 ) ) ;
#38535=VERTEX_POINT ( 'NONE', #19239 ) ;
#38544=CARTESIAN_POINT ( 'NONE',  ( 11.80000000000000071, 14.76315775485999993, -50.50083396221000243 ) ) ;
#38555=ORIENTED_EDGE ( 'NONE', *, *, #59294, .F. ) ;
#38559=LINE ( 'NONE', #27384, #41359 ) ;
#38569=EDGE_CURVE ( 'NONE', #23593, #40087, #43763, .T. ) ;
#38575=CARTESIAN_POINT ( 'NONE',  ( 11.84748603848200155, 3.299681227315999887, -11.83395064283000053 ) ) ;
#38577=AXIS2_PLACEMENT_3D ( 'NONE', #68352, #53578, #53915 ) ;
#38583=CARTESIAN_POINT ( 'NONE',  ( 24.40628504395400000, -3.359328441570999857, 12.19433831731000062 ) ) ;
#38588=CARTESIAN_POINT ( 'NONE',  ( 13.99999999231800096, -8.833253877201999060, -7.896562762484000686 ) ) ;
#38590=CARTESIAN_POINT ( 'NONE',  ( 11.43320764420671054, -12.36501421780136667, -1.521867707432055905 ) ) ;
#38593=EDGE_CURVE ( 'NONE', #55299, #26398, #26301, .T. ) ;
#38596=CARTESIAN_POINT ( 'NONE',  ( 21.65000086032551252, 3.970157536060000036E-13, 1.776356839399999796E-13 ) ) ;
#38597=CARTESIAN_POINT ( 'NONE',  ( 13.46122879894100066, 12.02747180725999954, 2.509215126660999662 ) ) ;
#38598=ORIENTED_EDGE ( 'NONE', *, *, #60534, .T. ) ;
#38610=B_SPLINE_CURVE_WITH_KNOTS ( 'NONE', 3,
 ( #38091, #59418, #21329, #53494 ),
 .UNSPECIFIED., .F., .F.,
 ( 4, 4 ),
 ( 0.000000000000000000, 1.000000000000000000 ),
 .UNSPECIFIED. ) ;
#38621=ORIENTED_EDGE ( 'NONE', *, *, #52495, .T. ) ;
#38628=CARTESIAN_POINT ( 'NONE',  ( 23.56666365135700403, 2.009474831917003268, 11.63289034803000455 ) ) ;
#38640=CARTESIAN_POINT ( 'NONE',  ( 25.37646586244400382, -2.613422027899000355, 11.31776839467000073 ) ) ;
#38650=CARTESIAN_POINT ( 'NONE',  ( 25.00270600450344105, 8.478844049630730240, -8.837091021818228143 ) ) ;
#38653=DIRECTION ( 'NONE',  ( 1.000000000000000000, 0.000000000000000000, 0.000000000000000000 ) ) ;
#38655=CARTESIAN_POINT ( 'NONE',  ( 24.25374608244500152, -8.963954835242001096, -8.909854536156000648 ) ) ;
#38659=ADVANCED_FACE ( 'NONE', ( #9094 ), #2758, .T. ) ;
#38669=CARTESIAN_POINT ( 'NONE',  ( 23.89320776801300283, 8.862674798062995407, -7.304122743114001004 ) ) ;
#38680=ORIENTED_EDGE ( 'NONE', *, *, #60534, .F. ) ;
#38688=AXIS2_PLACEMENT_3D ( 'NONE', #6176, #44653, #22608 ) ;
#38689=DIRECTION ( 'NONE',  ( -1.000000000000000000, 0.000000000000000000, 0.000000000000000000 ) ) ;
#38690=ORIENTED_EDGE ( 'NONE', *, *, #63620, .F. ) ;
#38700=CARTESIAN_POINT ( 'NONE',  ( 18.23777283046791098, -3.105167776281877234, 11.92942829619372702 ) ) ;
#38703=CARTESIAN_POINT ( 'NONE',  ( 23.51521505635600207, -13.45855365459000019, -4.318323883769999760 ) ) ;
#38705=DIRECTION ( 'NONE',  ( 1.000000000000000000, 0.000000000000000000, 0.000000000000000000 ) ) ;
#38706=AXIS2_PLACEMENT_3D ( 'NONE', #32133, #53446, #48198 ) ;
#38707=B_SPLINE_CURVE_WITH_KNOTS ( 'NONE', 3,
 ( #47461, #46430, #25441, #67733 ),
 .UNSPECIFIED., .F., .F.,
 ( 4, 4 ),
 ( 0.000000000000000000, 1.000000000000000000 ),
 .UNSPECIFIED. ) ;
#38708=CARTESIAN_POINT ( 'NONE',  ( 15.83590051321700010, -9.131200976137998637, -8.359844154751998602 ) ) ;
#38709=ORIENTED_EDGE ( 'NONE', *, *, #8989, .T. ) ;
#38713=DIRECTION ( 'NONE',  ( 0.000000000000000000, 0.000000000000000000, -1.000000000000000000 ) ) ;
#38714=CARTESIAN_POINT ( 'NONE',  ( 13.00000000005200107, -12.15994572112000149, -2.000334444851999738 ) ) ;
#38715=CARTESIAN_POINT ( 'NONE',  ( 11.50001544675000176, -12.52500000000000036, 0.000000000000000000 ) ) ;
#38722=CARTESIAN_POINT ( 'NONE',  ( 11.72764643456600098, -12.22218869479000070, -1.954421350659000023 ) ) ;
#38728=DIRECTION ( 'NONE',  ( -1.000000000000000000, 0.000000000000000000, 0.000000000000000000 ) ) ;
#38734=CARTESIAN_POINT ( 'NONE',  ( 18.23176382712000176, 2.916721637292999603, -11.52766586543999949 ) ) ;
#38739=CARTESIAN_POINT ( 'NONE',  ( 24.33740314120300141, -8.940160201810000373, -9.046312361204000396 ) ) ;
#38740=ADVANCED_FACE ( 'NONE', ( #69192 ), #42931, .T. ) ;
#38741=CARTESIAN_POINT ( 'NONE',  ( 24.02032928698500314, -9.295255963207001315, 9.130110662804000299 ) ) ;
#38742=DIRECTION ( 'NONE',  ( 1.000000000000000000, 0.000000000000000000, 0.000000000000000000 ) ) ;
#38747=EDGE_CURVE ( 'NONE', #33649, #40201, #3621, .T. ) ;
#38749=CARTESIAN_POINT ( 'NONE',  ( 23.56666365135700403, -2.488348886664998538, 11.45224114467999499 ) ) ;
#38752=TOROIDAL_SURFACE ( 'NONE', #30976, 10.75000000000000000, 1.500000000000000000 ) ;
#38753=CARTESIAN_POINT ( 'NONE',  ( 25.36465219829700146, 2.635499547415999899, -11.32507936926000092 ) ) ;
#38765=ORIENTED_EDGE ( 'NONE', *, *, #54865, .T. ) ;
#38768=CARTESIAN_POINT ( 'NONE',  ( 12.69408977940800121, -11.93156085714000092, 3.263088413970000268 ) ) ;
#38775=DIRECTION ( 'NONE',  ( 0.000000000000000000, 1.000000000000000000, 0.000000000000000000 ) ) ;
#38781=CARTESIAN_POINT ( 'NONE',  ( 23.58444978062600228, 13.25734564952999861, -4.306384313474000081 ) ) ;
#38795=CARTESIAN_POINT ( 'NONE',  ( 24.35365242081700288, 2.582848009804000533, -11.10541636511000085 ) ) ;
#38805=VERTEX_POINT ( 'NONE', #41856 ) ;
#38808=CARTESIAN_POINT ( 'NONE',  ( 11.80577368593200305, 12.32791529894999982, 1.878576500660000148 ) ) ;
#38816=ORIENTED_EDGE ( 'NONE', *, *, #31365, .F. ) ;
#38819=CARTESIAN_POINT ( 'NONE',  ( 11.79999999684100054, -12.15995044155999949, -2.000340912084999978 ) ) ;
#38831=EDGE_CURVE ( 'NONE', #6697, #4626, #16133, .T. ) ;
#38834=DIRECTION ( 'NONE',  ( -1.000000000000000000, 9.336940512380999085E-10, 4.862374338246000196E-11 ) ) ;
#38835=CARTESIAN_POINT ( 'NONE',  ( 24.74122213638286283, 11.75038693034401582, 3.191108129339069066 ) ) ;
#38841=B_SPLINE_CURVE_WITH_KNOTS ( 'NONE', 3,
 ( #39031, #22933, #66617, #17350, #54754, #12805, #49505, #6853, #18394, #28190, #23291, #2308, #18052, #60688, #40070, #55451, #39719, #18738, #33787, #7209, #23630, #56133, #22588, #61381, #1618, #7545, #8241, #29588, #28900, #65583, #7899 ),
 .UNSPECIFIED., .F., .F.,
 ( 4, 2, 2, 1, 1, 2, 2, 2, 1, 2, 2, 2, 2, 2, 2, 2, 4 ),
 ( 0.000000000000000000, 0.06249999999999727995, 0.09374999999999585054, 0.1093749999999960310, 0.1171874999999960032, 0.1210937499999974465, 0.1249999999999988898, 0.1874999999999890643, 0.2187499999999843459, 0.2343749999999831524, 0.2499999999999819311, 0.3749999999999888978, 0.4374999999999925060, 0.4687499999999932832, 0.4999999999999941158, 0.7499999999999971134, 1.000000000000000000 ),
 .UNSPECIFIED. ) ;
#38851=CARTESIAN_POINT ( 'NONE',  ( 24.02041540912000173, 3.259263043209999822, -12.61480718775999854 ) ) ;
#38852=CARTESIAN_POINT ( 'NONE',  ( 23.60000648208766805, 13.25016727112855186, 4.189782993036962999 ) ) ;
#38863=CARTESIAN_POINT ( 'NONE',  ( 18.30000000000000071, 52.95171880992000268, -18.02623547589999831 ) ) ;
#38866=CARTESIAN_POINT ( 'NONE',  ( 15.65828218294664254, 9.154335746262503903, 8.252742830647335381 ) ) ;
#38868=CARTESIAN_POINT ( 'NONE',  ( 11.35394403557610410, 3.574442861579692376, -11.79291672678741421 ) ) ;
#38869=CARTESIAN_POINT ( 'NONE',  ( 12.09999999995609876, -11.00695867695318420, 3.817557008989782563 ) ) ;
#38873=ORIENTED_EDGE ( 'NONE', *, *, #19334, .T. ) ;
#38875=LINE ( 'NONE', #60197, #19629 ) ;
#38879=CARTESIAN_POINT ( 'NONE',  ( 24.11584421453913762, 3.333336234422446420, -12.53522527563100653 ) ) ;
#38883=CARTESIAN_POINT ( 'NONE',  ( 11.56566386073000174, 3.232480401124999680, -11.43828361194000109 ) ) ;
#38892=VERTEX_POINT ( 'NONE', #57854 ) ;
#38893=CARTESIAN_POINT ( 'NONE',  ( 11.50004200479687633, -11.55567552917520935, -1.481524094250667556 ) ) ;
#38899=EDGE_LOOP ( 'NONE', ( #55905, #19498, #7769, #34675, #64809 ) ) ;
#38901=CYLINDRICAL_SURFACE ( 'NONE', #34820, 0.5000000000000004441 ) ;
#38903=ORIENTED_EDGE ( 'NONE', *, *, #38831, .F. ) ;
#38905=CARTESIAN_POINT ( 'NONE',  ( 18.36663043076582724, 2.717294527786511704, 11.46570543779412787 ) ) ;
#38906=CARTESIAN_POINT ( 'NONE',  ( 23.58678704957500116, -3.018899350941000037, -13.60646675873000078 ) ) ;
#38915=PLANE ( 'NONE',  #30780 ) ;
#38923=LINE ( 'NONE', #39607, #9379 ) ;
#38933=ORIENTED_EDGE ( 'NONE', *, *, #43405, .T. ) ;
#38941=CARTESIAN_POINT ( 'NONE',  ( 24.25374608244500152, -3.234182954713999969, 12.21793987376999979 ) ) ;
#38954=CARTESIAN_POINT ( 'NONE',  ( 24.78219853511300030, -8.655325328077999814, -9.168174285775998911 ) ) ;
#38957=CARTESIAN_POINT ( 'NONE',  ( 13.73936233968600185, 12.30487262812000004, 2.534071019599000163 ) ) ;
#38958=ORIENTED_EDGE ( 'NONE', *, *, #50292, .F. ) ;
#38959=CARTESIAN_POINT ( 'NONE',  ( 11.79999999771000141, 3.595163221087000149, -11.99793848941000007 ) ) ;
#38962=CARTESIAN_POINT ( 'NONE',  ( 25.46373029971899982, -8.354610197568000274, -8.148451206582999262 ) ) ;
#38965=CARTESIAN_POINT ( 'NONE',  ( 23.96074323759690472, -12.77529261571510588, 3.513705325918512923 ) ) ;
#38980=CARTESIAN_POINT ( 'NONE',  ( 15.86395943152100330, 3.857419000648000029, 11.66670712924999975 ) ) ;
#38984=CARTESIAN_POINT ( 'NONE',  ( 13.42725895571207140, -12.36922847561405803, -1.970373770729125562 ) ) ;
#38988=CARTESIAN_POINT ( 'NONE',  ( 13.48771849468917061, 12.09748862696537763, 2.366366213948144281 ) ) ;
#38994=ORIENTED_EDGE ( 'NONE', *, *, #7971, .F. ) ;
#39009=EDGE_CURVE ( 'NONE', #52535, #23213, #19478, .T. ) ;
#39011=CARTESIAN_POINT ( 'NONE',  ( 17.94405014054366987, 11.44468665172112942, -4.547234080929012379 ) ) ;
#39022=CARTESIAN_POINT ( 'NONE',  ( 24.44496488009700030, 8.810487470433001178, 8.810507756548000557 ) ) ;
#39024=B_SPLINE_SURFACE_WITH_KNOTS ( 'NONE', 3, 3, ( 
 ( #20714, #47635, #37476, #42388 ),
 ( #10907, #11582, #32251, #64372 ),
 ( #32926, #43065, #53560, #38157 ),
 ( #54238, #6693, #2491, #1113 ),
 ( #17892, #39555, #1456, #50045 ),
 ( #66459, #65418, #50391, #60879 ) ),
 .UNSPECIFIED., .F., .F., .F.,
 ( 4, 1, 1, 4 ),
 ( 4, 4 ),
 ( 0.1423941366080999915, 0.3333333333333000081, 0.6666666666667000474, 0.8219462302419999755 ),
 ( -0.1256563615234000120, 1.125656361508000192 ),
 .UNSPECIFIED. ) ;
#39031=CARTESIAN_POINT ( 'NONE',  ( 24.30001683613300045, -12.21047198529999989, -3.271805531187999883 ) ) ;
#39036=DIRECTION ( 'NONE',  ( 0.000000000000000000, -0.5000000000000168754, 0.8660254037844288266 ) ) ;
#39037=CARTESIAN_POINT ( 'NONE',  ( 25.30000327618300204, 10.83443035398000021, -3.855530949778000149 ) ) ;
#39042=VERTEX_POINT ( 'NONE', #59224 ) ;
#39044=CARTESIAN_POINT ( 'NONE',  ( 15.90542051561399894, 3.482376784026000038, 11.36410125839000074 ) ) ;
#39046=ORIENTED_EDGE ( 'NONE', *, *, #57433, .F. ) ;
#39048=DIRECTION ( 'NONE',  ( 0.000000000000000000, -4.343197676503999927E-12, 1.000000000000000000 ) ) ;
#39051=CARTESIAN_POINT ( 'NONE',  ( 17.79999999998900151, 3.595165934733000057, 11.99793354950999991 ) ) ;
#39054=CARTESIAN_POINT ( 'NONE',  ( 24.02092288169400192, -12.55342276724000072, -3.484368012066000109 ) ) ;
#39056=ORIENTED_EDGE ( 'NONE', *, *, #67709, .T. ) ;
#39057=CARTESIAN_POINT ( 'NONE',  ( 23.72389732855361189, 13.12882099560536631, -3.830240572390830600 ) ) ;
#39060=ADVANCED_FACE ( 'NONE', ( #49085 ), #5794, .T. ) ;
#39069=CARTESIAN_POINT ( 'NONE',  ( 11.44793382097000034, -12.36841772234000025, -1.594008128907999922 ) ) ;
#39074=CARTESIAN_POINT ( 'NONE',  ( 24.63625387988400206, 12.49728986131000141, 2.949034213397000226 ) ) ;
#39078=PLANE ( 'NONE',  #64833 ) ;
#39088=CARTESIAN_POINT ( 'NONE',  ( 23.58459662445000049, -10.19731050088000046, 9.579719261187998214 ) ) ;
#39097=CARTESIAN_POINT ( 'NONE',  ( 24.69899867863799869, 3.637718165649999946, -12.18533513769000010 ) ) ;
#39100=CARTESIAN_POINT ( 'NONE',  ( 19.89999890908300273, 12.52500000000000036, 0.000000000000000000 ) ) ;
#39110=CARTESIAN_POINT ( 'NONE',  ( 24.51228084553499897, 12.11225741666999944, -3.153589928160999811 ) ) ;
#39111=CARTESIAN_POINT ( 'NONE',  ( 12.34907277967800177, -11.89802509695999966, 3.395950604129000183 ) ) ;
#39119=CARTESIAN_POINT ( 'NONE',  ( 24.14062715026257422, -9.153323484003220045, 9.127327582134411088 ) ) ;
#39122=CYLINDRICAL_SURFACE ( 'NONE', #761, 0.6999999999999992895 ) ;
#39125=CARTESIAN_POINT ( 'NONE',  ( 23.86982554649200239, 13.28496237665000024, -3.447284652217000200 ) ) ;
#39129=CARTESIAN_POINT ( 'NONE',  ( 30.60000000000000142, 0.000000000000000000, 8.250000000000000000 ) ) ;
#39132=CARTESIAN_POINT ( 'NONE',  ( 25.30000327618300204, -2.078227429405999693, 11.31065739696999906 ) ) ;
#39133=EDGE_LOOP ( 'NONE', ( #58891, #65871, #38515, #19262 ) ) ;
#39138=CARTESIAN_POINT ( 'NONE',  ( 18.54231177413599951, -11.92501070728000023, 3.951221890208000520 ) ) ;
#39139=ADVANCED_FACE ( 'NONE', ( #54324 ), #11617, .F. ) ;
#39142=EDGE_CURVE ( 'NONE', #4046, #30003, #29280, .T. ) ;
#39146=EDGE_CURVE ( 'NONE', #19263, #30607, #40436, .T. ) ;
#39149=EDGE_LOOP ( 'NONE', ( #1659, #51660, #258, #18418 ) ) ;
#39154=CARTESIAN_POINT ( 'NONE',  ( 23.58568928767000372, -3.200696684098000233, 13.61875409421000072 ) ) ;
#39156=FACE_OUTER_BOUND ( 'NONE', #59460, .T. ) ;
#39172=EDGE_LOOP ( 'NONE', ( #7773, #3938, #24952, #18173 ) ) ;
#39175=DIRECTION ( 'NONE',  ( 0.000000000000000000, 0.9466492601157000530, -0.3222656952305000266 ) ) ;
#39182=CARTESIAN_POINT ( 'NONE',  ( 24.09352403733791448, -9.221943116806739837, -9.178216524599347892 ) ) ;
#39183=ADVANCED_FACE ( 'NONE', ( #7821 ), #23209, .T. ) ;
#39186=CARTESIAN_POINT ( 'NONE',  ( 24.70770306036100195, -12.32897093773000030, 2.948671853035999657 ) ) ;
#39190=DIRECTION ( 'NONE',  ( 0.000000000000000000, 1.000000000000000000, 0.000000000000000000 ) ) ;
#39191=CARTESIAN_POINT ( 'NONE',  ( 13.46122879894100066, -12.02747180725999954, -2.509215126660999662 ) ) ;
#39216=ORIENTED_EDGE ( 'NONE', *, *, #65999, .F. ) ;
#39219=CARTESIAN_POINT ( 'NONE',  ( 17.80000000005199823, -3.345268251980999974, -11.86064071431999878 ) ) ;
#39224=CARTESIAN_POINT ( 'NONE',  ( 11.40156680346000151, 3.471758886279999956, -11.27177987500999912 ) ) ;
#39229=CARTESIAN_POINT ( 'NONE',  ( 23.60000000000000142, 0.000000000000000000, 0.000000000000000000 ) ) ;
#39243=CARTESIAN_POINT ( 'NONE',  ( 12.78082384918899983, 11.55157311154999888, -4.942237549596000257 ) ) ;
#39247=CARTESIAN_POINT ( 'NONE',  ( 24.15330281760600073, -3.593703394715999977, -12.72474830072999907 ) ) ;
#39255=CARTESIAN_POINT ( 'NONE',  ( 20.00000000000000000, 0.000000000000000000, 0.000000000000000000 ) ) ;
#39259=B_SPLINE_CURVE_WITH_KNOTS ( 'NONE', 3,
 ( #44641, #28912, #29249, #28201 ),
 .UNSPECIFIED., .F., .F.,
 ( 4, 4 ),
 ( 0.000000000000000000, 1.000000000000000000 ),
 .UNSPECIFIED. ) ;
#39273=CARTESIAN_POINT ( 'NONE',  ( 12.80000000000000071, -10.78295181803999903, 4.410266442048000002 ) ) ;
#39274=CARTESIAN_POINT ( 'NONE',  ( 11.82312259374200103, 3.643624473348999970, -12.02372562982000126 ) ) ;
#39278=B_SPLINE_CURVE_WITH_KNOTS ( 'NONE', 3,
 ( #8447, #25206, #46543, #19970 ),
 .UNSPECIFIED., .F., .F.,
 ( 4, 4 ),
 ( 0.000000000000000000, 1.000000000000000000 ),
 .UNSPECIFIED. ) ;
#39281=CARTESIAN_POINT ( 'NONE',  ( 25.39994675527853474, 8.680020655622051606, 7.390263983914236334 ) ) ;
#39288=ORIENTED_EDGE ( 'NONE', *, *, #35325, .F. ) ;
#39291=CARTESIAN_POINT ( 'NONE',  ( 13.73869549901200315, -8.889050979574999900, -7.612322772148999661 ) ) ;
#39293=CARTESIAN_POINT ( 'NONE',  ( 13.66714157633443705, -11.44713007569920471, -2.165075719400535892 ) ) ;
#39299=ORIENTED_EDGE ( 'NONE', *, *, #35531, .F. ) ;
#39303=CARTESIAN_POINT ( 'NONE',  ( 23.89493773356269202, -12.87862618918174817, 3.583998245011372319 ) ) ;
#39306=FACE_OUTER_BOUND ( 'NONE', #43338, .T. ) ;
#39307=EDGE_LOOP ( 'NONE', ( #62467, #67116, #57718 ) ) ;
#39309=EDGE_CURVE ( 'NONE', #7194, #61329, #18094, .T. ) ;
#39310=EDGE_CURVE ( 'NONE', #60101, #67640, #67565, .T. ) ;
#39313=ORIENTED_EDGE ( 'NONE', *, *, #49391, .T. ) ;
#39316=ORIENTED_EDGE ( 'NONE', *, *, #40833, .T. ) ;
#39320=CARTESIAN_POINT ( 'NONE',  ( 24.44496483130000186, -3.224879855413000040, 12.03535978074999946 ) ) ;
#39321=DIRECTION ( 'NONE',  ( 1.000000000000000000, 0.000000000000000000, 0.000000000000000000 ) ) ;
#39322=CARTESIAN_POINT ( 'NONE',  ( 11.82333928233100018, -11.49420271256999904, -1.652349626741000055 ) ) ;
#39325=ORIENTED_EDGE ( 'NONE', *, *, #33395, .F. ) ;
#39326=CYLINDRICAL_SURFACE ( 'NONE', #40351, 0.6999999999999992895 ) ;
#39337=ORIENTED_EDGE ( 'NONE', *, *, #17526, .T. ) ;
#39341=CARTESIAN_POINT ( 'NONE',  ( 23.57797122970793069, 3.138867034835534753, -13.63060662545491830 ) ) ;
#39348=ORIENTED_EDGE ( 'NONE', *, *, #5481, .F. ) ;
#39353=DIRECTION ( 'NONE',  ( 0.000000000000000000, 0.000000000000000000, -1.000000000000000000 ) ) ;
#39356=CARTESIAN_POINT ( 'NONE',  ( 11.29998658800000122, 3.824194713071000340, -11.71675648045999907 ) ) ;
#39369=CYLINDRICAL_SURFACE ( 'NONE', #48776, 0.6999999999999992895 ) ;
#39382=CARTESIAN_POINT ( 'NONE',  ( 24.39664881864633372, 12.09373461225363577, -3.240506422828615118 ) ) ;
#39391=CARTESIAN_POINT ( 'NONE',  ( 24.45617574064404209, 8.883483999841056189, 9.170518729239159228 ) ) ;
#39396=CARTESIAN_POINT ( 'NONE',  ( 23.62018009300800259, -13.19635161574000115, -4.176881764676999786 ) ) ;
#39398=VECTOR ( 'NONE', #5805, 1000.000000000000227 ) ;
#39401=CARTESIAN_POINT ( 'NONE',  ( 25.29995873461299993, 11.13046969959000165, 3.427501705020000067 ) ) ;
#39403=LINE ( 'NONE', #23659, #66155 ) ;
#39410=VERTEX_POINT ( 'NONE', #4625 ) ;
#39411=AXIS2_PLACEMENT_3D ( 'NONE', #30615, #40757, #68342 ) ;
#39412=CARTESIAN_POINT ( 'NONE',  ( 25.29995823066400362, -11.13046982544999963, 3.427501264366999756 ) ) ;
#39415=ADVANCED_FACE ( 'NONE', ( #31903 ), #1033, .F. ) ;
#39418=FACE_OUTER_BOUND ( 'NONE', #25013, .T. ) ;
#39425=CARTESIAN_POINT ( 'NONE',  ( 25.34480935285659697, -2.689020825566641459, 11.33835534259811695 ) ) ;
#39431=CARTESIAN_POINT ( 'NONE',  ( 24.32733123024100053, -9.023571280490999769, 9.340699019152999938 ) ) ;
#39438=FACE_OUTER_BOUND ( 'NONE', #14247, .T. ) ;
#39440=ORIENTED_EDGE ( 'NONE', *, *, #39142, .F. ) ;
#39442=CARTESIAN_POINT ( 'NONE',  ( 12.09999922233642522, -11.66744139996562701, 3.971920075675145156 ) ) ;
#39447=ADVANCED_FACE ( 'NONE', ( #15477 ), #50472, .T. ) ;
#39449=ADVANCED_FACE ( 'NONE', ( #3090 ), #24075, .T. ) ;
#39456=CARTESIAN_POINT ( 'NONE',  ( 11.75744248190100016, -3.642994321184000128, 12.02392698342999999 ) ) ;
#39461=CARTESIAN_POINT ( 'NONE',  ( 23.55064464012300363, 2.917691328521999861, 13.72936262135999996 ) ) ;
#39464=CARTESIAN_POINT ( 'NONE',  ( 24.77777987740767429, -11.71376540346410344, -3.192706928545757439 ) ) ;
#39466=ORIENTED_EDGE ( 'NONE', *, *, #55660, .F. ) ;
#39472=DIRECTION ( 'NONE',  ( 1.000000000000000000, 0.000000000000000000, 0.000000000000000000 ) ) ;
#39477=ORIENTED_EDGE ( 'NONE', *, *, #52920, .F. ) ;
#39478=DIRECTION ( 'NONE',  ( 1.000000000000000000, 0.000000000000000000, 0.000000000000000000 ) ) ;
#39482=CARTESIAN_POINT ( 'NONE',  ( 25.29987261391899978, -8.756202924575998026, 7.455126447192999883 ) ) ;
#39483=VERTEX_POINT ( 'NONE', #67060 ) ;
#39487=CARTESIAN_POINT ( 'NONE',  ( 25.59997239626699894, 8.218962773316999204, -8.043525096612999192 ) ) ;
#39488=CARTESIAN_POINT ( 'NONE',  ( 18.21574065333400227, -11.85428844745999832, 3.556939559956999730 ) ) ;
#39497=CARTESIAN_POINT ( 'NONE',  ( 12.10941541359317775, -11.07487266634617029, 3.615341447084566173 ) ) ;
#39502=CARTESIAN_POINT ( 'NONE',  ( 18.38069952315600020, 3.381269036354999979, -12.09968217836000015 ) ) ;
#39509=CARTESIAN_POINT ( 'NONE',  ( 24.72544608131600086, -3.605127478668999963, -12.13010612098000074 ) ) ;
#39521=B_SPLINE_CURVE_WITH_KNOTS ( 'NONE', 3,
 ( #7931, #17737, #13188, #8272 ),
 .UNSPECIFIED., .F., .F.,
 ( 4, 4 ),
 ( 0.000000000000000000, 1.000000000000000000 ),
 .UNSPECIFIED. ) ;
#39527=EDGE_LOOP ( 'NONE', ( #48841, #26582, #61177, #23081 ) ) ;
#39528=B_SPLINE_CURVE_WITH_KNOTS ( 'NONE', 3,
 ( #32038, #11721, #22560, #557 ),
 .UNSPECIFIED., .F., .F.,
 ( 4, 4 ),
 ( 0.000000000000000000, 1.000000000000000000 ),
 .UNSPECIFIED. ) ;
#39538=CARTESIAN_POINT ( 'NONE',  ( 15.89994436294300151, 8.847904542234999781, 8.580301953175000662 ) ) ;
#39539=CARTESIAN_POINT ( 'NONE',  ( 13.06531638133300177, -12.22210578456000007, -1.955102404769999858 ) ) ;
#39541=EDGE_CURVE ( 'NONE', #7173, #28639, #48706, .T. ) ;
#39552=CARTESIAN_POINT ( 'NONE',  ( 18.50001572531399674, 1.956586078199225032, 12.40985500087345095 ) ) ;
#39555=CARTESIAN_POINT ( 'NONE',  ( 24.36504260745899941, 12.29008018610999819, 3.201257196435000285 ) ) ;
#39557=ORIENTED_EDGE ( 'NONE', *, *, #28904, .T. ) ;
#39562=ORIENTED_EDGE ( 'NONE', *, *, #56232, .T. ) ;
#39564=CARTESIAN_POINT ( 'NONE',  ( 18.49996808500600309, -0.9036517527673039174, 11.65000000008756054 ) ) ;
#39567=CARTESIAN_POINT ( 'NONE',  ( 24.30000000000000071, 3.224868684338999980, 12.03537377768999939 ) ) ;
#39571=CARTESIAN_POINT ( 'NONE',  ( 11.84835150974899953, 3.192438788486000156, -11.44998398973999976 ) ) ;
#39585=EDGE_CURVE ( 'NONE', #58094, #36031, #5360, .T. ) ;
#39588=ORIENTED_EDGE ( 'NONE', *, *, #65735, .F. ) ;
#39589=CARTESIAN_POINT ( 'NONE',  ( 23.73952401786024780, 13.33635412649179308, -3.648243621897288236 ) ) ;
#39594=B_SPLINE_SURFACE_WITH_KNOTS ( 'NONE', 3, 3, ( 
 ( #44556, #12025, #60270, #12724 ),
 ( #50816, #33361, #2911, #6774 ),
 ( #49423, #34742, #56053, #49778 ),
 ( #1536, #22854, #23206, #65848 ),
 ( #17972, #39291, #46607, #52181 ),
 ( #36104, #45910, #61641, #35428 ),
 ( #62998, #14448, #57764, #52525 ),
 ( #30522, #29855, #62665, #67222 ),
 ( #47289, #4282, #51836, #14785 ) ),
 .UNSPECIFIED., .F., .F., .F.,
 ( 4, 1, 1, 1, 1, 1, 4 ),
 ( 4, 4 ),
 ( 0.02209653170519000273, 0.1666666666667000196, 0.3333333333333000081, 0.5000000000000000000, 0.6666666666667000474, 0.8333333333333000637, 0.9492823795161999811 ),
 ( -0.1916656884162999952, 1.191851428473000185 ),
 .UNSPECIFIED. ) ;
#39607=CARTESIAN_POINT ( 'NONE',  ( 25.44994642811700203, 0.000000000000000000, -11.34994642770978501 ) ) ;
#39624=AXIS2_PLACEMENT_3D ( 'NONE', #44208, #28467, #43508 ) ;
#39629=DIRECTION ( 'NONE',  ( -0.9709491189737906591, -0.2392860387987982285, 0.000000000000000000 ) ) ;
#39638=DIRECTION ( 'NONE',  ( 0.000000000000000000, -0.7614089499631913061, -0.6482718649732923666 ) ) ;
#39642=CARTESIAN_POINT ( 'NONE',  ( 13.51587707751000167, 12.16770442808000041, 2.286102833273000012 ) ) ;
#39647=CARTESIAN_POINT ( 'NONE',  ( 24.84564481170258432, -8.580162300291068078, -9.011334502445274452 ) ) ;
#39659=ORIENTED_EDGE ( 'NONE', *, *, #4827, .F. ) ;
#39666=CARTESIAN_POINT ( 'NONE',  ( 24.30000000000000071, -11.77655473258999841, -4.190794510628000680 ) ) ;
#39668=CARTESIAN_POINT ( 'NONE',  ( 24.35365242081699932, 3.253466243142002057, 12.21167519476998464 ) ) ;
#39683=B_SPLINE_CURVE_WITH_KNOTS ( 'NONE', 3,
 ( #52807, #46534, #41286, #15407, #30455, #67841 ),
 .UNSPECIFIED., .F., .F.,
 ( 4, 2, 4 ),
 ( 0.000000000000000000, 0.5000000000000000000, 1.000000000000000000 ),
 .UNSPECIFIED. ) ;
#39688=CIRCLE ( 'NONE', #48615, 0.6999999999999992895 ) ;
#39692=CARTESIAN_POINT ( 'NONE',  ( 11.49977531252999974, 12.49365449110755222, 1.022561121909975057 ) ) ;
#39694=DIRECTION ( 'NONE',  ( 3.910744185214936488E-06, 0.9659310281233842721, 0.2587996307825956022 ) ) ;
#39696=EDGE_LOOP ( 'NONE', ( #62748, #30899, #15339, #40543, #39974, #17025 ) ) ;
#39702=ORIENTED_EDGE ( 'NONE', *, *, #47750, .F. ) ;
#39703=DIRECTION ( 'NONE',  ( -1.000000000000000000, 0.000000000000000000, 0.000000000000000000 ) ) ;
#39708=( BOUNDED_SURFACE ( )  B_SPLINE_SURFACE ( 3, 3, ( 
 ( #17470, #44742, #1048, #12920 ),
 ( #38795, #49625, #66040, #55568 ),
 ( #33552, #22360, #28302, #43698 ),
 ( #12571, #1386, #60119, #45082 ) ),
 .UNSPECIFIED., .F., .F., .T. ) 
 B_SPLINE_SURFACE_WITH_KNOTS ( ( 4, 4 ),
 ( 4, 4 ),
 ( 0.000000000000000000, 1.000000000000000000 ),
 ( 0.000000000000000000, 1.000000000000000000 ),
 .UNSPECIFIED. ) 
 GEOMETRIC_REPRESENTATION_ITEM ( )  RATIONAL_B_SPLINE_SURFACE ( (
 ( 1.512182578520000042, 1.160176301760999840, 1.160176301760999840, 1.512182578520000042),
 ( 1.111288591041000196, 0.8526025270081000196, 0.8526025270081000196, 1.111288591041000196),
 ( 1.111288591041000196, 0.8526025270081000196, 0.8526025270081000196, 1.111288591041000196),
 ( 1.512182578520000042, 1.160176301760999840, 1.160176301760999840, 1.512182578520000042) ) ) 
 REPRESENTATION_ITEM ( '' )  SURFACE ( )  );
#39719=CARTESIAN_POINT ( 'NONE',  ( 24.00946646489260061, -12.69708847614298364, -3.467516079534666673 ) ) ;
#39721=DIRECTION ( 'NONE',  ( 0.000000000000000000, 0.000000000000000000, -1.000000000000000000 ) ) ;
#39730=ORIENTED_EDGE ( 'NONE', *, *, #40346, .T. ) ;
#39734=DIRECTION ( 'NONE',  ( 1.000000000000000000, 0.000000000000000000, 0.000000000000000000 ) ) ;
#39737=ORIENTED_EDGE ( 'NONE', *, *, #61959, .T. ) ;
#39745=CARTESIAN_POINT ( 'NONE',  ( 23.66566003730900292, -13.24658845605999957, -3.907283439093999888 ) ) ;
#39749=CARTESIAN_POINT ( 'NONE',  ( 25.44993786153500182, 9.517611874540000017, -8.103398312166000039 ) ) ;
#39753=CARTESIAN_POINT ( 'NONE',  ( 23.79457394410595228, -3.298060182730888634, -13.14148511287618604 ) ) ;
#39763=VECTOR ( 'NONE', #18970, 1000.000000000000114 ) ;
#39767=CIRCLE ( 'NONE', #45357, 11.50000000000000178 ) ;
#39768=LINE ( 'NONE', #2699, #54001 ) ;
#39769=CARTESIAN_POINT ( 'NONE',  ( 24.25865930858300246, 12.09696615184000024, 3.327219372371000183 ) ) ;
#39770=ORIENTED_EDGE ( 'NONE', *, *, #60409, .F. ) ;
#39774=CARTESIAN_POINT ( 'NONE',  ( 11.29996927726999978, -12.23272628844000032, -1.505586261403999870 ) ) ;
#39783=EDGE_LOOP ( 'NONE', ( #63017, #18323, #24344, #40849 ) ) ;
#39788=CARTESIAN_POINT ( 'NONE',  ( 23.60205915885299888, -2.504446818059999469, 12.27382285987999211 ) ) ;
#39798=CARTESIAN_POINT ( 'NONE',  ( 13.49980696793000057, -9.514462421839999351, -7.834836582454001608 ) ) ;
#39804=CARTESIAN_POINT ( 'NONE',  ( 13.99999999231800096, 8.833253877201999060, 7.896562762484000686 ) ) ;
#39812=LINE ( 'NONE', #61134, #18758 ) ;
#39836=CARTESIAN_POINT ( 'NONE',  ( 17.60891751954699913, -11.55195517866999921, 4.941472061358999746 ) ) ;
#39848=CONICAL_SURFACE ( 'NONE', #43180, 11.75016914289000169, 0.7854125553233202162 ) ;
#39851=CARTESIAN_POINT ( 'NONE',  ( 18.16350100824700320, 3.138009765975000143, -11.88148072165000002 ) ) ;
#39854=AXIS2_PLACEMENT_3D ( 'NONE', #29685, #2067, #67056 ) ;
#39857=ORIENTED_EDGE ( 'NONE', *, *, #55004, .F. ) ;
#39868=VECTOR ( 'NONE', #11940, 1000.000000000000114 ) ;
#39875=DIRECTION ( 'NONE',  ( 0.000000000000000000, 0.3380237670531082705, 0.9411375738473234387 ) ) ;
#39884=CARTESIAN_POINT ( 'NONE',  ( 12.79999999975700042, 11.86189249994999884, -3.298671769835999967 ) ) ;
#39885=DIRECTION ( 'NONE',  ( 0.000000000000000000, -1.000000000000000000, -3.072868395130999887E-14 ) ) ;
#39886=CARTESIAN_POINT ( 'NONE',  ( 16.39999999379500295, 3.351248059343999941, 11.15756683833000018 ) ) ;
#39888=CARTESIAN_POINT ( 'NONE',  ( 25.29987654162099986, 9.517611874540000017, 8.103398312166000039 ) ) ;
#39890=CARTESIAN_POINT ( 'NONE',  ( 13.68724299200000161, -12.36060503258000054, -2.247042498203000171 ) ) ;
#39900=EDGE_CURVE ( 'NONE', #63935, #60029, #62800, .T. ) ;
#39906=CIRCLE ( 'NONE', #29885, 0.6999999999999992895 ) ;
#39907=LINE ( 'NONE', #55291, #43398 ) ;
#39924=CARTESIAN_POINT ( 'NONE',  ( 11.61719580513100247, 3.441045665385999985, -11.09087012887000157 ) ) ;
#39944=CARTESIAN_POINT ( 'NONE',  ( 23.95106197147099891, -3.419222116214999829, -12.90055402021999953 ) ) ;
#39960=CARTESIAN_POINT ( 'NONE',  ( 15.95296092448800174, -8.433319028468000411, -8.247373098099998856 ) ) ;
#39962=CARTESIAN_POINT ( 'NONE',  ( 23.62276920851202888, -13.40178483158021550, 3.911135730022063939 ) ) ;
#39964=CIRCLE ( 'NONE', #63333, 0.2000000000000007327 ) ;
#39970=AXIS2_PLACEMENT_3D ( 'NONE', #44027, #28992, #7996 ) ;
#39974=ORIENTED_EDGE ( 'NONE', *, *, #51055, .F. ) ;
#39977=B_SPLINE_CURVE_WITH_KNOTS ( 'NONE', 3,
 ( #26636, #21372, #62976, #64349, #10199, #63322 ),
 .UNSPECIFIED., .F., .F.,
 ( 4, 2, 4 ),
 ( 0.000000000000000000, 0.5000000000000000000, 1.000000000000000000 ),
 .UNSPECIFIED. ) ;
#39986=CARTESIAN_POINT ( 'NONE',  ( 25.19548556333399958, 11.71503697860999971, 2.904522712328000189 ) ) ;
#39990=CYLINDRICAL_SURFACE ( 'NONE', #13147, 1.000000000000000444 ) ;
#39995=DIRECTION ( 'NONE',  ( -1.000000000000000000, 0.000000000000000000, 0.000000000000000000 ) ) ;
#39997=ORIENTED_EDGE ( 'NONE', *, *, #18191, .F. ) ;
#39999=CARTESIAN_POINT ( 'NONE',  ( 24.99826568414079375, 2.941276671990348923, 11.56308286680369335 ) ) ;
#40002=CARTESIAN_POINT ( 'NONE',  ( 13.86901036581968860, -9.187486520156699754, -8.213234632844541139 ) ) ;
#40019=CARTESIAN_POINT ( 'NONE',  ( 23.89320776801300283, 2.594336453666000075, 11.06325219639999347 ) ) ;
#40023=EDGE_CURVE ( 'NONE', #60967, #25005, #66896, .T. ) ;
#40027=CARTESIAN_POINT ( 'NONE',  ( 24.53428985367600390, -3.614319203926000146, 12.31267510079000083 ) ) ;
#40042=APPLICATION_CONTEXT ( 'automotive_design' ) ;
#40043=CARTESIAN_POINT ( 'NONE',  ( 24.13681596746900127, 9.106586331126999667, -8.984417095254999097 ) ) ;
#40050=AXIS2_PLACEMENT_3D ( 'NONE', #26868, #27206, #21946 ) ;
#40051=CARTESIAN_POINT ( 'NONE',  ( 24.35365242081699932, -12.20235406300999514, -3.288253180468997172 ) ) ;
#40062=CARTESIAN_POINT ( 'NONE',  ( 24.44496356232399847, -3.224881240379999792, -12.03535804424000055 ) ) ;
#40070=CARTESIAN_POINT ( 'NONE',  ( 24.03569461241779237, -12.65453166998849177, -3.444226028244401494 ) ) ;
#40072=CARTESIAN_POINT ( 'NONE',  ( 13.60016906737400078, -1.856292897172999960E-13, -4.263256414560999963E-14 ) ) ;
#40078=CONICAL_SURFACE ( 'NONE', #991, 13.94234653057000095, 1.233427434088239627 ) ;
#40083=EDGE_LOOP ( 'NONE', ( #50, #35454, #26728, #8093 ) ) ;
#40084=CARTESIAN_POINT ( 'NONE',  ( 15.90003771078200145, -3.695138809391000034, -11.25918926437999978 ) ) ;
#40087=VERTEX_POINT ( 'NONE', #11263 ) ;
#40089=CARTESIAN_POINT ( 'NONE',  ( 25.29989727901499919, -2.078227429405999693, -11.31065739696999906 ) ) ;
#40091=CARTESIAN_POINT ( 'NONE',  ( 25.39409999158950271, 8.421103250990364941, -8.066018968039331938 ) ) ;
#40093=EDGE_LOOP ( 'NONE', ( #35841, #55042, #21824, #67714 ) ) ;
#40104=AXIS2_PLACEMENT_3D ( 'NONE', #13569, #43999, #27920 ) ;
#40109=ORIENTED_EDGE ( 'NONE', *, *, #16089, .T. ) ;
#40111=ORIENTED_EDGE ( 'NONE', *, *, #64901, .F. ) ;
#40116=PLANE ( 'NONE',  #30557 ) ;
#40121=CARTESIAN_POINT ( 'NONE',  ( 18.49996808500599954, -1.807259461627081842, -11.54438823547436499 ) ) ;
#40128=DIRECTION ( 'NONE',  ( 0.000000000000000000, 0.4998826579293298988, -0.8660931406618509465 ) ) ;
#40133=PLANE ( 'NONE',  #27669 ) ;
#40134=ORIENTED_EDGE ( 'NONE', *, *, #14218, .F. ) ;
#40137=CARTESIAN_POINT ( 'NONE',  ( 23.57793118131190724, 3.116419977577632672, 13.63419877650960821 ) ) ;
#40138=CARTESIAN_POINT ( 'NONE',  ( 24.30000000000000071, -8.810505093353000916, -8.810505093353000916 ) ) ;
#40139=ORIENTED_EDGE ( 'NONE', *, *, #3319, .T. ) ;
#40143=B_SPLINE_CURVE_WITH_KNOTS ( 'NONE', 3,
 ( #65052, #38501, #50729, #66801 ),
 .UNSPECIFIED., .F., .F.,
 ( 4, 4 ),
 ( 0.000000000000000000, 1.000000000000000000 ),
 .UNSPECIFIED. ) ;
#40148=ADVANCED_FACE ( 'NONE', ( #6014 ), #67181, .T. ) ;
#40152=CARTESIAN_POINT ( 'NONE',  ( 11.80707028823900195, -3.411567914393000223, 11.89801974982000132 ) ) ;
#40159=CARTESIAN_POINT ( 'NONE',  ( 18.50001572531400029, -2.908166856580999937, 12.18270046149000052 ) ) ;
#40160=B_SPLINE_CURVE_WITH_KNOTS ( 'NONE', 3,
 ( #22001, #63623, #15739, #47904 ),
 .UNSPECIFIED., .F., .F.,
 ( 4, 4 ),
 ( 0.000000000000000000, 1.000000000000000000 ),
 .UNSPECIFIED. ) ;
#40164=EDGE_LOOP ( 'NONE', ( #41902, #12358, #1996, #63450 ) ) ;
#40167=CARTESIAN_POINT ( 'NONE',  ( 13.99999999231800096, -8.833253877201999060, -7.896562762484000686 ) ) ;
#40168=DIRECTION ( 'NONE',  ( 1.000000000000000000, 0.000000000000000000, 0.000000000000000000 ) ) ;
#40176=ORIENTED_EDGE ( 'NONE', *, *, #50265, .T. ) ;
#40182=CARTESIAN_POINT ( 'NONE',  ( 17.76385332268500150, -3.526697956045000026, -11.96114712952999959 ) ) ;
#40183=CARTESIAN_POINT ( 'NONE',  ( 24.36504260833099877, -8.917410148446000662, 9.042893056734001789 ) ) ;
#40196=CARTESIAN_POINT ( 'NONE',  ( 13.49999720188826480, 11.61513859405367022, 2.353594668653353317 ) ) ;
#40201=VERTEX_POINT ( 'NONE', #1127 ) ;
#40207=ADVANCED_FACE ( 'NONE', ( #63713 ), #26103, .F. ) ;
#40235=CARTESIAN_POINT ( 'NONE',  ( 21.70000133425200062, 0.000000000000000000, 0.000000000000000000 ) ) ;
#40246=DIRECTION ( 'NONE',  ( -1.000000000000000000, 0.000000000000000000, 0.000000000000000000 ) ) ;
#40249=EDGE_LOOP ( 'NONE', ( #3772, #6427 ) ) ;
#40251=FACE_OUTER_BOUND ( 'NONE', #2417, .T. ) ;
#40252=VERTEX_POINT ( 'NONE', #65780 ) ;
#40273=CARTESIAN_POINT ( 'NONE',  ( 24.70907584035216686, 8.654457188012020907, 8.608358926410405232 ) ) ;
#40278=EDGE_LOOP ( 'NONE', ( #48463, #22899, #9992, #65517 ) ) ;
#40284=CARTESIAN_POINT ( 'NONE',  ( 24.45265319665800163, -3.540849845907999782, -12.31960893685999991 ) ) ;
#40295=CARTESIAN_POINT ( 'NONE',  ( 16.04720874474600123, -8.391565830097999168, -8.158729932893001191 ) ) ;
#40297=DIRECTION ( 'NONE',  ( -1.000000000000000000, 0.000000000000000000, 0.000000000000000000 ) ) ;
#40304=CIRCLE ( 'NONE', #3461, 0.6999999999999992895 ) ;
#40307=CARTESIAN_POINT ( 'NONE',  ( 17.80000000009400196, -3.216307036143000175, -11.40341376487999980 ) ) ;
#40310=DIRECTION ( 'NONE',  ( 0.000000000000000000, 0.2714570858282905341, 0.9624505444715651947 ) ) ;
#40314=EDGE_CURVE ( 'NONE', #65865, #7350, #52763, .T. ) ;
#40323=DIRECTION ( 'NONE',  ( 0.000000000000000000, 0.7614089499631907509, -0.6482718649732929217 ) ) ;
#40330=ORIENTED_EDGE ( 'NONE', *, *, #54444, .F. ) ;
#40334=CARTESIAN_POINT ( 'NONE',  ( 23.97711676181098639, -12.74913932280401063, 3.497788515081389882 ) ) ;
#40337=CARTESIAN_POINT ( 'NONE',  ( 11.79999999684100054, -12.15995044155999949, -2.000340912084999978 ) ) ;
#40345=CARTESIAN_POINT ( 'NONE',  ( 0.000000000000000000, 0.000000000000000000, 0.000000000000000000 ) ) ;
#40346=EDGE_CURVE ( 'NONE', #12493, #29053, #11917, .T. ) ;
#40347=ORIENTED_EDGE ( 'NONE', *, *, #25356, .F. ) ;
#40351=AXIS2_PLACEMENT_3D ( 'NONE', #6466, #60647, #33397 ) ;
#40352=CARTESIAN_POINT ( 'NONE',  ( 24.61098151538899970, -12.21941909980999874, -3.050810341055000041 ) ) ;
#40354=EDGE_LOOP ( 'NONE', ( #14816, #39557, #25395, #47540 ) ) ;
#40355=CARTESIAN_POINT ( 'NONE',  ( 24.30001694968100168, 3.271769180623000040, -12.21048179117000032 ) ) ;
#40370=CARTESIAN_POINT ( 'NONE',  ( 24.05250980246030679, 3.342975859377496750, 12.65038706989959927 ) ) ;
#40371=CARTESIAN_POINT ( 'NONE',  ( 23.51693413382500353, 10.50595995297999963, -9.452639959603999387 ) ) ;
#40372=CARTESIAN_POINT ( 'NONE',  ( 17.99211270977099986, -3.227071166021000082, -11.34499727797000013 ) ) ;
#40376=ORIENTED_EDGE ( 'NONE', *, *, #68270, .F. ) ;
#40378=CARTESIAN_POINT ( 'NONE',  ( 23.60205915885299888, -11.72032963060998867, -3.891881970952999481 ) ) ;
#40384=B_SPLINE_CURVE_WITH_KNOTS ( 'NONE', 3,
 ( #20710, #58453, #10557, #68588 ),
 .UNSPECIFIED., .F., .F.,
 ( 4, 4 ),
 ( 0.000000000000000000, 1.000000000000000000 ),
 .UNSPECIFIED. ) ;
#40393=CARTESIAN_POINT ( 'NONE',  ( 16.09997386696500143, 4.522001505202922544, 10.77728718286269149 ) ) ;
#40403=VERTEX_POINT ( 'NONE', #49681 ) ;
#40406=CARTESIAN_POINT ( 'NONE',  ( 16.10005255078199937, -3.632778330393000132, -11.06917548872000090 ) ) ;
#40408=VECTOR ( 'NONE', #30898, 1000.000000000000227 ) ;
#40414=CARTESIAN_POINT ( 'NONE',  ( 16.39999999231800132, -3.216285993016000155, -11.40340220863999932 ) ) ;
#40416=ORIENTED_EDGE ( 'NONE', *, *, #69169, .F. ) ;
#40422=ORIENTED_EDGE ( 'NONE', *, *, #45546, .T. ) ;
#40426=CARTESIAN_POINT ( 'NONE',  ( 23.80953449760752605, -3.305759387292704243, -13.11171555762221530 ) ) ;
#40432=ORIENTED_EDGE ( 'NONE', *, *, #17841, .T. ) ;
#40436=CIRCLE ( 'NONE', #42640, 13.92493900950999475 ) ;
#40440=FACE_OUTER_BOUND ( 'NONE', #9903, .T. ) ;
#40442=VERTEX_POINT ( 'NONE', #59470 ) ;
#40452=DIRECTION ( 'NONE',  ( -1.000000000000000000, 0.000000000000000000, 0.000000000000000000 ) ) ;
#40455=CARTESIAN_POINT ( 'NONE',  ( 24.50549018585800098, 3.501736898117000063, 12.23514954116999931 ) ) ;
#40457=LINE ( 'NONE', #15271, #42193 ) ;
#40464=CARTESIAN_POINT ( 'NONE',  ( 17.75870478550200104, 3.641518898264000548, 12.02435208579999859 ) ) ;
#40474=CARTESIAN_POINT ( 'NONE',  ( 24.30001694391200218, -12.21047201246000036, 3.271805662802000025 ) ) ;
#40478=ADVANCED_FACE ( 'NONE', ( #59822 ), #43054, .T. ) ;
#40486=TOROIDAL_SURFACE ( 'NONE', #20376, 12.20000000000000107, 0.6999999999999999556 ) ;
#40490=CARTESIAN_POINT ( 'NONE',  ( 24.30000000000000071, -9.240454295252998662, -8.250504801592001058 ) ) ;
#40491=ORIENTED_EDGE ( 'NONE', *, *, #45922, .F. ) ;
#40499=EDGE_CURVE ( 'NONE', #50417, #60537, #31141, .T. ) ;
#40504=CARTESIAN_POINT ( 'NONE',  ( 24.12730417462044130, 9.172513492733058271, 9.141935095995247451 ) ) ;
#40510=CARTESIAN_POINT ( 'NONE',  ( 18.23043922992600230, -3.518658233831999826, -12.06062508533999988 ) ) ;
#40511=CARTESIAN_POINT ( 'NONE',  ( 24.66271478023099917, -8.757902662108000058, 9.242626226729999672 ) ) ;
#40517=B_SPLINE_CURVE_WITH_KNOTS ( 'NONE', 3,
 ( #27772, #22159, #27075, #32327 ),
 .UNSPECIFIED., .F., .F.,
 ( 4, 4 ),
 ( 0.000000000000000000, 1.000000000000000000 ),
 .UNSPECIFIED. ) ;
#40528=ADVANCED_FACE ( 'NONE', ( #22410 ), #40486, .F. ) ;
#40535=AXIS2_PLACEMENT_3D ( 'NONE', #30082, #7708, #39875 ) ;
#40543=ORIENTED_EDGE ( 'NONE', *, *, #67603, .F. ) ;
#40556=CARTESIAN_POINT ( 'NONE',  ( 12.79999999838119962, 11.94789761932849004, -3.252399792653988264 ) ) ;
#40558=CARTESIAN_POINT ( 'NONE',  ( 11.79999998956225937, -3.428554832065387359, 11.90642801602077228 ) ) ;
#40575=DIRECTION ( 'NONE',  ( 1.000000000000000000, 0.000000000000000000, 0.000000000000000000 ) ) ;
#40578=CARTESIAN_POINT ( 'NONE',  ( 24.30000000000000071, -11.49391741900999975, 4.090215442373000165 ) ) ;
#40579=CARTESIAN_POINT ( 'NONE',  ( 18.30000000000000071, -2.775703640144308260, -11.68316444257406772 ) ) ;
#40583=CONICAL_SURFACE ( 'NONE', #47276, 1.150079926948000208, 0.7854585090185547402 ) ;
#40586=EDGE_LOOP ( 'NONE', ( #48791, #39348, #36596, #7619, #34892 ) ) ;
#40587=CONICAL_SURFACE ( 'NONE', #66235, 11.34994642770999818, 0.7853934433894341760 ) ;
#40593=CARTESIAN_POINT ( 'NONE',  ( 24.76117126521998557, -3.101100257814066730, -11.75475255056689505 ) ) ;
#40595=CARTESIAN_POINT ( 'NONE',  ( 24.30000000000000071, 0.000000000000000000, 0.000000000000000000 ) ) ;
#40605=FACE_OUTER_BOUND ( 'NONE', #57788, .T. ) ;
#40606=CARTESIAN_POINT ( 'NONE',  ( 24.81125947960093114, 8.606650034182759867, 8.517985928714615795 ) ) ;
#40616=FACE_OUTER_BOUND ( 'NONE', #25885, .T. ) ;
#40620=CARTESIAN_POINT ( 'NONE',  ( 23.59999462723899910, 13.22316330987000121, -4.267799687262000319 ) ) ;
#40621=CARTESIAN_POINT ( 'NONE',  ( 17.60000000000000142, -11.23412379136000006, 3.084957477885999833 ) ) ;
#40629=CARTESIAN_POINT ( 'NONE',  ( 15.84051303026600266, -8.692957937327999929, -7.975472622866001338 ) ) ;
#40640=CARTESIAN_POINT ( 'NONE',  ( 23.56666365135700403, 9.114812703071004663, -8.684180617907001576 ) ) ;
#40641=ORIENTED_EDGE ( 'NONE', *, *, #44282, .F. ) ;
#40643=ADVANCED_FACE ( 'NONE', ( #5639 ), #6951, .T. ) ;
#40644=AXIS2_PLACEMENT_3D ( 'NONE', #8339, #45744, #57589 ) ;
#40646=DIRECTION ( 'NONE',  ( 1.000000000000000000, 0.000000000000000000, 0.000000000000000000 ) ) ;
#40655=VERTEX_POINT ( 'NONE', #54731 ) ;
#40656=CARTESIAN_POINT ( 'NONE',  ( 24.32158561237937988, 3.683026774043987039, -12.56966788568789894 ) ) ;
#40659=CARTESIAN_POINT ( 'NONE',  ( 23.62794487920146835, 13.40242465305992070, 3.894877993122662474 ) ) ;
#40660=CARTESIAN_POINT ( 'NONE',  ( 16.42341781689399838, -3.643648243171000001, -12.02373124034999918 ) ) ;
#40672=CARTESIAN_POINT ( 'NONE',  ( 18.28832092577790291, 2.855728055076846683, -11.50255606648410023 ) ) ;
#40675=B_SPLINE_CURVE_WITH_KNOTS ( 'NONE', 3,
 ( #44999, #19449, #50925, #18774 ),
 .UNSPECIFIED., .F., .F.,
 ( 4, 4 ),
 ( 0.000000000000000000, 1.000000000000000000 ),
 .UNSPECIFIED. ) ;
#40677=FACE_OUTER_BOUND ( 'NONE', #40835, .T. ) ;
#40679=CARTESIAN_POINT ( 'NONE',  ( 25.60000000000000142, 8.527654132752997995, -7.260537518969999660 ) ) ;
#40688=CARTESIAN_POINT ( 'NONE',  ( 16.10004050617000004, 3.886235259787000018, 11.90683839252000098 ) ) ;
#40689=CARTESIAN_POINT ( 'NONE',  ( 24.44917776433500123, -12.41482580133999924, -3.103222239774000357 ) ) ;
#40691=ORIENTED_EDGE ( 'NONE', *, *, #58556, .T. ) ;
#40701=CARTESIAN_POINT ( 'NONE',  ( 18.12922381500399993, 3.157787539580000136, 11.36563583066999961 ) ) ;
#40709=CARTESIAN_POINT ( 'NONE',  ( 25.52342880444300022, 8.321935307164999074, -8.140383335223001282 ) ) ;
#40710=CARTESIAN_POINT ( 'NONE',  ( 23.91242621194999884, 9.487396930725999766, -9.248180533506999978 ) ) ;
#40717=CARTESIAN_POINT ( 'NONE',  ( 21.60000012424471194, 3.970157536060000036E-13, -13.89999856298982372 ) ) ;
#40730=B_SPLINE_SURFACE_WITH_KNOTS ( 'NONE', 3, 3, ( 
 ( #61987, #67559, #23892, #41005 ),
 ( #18309, #50462, #2563, #12719 ),
 ( #19329, #66533, #45573, #34051 ),
 ( #66879, #50124, #61300, #7461 ),
 ( #18653, #34399, #55717, #39986 ),
 ( #9179, #47286, #62328, #31550 ),
 ( #37134, #36101, #35763, #68942 ),
 ( #31216, #9521, #26304, #30519 ) ),
 .UNSPECIFIED., .F., .F., .F.,
 ( 4, 1, 1, 1, 1, 4 ),
 ( 4, 4 ),
 ( 0.7453054410233999061, 0.7647058823529000460, 0.8235294117646999590, 0.8823529411764999830, 0.9411764705882000870, 0.9905827552260000335 ),
 ( -0.1830915166815000050, 1.182948990397000077 ),
 .UNSPECIFIED. ) ;
#40731=CARTESIAN_POINT ( 'NONE',  ( 25.29986734212600297, -2.258942858049999725, 12.29419282279000036 ) ) ;
#40737=CARTESIAN_POINT ( 'NONE',  ( 14.00000000000000178, -50.50083396221999976, -44.47484963936999947 ) ) ;
#40744=CARTESIAN_POINT ( 'NONE',  ( 13.05728973496400336, -11.72286803092000085, -1.966956593348999860 ) ) ;
#40749=ORIENTED_EDGE ( 'NONE', *, *, #19624, .F. ) ;
#40755=ORIENTED_EDGE ( 'NONE', *, *, #868, .F. ) ;
#40756=CARTESIAN_POINT ( 'NONE',  ( 23.62967491266149977, 10.06690055933806782, 9.667224302797498225 ) ) ;
#40757=DIRECTION ( 'NONE',  ( 1.000000000000000000, 0.000000000000000000, 0.000000000000000000 ) ) ;
#40760=CARTESIAN_POINT ( 'NONE',  ( 24.52306329324777323, 3.339076860759809584, 12.06942449950906138 ) ) ;
#40770=CARTESIAN_POINT ( 'NONE',  ( 23.95415751879778199, -3.345976127950229806, -12.83253842359969710 ) ) ;
#40780=CARTESIAN_POINT ( 'NONE',  ( 24.30000000000000071, 11.85420044612000012, 3.901016762742000488 ) ) ;
#40792=CARTESIAN_POINT ( 'NONE',  ( 16.08724299200000019, 9.224388201582000235, 8.529033888242999240 ) ) ;
#40795=CARTESIAN_POINT ( 'NONE',  ( 24.35365242081700288, -2.582848009905001074, -11.10541636514000174 ) ) ;
#40797=CARTESIAN_POINT ( 'NONE',  ( 24.48566044703800060, -12.12924491941999960, 3.164389501723999576 ) ) ;
#40802=CARTESIAN_POINT ( 'NONE',  ( 24.30000000000000071, 11.76537389984999926, -3.877215761401999750 ) ) ;
#40804=CARTESIAN_POINT ( 'NONE',  ( 23.55075185133400240, 10.43333017688000020, 9.388795336593998897 ) ) ;
#40809=CARTESIAN_POINT ( 'NONE',  ( 24.53429010490700080, 8.855930189872001534, 9.286429716155000236 ) ) ;
#40810=ORIENTED_EDGE ( 'NONE', *, *, #65212, .T. ) ;
#40816=DIRECTION ( 'NONE',  ( 5.812104846703281941E-06, -0.9659358880878460285, -0.2587814909729125312 ) ) ;
#40817=CARTESIAN_POINT ( 'NONE',  ( 24.67921580188599862, 3.567514645466999923, -12.13750897870000145 ) ) ;
#40821=ORIENTED_EDGE ( 'NONE', *, *, #51605, .F. ) ;
#40825=CIRCLE ( 'NONE', #11778, 13.92493900950999652 ) ;
#40828=VERTEX_POINT ( 'NONE', #66248 ) ;
#40833=EDGE_CURVE ( 'NONE', #28283, #43730, #33475, .T. ) ;
#40835=EDGE_LOOP ( 'NONE', ( #5101, #68521, #5938, #53114 ) ) ;
#40846=VECTOR ( 'NONE', #38834, 1000.000000000000000 ) ;
#40849=ORIENTED_EDGE ( 'NONE', *, *, #58026, .T. ) ;
#40855=CARTESIAN_POINT ( 'NONE',  ( 18.16350100824700320, -3.138009765975000143, -11.88148072165000002 ) ) ;
#40862=ORIENTED_EDGE ( 'NONE', *, *, #15141, .T. ) ;
#40863=ORIENTED_EDGE ( 'NONE', *, *, #47317, .F. ) ;
#40871=CARTESIAN_POINT ( 'NONE',  ( 23.51511290156300404, -13.45754537663000150, 4.321901134974000414 ) ) ;
#40876=EDGE_CURVE ( 'NONE', #53930, #61548, #55427, .T. ) ;
#40893=ADVANCED_FACE ( 'NONE', ( #55772 ), #63492, .F. ) ;
#40897=CARTESIAN_POINT ( 'NONE',  ( 16.39999999379500295, 3.351248059343999941, 11.15756683833000018 ) ) ;
#40899=VERTEX_POINT ( 'NONE', #14497 ) ;
#40902=CARTESIAN_POINT ( 'NONE',  ( 12.11873369409612522, 11.72532246831247349, -3.796278118047919925 ) ) ;
#40904=CARTESIAN_POINT ( 'NONE',  ( 13.73837349797500096, -9.670565172354999461, -8.019813433522999802 ) ) ;
#40905=CARTESIAN_POINT ( 'NONE',  ( 23.66004879239100234, -9.998910854163000295, -9.691527647852998584 ) ) ;
#40906=CARTESIAN_POINT ( 'NONE',  ( 13.63350196149407267, 9.056970873722406168, 7.433404858428185769 ) ) ;
#40908=DIRECTION ( 'NONE',  ( 1.000000000000000000, 0.000000000000000000, 0.000000000000000000 ) ) ;
#40925=CARTESIAN_POINT ( 'NONE',  ( 23.77344028463681269, -3.285535634723865339, 13.18386468110849208 ) ) ;
#40926=EDGE_CURVE ( 'NONE', #41305, #51740, #2631, .T. ) ;
#40930=ORIENTED_EDGE ( 'NONE', *, *, #20371, .F. ) ;
#40936=CARTESIAN_POINT ( 'NONE',  ( 13.49998535730550664, -12.08447166622790014, -2.429352492459242896 ) ) ;
#40937=CYLINDRICAL_SURFACE ( 'NONE', #48334, 1.000000000000000444 ) ;
#40953=DIRECTION ( 'NONE',  ( 0.000000000000000000, 0.000000000000000000, -1.000000000000000000 ) ) ;
#40961=EDGE_CURVE ( 'NONE', #57158, #52029, #58471, .T. ) ;
#40965=CARTESIAN_POINT ( 'NONE',  ( 25.59994555223599733, 2.024003533649000097, -11.01554633311000053 ) ) ;
#40969=B_SPLINE_CURVE_WITH_KNOTS ( 'NONE', 3,
 ( #31529, #53542, #63670, #32229 ),
 .UNSPECIFIED., .F., .F.,
 ( 4, 4 ),
 ( 0.000000000000000000, 1.000000000000000000 ),
 .UNSPECIFIED. ) ;
#40976=CYLINDRICAL_SURFACE ( 'NONE', #43685, 12.52500000000000036 ) ;
#40980=CARTESIAN_POINT ( 'NONE',  ( 15.59211270977100128, -8.811013545169000594, -7.841491685545999069 ) ) ;
#40982=CARTESIAN_POINT ( 'NONE',  ( 23.59461952754617897, -13.38743028302391203, 4.020894998903971285 ) ) ;
#40986=PLANE ( 'NONE',  #48592 ) ;
#40992=ORIENTED_EDGE ( 'NONE', *, *, #18028, .F. ) ;
#41005=CARTESIAN_POINT ( 'NONE',  ( 25.59037530393599980, 11.08965754835999995, 3.240319064921999725 ) ) ;
#41006=ADVANCED_FACE ( 'NONE', ( #17859 ), #33246, .F. ) ;
#41009=CARTESIAN_POINT ( 'NONE',  ( 23.57056559309938493, 13.35854817469667744, 4.154943855177697820 ) ) ;
#41019=CARTESIAN_POINT ( 'NONE',  ( 24.98032478375984766, 2.955846862813865439, 11.57695784767182623 ) ) ;
#41026=CARTESIAN_POINT ( 'NONE',  ( 25.30000327618300204, 0.6965695964343684432, -11.50000000000000000 ) ) ;
#41027=CARTESIAN_POINT ( 'NONE',  ( 24.39664325360668684, -12.03536696638400016, 3.224866859253743279 ) ) ;
#41039=EDGE_CURVE ( 'NONE', #60315, #68087, #3595, .T. ) ;
#41041=ADVANCED_FACE ( 'NONE', ( #54210 ), #21704, .F. ) ;
#41042=EDGE_LOOP ( 'NONE', ( #22973, #39857, #58639, #20566 ) ) ;
#41044=CARTESIAN_POINT ( 'NONE',  ( 24.67921430886200085, -8.727631620858000261, -9.158313288899000426 ) ) ;
#41049=CARTESIAN_POINT ( 'NONE',  ( 17.65706414889024956, 11.53038916134920555, -4.891395587226483599 ) ) ;
#41052=ORIENTED_EDGE ( 'NONE', *, *, #2832, .T. ) ;
#41057=CARTESIAN_POINT ( 'NONE',  ( 25.08883434079300301, 8.444432640379998745, -8.588577351766998547 ) ) ;
#41060=CARTESIAN_POINT ( 'NONE',  ( 17.79421883851900077, -3.253172350820999981, -11.33701189166999868 ) ) ;
#41066=CARTESIAN_POINT ( 'NONE',  ( 25.26999579225652681, -11.52969365347296460, 2.996586438050647949 ) ) ;
#41074=CARTESIAN_POINT ( 'NONE',  ( 13.99974593105000231, 8.811008772734998828, 7.563940656188999689 ) ) ;
#41078=CIRCLE ( 'NONE', #10936, 13.92493900950999830 ) ;
#41083=B_SPLINE_CURVE_WITH_KNOTS ( 'NONE', 3,
 ( #56067, #28832, #8177, #17984 ),
 .UNSPECIFIED., .F., .F.,
 ( 4, 4 ),
 ( 0.000000000000000000, 1.000000000000000000 ),
 .UNSPECIFIED. ) ;
#41086=AXIS2_PLACEMENT_3D ( 'NONE', #13038, #3226, #34368 ) ;
#41092=CARTESIAN_POINT ( 'NONE',  ( 12.99518154839200257, -11.72294562696999876, -1.966205464704999795 ) ) ;
#41099=ORIENTED_EDGE ( 'NONE', *, *, #35907, .T. ) ;
#41102=CARTESIAN_POINT ( 'NONE',  ( 15.86001156276200064, 8.572187346067000391, 8.239473968622000655 ) ) ;
#41109=CARTESIAN_POINT ( 'NONE',  ( 16.39999999379500295, -3.351248059343999941, -11.15756683833000018 ) ) ;
#41111=EDGE_LOOP ( 'NONE', ( #54661, #11781, #34898, #61024 ) ) ;
#41130=B_SPLINE_CURVE_WITH_KNOTS ( 'NONE', 3,
 ( #50922, #3021, #66989, #61748, #13867, #35197, #39057, #60379, #12484, #55133, #7237, #8954, #14892, #63106, #35539, #31319, #57529, #36213, #9287, #57188, #3697, #15233, #67667, #20819, #42157, #67328, #25034, #46366, #63458, #4386, #36558, #19793 ),
 .UNSPECIFIED., .F., .F.,
 ( 4, 2, 2, 2, 2, 2, 2, 2, 1, 2, 2, 2, 1, 1, 1, 2, 2, 4 ),
 ( 0.000000000000000000, 0.2499999999999977796, 0.3749999999999976130, 0.4374999999999985567, 0.4687499999999993339, 0.5000000000000001110, 0.6249999999999926725, 0.6874999999999898970, 0.7187499999999898970, 0.7343749999999898970, 0.7499999999999900080, 0.8124999999999856781, 0.8437499999999835687, 0.8593749999999823475, 0.8671874999999817923, 0.8710937499999804601, 0.8749999999999792388, 1.000000000000000000 ),
 .UNSPECIFIED. ) ;
#41132=VERTEX_POINT ( 'NONE', #37792 ) ;
#41140=CARTESIAN_POINT ( 'NONE',  ( 25.30000327618300204, 9.659335867304687184, -6.394377797198702140 ) ) ;
#41141=CARTESIAN_POINT ( 'NONE',  ( 23.55356904242700367, 13.38988504594999895, 4.198910762617999559 ) ) ;
#41153=CARTESIAN_POINT ( 'NONE',  ( 25.47132200302800342, -11.11905954937000018, 3.299905938470999889 ) ) ;
#41156=B_SPLINE_CURVE_WITH_KNOTS ( 'NONE', 3,
 ( #47774, #58593, #69083, #32040 ),
 .UNSPECIFIED., .F., .F.,
 ( 4, 4 ),
 ( 0.000000000000000000, 1.000000000000000000 ),
 .UNSPECIFIED. ) ;
#41158=CARTESIAN_POINT ( 'NONE',  ( 24.46275371508600216, 3.515554276222999874, 12.28676815851000015 ) ) ;
#41160=CARTESIAN_POINT ( 'NONE',  ( 23.62945547067200280, 10.04812290079000014, 9.751475363001999241 ) ) ;
#41167=CARTESIAN_POINT ( 'NONE',  ( 14.80000000000000071, 3.470217030164000072, -11.92928724693999953 ) ) ;
#41171=LINE ( 'NONE', #29668, #23882 ) ;
#41175=CARTESIAN_POINT ( 'NONE',  ( 15.40000000005200143, 9.187454762873001002, 8.213177997099000649 ) ) ;
#41184=EDGE_LOOP ( 'NONE', ( #69099, #6127, #52332, #44660 ) ) ;
#41187=EDGE_CURVE ( 'NONE', #2494, #7968, #22658, .T. ) ;
#41188=EDGE_CURVE ( 'NONE', #16959, #12534, #10921, .T. ) ;
#41197=ORIENTED_EDGE ( 'NONE', *, *, #66997, .T. ) ;
#41200=CARTESIAN_POINT ( 'NONE',  ( 15.90018573812399971, -8.493548356068000516, -8.263529029821000904 ) ) ;
#41206=CARTESIAN_POINT ( 'NONE',  ( 17.93733281514800026, -12.03472983398000018, 3.255807327981000032 ) ) ;
#41232=EDGE_CURVE ( 'NONE', #10787, #47324, #47231, .T. ) ;
#41236=CARTESIAN_POINT ( 'NONE',  ( 11.26444844843000048, -3.604811106221999850, 11.32703155999000089 ) ) ;
#41244=ORIENTED_EDGE ( 'NONE', *, *, #17890, .F. ) ;
#41253=CARTESIAN_POINT ( 'NONE',  ( 15.90018573812399971, -8.493548356068000516, -8.263529029821000904 ) ) ;
#41261=PLANE ( 'NONE',  #10097 ) ;
#41273=CARTESIAN_POINT ( 'NONE',  ( 23.75090150694354563, -3.269774994020507641, 13.22953792649320448 ) ) ;
#41274=EDGE_CURVE ( 'NONE', #56214, #5868, #43889, .T. ) ;
#41276=CARTESIAN_POINT ( 'NONE',  ( 24.30000560035348656, 12.09374145920219767, -3.240508257462953345 ) ) ;
#41282=CARTESIAN_POINT ( 'NONE',  ( 15.57784398235336631, -9.457709274034865388, -8.211421075710321205 ) ) ;
#41284=ORIENTED_EDGE ( 'NONE', *, *, #31889, .T. ) ;
#41286=CARTESIAN_POINT ( 'NONE',  ( 15.90018573812067260, 5.468217585226911481, 10.55609518975849248 ) ) ;
#41289=CARTESIAN_POINT ( 'NONE',  ( 20.00000000000000000, 0.000000000000000000, 0.000000000000000000 ) ) ;
#41295=CARTESIAN_POINT ( 'NONE',  ( 24.30001685126999789, 8.938702716825000394, -8.938676159935001309 ) ) ;
#41305=VERTEX_POINT ( 'NONE', #68825 ) ;
#41310=CARTESIAN_POINT ( 'NONE',  ( 18.29995268966800026, 2.861739928647000220, 11.98821236628000086 ) ) ;
#41314=B_SPLINE_SURFACE_WITH_KNOTS ( 'NONE', 3, 3, ( 
 ( #65645, #55163, #38389, #43993 ),
 ( #54124, #65299, #22306, #17415 ),
 ( #65986, #49572, #39431, #11815 ),
 ( #38741, #64605, #33504, #48543 ),
 ( #33156, #43646, #17770, #54472 ),
 ( #16711, #21959, #6574, #27914 ),
 ( #2032, #54819, #49919, #1681 ),
 ( #6919, #22997, #49223, #22648 ),
 ( #1331, #44347, #39088, #28251 ),
 ( #23350, #60412, #12518, #648 ),
 ( #33849, #7268, #28607, #60752 ),
 ( #12866, #44692, #38041, #34195 ) ),
 .UNSPECIFIED., .F., .F., .F.,
 ( 4, 1, 1, 1, 1, 1, 1, 1, 1, 4 ),
 ( 4, 4 ),
 ( 0.01095806325966000062, 0.05000000000000000278, 0.1000000000000000056, 0.1499999999999999944, 0.2000000000000000111, 0.2500000000000000000, 0.2999999999999999889, 0.3499999999999999778, 0.4000000000000000222, 0.4461661505078000078 ),
 ( -0.2706701093251999701, 1.270791579988999942 ),
 .UNSPECIFIED. ) ;
#41316=CARTESIAN_POINT ( 'NONE',  ( 24.39664233851466690, -12.03536604771145413, -3.224866613121610381 ) ) ;
#41317=LINE ( 'NONE', #19994, #57738 ) ;
#41328=CARTESIAN_POINT ( 'NONE',  ( 23.59999441188499958, 10.30760541648000128, -9.317696302454001156 ) ) ;
#41336=CARTESIAN_POINT ( 'NONE',  ( 29.91622776601699840, 7.448825475110001390E-09, -6.772075922005999615 ) ) ;
#41353=ADVANCED_FACE ( 'NONE', ( #25844 ), #7049, .F. ) ;
#41355=ADVANCED_FACE ( 'NONE', ( #15359 ), #13745, .T. ) ;
#41356=CARTESIAN_POINT ( 'NONE',  ( 23.63077126582529175, 13.40261082913402113, 3.886325453134984897 ) ) ;
#41359=VECTOR ( 'NONE', #22822, 1000.000000000000227 ) ;
#41360=CARTESIAN_POINT ( 'NONE',  ( 18.17737860441360809, -11.15478131644662874, 3.361574628443296575 ) ) ;
#41365=ORIENTED_EDGE ( 'NONE', *, *, #18066, .F. ) ;
#41368=CARTESIAN_POINT ( 'NONE',  ( 18.50007554376852426, 2.772760791841625938, -11.31557096909393323 ) ) ;
#41372=DIRECTION ( 'NONE',  ( -1.000000000000000000, 0.000000000000000000, 0.000000000000000000 ) ) ;
#41377=EDGE_CURVE ( 'NONE', #60176, #36031, #65139, .T. ) ;
#41384=CARTESIAN_POINT ( 'NONE',  ( 24.66271477989500127, -12.38330044149000031, -2.963253076001000075 ) ) ;
#41395=CARTESIAN_POINT ( 'NONE',  ( 17.77447410014400120, 3.189754565392000085, 11.45074580414000032 ) ) ;
#41397=ORIENTED_EDGE ( 'NONE', *, *, #45546, .F. ) ;
#41399=CONICAL_SURFACE ( 'NONE', #30283, 12.42518894556000042, 0.7854133338342391690 ) ;
#41404=CARTESIAN_POINT ( 'NONE',  ( 23.67309812202378438, 3.197429271368524173, 13.39122446713678904 ) ) ;
#41405=CARTESIAN_POINT ( 'NONE',  ( 23.61340685958100138, 10.15619120159999866, -9.483135970162001271 ) ) ;
#41411=CARTESIAN_POINT ( 'NONE',  ( 24.84573432944931426, -12.09401906330531595, 2.924964065930268475 ) ) ;
#41414=DIRECTION ( 'NONE',  ( 1.000000000000000000, 0.000000000000000000, 0.000000000000000000 ) ) ;
#41422=CARTESIAN_POINT ( 'NONE',  ( 25.39991555675432267, -10.74016618265575573, -3.821986234823466777 ) ) ;
#41428=CARTESIAN_POINT ( 'NONE',  ( 24.60109542677746575, 3.453340786472776092, -12.10341549489917590 ) ) ;
#41432=AXIS2_PLACEMENT_3D ( 'NONE', #50266, #48975, #59454 ) ;
#41440=VERTEX_POINT ( 'NONE', #56892 ) ;
#41445=CARTESIAN_POINT ( 'NONE',  ( 15.86242637978999959, 8.523064092628001021, 8.288181269780999116 ) ) ;
#41480=EDGE_LOOP ( 'NONE', ( #58963, #40330, #19866, #60690, #16361, #37623, #7924, #30507, #67238, #6094, #58141, #43547, #16248, #34142, #36568, #5772, #18090, #39056, #49659, #42018, #37209, #21326 ) ) ;
#41482=CARTESIAN_POINT ( 'NONE',  ( 11.30000000000000071, 0.000000000000000000, -5.373479439185999994E-14 ) ) ;
#41484=CARTESIAN_POINT ( 'NONE',  ( 23.60000000000000142, 2.204728229456999866, -11.99913219504999873 ) ) ;
#41486=CARTESIAN_POINT ( 'NONE',  ( 24.35365242081699932, -3.253466243142002057, -12.21167519476998464 ) ) ;
#41494=CARTESIAN_POINT ( 'NONE',  ( 23.52015295616099877, 10.38924838980999965, 9.574931041765999851 ) ) ;
#41495=ORIENTED_EDGE ( 'NONE', *, *, #24564, .T. ) ;
#41498=CARTESIAN_POINT ( 'NONE',  ( 25.60000000000000142, 3.623466631435000362, -13.52296156804999860 ) ) ;
#41508=CARTESIAN_POINT ( 'NONE',  ( 24.30000000000000071, -12.03537377768999939, 3.224868684338999980 ) ) ;
#41511=CARTESIAN_POINT ( 'NONE',  ( 25.00267152972667972, -11.89262042224634897, -2.924336343934345717 ) ) ;
#41512=EDGE_CURVE ( 'NONE', #50502, #35889, #67324, .T. ) ;
#41517=ORIENTED_EDGE ( 'NONE', *, *, #27270, .T. ) ;
#41522=EDGE_LOOP ( 'NONE', ( #9886, #19840, #11232, #36122 ) ) ;
#41527=CARTESIAN_POINT ( 'NONE',  ( 23.60000000000000142, -11.49391741900999975, 4.090215442373000165 ) ) ;
#41537=EDGE_CURVE ( 'NONE', #46470, #55031, #52673, .T. ) ;
#41546=B_SPLINE_CURVE_WITH_KNOTS ( 'NONE', 3,
 ( #67143, #50736, #61908, #35350 ),
 .UNSPECIFIED., .F., .F.,
 ( 4, 4 ),
 ( 0.000000000000000000, 1.000000000000000000 ),
 .UNSPECIFIED. ) ;
#41552=AXIS2_PLACEMENT_3D ( 'NONE', #10516, #26954, #31856 ) ;
#41556=CARTESIAN_POINT ( 'NONE',  ( 24.60109143485134453, -8.755188789252855486, -9.042389807092181542 ) ) ;
#41559=CARTESIAN_POINT ( 'NONE',  ( 23.51705920820199935, -13.43782975258999990, 4.375924611141999598 ) ) ;
#41570=CARTESIAN_POINT ( 'NONE',  ( 24.59232956327399933, 8.769507425530997935, 9.082531692484000274 ) ) ;
#41573=ADVANCED_FACE ( 'NONE', ( #30331 ), #51639, .F. ) ;
#41574=FACE_OUTER_BOUND ( 'NONE', #51236, .T. ) ;
#41576=CARTESIAN_POINT ( 'NONE',  ( 11.55275411606000269, -3.402594452619000176, 11.19752650018000040 ) ) ;
#41614=CARTESIAN_POINT ( 'NONE',  ( 17.33333333127366771, -3.351260669886449772, -11.15757822838323499 ) ) ;
#41615=CARTESIAN_POINT ( 'NONE',  ( 18.36021383542241736, 3.331512994329992150, -12.07398673550631329 ) ) ;
#41622=CARTESIAN_POINT ( 'NONE',  ( 13.49994651945300284, -12.07042783918999795, -2.492331243371999960 ) ) ;
#41625=ADVANCED_FACE ( 'NONE', ( #27845 ), #42876, .F. ) ;
#41636=AXIS2_PLACEMENT_3D ( 'NONE', #24794, #14313, #18868 ) ;
#41638=CARTESIAN_POINT ( 'NONE',  ( 25.22250851510596448, -2.724056651873135060, 11.39870813624705370 ) ) ;
#41639=DIRECTION ( 'NONE',  ( 0.000000000000000000, 2.692747184616903860E-07, -0.9999999999999636957 ) ) ;
#41640=CARTESIAN_POINT ( 'NONE',  ( 11.79999999471800010, -11.69117318561000118, -1.923227876431999883 ) ) ;
#41644=CARTESIAN_POINT ( 'NONE',  ( 21.72233714749290101, 0.000000000000000000, 0.000000000000000000 ) ) ;
#41650=CARTESIAN_POINT ( 'NONE',  ( 15.75060268748879366, 9.413968701426712826, 8.261605506250123909 ) ) ;
#41673=CARTESIAN_POINT ( 'NONE',  ( 11.29998658800000122, 3.824194713071000340, -11.71675648045999907 ) ) ;
#41676=CARTESIAN_POINT ( 'NONE',  ( 23.81907629691099970, 3.247310101920000136, -13.04146647203000065 ) ) ;
#41692=CARTESIAN_POINT ( 'NONE',  ( 23.56684398259831781, 13.33616302248389118, 4.226923696159335719 ) ) ;
#41693=DIRECTION ( 'NONE',  ( -0.7071060218675399023, 0.7071075405047398954, -8.464089693328477533E-10 ) ) ;
#41703=B_SPLINE_CURVE_WITH_KNOTS ( 'NONE', 3,
 ( #38489, #55267, #54217, #65743, #28705, #48982 ),
 .UNSPECIFIED., .F., .F.,
 ( 4, 2, 4 ),
 ( 0.000000000000000000, 0.5000000000000000000, 1.000000000000000000 ),
 .UNSPECIFIED. ) ;
#41704=ORIENTED_EDGE ( 'NONE', *, *, #16995, .T. ) ;
#41706=EDGE_CURVE ( 'NONE', #63863, #31118, #15930, .T. ) ;
#41722=CARTESIAN_POINT ( 'NONE',  ( 11.53970701685000222, -11.52114570934000071, -1.450082077858000140 ) ) ;
#41726=CARTESIAN_POINT ( 'NONE',  ( 11.91753023736700179, 11.77475711121000224, -4.379243463657999769 ) ) ;
#41728=CARTESIAN_POINT ( 'NONE',  ( 17.79999999998900151, -3.595165934733000057, 11.99793354950999991 ) ) ;
#41729=DIRECTION ( 'NONE',  ( -1.000000000000000000, 0.000000000000000000, 0.000000000000000000 ) ) ;
#41732=CARTESIAN_POINT ( 'NONE',  ( 18.31802873821099809, 2.927761598026000112, 11.42873208727000112 ) ) ;
#41737=ORIENTED_EDGE ( 'NONE', *, *, #51225, .F. ) ;
#41743=CARTESIAN_POINT ( 'NONE',  ( 24.74066795589899925, 8.629132841860998937, -8.723415954201001909 ) ) ;
#41748=VECTOR ( 'NONE', #62140, 999.9999999999998863 ) ;
#41751=CARTESIAN_POINT ( 'NONE',  ( 25.29995734509200034, 8.533537492639000632, -7.925519463018001254 ) ) ;
#41758=CARTESIAN_POINT ( 'NONE',  ( 15.95436146409600120, -3.609635682399999546, -11.22945631340000006 ) ) ;
#41759=EDGE_CURVE ( 'NONE', #60364, #33864, #66024, .T. ) ;
#41760=CARTESIAN_POINT ( 'NONE',  ( 13.55436146409600262, 9.071829816454000550, 7.538704307477999578 ) ) ;
#41763=CARTESIAN_POINT ( 'NONE',  ( 18.49996808500599954, 1.807259460122252470, -11.54438823565103789 ) ) ;
#41764=CARTESIAN_POINT ( 'NONE',  ( 23.60000000000000142, -11.85420044612000012, 3.901016762742000488 ) ) ;
#41772=ORIENTED_EDGE ( 'NONE', *, *, #40314, .F. ) ;
#41775=CARTESIAN_POINT ( 'NONE',  ( 13.46001156276200028, -11.65487838447000080, -2.352687191044000148 ) ) ;
#41785=CARTESIAN_POINT ( 'NONE',  ( 15.67439970770000102, 8.782357275181000844, 8.013525452821999906 ) ) ;
#41787=CARTESIAN_POINT ( 'NONE',  ( 23.57822756410993748, 10.24958405627187119, 9.515671483802911723 ) ) ;
#41790=EDGE_CURVE ( 'NONE', #53272, #67920, #21885, .T. ) ;
#41792=CARTESIAN_POINT ( 'NONE',  ( 24.44496351116800170, 3.224881296174999967, 12.03535797436000010 ) ) ;
#41817=CARTESIAN_POINT ( 'NONE',  ( 25.57779276387900325, 2.768488786735999962, 11.23374265755999879 ) ) ;
#41819=CARTESIAN_POINT ( 'NONE',  ( 13.70003001321900449, -12.06139972930709447, -3.524828382075537725 ) ) ;
#41820=ORIENTED_EDGE ( 'NONE', *, *, #64544, .F. ) ;
#41824=EDGE_CURVE ( 'NONE', #15838, #47311, #11739, .T. ) ;
#41831=CARTESIAN_POINT ( 'NONE',  ( 25.57799114520100048, -11.11256384368000205, 3.219680944509000220 ) ) ;
#41842=B_SPLINE_CURVE_WITH_KNOTS ( 'NONE', 3,
 ( #40355, #2944, #62697, #14482 ),
 .UNSPECIFIED., .F., .F.,
 ( 4, 4 ),
 ( 0.000000000000000000, 1.000000000000000000 ),
 .UNSPECIFIED. ) ;
#41843=EDGE_LOOP ( 'NONE', ( #53129, #45669, #33133, #16006 ) ) ;
#41844=PLANE ( 'NONE',  #21076 ) ;
#41852=FACE_OUTER_BOUND ( 'NONE', #41522, .T. ) ;
#41855=CARTESIAN_POINT ( 'NONE',  ( 11.50001496185000249, 12.52500000000000036, 0.000000000000000000 ) ) ;
#41856=CARTESIAN_POINT ( 'NONE',  ( 25.29995873461299993, 11.13046969959000165, 3.427501705020000067 ) ) ;
#41861=CARTESIAN_POINT ( 'NONE',  ( 16.32966272177200295, -3.529531741950000079, -11.96032165934999902 ) ) ;
#41865=DIRECTION ( 'NONE',  ( 0.000000000000000000, -0.9659258262890756397, -0.2588190451024934280 ) ) ;
#41872=DIRECTION ( 'NONE',  ( 0.2392860387991979920, -0.9709491189736919603, -1.580732896240985235E-14 ) ) ;
#41881=B_SPLINE_SURFACE_WITH_KNOTS ( 'NONE', 3, 3, ( 
 ( #27881, #11779, #33120, #32092 ),
 ( #65609, #610, #44314, #65265 ),
 ( #6184, #38354, #16679, #11433 ),
 ( #21923, #17378, #38006, #59681 ),
 ( #37323, #6537, #42915, #5506 ),
 ( #54435, #26846, #38708, #53408 ),
 ( #22615, #64221, #21578, #6882 ),
 ( #37665, #58995, #33467, #54783 ),
 ( #11097, #58646, #43261, #10747 ),
 ( #28219, #27526, #49533, #59331 ) ),
 .UNSPECIFIED., .F., .F., .F.,
 ( 4, 1, 1, 1, 1, 1, 1, 4 ),
 ( 4, 4 ),
 ( 0.07203983506772999867, 0.1428571428570999946, 0.2857142857143000203, 0.4285714285713999594, 0.5714285714286000406, 0.7142857142856999797, 0.8571428571429000609, 0.9589780836993999635 ),
 ( -0.1900620218102000158, 1.190128522698000069 ),
 .UNSPECIFIED. ) ;
#41885=CARTESIAN_POINT ( 'NONE',  ( 23.56666365135700403, -8.694246338465996260, 8.392498551259993889 ) ) ;
#41893=VERTEX_POINT ( 'NONE', #41336 ) ;
#41900=CARTESIAN_POINT ( 'NONE',  ( 16.26904166988085620, 3.216266637185321020, 11.40336119490550004 ) ) ;
#41902=ORIENTED_EDGE ( 'NONE', *, *, #13284, .T. ) ;
#41904=ADVANCED_FACE ( 'NONE', ( #13145 ), #66609, .T. ) ;
#41911=CARTESIAN_POINT ( 'NONE',  ( 11.35400411985997948, -11.72677417300536362, -1.687001524046906287 ) ) ;
#41912=CARTESIAN_POINT ( 'NONE',  ( 23.66004879239100234, 0.000000000000000000, 0.000000000000000000 ) ) ;
#41925=ADVANCED_FACE ( 'NONE', ( #44623 ), #57655, .F. ) ;
#41928=ORIENTED_EDGE ( 'NONE', *, *, #22329, .T. ) ;
#41934=CARTESIAN_POINT ( 'NONE',  ( 13.89309513285500230, -9.135233488911998379, -8.214486393748998694 ) ) ;
#41949=FACE_OUTER_BOUND ( 'NONE', #67728, .T. ) ;
#41950=EDGE_LOOP ( 'NONE', ( #40930, #67052, #51585, #62374, #15526 ) ) ;
#41958=B_SPLINE_CURVE_WITH_KNOTS ( 'NONE', 3,
 ( #14460, #35780, #57095, #9194, #3946, #67924 ),
 .UNSPECIFIED., .F., .F.,
 ( 4, 2, 4 ),
 ( 0.000000000000000000, 0.5000000000000000000, 1.000000000000000000 ),
 .UNSPECIFIED. ) ;
#41959=CARTESIAN_POINT ( 'NONE',  ( 23.59999468372399889, -2.915558691838999739, 13.58549495651999983 ) ) ;
#41962=CARTESIAN_POINT ( 'NONE',  ( 25.31010560212500238, -2.730875805498000020, -11.36013797732000086 ) ) ;
#41971=ADVANCED_FACE ( 'NONE', ( #55441, #55093 ), #23281, .T. ) ;
#41985=DIRECTION ( 'NONE',  ( 0.000000000000000000, 0.4084292560226189250, -0.9127899773906427150 ) ) ;
#41986=CIRCLE ( 'NONE', #18537, 8.250000000000000000 ) ;
#41989=CARTESIAN_POINT ( 'NONE',  ( 13.69997185827400088, 11.21472423003503494, 3.290649947225259719 ) ) ;
#41991=CARTESIAN_POINT ( 'NONE',  ( 24.84573454058074660, 8.580102523463006392, 9.011245526633942404 ) ) ;
#41992=ADVANCED_FACE ( 'NONE', ( #9166 ), #36454, .F. ) ;
#41993=EDGE_LOOP ( 'NONE', ( #42639, #22553, #22941, #55388 ) ) ;
#41995=EDGE_CURVE ( 'NONE', #36015, #49775, #21807, .T. ) ;
#41996=B_SPLINE_CURVE_WITH_KNOTS ( 'NONE', 3,
 ( #41792, #40760, #62082, #14544 ),
 .UNSPECIFIED., .F., .F.,
 ( 4, 4 ),
 ( 0.000000000000000000, 1.000000000000000000 ),
 .UNSPECIFIED. ) ;
#42003=B_SPLINE_CURVE_WITH_KNOTS ( 'NONE', 3,
 ( #64252, #18447, #3042, #34872 ),
 .UNSPECIFIED., .F., .F.,
 ( 4, 4 ),
 ( 0.000000000000000000, 1.000000000000000000 ),
 .UNSPECIFIED. ) ;
#42012=CARTESIAN_POINT ( 'NONE',  ( 12.36003207187216013, 11.57530800953516703, -4.784147006775551603 ) ) ;
#42015=CARTESIAN_POINT ( 'NONE',  ( 11.79999999471800010, -11.69117318561000118, -1.923227876431999883 ) ) ;
#42018=ORIENTED_EDGE ( 'NONE', *, *, #26756, .T. ) ;
#42020=EDGE_CURVE ( 'NONE', #60415, #56347, #30999, .T. ) ;
#42026=LINE ( 'NONE', #68231, #16337 ) ;
#42036=CARTESIAN_POINT ( 'NONE',  ( 24.30001697071400457, -8.938702858184001343, 8.938676113071998941 ) ) ;
#42041=CARTESIAN_POINT ( 'NONE',  ( 24.17809389475516468, 9.100323006451731089, -9.085318127976481861 ) ) ;
#42043=CARTESIAN_POINT ( 'NONE',  ( 23.58303149431899826, 13.27303032590999976, -4.267677747246999331 ) ) ;
#42044=VERTEX_POINT ( 'NONE', #3494 ) ;
#42047=ORIENTED_EDGE ( 'NONE', *, *, #56359, .F. ) ;
#42059=CARTESIAN_POINT ( 'NONE',  ( 13.56648734862639216, -12.13584047101458552, -2.505837749223106758 ) ) ;
#42060=CARTESIAN_POINT ( 'NONE',  ( 12.96427412810700197, 11.57018092489999894, 1.758708699944000031 ) ) ;
#42064=ORIENTED_EDGE ( 'NONE', *, *, #17526, .F. ) ;
#42070=CARTESIAN_POINT ( 'NONE',  ( 23.56666365135700403, -9.069641144917994779, -7.556701426681005529 ) ) ;
#42071=DIRECTION ( 'NONE',  ( 0.000000000000000000, 0.9421243786071880066, 0.3352635608502960718 ) ) ;
#42073=CARTESIAN_POINT ( 'NONE',  ( 12.04524561587600040, 11.75582082520000071, -3.881266971570000113 ) ) ;
#42075=B_SPLINE_CURVE_WITH_KNOTS ( 'NONE', 3,
 ( #61542, #61885, #40558, #56644 ),
 .UNSPECIFIED., .F., .F.,
 ( 4, 4 ),
 ( 0.000000000000000000, 1.000000000000000000 ),
 .UNSPECIFIED. ) ;
#42081=( GEOMETRIC_REPRESENTATION_CONTEXT ( 3 ) GLOBAL_UNCERTAINTY_ASSIGNED_CONTEXT ( ( #37373 ) ) GLOBAL_UNIT_ASSIGNED_CONTEXT ( ( #67587, #8875, #35790 ) ) REPRESENTATION_CONTEXT ( 'NONE', 'WORKASPACE' ) );
#42082=CARTESIAN_POINT ( 'NONE',  ( 17.88705809229600163, -3.642474092890999771, 12.02409483768999898 ) ) ;
#42085=EDGE_LOOP ( 'NONE', ( #64653, #3759, #55624 ) ) ;
#42091=DIRECTION ( 'NONE',  ( 1.000000000000000000, 0.000000000000000000, 0.000000000000000000 ) ) ;
#42103=CARTESIAN_POINT ( 'NONE',  ( 13.99999999485600277, 9.471999751521998689, 8.194948195317001804 ) ) ;
#42104=CIRCLE ( 'NONE', #17558, 12.20000000000000284 ) ;
#42108=CARTESIAN_POINT ( 'NONE',  ( 15.65828218294665675, -9.154335746262512785, -8.252742830647335381 ) ) ;
#42114=FACE_OUTER_BOUND ( 'NONE', #8173, .T. ) ;
#42118=DIRECTION ( 'NONE',  ( 0.000000000000000000, 0.2588190451024927063, -0.9659258262890757507 ) ) ;
#42122=CARTESIAN_POINT ( 'NONE',  ( 18.30003129332100187, -2.732683818840999646, -11.53064095373000164 ) ) ;
#42125=B_SPLINE_CURVE_WITH_KNOTS ( 'NONE', 3,
 ( #65941, #3007, #34840, #43949, #8259, #33459 ),
 .UNSPECIFIED., .F., .F.,
 ( 4, 2, 4 ),
 ( 0.000000000000000000, 0.5000000000000000000, 1.000000000000000000 ),
 .UNSPECIFIED. ) ;
#42127=CARTESIAN_POINT ( 'NONE',  ( 13.64504292973000332, -11.45087266113000091, -2.419799131125000002 ) ) ;
#42134=ORIENTED_EDGE ( 'NONE', *, *, #13282, .F. ) ;
#42141=EDGE_CURVE ( 'NONE', #14432, #15277, #44252, .T. ) ;
#42143=VECTOR ( 'NONE', #8969, 1000.000000000000114 ) ;
#42149=EDGE_CURVE ( 'NONE', #42844, #31626, #8324, .T. ) ;
#42153=CIRCLE ( 'NONE', #68933, 0.6999999999999992895 ) ;
#42157=CARTESIAN_POINT ( 'NONE',  ( 24.11583214838473666, 12.52251212749843212, -3.380867675773815417 ) ) ;
#42161=CARTESIAN_POINT ( 'NONE',  ( 24.19055549696582119, 12.39716933831719814, 3.330586599044198959 ) ) ;
#42166=ORIENTED_EDGE ( 'NONE', *, *, #65361, .T. ) ;
#42175=CARTESIAN_POINT ( 'NONE',  ( 13.70003001321900271, -9.668726926528000476, -7.961868161445000425 ) ) ;
#42183=CARTESIAN_POINT ( 'NONE',  ( 23.89320776801300283, -1.894218448865001792, -11.32736289216000536 ) ) ;
#42192=EDGE_CURVE ( 'NONE', #1871, #67995, #16729, .T. ) ;
#42193=VECTOR ( 'NONE', #14924, 1000.000000000000114 ) ;
#42194=CARTESIAN_POINT ( 'NONE',  ( 18.26079396959979206, -3.428468831595210542, 12.04667397462565148 ) ) ;
#42201=AXIS2_PLACEMENT_3D ( 'NONE', #6338, #762, #10558 ) ;
#42202=CARTESIAN_POINT ( 'NONE',  ( 18.35168611684299833, 2.962034070680999776, 12.02052262816000017 ) ) ;
#42212=ORIENTED_EDGE ( 'NONE', *, *, #13415, .F. ) ;
#42213=CARTESIAN_POINT ( 'NONE',  ( 11.50001496185000605, 12.31773593199343786, -2.620250046340033556 ) ) ;
#42218=CARTESIAN_POINT ( 'NONE',  ( 16.27269624719400198, -3.670072847095000146, -12.01573327568000060 ) ) ;
#42220=ORIENTED_EDGE ( 'NONE', *, *, #47235, .F. ) ;
#42222=CARTESIAN_POINT ( 'NONE',  ( 24.51107830332481896, -8.765523554282413699, -8.765522532328214211 ) ) ;
#42240=ORIENTED_EDGE ( 'NONE', *, *, #29570, .F. ) ;
#42242=CARTESIAN_POINT ( 'NONE',  ( 18.11007341752342015, 3.284452655023115231, 11.17744038474791068 ) ) ;
#42254=CYLINDRICAL_SURFACE ( 'NONE', #45660, 11.65000000000000036 ) ;
#42257=CARTESIAN_POINT ( 'NONE',  ( 23.56665676678100141, -10.37811504717999966, -9.381458738969000066 ) ) ;
#42258=CARTESIAN_POINT ( 'NONE',  ( 25.60000000000000142, 0.000000000000000000, 0.000000000000000000 ) ) ;
#42283=CARTESIAN_POINT ( 'NONE',  ( 24.61098151538899970, 8.751788807388999558, -9.056922189400999912 ) ) ;
#42287=CARTESIAN_POINT ( 'NONE',  ( 13.70009528508592211, 8.955766972928957514, 7.451364690503321953 ) ) ;
#42291=CARTESIAN_POINT ( 'NONE',  ( 11.44437913529000106, 3.868861692926000462, -11.85573592760000139 ) ) ;
#42301=ORIENTED_EDGE ( 'NONE', *, *, #68357, .F. ) ;
#42315=CARTESIAN_POINT ( 'NONE',  ( 23.98813733208841015, -3.345690714576619040, 12.76941329706537331 ) ) ;
#42320=CARTESIAN_POINT ( 'NONE',  ( 25.40241773096400024, -3.096370345990000494, -11.38623249034000118 ) ) ;
#42324=CARTESIAN_POINT ( 'NONE',  ( 15.61911349846912067, -9.449623925635307842, -8.220739594291174512 ) ) ;
#42325=CARTESIAN_POINT ( 'NONE',  ( 23.56664675778400309, 10.37811020278999941, -9.381454169592000625 ) ) ;
#42342=EDGE_CURVE ( 'NONE', #65237, #61230, #18361, .T. ) ;
#42346=AXIS2_PLACEMENT_3D ( 'NONE', #57224, #29659, #63149 ) ;
#42352=CARTESIAN_POINT ( 'NONE',  ( 11.50001258332000020, 11.56502147876000031, 1.404302031979000054 ) ) ;
#42353=DIRECTION ( 'NONE',  ( -1.000000000000000000, 0.000000000000000000, 0.000000000000000000 ) ) ;
#42364=LINE ( 'NONE', #42015, #36358 ) ;
#42372=CARTESIAN_POINT ( 'NONE',  ( 23.56681659734730871, -2.990540295753150613, -13.66657933901271349 ) ) ;
#42376=ORIENTED_EDGE ( 'NONE', *, *, #44054, .T. ) ;
#42379=CARTESIAN_POINT ( 'NONE',  ( 24.84554641417578225, 3.513976416300454542, 11.93643034843086070 ) ) ;
#42387=CARTESIAN_POINT ( 'NONE',  ( 11.49999035076000276, -3.886252136122000156, 11.90689009355000039 ) ) ;
#42388=CARTESIAN_POINT ( 'NONE',  ( 24.72544608131600086, 12.30754379070000049, 2.942921080080999729 ) ) ;
#42400=DIRECTION ( 'NONE',  ( 1.000000000000000000, 0.000000000000000000, 0.000000000000000000 ) ) ;
#42402=CARTESIAN_POINT ( 'NONE',  ( 18.23887202961200060, -3.252214874110999965, 11.14733497513999971 ) ) ;
#42403=CARTESIAN_POINT ( 'NONE',  ( 13.99999999485600277, -9.471999751521998689, -8.194948195317001804 ) ) ;
#42416=CARTESIAN_POINT ( 'NONE',  ( 18.02663564786298522, 11.82897200926889347, -3.432444815763982415 ) ) ;
#42420=CARTESIAN_POINT ( 'NONE',  ( 12.65912070212100105, 11.49976653515000002, -4.814127980893999847 ) ) ;
#42421=CARTESIAN_POINT ( 'NONE',  ( 18.21444431150800014, 11.56145208044000050, -4.416819796118000241 ) ) ;
#42425=CARTESIAN_POINT ( 'NONE',  ( 18.31587707750999883, -3.089759977613000252, 11.98885651319999823 ) ) ;
#42427=VERTEX_POINT ( 'NONE', #22932 ) ;
#42438=ORIENTED_EDGE ( 'NONE', *, *, #52353, .T. ) ;
#42447=CARTESIAN_POINT ( 'NONE',  ( 44.24148000000000280, -2.258942858049999725, 12.29419282279000036 ) ) ;
#42448=CARTESIAN_POINT ( 'NONE',  ( 14.03176826122700227, 8.820984799833000878, 7.691098505213000536 ) ) ;
#42453=B_SPLINE_SURFACE_WITH_KNOTS ( 'NONE', 3, 3, ( 
 ( #25783, #58282, #31724, #47114 ),
 ( #26131, #37647, #48143, #36968 ),
 ( #69116, #10727, #53390, #57945 ),
 ( #53729, #48487, #593, #58626 ),
 ( #5828, #20882, #27165, #68414 ),
 ( #42218, #42553, #16662, #10041 ),
 ( #20536, #41861, #31380, #52692 ),
 ( #63523, #15976, #10385, #6518 ),
 ( #40660, #1628, #17005, #33101 ) ),
 .UNSPECIFIED., .F., .F., .F.,
 ( 4, 1, 1, 1, 1, 1, 4 ),
 ( 4, 4 ),
 ( 0.05214259105101000380, 0.1666666666667000196, 0.3333333333333000081, 0.5000000000000000000, 0.6666666666667000474, 0.8333333333333000637, 0.9777068595523999983 ),
 ( -0.1900882580235000174, 1.190231865545000156 ),
 .UNSPECIFIED. ) ;
#42459=CARTESIAN_POINT ( 'NONE',  ( 23.59999176271200128, 13.22318677037999812, 4.267778497637999102 ) ) ;
#42460=LINE ( 'NONE', #10635, #6337 ) ;
#42468=CARTESIAN_POINT ( 'NONE',  ( 24.69898681705700128, -8.733955352176000275, -9.243040794412999972 ) ) ;
#42471=CARTESIAN_POINT ( 'NONE',  ( 12.99403162610500040, 12.11619719077999946, 2.031914795679000019 ) ) ;
#42477=CARTESIAN_POINT ( 'NONE',  ( 13.61451884198527829, 11.47057857663811653, 2.038550092597725794 ) ) ;
#42487=CARTESIAN_POINT ( 'NONE',  ( 24.95780622180999941, 12.04100287684999948, -2.875622496761999880 ) ) ;
#42488=CARTESIAN_POINT ( 'NONE',  ( 21.72233714749290101, -1.140832415794000035E-13, 6.000000000000000000 ) ) ;
#42493=CARTESIAN_POINT ( 'NONE',  ( 23.57704543710643463, -10.25518402361791814, 9.510250455292135641 ) ) ;
#42495=DIRECTION ( 'NONE',  ( 0.000000000000000000, 0.3118250626419980520, -0.9501395320205942019 ) ) ;
#42497=AXIS2_PLACEMENT_3D ( 'NONE', #17490, #22377, #5950 ) ;
#42504=EDGE_LOOP ( 'NONE', ( #17245, #21562, #25095, #19504, #66287 ) ) ;
#42511=CARTESIAN_POINT ( 'NONE',  ( 25.59994555223599733, -8.527741194213000142, -7.260611644044000279 ) ) ;
#42513=CARTESIAN_POINT ( 'NONE',  ( 13.69992376746900042, -12.26631831379999937, -2.532779022035999805 ) ) ;
#42515=CARTESIAN_POINT ( 'NONE',  ( 17.10000426004115326, 12.52500000000000036, 2.429202523439327966E-10 ) ) ;
#42524=EDGE_CURVE ( 'NONE', #7379, #8238, #2503, .T. ) ;
#42534=DIRECTION ( 'NONE',  ( 0.000000000000000000, 0.000000000000000000, -1.000000000000000000 ) ) ;
#42540=VERTEX_POINT ( 'NONE', #26815 ) ;
#42547=CARTESIAN_POINT ( 'NONE',  ( 11.50001496185000249, 11.50879548940379493, -5.112724829163610707 ) ) ;
#42548=B_SPLINE_CURVE_WITH_KNOTS ( 'NONE', 3,
 ( #19297, #2876, #57046, #61953 ),
 .UNSPECIFIED., .F., .F.,
 ( 4, 4 ),
 ( 0.000000000000000000, 1.000000000000000000 ),
 .UNSPECIFIED. ) ;
#42552=ORIENTED_EDGE ( 'NONE', *, *, #13301, .F. ) ;
#42553=CARTESIAN_POINT ( 'NONE',  ( 16.22798078375900133, -3.564332247067999671, -11.94996243427999971 ) ) ;
#42557=CARTESIAN_POINT ( 'NONE',  ( 24.69609434945602544, -8.660954285513374984, -8.619379122962911310 ) ) ;
#42566=ORIENTED_EDGE ( 'NONE', *, *, #25754, .T. ) ;
#42568=ORIENTED_EDGE ( 'NONE', *, *, #48924, .F. ) ;
#42572=ORIENTED_EDGE ( 'NONE', *, *, #50357, .F. ) ;
#42586=B_SPLINE_CURVE_WITH_KNOTS ( 'NONE', 3,
 ( #20074, #63742, #26357, #15852 ),
 .UNSPECIFIED., .F., .F.,
 ( 4, 4 ),
 ( 0.000000000000000000, 1.000000000000000000 ),
 .UNSPECIFIED. ) ;
#42593=CARTESIAN_POINT ( 'NONE',  ( 23.73965757102299889, -13.16312038164999976, 3.763220966169999571 ) ) ;
#42606=DIRECTION ( 'NONE',  ( -1.000000000000000000, 0.000000000000000000, 0.000000000000000000 ) ) ;
#42609=CARTESIAN_POINT ( 'NONE',  ( 11.44795901272999927, -3.583381594953999549, 11.14153199795000049 ) ) ;
#42621=CARTESIAN_POINT ( 'NONE',  ( 12.40000000000000213, -11.60847947989999973, -1.809983899806999919 ) ) ;
#42624=CARTESIAN_POINT ( 'NONE',  ( 25.55276892244668474, -11.13096414089930164, 3.116574921624185368 ) ) ;
#42625=ORIENTED_EDGE ( 'NONE', *, *, #60838, .F. ) ;
#42631=EDGE_LOOP ( 'NONE', ( #60399, #47207, #53580, #64806 ) ) ;
#42639=ORIENTED_EDGE ( 'NONE', *, *, #36441, .T. ) ;
#42640=AXIS2_PLACEMENT_3D ( 'NONE', #55371, #12026, #65149 ) ;
#42648=CARTESIAN_POINT ( 'NONE',  ( 24.74075890553500301, -3.240096724082000001, -11.83467285805000024 ) ) ;
#42651=ORIENTED_EDGE ( 'NONE', *, *, #21995, .F. ) ;
#42669=CARTESIAN_POINT ( 'NONE',  ( 24.69607615698642533, -3.134132996396517434, 11.81031189595167952 ) ) ;
#42670=CARTESIAN_POINT ( 'NONE',  ( 24.62620337042029206, -8.774568047083310063, -9.205177742587718370 ) ) ;
#42676=B_SPLINE_CURVE_WITH_KNOTS ( 'NONE', 3,
 ( #59420, #26931, #52810, #16426 ),
 .UNSPECIFIED., .F., .F.,
 ( 4, 4 ),
 ( 0.000000000000000000, 0.5000000000000298650 ),
 .UNSPECIFIED. ) ;
#42681=CARTESIAN_POINT ( 'NONE',  ( 23.59999192078999997, 10.30759737717999869, 9.317725909430999209 ) ) ;
#42695=EDGE_CURVE ( 'NONE', #51578, #28388, #5834, .T. ) ;
#42703=AXIS2_PLACEMENT_3D ( 'NONE', #52093, #67827, #25877 ) ;
#42712=ORIENTED_EDGE ( 'NONE', *, *, #17205, .T. ) ;
#42717=CARTESIAN_POINT ( 'NONE',  ( 17.84632887397102863, -3.351233551899249985, 11.15758637348127458 ) ) ;
#42725=B_SPLINE_SURFACE_WITH_KNOTS ( 'NONE', 3, 3, ( 
 ( #42838, #64148, #49113, #38980 ),
 ( #54706, #59948, #28492, #33738 ),
 ( #6805, #189, #21505, #28142 ),
 ( #16262, #11022, #1564, #37586 ),
 ( #58919, #22886, #44237, #32359 ),
 ( #48427, #53675, #22198, #5769 ),
 ( #17657, #27111, #60298, #1225 ),
 ( #43534, #12407, #535, #21847 ),
 ( #22538, #43182, #64486, #32696 ) ),
 .UNSPECIFIED., .F., .F., .F.,
 ( 4, 1, 1, 1, 1, 1, 4 ),
 ( 4, 4 ),
 ( 0.05214259105100000485, 0.1666666666667000196, 0.3333333333333000081, 0.5000000000000000000, 0.6666666666667000474, 0.8333333333333000637, 0.9777068595523999983 ),
 ( -0.1900882580235000174, 1.190231865545000156 ),
 .UNSPECIFIED. ) ;
#42727=CARTESIAN_POINT ( 'NONE',  ( 23.61456325407660017, 10.17980770879276697, -9.423256655973792917 ) ) ;
#42729=ORIENTED_EDGE ( 'NONE', *, *, #12478, .F. ) ;
#42739=B_SPLINE_CURVE_WITH_KNOTS ( 'NONE', 3,
 ( #3793, #19198, #61167, #46117 ),
 .UNSPECIFIED., .F., .F.,
 ( 4, 4 ),
 ( 0.5000023781865966521, 1.000000000000000000 ),
 .UNSPECIFIED. ) ;
#42740=CARTESIAN_POINT ( 'NONE',  ( 17.89159592529800236, -3.376698609984999599, 11.11057657535000054 ) ) ;
#42744=CARTESIAN_POINT ( 'NONE',  ( 13.51802873821100270, 11.59174185862000073, 2.195273509308000026 ) ) ;
#42754=CARTESIAN_POINT ( 'NONE',  ( 24.97036873516232092, -8.550788777872098123, 8.359011271273349308 ) ) ;
#42756=CARTESIAN_POINT ( 'NONE',  ( 23.89320776801300283, -8.862674798131001452, -7.304122743059000555 ) ) ;
#42759=CARTESIAN_POINT ( 'NONE',  ( 12.18592533278400047, 11.71489335541000010, -3.703722432179000101 ) ) ;
#42760=CARTESIAN_POINT ( 'NONE',  ( 18.44593829204400137, 11.84685177148000079, -3.896686237526999719 ) ) ;
#42765=FACE_OUTER_BOUND ( 'NONE', #65302, .T. ) ;
#42768=EDGE_LOOP ( 'NONE', ( #8077, #17969, #64744, #64247 ) ) ;
#42771=CYLINDRICAL_SURFACE ( 'NONE', #31878, 12.52500000000000036 ) ;
#42789=CARTESIAN_POINT ( 'NONE',  ( 25.46373329105799854, 11.23406619596999967, -3.161081784610999978 ) ) ;
#42790=CARTESIAN_POINT ( 'NONE',  ( 13.05446786537200232, -12.11615129267999968, -2.032410325197000045 ) ) ;
#42807=CARTESIAN_POINT ( 'NONE',  ( 25.20346112680899964, -11.20001863952999877, -3.404198054529000039 ) ) ;
#42811=CARTESIAN_POINT ( 'NONE',  ( 11.49999672495000169, -4.789193247147717436, 10.68959786790916588 ) ) ;
#42816=EDGE_LOOP ( 'NONE', ( #20951, #68756, #1620, #27592 ) ) ;
#42820=ORIENTED_EDGE ( 'NONE', *, *, #56798, .T. ) ;
#42821=CARTESIAN_POINT ( 'NONE',  ( 23.57776935471744650, -2.928921454179648887, -13.64745658425302643 ) ) ;
#42834=CYLINDRICAL_SURFACE ( 'NONE', #49915, 0.6999999999999992895 ) ;
#42838=CARTESIAN_POINT ( 'NONE',  ( 16.13899430609699692, 3.920333201250000066, 11.93553532998999955 ) ) ;
#42840=CARTESIAN_POINT ( 'NONE',  ( 24.14319150313052731, 12.47686771584972831, 3.361582803975455835 ) ) ;
#42841=EDGE_CURVE ( 'NONE', #36843, #33549, #25907, .T. ) ;
#42843=CARTESIAN_POINT ( 'NONE',  ( 13.69992376746900042, -12.26631831379999937, -2.532779022035999805 ) ) ;
#42844=VERTEX_POINT ( 'NONE', #11318 ) ;
#42863=CARTESIAN_POINT ( 'NONE',  ( 18.29058462260969975, 11.07487261139536194, -3.615341608537649964 ) ) ;
#42865=ADVANCED_FACE ( 'NONE', ( #30403 ), #64059, .F. ) ;
#42872=CARTESIAN_POINT ( 'NONE',  ( 24.22080089608900266, 8.983041208896999308, 8.867674127912000159 ) ) ;
#42876=CYLINDRICAL_SURFACE ( 'NONE', #60599, 1.000000000000000000 ) ;
#42884=ORIENTED_EDGE ( 'NONE', *, *, #44761, .F. ) ;
#42890=ORIENTED_EDGE ( 'NONE', *, *, #386, .F. ) ;
#42915=CARTESIAN_POINT ( 'NONE',  ( 15.72310803393400036, -9.201544169428000686, -8.280720087647999605 ) ) ;
#42930=VERTEX_POINT ( 'NONE', #16032 ) ;
#42931=CONICAL_SURFACE ( 'NONE', #11675, 12.42518024156999878, 0.7854126340177727261 ) ;
#42932=CARTESIAN_POINT ( 'NONE',  ( 11.56599877858000092, -12.45298756855999933, -1.663864064400000009 ) ) ;
#42950=CARTESIAN_POINT ( 'NONE',  ( 23.58303273028899838, -10.33244704280000015, -9.360922793932001440 ) ) ;
#42952=CARTESIAN_POINT ( 'NONE',  ( 23.59999172348799945, -10.30759808834999980, 9.317726582648999667 ) ) ;
#42953=EDGE_LOOP ( 'NONE', ( #44818, #50374, #46835, #40749 ) ) ;
#42963=ADVANCED_FACE ( 'NONE', ( #5543 ), #26538, .F. ) ;
#42966=CARTESIAN_POINT ( 'NONE',  ( 24.84571236082737045, 12.09404552098319918, -2.924969662484652844 ) ) ;
#42973=EDGE_LOOP ( 'NONE', ( #54391, #20454, #62872, #12526 ) ) ;
#42981=CARTESIAN_POINT ( 'NONE',  ( 25.02476335228798376, -11.45589514262583464, -3.243232877822501248 ) ) ;
#42985=ORIENTED_EDGE ( 'NONE', *, *, #53924, .T. ) ;
#43011=CARTESIAN_POINT ( 'NONE',  ( 25.10985785448133356, -2.855902626858047633, 11.47560089494121094 ) ) ;
#43012=CARTESIAN_POINT ( 'NONE',  ( 24.66708179568188442, -8.738412506716594308, -9.169048261100254393 ) ) ;
#43013=CARTESIAN_POINT ( 'NONE',  ( 11.48381255716000027, 12.35454260995000020, 1.695649549036999826 ) ) ;
#43021=ORIENTED_EDGE ( 'NONE', *, *, #5998, .F. ) ;
#43024=CARTESIAN_POINT ( 'NONE',  ( 21.70000133425200062, 14.00000000000000000, 0.000000000000000000 ) ) ;
#43035=CARTESIAN_POINT ( 'NONE',  ( 18.49993212792200126, -2.908182645667999999, -12.18276646858999968 ) ) ;
#43038=CARTESIAN_POINT ( 'NONE',  ( 17.60000000064766823, 12.03387897622311797, -3.206083669095133981 ) ) ;
#43040=CARTESIAN_POINT ( 'NONE',  ( 12.80000000000000071, 10.78295181803999903, -4.410266442048000002 ) ) ;
#43042=CARTESIAN_POINT ( 'NONE',  ( 16.39999999231800132, 3.216285993016000155, 11.40340220863999932 ) ) ;
#43043=ORIENTED_EDGE ( 'NONE', *, *, #10951, .F. ) ;
#43054=PLANE ( 'NONE',  #30417 ) ;
#43059=CARTESIAN_POINT ( 'NONE',  ( 21.00000000000000000, 11.79499999999999993, 0.000000000000000000 ) ) ;
#43061=CARTESIAN_POINT ( 'NONE',  ( 11.79999999771000141, -3.595163221087000149, 11.99793848941000007 ) ) ;
#43064=CARTESIAN_POINT ( 'NONE',  ( 25.29986325275000070, 2.078227429405999693, 11.31065739696999906 ) ) ;
#43065=CARTESIAN_POINT ( 'NONE',  ( 24.46729256464000457, 12.16659091368999945, 3.168154674931000336 ) ) ;
#43067=ORIENTED_EDGE ( 'NONE', *, *, #31067, .F. ) ;
#43071=AXIS2_PLACEMENT_3D ( 'NONE', #13359, #23834, #55999 ) ;
#43072=CARTESIAN_POINT ( 'NONE',  ( 24.63332964936066816, 10.83443035059421433, -3.855530959300003335 ) ) ;
#43077=CARTESIAN_POINT ( 'NONE',  ( 23.74395678421098310, 3.264333397773110157, -13.24373423702363617 ) ) ;
#43083=B_SPLINE_CURVE_WITH_KNOTS ( 'NONE', 3,
 ( #24285, #2274, #23592, #34450 ),
 .UNSPECIFIED., .F., .F.,
 ( 4, 4 ),
 ( 0.000000000000000000, 1.000000000000000000 ),
 .UNSPECIFIED. ) ;
#43085=CARTESIAN_POINT ( 'NONE',  ( 12.99421883851900184, 11.64667883987999986, 1.861676925984000031 ) ) ;
#43086=ORIENTED_EDGE ( 'NONE', *, *, #37092, .F. ) ;
#43095=CARTESIAN_POINT ( 'NONE',  ( 11.50029455687000102, -11.56505190006999939, -1.404305717648999918 ) ) ;
#43099=CARTESIAN_POINT ( 'NONE',  ( 13.49994651945300284, 12.07042783918999795, 2.492331243371999960 ) ) ;
#43104=CARTESIAN_POINT ( 'NONE',  ( 12.79484580939900162, 11.81466332729999991, -3.323431527667999763 ) ) ;
#43105=CARTESIAN_POINT ( 'NONE',  ( 18.15988268186300303, 12.12177778538999995, -3.303327906654999868 ) ) ;
#43110=CARTESIAN_POINT ( 'NONE',  ( 17.60000001947600268, -11.86186880240999919, 3.298627760718999991 ) ) ;
#43116=FACE_OUTER_BOUND ( 'NONE', #23353, .T. ) ;
#43125=DIRECTION ( 'NONE',  ( -1.000000000000000000, 0.000000000000000000, 0.000000000000000000 ) ) ;
#43133=CARTESIAN_POINT ( 'NONE',  ( 16.20679720086500097, -3.450734216086000394, -11.08786462205999968 ) ) ;
#43137=CARTESIAN_POINT ( 'NONE',  ( 23.60000000000000142, 2.258942858049999725, -12.29419282279000036 ) ) ;
#43142=B_SPLINE_CURVE_WITH_KNOTS ( 'NONE', 3,
 ( #38105, #63292, #59431, #31166 ),
 .UNSPECIFIED., .F., .F.,
 ( 4, 4 ),
 ( 0.000000000000000000, 1.000000000000000000 ),
 .UNSPECIFIED. ) ;
#43144=CARTESIAN_POINT ( 'NONE',  ( 17.80000000001300009, -3.351264566333000072, -11.15757590352999884 ) ) ;
#43147=VERTEX_POINT ( 'NONE', #51555 ) ;
#43151=CARTESIAN_POINT ( 'NONE',  ( 12.79999999914999975, -12.11987927271999865, 3.159802730921999814 ) ) ;
#43154=EDGE_LOOP ( 'NONE', ( #18253, #42064, #61348, #1714 ) ) ;
#43159=CARTESIAN_POINT ( 'NONE',  ( 25.12927996638910955, 8.519456805637897645, -8.174607305189095285 ) ) ;
#43161=ORIENTED_EDGE ( 'NONE', *, *, #6209, .T. ) ;
#43168=EDGE_CURVE ( 'NONE', #27228, #16591, #34956, .T. ) ;
#43169=ADVANCED_FACE ( 'NONE', ( #67285 ), #35827, .F. ) ;
#43170=CARTESIAN_POINT ( 'NONE',  ( 24.85113676206800193, 11.95314342760000059, -2.993325325037999640 ) ) ;
#43172=ORIENTED_EDGE ( 'NONE', *, *, #4827, .T. ) ;
#43180=AXIS2_PLACEMENT_3D ( 'NONE', #11259, #16848, #21406 ) ;
#43182=CARTESIAN_POINT ( 'NONE',  ( 16.43164332880499856, 3.528999066054999467, 11.96046905204000055 ) ) ;
#43184=CARTESIAN_POINT ( 'NONE',  ( 24.15455527622187049, 12.45781941376721136, 3.353847473082901764 ) ) ;
#43186=ORIENTED_EDGE ( 'NONE', *, *, #6209, .F. ) ;
#43196=ADVANCED_FACE ( 'NONE', ( #8571 ), #29917, .F. ) ;
#43199=CARTESIAN_POINT ( 'NONE',  ( 24.59232786471100241, -3.480949894194999672, 12.13588334916000022 ) ) ;
#43202=CARTESIAN_POINT ( 'NONE',  ( 12.64393528606200334, -11.55448221446000012, 4.935476321030999536 ) ) ;
#43205=DIRECTION ( 'NONE',  ( 1.000000000000000000, 0.000000000000000000, 0.000000000000000000 ) ) ;
#43210=CARTESIAN_POINT ( 'NONE',  ( 24.60170725920900026, -8.811863727701000570, -9.296544040758000449 ) ) ;
#43214=CARTESIAN_POINT ( 'NONE',  ( 17.79999999998900151, -3.595165934733000057, 11.99793354950999991 ) ) ;
#43220=AXIS2_PLACEMENT_3D ( 'NONE', #32972, #54284, #7087 ) ;
#43221=B_SPLINE_CURVE_WITH_KNOTS ( 'NONE', 3,
 ( #42403, #89, #10234, #5329 ),
 .UNSPECIFIED., .F., .F.,
 ( 4, 4 ),
 ( 0.000000000000000000, 1.000000000000000000 ),
 .UNSPECIFIED. ) ;
#43227=EDGE_CURVE ( 'NONE', #14826, #38133, #60826, .T. ) ;
#43241=CARTESIAN_POINT ( 'NONE',  ( 11.30000285318000230, 11.76356368987999979, 1.428410073821000159 ) ) ;
#43242=CARTESIAN_POINT ( 'NONE',  ( 11.35619132127000164, 11.69822877698999974, 1.509327410273999970 ) ) ;
#43254=ORIENTED_EDGE ( 'NONE', *, *, #48466, .T. ) ;
#43257=EDGE_CURVE ( 'NONE', #10372, #15717, #19790, .T. ) ;
#43261=CARTESIAN_POINT ( 'NONE',  ( 15.95500032369699994, -8.890098389148999303, -8.614471248541999415 ) ) ;
#43266=CARTESIAN_POINT ( 'NONE',  ( 23.59999999999999787, -0.9826074631703644036, 13.89481016226972798 ) ) ;
#43267=CARTESIAN_POINT ( 'NONE',  ( 24.26287167771109310, -3.288955327281299024, -12.27454490589861358 ) ) ;
#43272=ORIENTED_EDGE ( 'NONE', *, *, #60389, .T. ) ;
#43283=CARTESIAN_POINT ( 'NONE',  ( 24.22080405609500176, -12.17114551901999953, 3.345703174095000065 ) ) ;
#43288=PLANE ( 'NONE',  #30225 ) ;
#43296=CARTESIAN_POINT ( 'NONE',  ( 23.62003649549700057, -10.21603048626000110, -9.339736802856998921 ) ) ;
#43297=DIRECTION ( 'NONE',  ( 1.000000000000000000, 0.000000000000000000, 0.000000000000000000 ) ) ;
#43305=LINE ( 'NONE', #17064, #64622 ) ;
#43309=B_SPLINE_CURVE_WITH_KNOTS ( 'NONE', 3,
 ( #15365, #57657, #16041, #37372, #42287, #5210 ),
 .UNSPECIFIED., .F., .F.,
 ( 4, 2, 4 ),
 ( 0.000000000000000000, 0.5000000000000000000, 1.000000000000000000 ),
 .UNSPECIFIED. ) ;
#43313=FACE_OUTER_BOUND ( 'NONE', #51911, .T. ) ;
#43317=ADVANCED_FACE ( 'NONE', ( #15536 ), #27838, .F. ) ;
#43324=CARTESIAN_POINT ( 'NONE',  ( 24.43232361759900328, 11.98245802077999933, -3.250304477315999918 ) ) ;
#43326=CARTESIAN_POINT ( 'NONE',  ( 11.93277786803400176, -12.01216300861999997, 3.678628708156000293 ) ) ;
#43330=CARTESIAN_POINT ( 'NONE',  ( 24.67921321864300310, 12.29514728640000065, 2.979192498689000157 ) ) ;
#43333=CARTESIAN_POINT ( 'NONE',  ( 25.26126434830474565, -11.18200453048727283, -3.383907761729669339 ) ) ;
#43338=EDGE_LOOP ( 'NONE', ( #19788, #65891, #33546, #40376 ) ) ;
#43340=AXIS2_PLACEMENT_3D ( 'NONE', #54821, #6920, #7269 ) ;
#43343=B_SPLINE_CURVE_WITH_KNOTS ( 'NONE', 3,
 ( #6378, #6727, #28068, #2526 ),
 .UNSPECIFIED., .F., .F.,
 ( 4, 4 ),
 ( 0.000000000000000000, 1.000000000000000000 ),
 .UNSPECIFIED. ) ;
#43350=EDGE_LOOP ( 'NONE', ( #66534, #58234, #39997, #10744 ) ) ;
#43352=CARTESIAN_POINT ( 'NONE',  ( 23.75091569058821861, 9.822198688071051009, 9.446472845318485412 ) ) ;
#43370=CARTESIAN_POINT ( 'NONE',  ( 11.26395919764000197, 12.20155262497000059, 1.453968487665999954 ) ) ;
#43377=ORIENTED_EDGE ( 'NONE', *, *, #17117, .T. ) ;
#43389=CARTESIAN_POINT ( 'NONE',  ( 18.43044927002210898, -3.211191212929379368, -12.10643352320191291 ) ) ;
#43396=DIRECTION ( 'NONE',  ( 0.000000000000000000, 0.2714570858282905341, 0.9624505444715651947 ) ) ;
#43398=VECTOR ( 'NONE', #23814, 1000.000000000000227 ) ;
#43402=FACE_OUTER_BOUND ( 'NONE', #32714, .T. ) ;
#43405=EDGE_CURVE ( 'NONE', #60537, #59934, #6754, .T. ) ;
#43407=CARTESIAN_POINT ( 'NONE',  ( 11.29996849689000271, 12.23272706294999956, 1.505586356912999912 ) ) ;
#43409=ORIENTED_EDGE ( 'NONE', *, *, #54696, .T. ) ;
#43410=ADVANCED_FACE ( 'NONE', ( #17956 ), #49035, .F. ) ;
#43414=DIRECTION ( 'NONE',  ( 0.000000000000000000, 0.000000000000000000, 1.000000000000000000 ) ) ;
#43416=CARTESIAN_POINT ( 'NONE',  ( 19.99999987597299977, 0.000000000000000000, -12.42499880353994790 ) ) ;
#43417=CARTESIAN_POINT ( 'NONE',  ( 18.29999039390560611, -11.60794187010165679, 4.146723114213013872 ) ) ;
#43420=CARTESIAN_POINT ( 'NONE',  ( 15.89998535262536805, 8.893549080881223645, 8.534693534631724532 ) ) ;
#43423=B_SPLINE_CURVE_WITH_KNOTS ( 'NONE', 3,
 ( #67185, #29816, #51798, #40621 ),
 .UNSPECIFIED., .F., .F.,
 ( 4, 4 ),
 ( 0.000000000000000000, 1.000000000000000000 ),
 .UNSPECIFIED. ) ;
#43425=CARTESIAN_POINT ( 'NONE',  ( 23.85842739849388039, 9.609046041819039985, -9.387911839951371462 ) ) ;
#43433=ORIENTED_EDGE ( 'NONE', *, *, #26589, .F. ) ;
#43436=CARTESIAN_POINT ( 'NONE',  ( 24.30000560072254956, -3.240508257516428348, 12.09374145940176781 ) ) ;
#43443=ORIENTED_EDGE ( 'NONE', *, *, #23622, .F. ) ;
#43446=CARTESIAN_POINT ( 'NONE',  ( 24.57788509330325866, -12.41755320267419016, 3.012067450276798120 ) ) ;
#43452=CARTESIAN_POINT ( 'NONE',  ( 24.73255479474749663, -8.642945031846046788, 8.588131473315229414 ) ) ;
#43461=CARTESIAN_POINT ( 'NONE',  ( 12.78642148534500045, 11.38816520531000087, -4.576060180783999343 ) ) ;
#43462=CARTESIAN_POINT ( 'NONE',  ( 17.90267118914800193, 12.03818693049999844, -3.242368311117000079 ) ) ;
#43466=CARTESIAN_POINT ( 'NONE',  ( 18.35309808591700076, -2.844562563850999926, 12.04738788559999918 ) ) ;
#43470=CARTESIAN_POINT ( 'NONE',  ( 23.60000000000000142, 0.000000000000000000, 0.000000000000000000 ) ) ;
#43473=CARTESIAN_POINT ( 'NONE',  ( 13.46376629110800138, 9.221173139870998625, 7.505113150216000228 ) ) ;
#43485=ADVANCED_FACE ( 'NONE', ( #46840 ), #65215, .F. ) ;
#43490=ADVANCED_FACE ( 'NONE', ( #30760 ), #38752, .F. ) ;
#43493=DIRECTION ( 'NONE',  ( 0.000000000000000000, 0.000000000000000000, -1.000000000000000000 ) ) ;
#43502=SHAPE_DEFINITION_REPRESENTATION ( #2556, #27655 ) ;
#43507=DIRECTION ( 'NONE',  ( -1.000000000000000000, 0.000000000000000000, 0.000000000000000000 ) ) ;
#43508=DIRECTION ( 'NONE',  ( 0.000000000000000000, -1.000000000000000000, 0.000000000000000000 ) ) ;
#43513=CARTESIAN_POINT ( 'NONE',  ( 17.60000001287599858, 11.53033693765999779, -4.891431908114999949 ) ) ;
#43514=CARTESIAN_POINT ( 'NONE',  ( 24.89166245840957359, 8.575309574094205800, -8.440744490289855406 ) ) ;
#43517=CARTESIAN_POINT ( 'NONE',  ( 23.71153097368373253, -13.14506149773556665, 3.853782021005720093 ) ) ;
#43524=CARTESIAN_POINT ( 'NONE',  ( 25.25799237449400181, 11.13203901161000076, -3.460366607564000496 ) ) ;
#43527=CARTESIAN_POINT ( 'NONE',  ( 11.29998636608000062, -3.695122995756999984, 11.25914041192000070 ) ) ;
#43534=CARTESIAN_POINT ( 'NONE',  ( 16.39967273502900014, 3.641490841173999904, 12.02437761214999945 ) ) ;
#43538=VERTEX_POINT ( 'NONE', #48207 ) ;
#43541=CARTESIAN_POINT ( 'NONE',  ( 13.25828219467840086, 12.15323025559004222, 2.051492516881130879 ) ) ;
#43543=CARTESIAN_POINT ( 'NONE',  ( 24.54223752884296061, -12.46060277342660783, -3.023618805801078224 ) ) ;
#43544=CARTESIAN_POINT ( 'NONE',  ( 24.48513953661800358, 3.324320571727000129, 12.08694663984000073 ) ) ;
#43546=CARTESIAN_POINT ( 'NONE',  ( 24.46225083065800376, -3.149516733939000002, 11.96334735801000093 ) ) ;
#43547=ORIENTED_EDGE ( 'NONE', *, *, #9160, .T. ) ;
#43548=ORIENTED_EDGE ( 'NONE', *, *, #6309, .T. ) ;
#43562=CARTESIAN_POINT ( 'NONE',  ( 23.63944133423405347, 10.04331723767212914, -9.682724240561979556 ) ) ;
#43566=DIRECTION ( 'NONE',  ( 0.000000000000000000, -0.9867381147929490393, -0.1623203401144079905 ) ) ;
#43567=EDGE_LOOP ( 'NONE', ( #17106, #68979, #54243, #46040 ) ) ;
#43568=DIRECTION ( 'NONE',  ( 0.000000000000000000, 1.000000000000000000, 0.000000000000000000 ) ) ;
#43571=EDGE_CURVE ( 'NONE', #67640, #56058, #53273, .T. ) ;
#43577=VERTEX_POINT ( 'NONE', #6235 ) ;
#43587=B_SPLINE_CURVE_WITH_KNOTS ( 'NONE', 3,
 ( #40138, #24045, #25072, #62131 ),
 .UNSPECIFIED., .F., .F.,
 ( 4, 4 ),
 ( 0.000000000000000000, 1.000000000000000000 ),
 .UNSPECIFIED. ) ;
#43594=ORIENTED_EDGE ( 'NONE', *, *, #68027, .T. ) ;
#43598=CARTESIAN_POINT ( 'NONE',  ( 16.39974593105000267, 3.376006003137999922, 11.11079012987999981 ) ) ;
#43628=VERTEX_POINT ( 'NONE', #27576 ) ;
#43634=CARTESIAN_POINT ( 'NONE',  ( 23.99052667663800165, 13.00930538603000031, 3.385156461033000053 ) ) ;
#43637=DIRECTION ( 'NONE',  ( 0.000000000000000000, 1.000000000000000000, 0.000000000000000000 ) ) ;
#43645=CARTESIAN_POINT ( 'NONE',  ( 23.55075815555500185, -10.43336509543999924, -9.388742684132997951 ) ) ;
#43646=CARTESIAN_POINT ( 'NONE',  ( 23.95108089639600379, -9.462566780697001079, 9.411396329312999853 ) ) ;
#43648=CARTESIAN_POINT ( 'NONE',  ( 24.54174074856994636, 3.611931245565921156, -12.30360799778222969 ) ) ;
#43649=EDGE_LOOP ( 'NONE', ( #21012, #49965, #51029, #13571 ) ) ;
#43658=CARTESIAN_POINT ( 'NONE',  ( 24.98632622962700012, 3.086021350299999799, -11.61344612987000069 ) ) ;
#43662=CARTESIAN_POINT ( 'NONE',  ( 25.30000327618300204, -10.83443035398000021, 3.855530949778000149 ) ) ;
#43663=ORIENTED_EDGE ( 'NONE', *, *, #18233, .F. ) ;
#43669=ORIENTED_EDGE ( 'NONE', *, *, #3228, .F. ) ;
#43670=FACE_OUTER_BOUND ( 'NONE', #5472, .T. ) ;
#43671=CARTESIAN_POINT ( 'NONE',  ( 12.04524561587600040, -11.75582082520000071, 3.881266971570999758 ) ) ;
#43675=CARTESIAN_POINT ( 'NONE',  ( 23.58549486637999948, 3.200144626573000028, 13.61915301421999835 ) ) ;
#43684=CARTESIAN_POINT ( 'NONE',  ( 23.74333464321300013, 13.04438545414000039, -3.827011755022000195 ) ) ;
#43685=AXIS2_PLACEMENT_3D ( 'NONE', #25236, #46912, #35056 ) ;
#43688=ORIENTED_EDGE ( 'NONE', *, *, #44538, .T. ) ;
#43694=CARTESIAN_POINT ( 'NONE',  ( 23.89493791382834331, 9.543146308824796975, 9.361218189416669944 ) ) ;
#43698=CARTESIAN_POINT ( 'NONE',  ( 23.60205915885299888, 2.489696159912998752, -12.09604418629000122 ) ) ;
#43700=DIRECTION ( 'NONE',  ( 1.000000000000000000, 0.000000000000000000, 0.000000000000000000 ) ) ;
#43702=CARTESIAN_POINT ( 'NONE',  ( 13.99932787941000178, 9.131694343880999654, 8.218494815692999111 ) ) ;
#43708=EDGE_LOOP ( 'NONE', ( #54613, #15785, #36177, #3716 ) ) ;
#43710=CARTESIAN_POINT ( 'NONE',  ( 23.56666365135700403, -11.16210620489000327, 3.571147223011999827 ) ) ;
#43712=CARTESIAN_POINT ( 'NONE',  ( 11.25951067610000145, 12.19482939020999979, 1.501993453007000046 ) ) ;
#43716=ADVANCED_FACE ( 'NONE', ( #43313 ), #22319, .F. ) ;
#43720=ORIENTED_EDGE ( 'NONE', *, *, #63025, .F. ) ;
#43730=VERTEX_POINT ( 'NONE', #11829 ) ;
#43741=EDGE_LOOP ( 'NONE', ( #54522, #55647, #26573, #25620 ) ) ;
#43746=DIRECTION ( 'NONE',  ( 1.000000000000000000, 0.000000000000000000, 0.000000000000000000 ) ) ;
#43753=DIRECTION ( 'NONE',  ( 1.000000000000000000, 0.000000000000000000, 0.000000000000000000 ) ) ;
#43763=B_SPLINE_CURVE_WITH_KNOTS ( 'NONE', 3,
 ( #51404, #50723, #55626, #66446 ),
 .UNSPECIFIED., .F., .F.,
 ( 4, 4 ),
 ( 0.000000000000000000, 1.000000000000000000 ),
 .UNSPECIFIED. ) ;
#43766=DIRECTION ( 'NONE',  ( 1.000000000000000000, 0.000000000000000000, 0.000000000000000000 ) ) ;
#43768=CARTESIAN_POINT ( 'NONE',  ( 12.73341336112467559, -10.78295181804177894, 4.410266442042688695 ) ) ;
#43787=EDGE_LOOP ( 'NONE', ( #50270, #21768, #11420, #5973 ) ) ;
#43791=DIRECTION ( 'NONE',  ( 0.000000000000000000, 1.000000000000000000, 0.000000000000000000 ) ) ;
#43794=CARTESIAN_POINT ( 'NONE',  ( 23.58885762929001473, 13.25331360343164278, -4.277525096992856213 ) ) ;
#43802=VERTEX_POINT ( 'NONE', #5475 ) ;
#43810=AXIS2_PLACEMENT_3D ( 'NONE', #6121, #37600, #27459 ) ;
#43814=CARTESIAN_POINT ( 'NONE',  ( 18.30003129334700063, 2.732683817159999862, -11.53064095410000078 ) ) ;
#43816=DIRECTION ( 'NONE',  ( 1.267684221833849905E-20, -0.9999999999999997780, -2.657887425080999156E-08 ) ) ;
#43824=EDGE_LOOP ( 'NONE', ( #53487, #47804, #5066, #3734 ) ) ;
#43828=CARTESIAN_POINT ( 'NONE',  ( 11.29998770065200731, -3.699024161916728115, 11.75540420325642543 ) ) ;
#43829=B_SPLINE_CURVE_WITH_KNOTS ( 'NONE', 3,
 ( #2887, #8483, #24901, #61965, #30495, #35740, #51808, #46231, #13047, #3906, #44864, #61616, #57058, #34376, #55696, #2542, #7792, #40982, #56380, #24562, #30166, #29132, #45885, #50440, #67195, #8823, #14078, #23869, #45208, #66511, #51469, #18633, #39962, #67538, #8139, #61280 ),
 .UNSPECIFIED., .F., .F.,
 ( 4, 2, 2, 1, 2, 2, 2, 1, 1, 1, 2, 2, 2, 2, 2, 2, 2, 2, 2, 4 ),
 ( 0.000000000000000000, 0.1249999999992055799, 0.1874999999988075372, 0.2187499999986079191, 0.2343749999985092758, 0.2499999999984106325, 0.3749999999976186826, 0.4374999999972214448, 0.4687499999970250464, 0.4843749999969280129, 0.4921874999968802733, 0.4999999999968325337, 0.5624999999972273290, 0.5937499999974238385, 0.6093749999975215381, 0.6249999999976191267, 0.6874999999980111465, 0.7187499999982103205, 0.7499999999984094945, 1.000000000000000000 ),
 .UNSPECIFIED. ) ;
#43843=CARTESIAN_POINT ( 'NONE',  ( 24.45999032648100169, -8.787256713296999422, 8.710686399493999588 ) ) ;
#43846=CARTESIAN_POINT ( 'NONE',  ( 11.36656731458420033, -12.29889127619872724, -1.513729328724678469 ) ) ;
#43848=CARTESIAN_POINT ( 'NONE',  ( 25.36464211350600451, -8.490054962244000691, -7.944963175427000479 ) ) ;
#43851=CARTESIAN_POINT ( 'NONE',  ( 13.55309301929700005, 12.11670754034000019, 2.533073449765999907 ) ) ;
#43852=ORIENTED_EDGE ( 'NONE', *, *, #5533, .T. ) ;
#43856=CARTESIAN_POINT ( 'NONE',  ( 25.00274840847853142, -8.478821250423088429, -8.837051340891205697 ) ) ;
#43857=CARTESIAN_POINT ( 'NONE',  ( 25.09891544561744681, 8.522828975275432484, -8.212590430020295429 ) ) ;
#43862=CARTESIAN_POINT ( 'NONE',  ( 15.89979320885400327, -3.824231472901999496, -11.71686814605000038 ) ) ;
#43866=CARTESIAN_POINT ( 'NONE',  ( 27.09999999999999787, 0.000000000000000000, 0.000000000000000000 ) ) ;
#43871=ORIENTED_EDGE ( 'NONE', *, *, #17313, .F. ) ;
#43876=CARTESIAN_POINT ( 'NONE',  ( 24.71765909950762108, 11.77379917328191183, -3.190796897422294887 ) ) ;
#43889=CIRCLE ( 'NONE', #3645, 0.6999999999999992895 ) ;
#43893=CARTESIAN_POINT ( 'NONE',  ( 25.09299735342200321, -3.211993599267000121, 11.60337401171999971 ) ) ;
#43896=ORIENTED_EDGE ( 'NONE', *, *, #2298, .F. ) ;
#43908=CARTESIAN_POINT ( 'NONE',  ( 17.60000000000000142, 48.67241131317999958, -16.56944037379999912 ) ) ;
#43910=AXIS2_PLACEMENT_3D ( 'NONE', #66223, #34084, #7495 ) ;
#43911=CARTESIAN_POINT ( 'NONE',  ( 23.56664675778400309, 10.37811020278999941, -9.381454169592000625 ) ) ;
#43920=CARTESIAN_POINT ( 'NONE',  ( 24.35365242081700288, 8.355077740100997019, -8.511587483919999642 ) ) ;
#43940=CONICAL_SURFACE ( 'NONE', #28313, 1.150090567076000214, 0.7854665416972951286 ) ;
#43943=ORIENTED_EDGE ( 'NONE', *, *, #39009, .F. ) ;
#43945=CARTESIAN_POINT ( 'NONE',  ( 16.13869549901199818, 3.415897281711999689, 11.19349503352999875 ) ) ;
#43948=CARTESIAN_POINT ( 'NONE',  ( 15.82968830470041866, -8.721231603649751918, -7.724200095968971169 ) ) ;
#43949=CARTESIAN_POINT ( 'NONE',  ( 24.14471467316711539, -9.246855113160467710, -9.586736432819547460 ) ) ;
#43955=CARTESIAN_POINT ( 'NONE',  ( 23.63066792764499979, -13.46837681827999944, -3.823564519506999826 ) ) ;
#43958=DIRECTION ( 'NONE',  ( 0.000000000000000000, -1.000000000000000000, 0.000000000000000000 ) ) ;
#43959=ORIENTED_EDGE ( 'NONE', *, *, #27755, .T. ) ;
#43974=CARTESIAN_POINT ( 'NONE',  ( 11.60578299225600141, -12.22760809526000081, -1.919009911369000010 ) ) ;
#43979=CARTESIAN_POINT ( 'NONE',  ( 24.32734093809899889, 12.60105586225999907, 3.144288050074000029 ) ) ;
#43992=CARTESIAN_POINT ( 'NONE',  ( 24.03156049766399960, -9.408031995601998432, -9.735591824543000428 ) ) ;
#43993=CARTESIAN_POINT ( 'NONE',  ( 24.63625278502800242, -8.802584369108002349, 9.348454315309000506 ) ) ;
#43994=CARTESIAN_POINT ( 'NONE',  ( 23.60000000000000497, -12.92119876218218977, 5.203224594798002478 ) ) ;
#43995=EDGE_LOOP ( 'NONE', ( #5185, #963, #7659, #9026 ) ) ;
#43999=DIRECTION ( 'NONE',  ( 1.000000000000000000, 0.000000000000000000, 0.000000000000000000 ) ) ;
#44003=CARTESIAN_POINT ( 'NONE',  ( 24.87965708725800340, 2.960048322974000001, -11.62351559612999807 ) ) ;
#44016=AXIS2_PLACEMENT_3D ( 'NONE', #63435, #48397, #20450 ) ;
#44020=CARTESIAN_POINT ( 'NONE',  ( 12.46470380486700158, -12.15408297959000095, 3.184072412108000183 ) ) ;
#44027=CARTESIAN_POINT ( 'NONE',  ( 25.29987261391899978, -9.517611874540000017, 8.103398312166998352 ) ) ;
#44040=CARTESIAN_POINT ( 'NONE',  ( 24.35365242081699932, 10.79182034090998776, 4.028979491970003934 ) ) ;
#44041=CARTESIAN_POINT ( 'NONE',  ( 23.59999192078999997, 10.30759737717999869, 9.317725909430999209 ) ) ;
#44042=VERTEX_POINT ( 'NONE', #17702 ) ;
#44043=B_SPLINE_SURFACE_WITH_KNOTS ( 'NONE', 3, 3, ( 
 ( #28317, #22373, #38458, #43370 ),
 ( #65364, #5944, #44413, #43712 ),
 ( #27978, #65006, #59779, #49288 ),
 ( #33220, #43013, #58743, #1399 ),
 ( #27286, #32873, #54186, #59091 ),
 ( #26943, #48254, #54542, #64317 ),
 ( #37422, #44062, #48953, #17484 ),
 ( #23064, #38808, #6284, #48607 ),
 ( #16437, #21677, #60132, #711 ) ),
 .UNSPECIFIED., .F., .F., .F.,
 ( 4, 1, 1, 1, 1, 1, 4 ),
 ( 4, 4 ),
 ( 0.02288375853140000096, 0.1666666666667000196, 0.3333333333333000081, 0.5000000000000000000, 0.6666666666667000474, 0.8333333333333000637, 0.9485331614076999429 ),
 ( -0.1900389547208000129, 1.190219847277000031 ),
 .UNSPECIFIED. ) ;
#44048=CARTESIAN_POINT ( 'NONE',  ( 17.56118420217200082, -11.55273616383000146, 4.939615522132000613 ) ) ;
#44054=EDGE_CURVE ( 'NONE', #47396, #27357, #50798, .T. ) ;
#44058=AXIS2_PLACEMENT_3D ( 'NONE', #43866, #1908, #65171 ) ;
#44062=CARTESIAN_POINT ( 'NONE',  ( 11.74257329013500240, 12.32813410531000109, 1.877195977750000022 ) ) ;
#44063=B_SPLINE_CURVE_WITH_KNOTS ( 'NONE', 3,
 ( #47767, #10689, #31340, #4406 ),
 .UNSPECIFIED., .F., .F.,
 ( 4, 4 ),
 ( 0.000000000000000000, 1.000000000000000000 ),
 .UNSPECIFIED. ) ;
#44073=CARTESIAN_POINT ( 'NONE',  ( 24.56500367226799852, -3.482495402162000264, -12.16326672459999791 ) ) ;
#44089=CARTESIAN_POINT ( 'NONE',  ( 12.48079089729741398, 10.80976533105202542, -4.345114765769909404 ) ) ;
#44090=CARTESIAN_POINT ( 'NONE',  ( 24.76117192814322365, 11.73046401989726029, 3.191744692855882359 ) ) ;
#44098=CARTESIAN_POINT ( 'NONE',  ( 12.79999999914999975, -12.11987927271999865, 3.159802730921999814 ) ) ;
#44104=CARTESIAN_POINT ( 'NONE',  ( 13.24816728597000193, -12.42904273309000018, -1.833878933190999927 ) ) ;
#44111=B_SPLINE_CURVE_WITH_KNOTS ( 'NONE', 3,
 ( #4831, #32796, #38027, #47848 ),
 .UNSPECIFIED., .F., .F.,
 ( 4, 4 ),
 ( 0.000000000000000000, 1.000000000000000000 ),
 .UNSPECIFIED. ) ;
#44113=DIRECTION ( 'NONE',  ( 1.000000000000000000, 0.000000000000000000, 0.000000000000000000 ) ) ;
#44118=EDGE_CURVE ( 'NONE', #68740, #34308, #62490, .T. ) ;
#44121=CARTESIAN_POINT ( 'NONE',  ( 11.53142628873784226, 3.735369189129102097, -11.95516350776760106 ) ) ;
#44122=CARTESIAN_POINT ( 'NONE',  ( 12.80000000000000071, -10.78295181803999903, 4.410266442048000002 ) ) ;
#44124=VERTEX_POINT ( 'NONE', #9247 ) ;
#44132=CARTESIAN_POINT ( 'NONE',  ( 23.80818434440886833, 3.306688368710591241, -13.11409483359108208 ) ) ;
#44134=CARTESIAN_POINT ( 'NONE',  ( 24.30001694391200218, -12.21047201246000036, 3.271805662802000025 ) ) ;
#44157=CARTESIAN_POINT ( 'NONE',  ( 12.78455560662700208, 11.44263450739000021, -4.698119303721000506 ) ) ;
#44161=EDGE_CURVE ( 'NONE', #68087, #63300, #62253, .T. ) ;
#44167=CYLINDRICAL_SURFACE ( 'NONE', #45994, 0.5000000000000004441 ) ;
#44171=DIRECTION ( 'NONE',  ( 1.000000000000000000, 0.000000000000000000, 0.000000000000000000 ) ) ;
#44185=CARTESIAN_POINT ( 'NONE',  ( 11.48828127163000268, 3.524947629324000076, -11.86450458095000116 ) ) ;
#44189=CARTESIAN_POINT ( 'NONE',  ( 11.30000285318000230, -11.76356368987999979, -1.428410073821000159 ) ) ;
#44193=VECTOR ( 'NONE', #22400, 1000.000000000000227 ) ;
#44194=CARTESIAN_POINT ( 'NONE',  ( 11.49999672495000169, 3.632761979779000061, -11.06912554803999882 ) ) ;
#44195=EDGE_CURVE ( 'NONE', #14147, #18158, #44932, .T. ) ;
#44200=CARTESIAN_POINT ( 'NONE',  ( 24.48514019804499853, -8.805442486866001062, 8.922418878371999540 ) ) ;
#44203=CARTESIAN_POINT ( 'NONE',  ( 25.60000000000000142, 8.527654132752997995, -7.260537518969999660 ) ) ;
#44207=CARTESIAN_POINT ( 'NONE',  ( 13.67905361531531838, -11.43958844919984585, -2.204572756906674424 ) ) ;
#44208=CARTESIAN_POINT ( 'NONE',  ( 21.10000109091659937, 0.000000000000000000, 0.000000000000000000 ) ) ;
#44209=CARTESIAN_POINT ( 'NONE',  ( 13.55168611684300117, 12.14221570691000096, 2.415203473206000151 ) ) ;
#44212=CARTESIAN_POINT ( 'NONE',  ( 23.60205915885299888, 9.377218989177011466, 8.305825996807000067 ) ) ;
#44216=CARTESIAN_POINT ( 'NONE',  ( 18.20279897513206180, 3.027817981728711860, 11.45825916391118859 ) ) ;
#44219=CARTESIAN_POINT ( 'NONE',  ( 13.99999999347100044, -9.187456302440001110, -8.213201953411001455 ) ) ;
#44232=EDGE_CURVE ( 'NONE', #37319, #24248, #61166, .T. ) ;
#44237=CARTESIAN_POINT ( 'NONE',  ( 16.07057712374000147, 3.541973289920000045, 11.85942491664999920 ) ) ;
#44238=CARTESIAN_POINT ( 'NONE',  ( 23.56666365135700403, 2.963314674624001999, 12.23574966054999358 ) ) ;
#44244=CARTESIAN_POINT ( 'NONE',  ( 18.14395184984607567, -12.07230981080912890, 3.337076190873973225 ) ) ;
#44247=CARTESIAN_POINT ( 'NONE',  ( 24.56665315110400272, 3.304344730019999954, 12.00442456974999850 ) ) ;
#44248=EDGE_CURVE ( 'NONE', #51109, #46470, #9796, .T. ) ;
#44252=B_SPLINE_CURVE_WITH_KNOTS ( 'NONE', 3,
 ( #40817, #8326, #7286, #2050, #18129, #60770 ),
 .UNSPECIFIED., .F., .F.,
 ( 4, 2, 4 ),
 ( 0.000000000000000000, 0.5000000000000000000, 1.000000000000000000 ),
 .UNSPECIFIED. ) ;
#44263=CARTESIAN_POINT ( 'NONE',  ( 25.30000327618300204, -6.604245036507551141E-15, -11.49994408209238017 ) ) ;
#44281=ADVANCED_FACE ( 'NONE', ( #58186 ), #25419, .F. ) ;
#44282=EDGE_CURVE ( 'NONE', #63154, #17632, #10978, .T. ) ;
#44293=CARTESIAN_POINT ( 'NONE',  ( 23.56664678325900297, -13.31363270032999857, -4.296980171176000063 ) ) ;
#44295=ORIENTED_EDGE ( 'NONE', *, *, #20131, .F. ) ;
#44301=CARTESIAN_POINT ( 'NONE',  ( 24.91842629950604149, -8.566757067395633030, -8.413190967713612523 ) ) ;
#44312=CARTESIAN_POINT ( 'NONE',  ( 24.23232874665299974, -12.46722082417999999, -3.269194826637000340 ) ) ;
#44314=CARTESIAN_POINT ( 'NONE',  ( 15.39284288850700122, -9.264553731144999915, -8.207894312349999666 ) ) ;
#44317=CARTESIAN_POINT ( 'NONE',  ( 16.10004050617000004, -4.849232186851411441, -11.59252887645439678 ) ) ;
#44326=CARTESIAN_POINT ( 'NONE',  ( 11.64585080655600002, -12.33238363550000116, -1.848877788567000024 ) ) ;
#44330=EDGE_CURVE ( 'NONE', #53410, #26903, #32123, .T. ) ;
#44333=LINE ( 'NONE', #38377, #4294 ) ;
#44339=DIRECTION ( 'NONE',  ( 0.000000000000000000, 1.000000000000000000, 0.000000000000000000 ) ) ;
#44347=CARTESIAN_POINT ( 'NONE',  ( 23.61266196672000106, -10.15867583602999957, 9.482229976157999118 ) ) ;
#44348=DIRECTION ( 'NONE',  ( 0.000000000000000000, -0.001239076634196937133, 0.9999992323442525866 ) ) ;
#44353=CARTESIAN_POINT ( 'NONE',  ( 23.63989407724920255, 3.364481845875844090, 13.53838179598365876 ) ) ;
#44370=CARTESIAN_POINT ( 'NONE',  ( 24.72545694048200104, 12.30753067676000079, -2.942917560469000104 ) ) ;
#44373=CARTESIAN_POINT ( 'NONE',  ( 12.20391894010200140, -11.86124369401000145, 3.532130569927999897 ) ) ;
#44377=CARTESIAN_POINT ( 'NONE',  ( 23.61806549638300012, 2.886582507844000389, 13.53859147826000076 ) ) ;
#44380=CARTESIAN_POINT ( 'NONE',  ( 24.83134064321769330, -11.65949623918286093, -3.197451102845753290 ) ) ;
#44386=CARTESIAN_POINT ( 'NONE',  ( 23.52038098767900109, 13.48733383052000079, -4.207157608410000194 ) ) ;
#44393=EDGE_LOOP ( 'NONE', ( #36272, #58232, #49265, #53939 ) ) ;
#44401=CARTESIAN_POINT ( 'NONE',  ( 17.86987531604100354, -11.45991251204999983, 4.658960512821999522 ) ) ;
#44409=ORIENTED_EDGE ( 'NONE', *, *, #47998, .T. ) ;
#44413=CARTESIAN_POINT ( 'NONE',  ( 11.35194613850999978, 12.28618680900000015, 1.513058913260000082 ) ) ;
#44414=CARTESIAN_POINT ( 'NONE',  ( 23.83662517011200066, -3.384089299514999816, 13.10251501914999928 ) ) ;
#44420=LINE ( 'NONE', #49996, #20173 ) ;
#44422=ORIENTED_EDGE ( 'NONE', *, *, #33393, .T. ) ;
#44425=DIRECTION ( 'NONE',  ( 1.000000000000000000, 0.000000000000000000, 0.000000000000000000 ) ) ;
#44428=ORIENTED_EDGE ( 'NONE', *, *, #31509, .F. ) ;
#44434=CARTESIAN_POINT ( 'NONE',  ( 25.20466183898900070, 8.548377718155000693, 7.995577011338999007 ) ) ;
#44439=CARTESIAN_POINT ( 'NONE',  ( 12.17041751256825144, 10.92137764454934690, -4.055351144145800113 ) ) ;
#44464=ORIENTED_EDGE ( 'NONE', *, *, #48297, .T. ) ;
#44475=EDGE_CURVE ( 'NONE', #10719, #33864, #42153, .T. ) ;
#44478=ORIENTED_EDGE ( 'NONE', *, *, #35907, .F. ) ;
#44489=CARTESIAN_POINT ( 'NONE',  ( 11.80756411264299999, 3.251511910489000012, -11.33753290789000090 ) ) ;
#44493=EDGE_LOOP ( 'NONE', ( #25223, #57331, #23474, #19579 ) ) ;
#44502=ORIENTED_EDGE ( 'NONE', *, *, #30476, .T. ) ;
#44509=AXIS2_PLACEMENT_3D ( 'NONE', #67286, #15188, #36512 ) ;
#44526=VECTOR ( 'NONE', #51951, 1000.000000000000114 ) ;
#44532=CARTESIAN_POINT ( 'NONE',  ( 17.60000001072100062, -11.41073498373000028, 4.623967591968000335 ) ) ;
#44535=CARTESIAN_POINT ( 'NONE',  ( 11.80707028823900195, 3.411567914393000223, -11.89801974982000132 ) ) ;
#44538=EDGE_CURVE ( 'NONE', #20915, #37115, #61631, .T. ) ;
#44552=CARTESIAN_POINT ( 'NONE',  ( 23.56665657345700282, -13.31365812469000076, 4.296923216748999685 ) ) ;
#44556=CARTESIAN_POINT ( 'NONE',  ( 14.02348875342600110, -8.812421938351000961, -7.562304860556999131 ) ) ;
#44566=PLANE ( 'NONE',  #35082 ) ;
#44567=CARTESIAN_POINT ( 'NONE',  ( 24.92851483856576777, 8.562961969008355823, -8.403401768322540377 ) ) ;
#44573=ORIENTED_EDGE ( 'NONE', *, *, #41824, .T. ) ;
#44577=ORIENTED_EDGE ( 'NONE', *, *, #955, .F. ) ;
#44584=CARTESIAN_POINT ( 'NONE',  ( 11.60581233665799950, -11.65209074823999913, -1.826497490784000144 ) ) ;
#44596=CARTESIAN_POINT ( 'NONE',  ( 25.31135185429100076, -2.728831955372000184, 11.35931141337999861 ) ) ;
#44597=EDGE_CURVE ( 'NONE', #52918, #55782, #36438, .T. ) ;
#44610=CYLINDRICAL_SURFACE ( 'NONE', #22966, 0.6999999999999992895 ) ;
#44614=B_SPLINE_SURFACE_WITH_KNOTS ( 'NONE', 3, 3, ( 
 ( #32373, #47071, #47763, #27124 ),
 ( #548, #31680, #9649, #41817 ),
 ( #63124, #57899, #36573, #53001 ),
 ( #28153, #59959, #18015, #22896 ),
 ( #1578, #54367, #11712, #34094 ),
 ( #49467, #65887, #33750, #2272 ),
 ( #23590, #44247, #28506, #55414 ),
 ( #1931, #43544, #44933, #6818 ) ),
 .UNSPECIFIED., .F., .F., .F.,
 ( 4, 1, 1, 1, 1, 4 ),
 ( 4, 4 ),
 ( 0.7453233389708999734, 0.7647058823529000460, 0.8235294117646999590, 0.8823529411764999830, 0.9411764705882000870, 0.9905821372920999845 ),
 ( -0.1830924183985000175, 1.182948959795000032 ),
 .UNSPECIFIED. ) ;
#44617=ORIENTED_EDGE ( 'NONE', *, *, #24919, .T. ) ;
#44618=CARTESIAN_POINT ( 'NONE',  ( 23.60000000000000142, 0.000000000000000000, 0.000000000000000000 ) ) ;
#44621=( BOUNDED_SURFACE ( )  B_SPLINE_SURFACE ( 3, 3, ( 
 ( #39668, #60643, #44238, #34437 ),
 ( #60299, #2940, #50160, #1565 ),
 ( #12755, #40019, #44920, #22887 ),
 ( #1920, #61334, #38628, #59949 ) ),
 .UNSPECIFIED., .F., .F., .T. ) 
 B_SPLINE_SURFACE_WITH_KNOTS ( ( 4, 4 ),
 ( 4, 4 ),
 ( 0.000000000000000000, 1.000000000000000000 ),
 ( 0.000000000000000000, 1.000000000000000000 ),
 .UNSPECIFIED. ) 
 GEOMETRIC_REPRESENTATION_ITEM ( )  RATIONAL_B_SPLINE_SURFACE ( (
 ( 1.512182578520000042, 1.160176301760999840, 1.160176301760999840, 1.512182578520000042),
 ( 1.111288591041000196, 0.8526025270081000196, 0.8526025270081000196, 1.111288591041000196),
 ( 1.111288591041000196, 0.8526025270081000196, 0.8526025270081000196, 1.111288591041000196),
 ( 1.512182578520000042, 1.160176301760999840, 1.160176301760999840, 1.512182578520000042) ) ) 
 REPRESENTATION_ITEM ( '' )  SURFACE ( )  );
#44622=EDGE_CURVE ( 'NONE', #13468, #59568, #48653, .T. ) ;
#44623=FACE_OUTER_BOUND ( 'NONE', #58726, .T. ) ;
#44626=B_SPLINE_SURFACE_WITH_KNOTS ( 'NONE', 3, 3, ( 
 ( #54806, #37692, #21604, #53773 ),
 ( #6906, #38029, #22638, #33838 ),
 ( #64248, #5870, #27208, #48531 ),
 ( #59357, #9566, #41732, #57119 ),
 ( #67600, #25654, #56793, #68287 ),
 ( #46986, #46645, #40701, #62702 ),
 ( #50255, #12855, #63037, #28952 ),
 ( #62028, #14823, #20407, #15164 ),
 ( #51534, #46301, #52219, #30906 ),
 ( #4319, #67952, #20068, #41395 ) ),
 .UNSPECIFIED., .F., .F., .F.,
 ( 4, 1, 1, 1, 1, 1, 1, 4 ),
 ( 4, 4 ),
 ( 0.04183311431308000400, 0.1428571428570999946, 0.2857142857143000203, 0.4285714285713999594, 0.5714285714286000406, 0.7142857142856999797, 0.8571428571429000609, 0.9292981235707000742 ),
 ( -0.1917799910644999994, 1.191756862851000021 ),
 .UNSPECIFIED. ) ;
#44632=CARTESIAN_POINT ( 'NONE',  ( 12.80000000000000071, 50.14170351282000127, -17.06962823869000090 ) ) ;
#44641=CARTESIAN_POINT ( 'NONE',  ( 12.79999998712400178, -11.53033693765999779, 4.891431908114999949 ) ) ;
#44645=CARTESIAN_POINT ( 'NONE',  ( 24.34833280985366954, 12.15210571723978461, -3.256146913270965282 ) ) ;
#44649=B_SPLINE_CURVE_WITH_KNOTS ( 'NONE', 3,
 ( #68137, #62891, #20948, #53103 ),
 .UNSPECIFIED., .F., .F.,
 ( 4, 4 ),
 ( 0.000000000000000000, 1.000000000000000000 ),
 .UNSPECIFIED. ) ;
#44650=B_SPLINE_CURVE_WITH_KNOTS ( 'NONE', 3,
 ( #56817, #8916, #62727, #57482, #67628, #19752 ),
 .UNSPECIFIED., .F., .F.,
 ( 4, 2, 4 ),
 ( 0.000000000000000000, 0.5000000000000000000, 1.000000000000000000 ),
 .UNSPECIFIED. ) ;
#44653=DIRECTION ( 'NONE',  ( -1.000000000000000000, 0.000000000000000000, 0.000000000000000000 ) ) ;
#44655=ORIENTED_EDGE ( 'NONE', *, *, #21131, .F. ) ;
#44657=CARTESIAN_POINT ( 'NONE',  ( 23.58549534400300018, -13.39460428332999875, -4.038169368742999588 ) ) ;
#44660=ORIENTED_EDGE ( 'NONE', *, *, #38220, .T. ) ;
#44661=CARTESIAN_POINT ( 'NONE',  ( 25.39409943791158142, 11.19591960080123805, 3.259891097492937817 ) ) ;
#44668=VERTEX_POINT ( 'NONE', #52865 ) ;
#44670=VERTEX_POINT ( 'NONE', #43059 ) ;
#44678=EDGE_CURVE ( 'NONE', #18715, #23593, #409, .T. ) ;
#44679=CARTESIAN_POINT ( 'NONE',  ( 23.56665676678700194, 0.01733454660186801305, -13.98987989644267671 ) ) ;
#44683=EDGE_CURVE ( 'NONE', #67010, #19021, #34311, .T. ) ;
#44686=CARTESIAN_POINT ( 'NONE',  ( 25.30000327618300204, -8.756202924575998026, -7.455126447192999883 ) ) ;
#44687=DIRECTION ( 'NONE',  ( -0.9999999999995587974, 4.522743910255808775E-07, 8.233165790437657900E-07 ) ) ;
#44690=CARTESIAN_POINT ( 'NONE',  ( 24.30001683613300045, -12.21047198529999989, -3.271805531187999883 ) ) ;
#44692=CARTESIAN_POINT ( 'NONE',  ( 23.58437014357399875, -10.35669085107999976, 9.329830741018000140 ) ) ;
#44700=B_SPLINE_CURVE_WITH_KNOTS ( 'NONE', 3,
 ( #10624, #20432, #67976, #52939 ),
 .UNSPECIFIED., .F., .F.,
 ( 4, 4 ),
 ( 0.000000000000000000, 1.000000000000000000 ),
 .UNSPECIFIED. ) ;
#44701=EDGE_LOOP ( 'NONE', ( #12238, #68037, #49953, #4895, #50305 ) ) ;
#44702=CARTESIAN_POINT ( 'NONE',  ( 24.67559728077000258, 3.457949410299000270, -12.04093993320999978 ) ) ;
#44728=ADVANCED_FACE ( 'NONE', ( #17533 ), #12989, .T. ) ;
#44738=FACE_OUTER_BOUND ( 'NONE', #14275, .T. ) ;
#44742=CARTESIAN_POINT ( 'NONE',  ( 23.89320776801300283, 1.894218448783000941, -11.32736289219000270 ) ) ;
#44761=EDGE_CURVE ( 'NONE', #51740, #58690, #14949, .T. ) ;
#44764=ORIENTED_EDGE ( 'NONE', *, *, #24948, .F. ) ;
#44768=AXIS2_PLACEMENT_3D ( 'NONE', #1102, #60180, #23109 ) ;
#44779=DIRECTION ( 'NONE',  ( 0.000000000000000000, -0.9835354258236025382, -0.1807154286440004198 ) ) ;
#44784=ORIENTED_EDGE ( 'NONE', *, *, #44118, .T. ) ;
#44786=CARTESIAN_POINT ( 'NONE',  ( 23.61437290050061577, -10.18035114601963897, -9.423216756301032504 ) ) ;
#44790=CARTESIAN_POINT ( 'NONE',  ( 15.86547101025934126, 8.701845401024112192, 7.746061882573283874 ) ) ;
#44795=CARTESIAN_POINT ( 'NONE',  ( 21.70000133425200062, 3.970157536060000036E-13, -13.99999976176021299 ) ) ;
#44802=AXIS2_PLACEMENT_3D ( 'NONE', #51696, #56606, #7683 ) ;
#44811=CARTESIAN_POINT ( 'NONE',  ( 12.22262912555220993, -10.88886164594843109, 4.142707164971341172 ) ) ;
#44813=ORIENTED_EDGE ( 'NONE', *, *, #41188, .F. ) ;
#44818=ORIENTED_EDGE ( 'NONE', *, *, #34689, .T. ) ;
#44821=CARTESIAN_POINT ( 'NONE',  ( 24.52306328733310892, -3.339076862689864811, -12.06942450666826616 ) ) ;
#44826=CARTESIAN_POINT ( 'NONE',  ( 25.60000000000000142, 9.517611874540000017, 8.103398312166998352 ) ) ;
#44827=CARTESIAN_POINT ( 'NONE',  ( 11.48394322905000031, 3.487217528443000258, -11.17162453992000160 ) ) ;
#44830=DIRECTION ( 'NONE',  ( 0.000000000000000000, -0.9421243786071880066, -0.3352635608502960163 ) ) ;
#44847=CARTESIAN_POINT ( 'NONE',  ( 23.73387382971900195, -3.552757729846999890, -13.41925964844999974 ) ) ;
#44848=CARTESIAN_POINT ( 'NONE',  ( 16.09992084546400193, 8.991497430826001391, 8.719551690569000257 ) ) ;
#44854=CARTESIAN_POINT ( 'NONE',  ( 24.14469707708988011, 3.678927588120181280, 12.80140320797930187 ) ) ;
#44862=CARTESIAN_POINT ( 'NONE',  ( 15.91386961183700244, -8.663061527162000175, -7.870519177131000355 ) ) ;
#44864=CARTESIAN_POINT ( 'NONE',  ( 23.57687597998769036, -13.36283493320904547, 4.129073899263432601 ) ) ;
#44877=CARTESIAN_POINT ( 'NONE',  ( 23.50387503050299998, 0.000000000000000000, 0.000000000000000000 ) ) ;
#44889=LINE ( 'NONE', #18315, #55560 ) ;
#44890=CARTESIAN_POINT ( 'NONE',  ( 24.98633618363800224, -8.514521811727000511, -8.479283273084000427 ) ) ;
#44892=DIRECTION ( 'NONE',  ( 1.000000000000000000, 0.000000000000000000, 0.000000000000000000 ) ) ;
#44893=CARTESIAN_POINT ( 'NONE',  ( 13.64718133169100156, 12.21462133634999958, 2.516296819814999974 ) ) ;
#44896=CARTESIAN_POINT ( 'NONE',  ( 23.56666365135700403, 9.114812703021994977, 8.684180617873007435 ) ) ;
#44899=CARTESIAN_POINT ( 'NONE',  ( 25.37957587859375508, -8.342525504610193821, -8.311485206920414370 ) ) ;
#44905=B_SPLINE_CURVE_WITH_KNOTS ( 'NONE', 3,
 ( #4200, #41276, #30114, #36369 ),
 .UNSPECIFIED., .F., .F.,
 ( 4, 4 ),
 ( 0.000000000000000000, 1.000000000000000000 ),
 .UNSPECIFIED. ) ;
#44907=VERTEX_POINT ( 'NONE', #39037 ) ;
#44920=CARTESIAN_POINT ( 'NONE',  ( 23.56666365135700403, 2.488348886737001386, 11.45224114470000565 ) ) ;
#44932=B_SPLINE_CURVE_WITH_KNOTS ( 'NONE', 3,
 ( #56819, #30256, #57151, #30936, #47013, #52252 ),
 .UNSPECIFIED., .F., .F.,
 ( 4, 2, 4 ),
 ( 0.000000000000000000, 0.5000000000000000000, 1.000000000000000000 ),
 .UNSPECIFIED. ) ;
#44933=CARTESIAN_POINT ( 'NONE',  ( 24.59180944708200300, 3.481108335742999937, 12.13646551132999996 ) ) ;
#44937=VERTEX_POINT ( 'NONE', #44293 ) ;
#44943=EDGE_CURVE ( 'NONE', #61230, #25637, #31544, .T. ) ;
#44944=CARTESIAN_POINT ( 'NONE',  ( 19.39373726536100051, -11.26964301940000013, -9.703002290528998444E-14 ) ) ;
#44955=EDGE_LOOP ( 'NONE', ( #63648, #15516, #11086, #21645, #9018 ) ) ;
#44956=DIRECTION ( 'NONE',  ( 0.000000000000000000, 0.000000000000000000, -1.000000000000000000 ) ) ;
#44980=CARTESIAN_POINT ( 'NONE',  ( 24.87152730243871446, -8.583156850595695886, -8.460088049133823063 ) ) ;
#44990=ORIENTED_EDGE ( 'NONE', *, *, #63113, .F. ) ;
#44995=ORIENTED_EDGE ( 'NONE', *, *, #13444, .T. ) ;
#44999=CARTESIAN_POINT ( 'NONE',  ( 25.29986325275000070, 2.078227429405999693, 11.31065739696999906 ) ) ;
#45004=ADVANCED_FACE ( 'NONE', ( #20796 ), #11055, .F. ) ;
#45007=ORIENTED_EDGE ( 'NONE', *, *, #32740, .T. ) ;
#45008=CIRCLE ( 'NONE', #8169, 0.5000000000000004441 ) ;
#45009=FACE_OUTER_BOUND ( 'NONE', #17183, .T. ) ;
#45025=CARTESIAN_POINT ( 'NONE',  ( 24.85114900759599976, -11.95312945982000130, 2.993324385169999768 ) ) ;
#45028=CARTESIAN_POINT ( 'NONE',  ( 24.60320129348500018, 3.644628662557000354, 12.27776523668999786 ) ) ;
#45040=CARTESIAN_POINT ( 'NONE',  ( 18.90826270587400160, 0.000000000000000000, 0.000000000000000000 ) ) ;
#45050=CARTESIAN_POINT ( 'NONE',  ( 11.83124374198900064, -3.528976724670999765, 11.96046730081999954 ) ) ;
#45073=ORIENTED_EDGE ( 'NONE', *, *, #46900, .T. ) ;
#45082=CARTESIAN_POINT ( 'NONE',  ( 23.60205915885299888, 2.504446818059999469, -12.27382285987999211 ) ) ;
#45093=CARTESIAN_POINT ( 'NONE',  ( 12.10000669845703847, -11.02846243759423039, 3.754394857303111621 ) ) ;
#45095=EDGE_CURVE ( 'NONE', #21396, #59370, #57805, .T. ) ;
#45098=CARTESIAN_POINT ( 'NONE',  ( 18.26281727343199890, 2.856883730594999893, -11.95041273044000008 ) ) ;
#45102=ORIENTED_EDGE ( 'NONE', *, *, #35996, .F. ) ;
#45116=CARTESIAN_POINT ( 'NONE',  ( 25.47132167539000136, 8.417332019620999972, 7.979435755108000627 ) ) ;
#45123=ORIENTED_EDGE ( 'NONE', *, *, #48052, .F. ) ;
#45128=CARTESIAN_POINT ( 'NONE',  ( 24.25374608244400321, -12.19813778996000053, 3.308085337617999944 ) ) ;
#45132=CARTESIAN_POINT ( 'NONE',  ( 13.37677363193000168, -12.31133347089000019, -1.988942882797000156 ) ) ;
#45140=ORIENTED_EDGE ( 'NONE', *, *, #3629, .T. ) ;
#45142=CARTESIAN_POINT ( 'NONE',  ( 11.79999999684100054, -12.15995044155999949, -2.000340912084999978 ) ) ;
#45145=EDGE_CURVE ( 'NONE', #52892, #49685, #9866, .T. ) ;
#45147=DIRECTION ( 'NONE',  ( 0.000000000000000000, -0.3352635608502960163, -0.9421243786071880066 ) ) ;
#45150=EDGE_CURVE ( 'NONE', #68281, #68269, #33971, .T. ) ;
#45167=CARTESIAN_POINT ( 'NONE',  ( 16.26901036074197648, -3.345264657739864589, -11.86070554647184316 ) ) ;
#45173=ORIENTED_EDGE ( 'NONE', *, *, #41512, .T. ) ;
#45174=ADVANCED_FACE ( 'NONE', ( #64456 ), #7555, .F. ) ;
#45182=VERTEX_POINT ( 'NONE', #11327 ) ;
#45190=B_SPLINE_CURVE_WITH_KNOTS ( 'NONE', 3,
 ( #31355, #21881, #37965, #5115 ),
 .UNSPECIFIED., .F., .F.,
 ( 4, 4 ),
 ( 0.000000000000000000, 1.000000000000000000 ),
 .UNSPECIFIED. ) ;
#45197=EDGE_CURVE ( 'NONE', #60567, #10372, #39964, .T. ) ;
#45201=FACE_OUTER_BOUND ( 'NONE', #61247, .T. ) ;
#45208=CARTESIAN_POINT ( 'NONE',  ( 23.61450813208451649, -13.39969347648717068, 3.938932084374531684 ) ) ;
#45211=AXIS2_PLACEMENT_3D ( 'NONE', #58552, #11009, #21834 ) ;
#45218=AXIS2_PLACEMENT_3D ( 'NONE', #47561, #9795, #20290 ) ;
#45223=DIRECTION ( 'NONE',  ( -1.000000000000000000, 0.000000000000000000, 0.000000000000000000 ) ) ;
#45227=FACE_OUTER_BOUND ( 'NONE', #57850, .T. ) ;
#45230=ADVANCED_FACE ( 'NONE', ( #32668 ), #23179, .F. ) ;
#45233=CARTESIAN_POINT ( 'NONE',  ( 25.60000000000000142, -11.77655473258999841, -4.190794510628000680 ) ) ;
#45246=CARTESIAN_POINT ( 'NONE',  ( 24.09354147538195434, -12.55951106403002093, 3.397315377048726770 ) ) ;
#45255=EDGE_CURVE ( 'NONE', #33910, #21413, #47338, .T. ) ;
#45263=CARTESIAN_POINT ( 'NONE',  ( 25.29987931604000195, 11.13052921044000065, -3.427478701325000099 ) ) ;
#45264=CARTESIAN_POINT ( 'NONE',  ( 11.56631965465000178, -11.51200727500000021, -1.523108403756999962 ) ) ;
#45270=CARTESIAN_POINT ( 'NONE',  ( 24.30000000000000071, 8.810505093353000916, -8.810505093353000916 ) ) ;
#45273=CARTESIAN_POINT ( 'NONE',  ( 17.79999999998900151, -3.595165934733000057, -11.99793354950999991 ) ) ;
#45277=ORIENTED_EDGE ( 'NONE', *, *, #69169, .T. ) ;
#45285=CARTESIAN_POINT ( 'NONE',  ( 24.02092319654100194, 9.294262032018000497, -9.129398518842998911 ) ) ;
#45298=CARTESIAN_POINT ( 'NONE',  ( 24.44496482743900145, 12.03536723905999928, -3.224852005146999989 ) ) ;
#45300=B_SPLINE_CURVE_WITH_KNOTS ( 'NONE', 3,
 ( #43862, #21833, #33376, #18936, #45167, #1211 ),
 .UNSPECIFIED., .F., .F.,
 ( 4, 2, 4 ),
 ( 0.000000000000000000, 0.5000000000000000000, 1.000000000000000000 ),
 .UNSPECIFIED. ) ;
#45312=CARTESIAN_POINT ( 'NONE',  ( 24.51228084553499897, 3.325039717427999975, -12.06631758408999922 ) ) ;
#45318=CARTESIAN_POINT ( 'NONE',  ( 24.30000000000000071, 9.517611874540000017, 8.103398312166000039 ) ) ;
#45319=CARTESIAN_POINT ( 'NONE',  ( 24.62769666408257052, -8.773247285887615377, 9.203857927720639154 ) ) ;
#45322=EDGE_LOOP ( 'NONE', ( #13048, #43067, #61586, #41284, #38177 ) ) ;
#45329=CARTESIAN_POINT ( 'NONE',  ( 18.30017264560541079, 0.9191760165933146043, 11.85014035445314740 ) ) ;
#45332=CARTESIAN_POINT ( 'NONE',  ( 25.39940350028005156, 8.416042725244727407, 8.072285808956092268 ) ) ;
#45335=CARTESIAN_POINT ( 'NONE',  ( 23.86947894555299854, -13.28527095192000118, -3.447687139233999609 ) ) ;
#45337=ADVANCED_FACE ( 'NONE', ( #33363 ), #10894, .T. ) ;
#45341=FACE_OUTER_BOUND ( 'NONE', #45322, .T. ) ;
#45345=CARTESIAN_POINT ( 'NONE',  ( 23.81728226941260118, -3.309408472638277310, -13.09637078731351778 ) ) ;
#45352=DIRECTION ( 'NONE',  ( 0.000000000000000000, -1.000000000000000000, 0.000000000000000000 ) ) ;
#45357=AXIS2_PLACEMENT_3D ( 'NONE', #64915, #6191, #33473 ) ;
#45358=CARTESIAN_POINT ( 'NONE',  ( 17.79999999998900151, 3.595165934733000057, -11.99793354950999991 ) ) ;
#45363=CARTESIAN_POINT ( 'NONE',  ( 25.29986734212600297, -2.596989636639000398, 11.35306351421000137 ) ) ;
#45368=CARTESIAN_POINT ( 'NONE',  ( 25.59997774154300032, -2.856411620672000051, -11.13959722905999961 ) ) ;
#45371=B_SPLINE_CURVE_WITH_KNOTS ( 'NONE', 3,
 ( #59206, #37886, #33688, #831 ),
 .UNSPECIFIED., .F., .F.,
 ( 4, 4 ),
 ( 0.000000000000000000, 1.000000000000000000 ),
 .UNSPECIFIED. ) ;
#45373=CARTESIAN_POINT ( 'NONE',  ( 24.56500367226799852, 3.482495402162000264, 12.16326672459999791 ) ) ;
#45375=FACE_OUTER_BOUND ( 'NONE', #68712, .T. ) ;
#45376=VERTEX_POINT ( 'NONE', #37788 ) ;
#45386=VERTEX_POINT ( 'NONE', #59452 ) ;
#45392=EDGE_LOOP ( 'NONE', ( #59683, #29221, #38291, #6755 ) ) ;
#45402=ORIENTED_EDGE ( 'NONE', *, *, #49303, .T. ) ;
#45405=B_SPLINE_CURVE_WITH_KNOTS ( 'NONE', 3,
 ( #60788, #66717, #12902, #45746 ),
 .UNSPECIFIED., .F., .F.,
 ( 4, 4 ),
 ( 0.000000000000000000, 1.000000000000000000 ),
 .UNSPECIFIED. ) ;
#45409=ORIENTED_EDGE ( 'NONE', *, *, #65365, .F. ) ;
#45417=EDGE_LOOP ( 'NONE', ( #53192, #5351, #17561, #22104 ) ) ;
#45420=PLANE ( 'NONE',  #60323 ) ;
#45421=ORIENTED_EDGE ( 'NONE', *, *, #12672, .F. ) ;
#45427=CARTESIAN_POINT ( 'NONE',  ( 17.70961302874500021, -11.81369488050999905, 3.327702596852999850 ) ) ;
#45428=CARTESIAN_POINT ( 'NONE',  ( 24.51327040722500072, -8.786342692851000891, 8.911852834696000869 ) ) ;
#45435=CARTESIAN_POINT ( 'NONE',  ( 12.17041389150293185, -11.12724490998814453, 3.450620877153329324 ) ) ;
#45441=CARTESIAN_POINT ( 'NONE',  ( 17.85449583315300259, 3.297641659324999974, -11.83458394846000061 ) ) ;
#45445=EDGE_LOOP ( 'NONE', ( #12966, #34410, #13270, #28670 ) ) ;
#45458=ORIENTED_EDGE ( 'NONE', *, *, #53039, .T. ) ;
#45462=CARTESIAN_POINT ( 'NONE',  ( 25.29987667925500361, 10.83443035398000021, 3.855530949778000149 ) ) ;
#45466=ORIENTED_EDGE ( 'NONE', *, *, #48217, .F. ) ;
#45478=B_SPLINE_CURVE_WITH_KNOTS ( 'NONE', 3,
 ( #54078, #10394, #36978, #26834 ),
 .UNSPECIFIED., .F., .F.,
 ( 4, 4 ),
 ( 0.000000000000000000, 1.000000000000000000 ),
 .UNSPECIFIED. ) ;
#45479=EDGE_CURVE ( 'NONE', #23870, #56039, #10545, .T. ) ;
#45491=B_SPLINE_CURVE_WITH_KNOTS ( 'NONE', 3,
 ( #3951, #19706, #45597, #40679 ),
 .UNSPECIFIED., .F., .F.,
 ( 4, 4 ),
 ( 0.000000000000000000, 1.000000000000000000 ),
 .UNSPECIFIED. ) ;
#45496=CARTESIAN_POINT ( 'NONE',  ( 25.44993977744900349, -9.517611874540000017, -8.103398312166000039 ) ) ;
#45505=CARTESIAN_POINT ( 'NONE',  ( 25.09890362839945510, -2.850910023355439638, -11.48729055544455413 ) ) ;
#45508=DIRECTION ( 'NONE',  ( 1.000000000000000000, 0.000000000000000000, 0.000000000000000000 ) ) ;
#45511=CARTESIAN_POINT ( 'NONE',  ( 18.36682228790370530, 2.717338739979867412, -11.46589211741044778 ) ) ;
#45513=B_SPLINE_CURVE_WITH_KNOTS ( 'NONE', 3,
 ( #23091, #22399, #60161, #66080 ),
 .UNSPECIFIED., .F., .F.,
 ( 4, 4 ),
 ( 0.000000000000000000, 1.000000000000000000 ),
 .UNSPECIFIED. ) ;
#45515=AXIS2_PLACEMENT_3D ( 'NONE', #29272, #13536, #1306 ) ;
#45516=CARTESIAN_POINT ( 'NONE',  ( 25.46373185538400463, 11.23406899464000119, 3.161078463958999496 ) ) ;
#45532=LINE ( 'NONE', #56361, #66676 ) ;
#45533=CARTESIAN_POINT ( 'NONE',  ( 18.43317799840264115, 2.892723637958514171, 12.11800683821377156 ) ) ;
#45534=CARTESIAN_POINT ( 'NONE',  ( 23.86791715242600276, -3.655973686719000249, -13.23133700220999920 ) ) ;
#45542=CARTESIAN_POINT ( 'NONE',  ( 18.50013789939208664, 2.065999734462983189E-14, -11.64999999999999325 ) ) ;
#45546=EDGE_CURVE ( 'NONE', #2158, #65247, #51419, .T. ) ;
#45548=CARTESIAN_POINT ( 'NONE',  ( 23.50387503050299998, -0.02080343500003916865, 13.99998454345904442 ) ) ;
#45551=CARTESIAN_POINT ( 'NONE',  ( 15.95192027319500205, -8.515023616297000331, -8.165096030563999463 ) ) ;
#45553=CARTESIAN_POINT ( 'NONE',  ( 30.60000000000000142, 0.000000000000000000, 0.000000000000000000 ) ) ;
#45559=CARTESIAN_POINT ( 'NONE',  ( 17.60000004896734893, -11.45068297995442386, 4.713086259421401358 ) ) ;
#45566=CARTESIAN_POINT ( 'NONE',  ( 24.53429014662800256, -8.855930250654999725, 9.286429702500999639 ) ) ;
#45573=CARTESIAN_POINT ( 'NONE',  ( 25.41677650706899882, 11.20716069352000055, 3.225949357593000055 ) ) ;
#45577=CARTESIAN_POINT ( 'NONE',  ( 44.24148000000000280, -11.77655473258999841, -4.190794510628000680 ) ) ;
#45582=ORIENTED_EDGE ( 'NONE', *, *, #27470, .T. ) ;
#45590=CARTESIAN_POINT ( 'NONE',  ( 24.07543054079696532, -12.58937790781994792, 3.411500176492500369 ) ) ;
#45593=ADVANCED_FACE ( 'NONE', ( #43670 ), #54625, .F. ) ;
#45594=CIRCLE ( 'NONE', #43340, 11.50000000000000533 ) ;
#45597=CARTESIAN_POINT ( 'NONE',  ( 25.49995753756342864, 8.603837101912144902, -7.325400450398672270 ) ) ;
#45607=AXIS2_PLACEMENT_3D ( 'NONE', #38334, #48833, #6864 ) ;
#45611=CARTESIAN_POINT ( 'NONE',  ( 24.62620337095130907, -3.584633747652771429, 12.20158770660386161 ) ) ;
#45612=B_SPLINE_CURVE_WITH_KNOTS ( 'NONE', 3,
 ( #68674, #15884, #36527, #42122 ),
 .UNSPECIFIED., .F., .F.,
 ( 4, 4 ),
 ( 0.4999999998439638160, 1.000000000000000000 ),
 .UNSPECIFIED. ) ;
#45628=CARTESIAN_POINT ( 'NONE',  ( 24.30001683570900184, 3.271769286791000209, 12.21048169671000139 ) ) ;
#45629=CARTESIAN_POINT ( 'NONE',  ( 23.64132359913000059, 10.11790787233000088, -9.385294766974999092 ) ) ;
#45630=CARTESIAN_POINT ( 'NONE',  ( 18.31802873821099809, -2.927761598026000112, -11.42873208727000112 ) ) ;
#45637=CARTESIAN_POINT ( 'NONE',  ( 23.89320776801300283, -10.75689324692999804, -4.023240149044999825 ) ) ;
#45646=CARTESIAN_POINT ( 'NONE',  ( 25.46372779695100164, -11.23407511953000082, -3.161075425950000017 ) ) ;
#45656=ORIENTED_EDGE ( 'NONE', *, *, #59342, .T. ) ;
#45660=AXIS2_PLACEMENT_3D ( 'NONE', #68447, #63202, #36306 ) ;
#45663=ORIENTED_EDGE ( 'NONE', *, *, #12563, .F. ) ;
#45669=ORIENTED_EDGE ( 'NONE', *, *, #24919, .F. ) ;
#45673=ADVANCED_FACE ( 'NONE', ( #38065, #59390 ), #22673, .F. ) ;
#45688=AXIS2_PLACEMENT_3D ( 'NONE', #3975, #34791, #18705 ) ;
#45691=ORIENTED_EDGE ( 'NONE', *, *, #25332, .T. ) ;
#45705=CARTESIAN_POINT ( 'NONE',  ( 15.40000000001299973, 8.815237407733999220, 7.616696375847999967 ) ) ;
#45708=CARTESIAN_POINT ( 'NONE',  ( 23.59999176271200128, 13.22318677037999812, 4.267778497637999102 ) ) ;
#45734=FACE_OUTER_BOUND ( 'NONE', #57273, .T. ) ;
#45736=CARTESIAN_POINT ( 'NONE',  ( 11.71260115691700143, -3.298410940261000235, 11.83433202606999934 ) ) ;
#45744=DIRECTION ( 'NONE',  ( -1.000000000000000000, 0.000000000000000000, 0.000000000000000000 ) ) ;
#45746=CARTESIAN_POINT ( 'NONE',  ( 18.29995268966800026, -2.861739928647000220, -11.98821236628000086 ) ) ;
#45760=ORIENTED_EDGE ( 'NONE', *, *, #35769, .T. ) ;
#45766=CARTESIAN_POINT ( 'NONE',  ( 17.56043577778200060, -12.16710011284000181, 3.134847618462999641 ) ) ;
#45775=CARTESIAN_POINT ( 'NONE',  ( 12.65360965127988813, -11.23193385081858331, 3.094113056522455718 ) ) ;
#45777=CARTESIAN_POINT ( 'NONE',  ( 23.91260411953700071, -3.265466992718999872, 12.84004109222999901 ) ) ;
#45784=ORIENTED_EDGE ( 'NONE', *, *, #69045, .F. ) ;
#45796=CARTESIAN_POINT ( 'NONE',  ( 25.36465253276900000, 8.490056772567001531, 7.944948624166999984 ) ) ;
#45799=CARTESIAN_POINT ( 'NONE',  ( 25.30000327618300204, 8.756202924575998026, 7.455126447192999883 ) ) ;
#45802=AXIS2_PLACEMENT_3D ( 'NONE', #21404, #42400, #53226 ) ;
#45809=CARTESIAN_POINT ( 'NONE',  ( 11.56599877858000092, 3.774257655232999831, -11.98333518513999962 ) ) ;
#45814=CARTESIAN_POINT ( 'NONE',  ( 21.10000109091659937, 12.52500000000000036, 0.000000000000000000 ) ) ;
#45822=ORIENTED_EDGE ( 'NONE', *, *, #36724, .T. ) ;
#45823=DIRECTION ( 'NONE',  ( 1.000000000000000000, 0.000000000000000000, 0.000000000000000000 ) ) ;
#45825=DIRECTION ( 'NONE',  ( 0.000000000000000000, -0.9421243786071872295, 0.3352635608502975151 ) ) ;
#45828=FACE_OUTER_BOUND ( 'NONE', #38369, .T. ) ;
#45834=ORIENTED_EDGE ( 'NONE', *, *, #28946, .F. ) ;
#45840=CARTESIAN_POINT ( 'NONE',  ( 24.60115016800667220, -3.453285475674932048, -12.10347685339371893 ) ) ;
#45842=DIRECTION ( 'NONE',  ( 0.000000000000000000, -0.2098318009950989882, 0.9777374981512947372 ) ) ;
#45846=ADVANCED_FACE ( 'NONE', ( #7988 ), #17806, .F. ) ;
#45867=ORIENTED_EDGE ( 'NONE', *, *, #12169, .F. ) ;
#45870=CARTESIAN_POINT ( 'NONE',  ( 24.60109517054022987, -3.453341049831690324, 12.10341519414737199 ) ) ;
#45871=CARTESIAN_POINT ( 'NONE',  ( 15.82725884711995512, 9.380130419263576158, 8.300201155565265054 ) ) ;
#45878=CARTESIAN_POINT ( 'NONE',  ( 18.30000000000000071, 2.775703640144308260, 11.68316444257406772 ) ) ;
#45883=CARTESIAN_POINT ( 'NONE',  ( 15.67439970770000102, -8.782357275181000844, -8.013525452821999906 ) ) ;
#45885=CARTESIAN_POINT ( 'NONE',  ( 23.60093109724832772, -13.39265514436702098, 3.991923406020022824 ) ) ;
#45891=CARTESIAN_POINT ( 'NONE',  ( 25.60000000000000142, -2.258942858049999725, 12.29419282279000036 ) ) ;
#45892=CIRCLE ( 'NONE', #53678, 1.000000000000000444 ) ;
#45897=ORIENTED_EDGE ( 'NONE', *, *, #65734, .F. ) ;
#45907=VERTEX_POINT ( 'NONE', #63162 ) ;
#45910=CARTESIAN_POINT ( 'NONE',  ( 13.67488484168399943, -8.948943314763999624, -7.542122959438999352 ) ) ;
#45916=CARTESIAN_POINT ( 'NONE',  ( 27.09999999999999787, 0.000000000000000000, 9.250000000000000000 ) ) ;
#45922=EDGE_CURVE ( 'NONE', #60348, #23570, #57857, .T. ) ;
#45927=EDGE_CURVE ( 'NONE', #46284, #41305, #56503, .T. ) ;
#45939=CARTESIAN_POINT ( 'NONE',  ( 11.44794916906000104, -11.60968724315999978, -1.479704744065999833 ) ) ;
#45954=B_SPLINE_CURVE_WITH_KNOTS ( 'NONE', 3,
 ( #31466, #43333, #26568, #21990, #21646, #38072, #42981, #37735, #11163, #27252, #64637, #59399, #44380, #34576, #39464, #22338, #12898, #33880, #1365, #50300, #50642, #34227, #66018 ),
 .UNSPECIFIED., .F., .F.,
 ( 4, 2, 2, 1, 2, 2, 2, 2, 1, 1, 2, 2, 4 ),
 ( 0.000000000000000000, 0.2500000000000023315, 0.3750000000000046629, 0.4375000000000032196, 0.4687500000000038858, 0.5000000000000044409, 0.6250000000000305311, 0.6875000000000408562, 0.7187500000000447420, 0.7343750000000456302, 0.7421875000000482947, 0.7500000000000510703, 1.000000000000000000 ),
 .UNSPECIFIED. ) ;
#45958=CARTESIAN_POINT ( 'NONE',  ( 21.60000000000000142, 0.000000000000000000, 0.000000000000000000 ) ) ;
#45960=CARTESIAN_POINT ( 'NONE',  ( 24.14075185647167032, 3.327828376135185451, 12.49053418803123705 ) ) ;
#45961=CARTESIAN_POINT ( 'NONE',  ( 23.55757338048400129, 10.23275786013000044, -9.678818376535998524 ) ) ;
#45962=CARTESIAN_POINT ( 'NONE',  ( 18.12922381500399993, -3.157787539580000136, -11.36563583066999961 ) ) ;
#45969=EDGE_CURVE ( 'NONE', #47655, #22693, #53158, .T. ) ;
#45970=CARTESIAN_POINT ( 'NONE',  ( 23.60205915885299888, -11.88166580726000454, -3.967996863081999948 ) ) ;
#45979=DIRECTION ( 'NONE',  ( 1.000000000000000000, 0.000000000000000000, 0.000000000000000000 ) ) ;
#45981=EDGE_LOOP ( 'NONE', ( #59389, #17430, #25860, #53562 ) ) ;
#45984=CARTESIAN_POINT ( 'NONE',  ( 13.63315305048522319, 12.20113081363246543, 2.519319003639657328 ) ) ;
#45985=CARTESIAN_POINT ( 'NONE',  ( 24.60170725920900026, 3.645111442846999950, -12.27956986324999988 ) ) ;
#45991=CARTESIAN_POINT ( 'NONE',  ( 13.22410434383600197, -11.56587205782000005, -1.788415454164999918 ) ) ;
#45994=AXIS2_PLACEMENT_3D ( 'NONE', #7431, #55334, #55686 ) ;
#46003=ORIENTED_EDGE ( 'NONE', *, *, #14074, .F. ) ;
#46010=DIRECTION ( 'NONE',  ( 0.000000000000000000, -0.9466492601157000530, 0.3222656952305000266 ) ) ;
#46022=CARTESIAN_POINT ( 'NONE',  ( 11.49999672495000169, 3.632761979779000061, -11.06912554803999882 ) ) ;
#46031=EDGE_CURVE ( 'NONE', #12604, #63987, #45612, .T. ) ;
#46040=ORIENTED_EDGE ( 'NONE', *, *, #9291, .F. ) ;
#46043=CARTESIAN_POINT ( 'NONE',  ( 15.76350100824699929, 9.023747925888001120, 8.341981946770999912 ) ) ;
#46049=CARTESIAN_POINT ( 'NONE',  ( 20.75138802851920161, -5.760487483753345295, 0.05108123232907683942 ) ) ;
#46057=DIRECTION ( 'NONE',  ( -1.000000000000000000, 0.000000000000000000, 0.000000000000000000 ) ) ;
#46068=ORIENTED_EDGE ( 'NONE', *, *, #3876, .T. ) ;
#46075=CARTESIAN_POINT ( 'NONE',  ( 11.83936489023500194, -3.414328975993000004, 11.89720897182000137 ) ) ;
#46096=ORIENTED_EDGE ( 'NONE', *, *, #21601, .F. ) ;
#46097=CARTESIAN_POINT ( 'NONE',  ( 25.44993910976900153, -11.77655473258999841, 4.190794510628000680 ) ) ;
#46105=DIRECTION ( 'NONE',  ( 0.000000000000000000, -0.9867381147929490393, -0.1623203401144079905 ) ) ;
#46106=CARTESIAN_POINT ( 'NONE',  ( 18.44331666222400301, -2.998518551215999750, -12.10579027554000042 ) ) ;
#46107=CARTESIAN_POINT ( 'NONE',  ( 24.44917776433500123, -8.894882193901999301, 9.199943407630001957 ) ) ;
#46117=CARTESIAN_POINT ( 'NONE',  ( 23.59999196693599899, 2.915561532799999966, -13.58550759281999909 ) ) ;
#46122=CARTESIAN_POINT ( 'NONE',  ( 25.50766902656323509, 2.874072089164859456, -11.25422662531584628 ) ) ;
#46132=B_SPLINE_CURVE_WITH_KNOTS ( 'NONE', 3,
 ( #55463, #17720, #29252, #34834 ),
 .UNSPECIFIED., .F., .F.,
 ( 4, 4 ),
 ( 0.000000000000000000, 1.000000000000000000 ),
 .UNSPECIFIED. ) ;
#46151=DIRECTION ( 'NONE',  ( 1.000000000000000000, 0.000000000000000000, 0.000000000000000000 ) ) ;
#46152=VECTOR ( 'NONE', #15068, 1000.000000000000114 ) ;
#46154=CARTESIAN_POINT ( 'NONE',  ( 13.55563772304700088, -9.581334502426001265, -7.839063693813000278 ) ) ;
#46158=CARTESIAN_POINT ( 'NONE',  ( 24.30000565784163058, -3.240508265789169506, -12.09374149026787570 ) ) ;
#46159=CARTESIAN_POINT ( 'NONE',  ( 24.90043558836852000, -11.58828833617089948, 3.208336305466431781 ) ) ;
#46164=CARTESIAN_POINT ( 'NONE',  ( 11.79999999471800010, 11.69117318561000118, 1.923227876431999883 ) ) ;
#46175=B_SPLINE_CURVE_WITH_KNOTS ( 'NONE', 3,
 ( #19008, #22868, #34067, #2248, #40002, #44219 ),
 .UNSPECIFIED., .F., .F.,
 ( 4, 2, 4 ),
 ( 0.000000000000000000, 0.5000000000000000000, 1.000000000000000000 ),
 .UNSPECIFIED. ) ;
#46176=CARTESIAN_POINT ( 'NONE',  ( 23.67741535593912161, -3.195755220888627957, 13.38330436814928248 ) ) ;
#46177=PLANE ( 'NONE',  #20969 ) ;
#46187=CARTESIAN_POINT ( 'NONE',  ( 25.29996559941400136, -2.596925179230000325, -11.35302181744000016 ) ) ;
#46192=DIRECTION ( 'NONE',  ( -1.000000000000000000, 0.000000000000000000, 0.000000000000000000 ) ) ;
#46213=ORIENTED_EDGE ( 'NONE', *, *, #5695, .T. ) ;
#46217=CARTESIAN_POINT ( 'NONE',  ( 13.99999999270239570, 8.951333082579457923, 8.002096037671929452 ) ) ;
#46229=CARTESIAN_POINT ( 'NONE',  ( 15.83176382712000319, -8.647155996545000889, -8.162171193140999037 ) ) ;
#46231=CARTESIAN_POINT ( 'NONE',  ( 23.57355549871708433, -13.35445022547162708, 4.160309226275855643 ) ) ;
#46234=FACE_OUTER_BOUND ( 'NONE', #27041, .T. ) ;
#46236=EDGE_CURVE ( 'NONE', #62317, #44668, #34714, .T. ) ;
#46237=EDGE_CURVE ( 'NONE', #42044, #50821, #67990, .T. ) ;
#46239=FACE_OUTER_BOUND ( 'NONE', #51989, .T. ) ;
#46240=CARTESIAN_POINT ( 'NONE',  ( 24.35365242081700288, 11.54878985755999388, -2.979915831581000152 ) ) ;
#46244=VECTOR ( 'NONE', #40816, 1000.000000000000114 ) ;
#46256=CONICAL_SURFACE ( 'NONE', #68543, 12.71246950475999959, 0.8960553845711767273 ) ;
#46258=CARTESIAN_POINT ( 'NONE',  ( 23.56664318980499928, 10.37807351222000030, 9.381504534996999212 ) ) ;
#46261=EDGE_CURVE ( 'NONE', #55299, #60029, #40517, .T. ) ;
#46263=CARTESIAN_POINT ( 'NONE',  ( 17.74639017890735104, -11.23193386242373748, 3.094113022437827265 ) ) ;
#46271=CARTESIAN_POINT ( 'NONE',  ( 25.21374952102824096, 2.724994458594768076, 11.40631079751203814 ) ) ;
#46272=CARTESIAN_POINT ( 'NONE',  ( 18.41067102831330615, 3.015843532951033357, -11.25293825120812663 ) ) ;
#46277=ORIENTED_EDGE ( 'NONE', *, *, #51225, .T. ) ;
#46284=VERTEX_POINT ( 'NONE', #16575 ) ;
#46288=CARTESIAN_POINT ( 'NONE',  ( 11.25913316395000052, -11.80170809442000035, -1.433206434934999995 ) ) ;
#46293=CARTESIAN_POINT ( 'NONE',  ( 24.67921570607400383, -3.567514742249000115, 12.13750887372000165 ) ) ;
#46295=B_SPLINE_CURVE_WITH_KNOTS ( 'NONE', 3,
 ( #43662, #47877, #64959, #21631 ),
 .UNSPECIFIED., .F., .F.,
 ( 4, 4 ),
 ( 0.000000000000000000, 1.000000000000000000 ),
 .UNSPECIFIED. ) ;
#46296=CIRCLE ( 'NONE', #66342, 14.00000000000000000 ) ;
#46300=AXIS2_PLACEMENT_3D ( 'NONE', #14880, #46010, #36202 ) ;
#46301=CARTESIAN_POINT ( 'NONE',  ( 17.79325612864500172, 3.315492466914999881, 11.22361417850999921 ) ) ;
#46308=CARTESIAN_POINT ( 'NONE',  ( 24.01983208508439560, 3.345235842750158728, 12.71056888070838475 ) ) ;
#46310=CARTESIAN_POINT ( 'NONE',  ( 18.02410434383600091, -3.285250940561000199, -11.23276246309000115 ) ) ;
#46315=ORIENTED_EDGE ( 'NONE', *, *, #42192, .F. ) ;
#46318=ADVANCED_FACE ( 'NONE', ( #65146 ), #47898, .F. ) ;
#46337=CARTESIAN_POINT ( 'NONE',  ( 25.29987261392200182, 9.517611874540000017, -8.103398312166000039 ) ) ;
#46341=CARTESIAN_POINT ( 'NONE',  ( 13.06873602477000063, -11.64657800763999873, -1.862567138450999860 ) ) ;
#46352=EDGE_LOOP ( 'NONE', ( #4438, #42552, #14196, #28530, #67776 ) ) ;
#46353=CARTESIAN_POINT ( 'NONE',  ( 23.59379317251364228, 10.17887641161417278, 9.580899070374313098 ) ) ;
#46356=CARTESIAN_POINT ( 'NONE',  ( 23.66004879239100234, 13.39256428908000096, 3.813547978107000080 ) ) ;
#46361=CARTESIAN_POINT ( 'NONE',  ( 12.09999922233642344, 11.66744139996707119, -3.971920075670921424 ) ) ;
#46366=CARTESIAN_POINT ( 'NONE',  ( 24.13558027894506353, 12.48959359056989094, -3.366848964696536051 ) ) ;
#46368=CARTESIAN_POINT ( 'NONE',  ( 17.60000000000000142, 52.95171880992000268, -18.02623547589999831 ) ) ;
#46369=CARTESIAN_POINT ( 'NONE',  ( 15.39999999998900293, -9.471998555523999386, -8.194929586088999685 ) ) ;
#46372=AXIS2_PLACEMENT_3D ( 'NONE', #10681, #27120, #11709 ) ;
#46381=CARTESIAN_POINT ( 'NONE',  ( 17.80000000001300009, 3.351264566333000072, -11.15757590352999884 ) ) ;
#46388=CARTESIAN_POINT ( 'NONE',  ( 15.35870478550200069, 9.525289020731998235, 8.192348383776000276 ) ) ;
#46389=CARTESIAN_POINT ( 'NONE',  ( 24.14474089025218717, 9.246824087223631139, 9.586721689821816383 ) ) ;
#46391=CARTESIAN_POINT ( 'NONE',  ( 13.70003001321900271, 9.668726926528000476, 7.961868161445000425 ) ) ;
#46399=CARTESIAN_POINT ( 'NONE',  ( 24.43231275843400141, 3.176386277817000003, 12.00227839950999886 ) ) ;
#46410=CARTESIAN_POINT ( 'NONE',  ( 17.98628609634500108, 3.388648274289000284, 11.90503202562999974 ) ) ;
#46417=CARTESIAN_POINT ( 'NONE',  ( 13.92020863217304338, -9.472241403191583586, -8.194648738509743069 ) ) ;
#46418=CARTESIAN_POINT ( 'NONE',  ( 14.70000000000000107, 8.824259102667999954, 7.756628703356000187 ) ) ;
#46422=B_SPLINE_CURVE_WITH_KNOTS ( 'NONE', 3,
 ( #62847, #26151, #62169, #68433 ),
 .UNSPECIFIED., .F., .F.,
 ( 4, 4 ),
 ( 0.000000000000000000, 1.000000000000000000 ),
 .UNSPECIFIED. ) ;
#46424=CONICAL_SURFACE ( 'NONE', #43071, 11.34994642770999818, 0.7853934433896081480 ) ;
#46429=EDGE_LOOP ( 'NONE', ( #52328, #60539, #33799, #62894 ) ) ;
#46430=CARTESIAN_POINT ( 'NONE',  ( 11.50029455687000102, -11.62161504227245779, -0.9384843035876943018 ) ) ;
#46432=EDGE_LOOP ( 'NONE', ( #54711, #1886, #45073, #2211 ) ) ;
#46439=PLANE ( 'NONE',  #51039 ) ;
#46442=B_SPLINE_CURVE_WITH_KNOTS ( 'NONE', 3,
 ( #5240, #25540, #63621, #68862 ),
 .UNSPECIFIED., .F., .F.,
 ( 4, 4 ),
 ( 0.000000000000000000, 1.000000000000000000 ),
 .UNSPECIFIED. ) ;
#46452=CARTESIAN_POINT ( 'NONE',  ( 17.79403162610499933, -3.298115360370000193, -11.83441368098000090 ) ) ;
#46453=CARTESIAN_POINT ( 'NONE',  ( 24.35146665670700017, -8.929414329885000612, 9.054894786836999998 ) ) ;
#46459=EDGE_LOOP ( 'NONE', ( #30311, #52407, #2240, #28740 ) ) ;
#46467=CARTESIAN_POINT ( 'NONE',  ( 17.86534991953400109, 3.412585803847000054, -11.89775424487000066 ) ) ;
#46470=VERTEX_POINT ( 'NONE', #26305 ) ;
#46477=CARTESIAN_POINT ( 'NONE',  ( 24.98632682924400328, 8.514528481086999889, 8.479295295784998743 ) ) ;
#46494=CIRCLE ( 'NONE', #21922, 0.2999999999999993228 ) ;
#46500=DIRECTION ( 'NONE',  ( 0.000000000000000000, 0.1807154286440006141, -0.9835354258236025382 ) ) ;
#46501=B_SPLINE_CURVE_WITH_KNOTS ( 'NONE', 3,
 ( #30559, #5010, #22121, #31253, #47674, #10258, #32291, #26346, #5696, #52563 ),
 .UNSPECIFIED., .F., .F.,
 ( 4, 2, 2, 2, 4 ),
 ( 0.000000000000000000, 0.1248149689023889258, 0.2496299378047778517, 0.3744449067071667914, 0.4992598756095557033 ),
 .UNSPECIFIED. ) ;
#46502=CARTESIAN_POINT ( 'NONE',  ( 25.55273627768460543, -8.264546374049874800, 8.081436664941460180 ) ) ;
#46507=VERTEX_POINT ( 'NONE', #57080 ) ;
#46521=CARTESIAN_POINT ( 'NONE',  ( 23.65871200092008309, -3.166282759754092346, 13.42477648256529044 ) ) ;
#46524=CARTESIAN_POINT ( 'NONE',  ( 24.48514017958100197, -3.324320173708000148, -12.08694633982000077 ) ) ;
#46528=B_SPLINE_CURVE_WITH_KNOTS ( 'NONE', 3,
 ( #29307, #18811, #12524, #55520, #28259, #34555 ),
 .UNSPECIFIED., .F., .F.,
 ( 4, 2, 4 ),
 ( 0.000000000000000000, 0.5000000000000000000, 1.000000000000000000 ),
 .UNSPECIFIED. ) ;
#46529=ORIENTED_EDGE ( 'NONE', *, *, #25332, .F. ) ;
#46533=FACE_OUTER_BOUND ( 'NONE', #44393, .T. ) ;
#46534=CARTESIAN_POINT ( 'NONE',  ( 15.90018573812067260, 4.599694346030502423, 10.96245233228960814 ) ) ;
#46543=CARTESIAN_POINT ( 'NONE',  ( 24.30000561204433396, -12.09374146552009499, -3.240508259158020987 ) ) ;
#46546=VERTEX_POINT ( 'NONE', #36445 ) ;
#46552=CARTESIAN_POINT ( 'NONE',  ( 11.79999999550100220, -11.52577121388000059, -1.696750555870000010 ) ) ;
#46553=DIRECTION ( 'NONE',  ( -1.000000000000000000, 0.000000000000000000, 0.000000000000000000 ) ) ;
#46561=CARTESIAN_POINT ( 'NONE',  ( 24.44496483130000186, -3.224879855413000040, 12.03535978074999946 ) ) ;
#46564=DIRECTION ( 'NONE',  ( -1.000000000000000000, 0.000000000000000000, 0.000000000000000000 ) ) ;
#46570=CARTESIAN_POINT ( 'NONE',  ( 17.80000000005199823, 3.345268251980999974, 11.86064071431999878 ) ) ;
#46572=EDGE_CURVE ( 'NONE', #2494, #18236, #32236, .T. ) ;
#46578=ORIENTED_EDGE ( 'NONE', *, *, #28012, .F. ) ;
#46579=CIRCLE ( 'NONE', #43220, 0.3000000000000007105 ) ;
#46584=CARTESIAN_POINT ( 'NONE',  ( 23.51706668766000163, -2.929178272971999952, 13.82547084486999900 ) ) ;
#46587=CARTESIAN_POINT ( 'NONE',  ( 25.44993529014200107, -2.258942858049999725, 12.29419282279000036 ) ) ;
#46589=CARTESIAN_POINT ( 'NONE',  ( 23.55667344479600089, 3.263152516149000260, -13.70292389877999817 ) ) ;
#46597=EDGE_CURVE ( 'NONE', #5919, #23499, #29940, .T. ) ;
#46605=CARTESIAN_POINT ( 'NONE',  ( 23.66004879239100234, 3.393652551760000247, -13.50507492672999987 ) ) ;
#46607=CARTESIAN_POINT ( 'NONE',  ( 13.67059379716000045, -8.916337866955000635, -7.720150512555999711 ) ) ;
#46610=CARTESIAN_POINT ( 'NONE',  ( 23.59999999999999787, -11.54195482626477798, -7.798368141167753897 ) ) ;
#46611=CARTESIAN_POINT ( 'NONE',  ( 16.26901036074197648, 3.345264657739864145, 11.86070554647184316 ) ) ;
#46626=ORIENTED_EDGE ( 'NONE', *, *, #56853, .F. ) ;
#46642=CARTESIAN_POINT ( 'NONE',  ( 11.79999999471800010, -3.216299622513999701, 11.40340969442000052 ) ) ;
#46645=CARTESIAN_POINT ( 'NONE',  ( 18.18404792230800382, 3.205001206845999651, 11.25648540289999922 ) ) ;
#46651=CYLINDRICAL_SURFACE ( 'NONE', #13308, 12.52500000000000036 ) ;
#46653=CARTESIAN_POINT ( 'NONE',  ( 24.67326002361100024, 8.700705800976999527, -9.017089022949001276 ) ) ;
#46656=CARTESIAN_POINT ( 'NONE',  ( 24.32784158250700202, 9.023045772892999139, -9.340248004790000280 ) ) ;
#46657=CARTESIAN_POINT ( 'NONE',  ( 18.38722619340700248, -3.117741388420999904, -11.18549237633000004 ) ) ;
#46662=B_SPLINE_CURVE_WITH_KNOTS ( 'NONE', 3,
 ( #60168, #7715, #12970, #34984, #9082, #18207, #3824, #40902, #56300, #3152 ),
 .UNSPECIFIED., .F., .F.,
 ( 4, 2, 2, 2, 4 ),
 ( 0.000000000000000000, 0.1248149689018965974, 0.2496299378037931949, 0.3744449067056898062, 0.4992598756075863897 ),
 .UNSPECIFIED. ) ;
#46663=CARTESIAN_POINT ( 'NONE',  ( 24.67921580316900076, -12.29514843751999997, 2.979196179828000002 ) ) ;
#46665=CYLINDRICAL_SURFACE ( 'NONE', #60373, 5.000000000000000000 ) ;
#46666=FACE_OUTER_BOUND ( 'NONE', #40354, .T. ) ;
#46670=CARTESIAN_POINT ( 'NONE',  ( 13.67488484168399943, 8.948943314763999624, 7.542122959438999352 ) ) ;
#46674=VECTOR ( 'NONE', #8067, 1000.000000000000000 ) ;
#46684=ORIENTED_EDGE ( 'NONE', *, *, #134, .F. ) ;
#46695=CARTESIAN_POINT ( 'NONE',  ( 21.60000000000000142, 0.000000000000000000, 0.000000000000000000 ) ) ;
#46699=CARTESIAN_POINT ( 'NONE',  ( 23.59644478421662583, 10.16908198660547846, 9.589309125383387311 ) ) ;
#46702=DIRECTION ( 'NONE',  ( -1.000000000000000000, 0.000000000000000000, 0.000000000000000000 ) ) ;
#46714=CYLINDRICAL_SURFACE ( 'NONE', #12023, 0.6999999999999992895 ) ;
#46718=ADVANCED_FACE ( 'NONE', ( #59832 ), #923, .T. ) ;
#46723=ORIENTED_EDGE ( 'NONE', *, *, #48260, .T. ) ;
#46729=CARTESIAN_POINT ( 'NONE',  ( 25.29987261392200182, 8.756202924575998026, -7.455126447192999883 ) ) ;
#46730=CARTESIAN_POINT ( 'NONE',  ( 23.58312284468700071, 13.27301453609000070, 4.267237745444000474 ) ) ;
#46740=EDGE_CURVE ( 'NONE', #27711, #12790, #20984, .T. ) ;
#46747=CARTESIAN_POINT ( 'NONE',  ( 23.61702365891200373, 10.26369571899999933, 9.293522352232999495 ) ) ;
#46759=CARTESIAN_POINT ( 'NONE',  ( 11.79999999523987420, 3.306280043674564517, -11.23952258183352093 ) ) ;
#46760=CARTESIAN_POINT ( 'NONE',  ( 24.30000000000000071, 3.224868684338999980, -12.03537377768999939 ) ) ;
#46764=ORIENTED_EDGE ( 'NONE', *, *, #15312, .F. ) ;
#46769=ORIENTED_EDGE ( 'NONE', *, *, #15011, .T. ) ;
#46792=CARTESIAN_POINT ( 'NONE',  ( 18.12310803393399894, -3.320912951897000198, -11.92519506916999994 ) ) ;
#46796=EDGE_CURVE ( 'NONE', #31999, #46284, #521, .T. ) ;
#46799=EDGE_CURVE ( 'NONE', #36266, #28289, #36303, .T. ) ;
#46803=CARTESIAN_POINT ( 'NONE',  ( 21.10000033274619824, 12.52499966719000035, 3.709620195857000057E-10 ) ) ;
#46804=CARTESIAN_POINT ( 'NONE',  ( 19.94999927679900154, 1.497292381259999763E-13, 3.463895836829999943E-14 ) ) ;
#46809=CARTESIAN_POINT ( 'NONE',  ( 23.55340715333399970, -13.38991586735000183, 4.199558039904999873 ) ) ;
#46815=B_SPLINE_CURVE_WITH_KNOTS ( 'NONE', 3,
 ( #60330, #5796, #33073, #39011, #55083, #27836, #7189, #37962 ),
 .UNSPECIFIED., .F., .F.,
 ( 4, 2, 2, 4 ),
 ( 0.000000000000000000, 0.1251850562541942935, 0.2503701125083885870, 0.5007402250167770630 ),
 .UNSPECIFIED. ) ;
#46827=CARTESIAN_POINT ( 'NONE',  ( 11.35562122949000141, -3.716778816705999855, 11.19591510979999960 ) ) ;
#46832=CARTESIAN_POINT ( 'NONE',  ( 25.30000327618300204, -10.83443035398000021, 3.855530949778000149 ) ) ;
#46833=CARTESIAN_POINT ( 'NONE',  ( 24.66708179685990743, 8.738412505656103946, 9.169048259976223747 ) ) ;
#46835=ORIENTED_EDGE ( 'NONE', *, *, #61960, .F. ) ;
#46840=FACE_OUTER_BOUND ( 'NONE', #12196, .T. ) ;
#46851=CARTESIAN_POINT ( 'NONE',  ( 13.70003001321900449, 11.73562684670656431, 4.491863874615371621 ) ) ;
#46856=CARTESIAN_POINT ( 'NONE',  ( 24.03127928945400171, 3.727176143476999659, 13.01575025216999926 ) ) ;
#46864=DIRECTION ( 'NONE',  ( 0.000000000000000000, 0.000000000000000000, 1.000000000000000000 ) ) ;
#46867=CARTESIAN_POINT ( 'NONE',  ( 24.33654850364300160, -12.30574143627999995, -3.219652787269999816 ) ) ;
#46870=CARTESIAN_POINT ( 'NONE',  ( 16.08259915475489166, -9.118254932978855365, -8.587227412616224242 ) ) ;
#46871=CARTESIAN_POINT ( 'NONE',  ( 23.57776922997304681, 13.28350420490069617, 4.287209407939693406 ) ) ;
#46872=ORIENTED_EDGE ( 'NONE', *, *, #29251, .T. ) ;
#46879=EDGE_CURVE ( 'NONE', #13082, #48412, #7953, .T. ) ;
#46900=EDGE_CURVE ( 'NONE', #8563, #56058, #39907, .T. ) ;
#46912=DIRECTION ( 'NONE',  ( -1.000000000000000000, 0.000000000000000000, 0.000000000000000000 ) ) ;
#46915=CARTESIAN_POINT ( 'NONE',  ( 15.39325612864500137, -8.820489328074000213, -7.691617095226000345 ) ) ;
#46925=CARTESIAN_POINT ( 'NONE',  ( 23.66004879239100234, -3.393652723963000106, -13.50507488346000073 ) ) ;
#46928=CARTESIAN_POINT ( 'NONE',  ( 23.56695615185851977, -3.042046339845886127, 13.65547877525810350 ) ) ;
#46929=CARTESIAN_POINT ( 'NONE',  ( 23.73686952991999988, 3.437738207072000396, -13.35009212917000099 ) ) ;
#46951=B_SPLINE_CURVE_WITH_KNOTS ( 'NONE', 3,
 ( #1236, #55065, #1930, #45273 ),
 .UNSPECIFIED., .F., .F.,
 ( 4, 4 ),
 ( 0.000000000000000000, 1.000000000000000000 ),
 .UNSPECIFIED. ) ;
#46952=CARTESIAN_POINT ( 'NONE',  ( 13.17784398560650061, 12.38705052588331590, 1.853828488290521159 ) ) ;
#46962=CARTESIAN_POINT ( 'NONE',  ( 24.30000000000000071, -2.078227429405999693, -11.31065739696999906 ) ) ;
#46963=VERTEX_POINT ( 'NONE', #36976 ) ;
#46969=PRESENTATION_STYLE_ASSIGNMENT (( #9203 ) ) ;
#46973=DIRECTION ( 'NONE',  ( 0.000000000000000000, 1.000000000000000000, 0.000000000000000000 ) ) ;
#46978=CARTESIAN_POINT ( 'NONE',  ( 11.93277786803400176, 12.01216300861999997, -3.678628708156000293 ) ) ;
#46983=ADVANCED_FACE ( 'NONE', ( #31730 ), #58287, .T. ) ;
#46986=CARTESIAN_POINT ( 'NONE',  ( 18.23887202961200060, 3.252214874110999965, 11.14733497513999971 ) ) ;
#46994=CARTESIAN_POINT ( 'NONE',  ( 24.19015447988511269, 3.314354331839912682, 12.40233438014860035 ) ) ;
#47002=CARTESIAN_POINT ( 'NONE',  ( 25.37957500006017852, -11.36922400990947501, 3.069089490420214172 ) ) ;
#47010=CARTESIAN_POINT ( 'NONE',  ( 13.91144947526900033, 8.829982735797999638, 7.819410275689000045 ) ) ;
#47013=CARTESIAN_POINT ( 'NONE',  ( 25.37956046633510354, -3.026721893553028231, 11.38059512590412581 ) ) ;
#47014=CARTESIAN_POINT ( 'NONE',  ( 25.60000000000000142, -10.55163788719000095, -3.754896668835000284 ) ) ;
#47022=ORIENTED_EDGE ( 'NONE', *, *, #48322, .F. ) ;
#47037=CARTESIAN_POINT ( 'NONE',  ( 23.58477818954033722, 10.21639588674304910, 9.547105905782643731 ) ) ;
#47043=VERTEX_POINT ( 'NONE', #30113 ) ;
#47053=CARTESIAN_POINT ( 'NONE',  ( 23.62975776114408077, -10.06704571337557574, 9.666453531962270418 ) ) ;
#47061=FACE_OUTER_BOUND ( 'NONE', #39527, .T. ) ;
#47071=CARTESIAN_POINT ( 'NONE',  ( 25.37703081959900331, 2.612361302726000201, 11.31741887482999864 ) ) ;
#47078=CARTESIAN_POINT ( 'NONE',  ( 15.20000000000000107, 11.99088163391999906, -3.229229350024999778 ) ) ;
#47081=CARTESIAN_POINT ( 'NONE',  ( 23.56666365135700403, -2.963314674624001999, -12.23574966054999358 ) ) ;
#47084=CARTESIAN_POINT ( 'NONE',  ( 24.87965828714900240, -11.54628276867000025, 3.248280990976000204 ) ) ;
#47096=DIRECTION ( 'NONE',  ( 0.000000000000000000, -0.4815106998112011483, -0.8764402124317022258 ) ) ;
#47099=ADVANCED_FACE ( 'NONE', ( #9969 ), #64583, .T. ) ;
#47101=EDGE_CURVE ( 'NONE', #31118, #36190, #22167, .T. ) ;
#47102=B_SPLINE_CURVE_WITH_KNOTS ( 'NONE', 3,
 ( #16861, #27718, #17214, #54969, #792, #28405, #1831, #37505, #32278, #42754, #53925, #64057, #5684, #58828, #53589, #27365, #22108, #43452, #29415, #8759, #18217, #30101, #56653 ),
 .UNSPECIFIED., .F., .F.,
 ( 4, 2, 2, 1, 2, 2, 2, 2, 1, 1, 2, 2, 4 ),
 ( 0.000000000000000000, 0.2500000000000290323, 0.3750000000000388023, 0.4375000000000434652, 0.4687500000000431322, 0.5000000000000427436, 0.6250000000000321965, 0.6875000000000294209, 0.7187500000000291989, 0.7343750000000306422, 0.7421875000000303091, 0.7500000000000299760, 1.000000000000000000 ),
 .UNSPECIFIED. ) ;
#47107=CARTESIAN_POINT ( 'NONE',  ( 13.99999997735699253, -8.821177874197182689, -7.709989353259452116 ) ) ;
#47109=CARTESIAN_POINT ( 'NONE',  ( 11.50001496185000249, 9.368387413230685468, -8.415797411492746960 ) ) ;
#47114=CARTESIAN_POINT ( 'NONE',  ( 15.86395943152100330, -3.857419000648000029, -11.66670712924999975 ) ) ;
#47116=ORIENTED_EDGE ( 'NONE', *, *, #14370, .F. ) ;
#47134=CARTESIAN_POINT ( 'NONE',  ( 25.59997324745700098, -8.218963665681000563, -8.043524865771999544 ) ) ;
#47137=CARTESIAN_POINT ( 'NONE',  ( 18.41451919223379718, 3.018310540774385764, 11.25254019301550379 ) ) ;
#47138=CARTESIAN_POINT ( 'NONE',  ( 23.60205915885299888, -9.377218989194005871, 8.305825996818995804 ) ) ;
#47139=CARTESIAN_POINT ( 'NONE',  ( 23.57777180426788277, -13.36543806030607939, -4.119497871640947828 ) ) ;
#47142=CARTESIAN_POINT ( 'NONE',  ( 17.89019624313516843, 3.590943193543202572, 11.99920113072226080 ) ) ;
#47144=ORIENTED_EDGE ( 'NONE', *, *, #27643, .F. ) ;
#47147=FACE_OUTER_BOUND ( 'NONE', #19154, .T. ) ;
#47149=ADVANCED_FACE ( 'NONE', ( #68000 ), #32847, .F. ) ;
#47150=CARTESIAN_POINT ( 'NONE',  ( 18.40015514469800095, 2.597921877622999464E-14, -11.75015521449979516 ) ) ;
#47153=CARTESIAN_POINT ( 'NONE',  ( 24.63805894150500109, -12.49525856262000012, 2.948554912134000006 ) ) ;
#47155=ORIENTED_EDGE ( 'NONE', *, *, #16995, .F. ) ;
#47157=VERTEX_POINT ( 'NONE', #28475 ) ;
#47162=CARTESIAN_POINT ( 'NONE',  ( 11.79999999471800010, -11.69117318561000118, -1.923227876431999883 ) ) ;
#47163=DIRECTION ( 'NONE',  ( 1.000000000000000000, 0.000000000000000000, 0.000000000000000000 ) ) ;
#47177=ORIENTED_EDGE ( 'NONE', *, *, #36607, .T. ) ;
#47183=CARTESIAN_POINT ( 'NONE',  ( 11.35194303199000032, 3.840151595817999919, -11.76830449990999838 ) ) ;
#47188=CARTESIAN_POINT ( 'NONE',  ( 15.96663596566263976, 3.844870426479619852, 11.78010250471070997 ) ) ;
#47191=CARTESIAN_POINT ( 'NONE',  ( 25.22257210903613611, -11.23352489450897451, 3.340298631152402997 ) ) ;
#47199=DIRECTION ( 'NONE',  ( -1.000000000000000000, 0.000000000000000000, 0.000000000000000000 ) ) ;
#47200=CARTESIAN_POINT ( 'NONE',  ( 24.13681679563899962, 3.227440004341000090, 12.37874214852999977 ) ) ;
#47207=ORIENTED_EDGE ( 'NONE', *, *, #61424, .T. ) ;
#47211=CARTESIAN_POINT ( 'NONE',  ( 24.30000000000000071, -2.078227429405999693, 11.31065739696999906 ) ) ;
#47213=CARTESIAN_POINT ( 'NONE',  ( 25.44994113074799813, 11.77655473258999841, -4.190794510628000680 ) ) ;
#47218=CARTESIAN_POINT ( 'NONE',  ( 23.57777264369916992, 10.35461123704867781, -9.360203869705690849 ) ) ;
#47231=CIRCLE ( 'NONE', #40535, 1.000000000000000222 ) ;
#47234=CARTESIAN_POINT ( 'NONE',  ( 25.29987654162099986, 8.533547811387000692, 7.925584028117998336 ) ) ;
#47235=EDGE_CURVE ( 'NONE', #30098, #68740, #68021, .T. ) ;
#47243=CARTESIAN_POINT ( 'NONE',  ( 24.26682857475500299, 8.952388712744999921, 8.898287395196000205 ) ) ;
#47245=CARTESIAN_POINT ( 'NONE',  ( 11.30000285318000230, 11.76356368987999979, 1.428410073821000159 ) ) ;
#47256=CARTESIAN_POINT ( 'NONE',  ( 11.92270903091196921, 11.93179002798790123, -3.810633631264379595 ) ) ;
#47272=CYLINDRICAL_SURFACE ( 'NONE', #58945, 1.000000000000000444 ) ;
#47276=AXIS2_PLACEMENT_3D ( 'NONE', #47213, #53824, #32508 ) ;
#47286=CARTESIAN_POINT ( 'NONE',  ( 24.74075988380799984, 11.86917468414000076, 3.111330255459000327 ) ) ;
#47289=CARTESIAN_POINT ( 'NONE',  ( 13.73937158902900180, -8.990218567665001714, -7.348698335466000486 ) ) ;
#47291=CARTESIAN_POINT ( 'NONE',  ( 23.74082935151600182, 13.16168609087999819, -3.761290584336999920 ) ) ;
#47292=EDGE_CURVE ( 'NONE', #55031, #67995, #55530, .T. ) ;
#47293=ORIENTED_EDGE ( 'NONE', *, *, #31104, .F. ) ;
#47311=VERTEX_POINT ( 'NONE', #26669 ) ;
#47313=SHAPE_REPRESENTATION_RELATIONSHIP ( 'NONE' , 'NONE' ,  #27655, #8521 ) ;
#47317=EDGE_CURVE ( 'NONE', #59008, #52535, #36329, .T. ) ;
#47318=LINE ( 'NONE', #3620, #65297 ) ;
#47323=CIRCLE ( 'NONE', #22758, 5.000000000000000000 ) ;
#47324=VERTEX_POINT ( 'NONE', #58813 ) ;
#47325=CARTESIAN_POINT ( 'NONE',  ( 12.49732881085200020, 12.03818693049999844, -3.242368311117000079 ) ) ;
#47326=CARTESIAN_POINT ( 'NONE',  ( 17.74071352830300086, 11.49974814740000006, -4.814170953196000191 ) ) ;
#47330=CARTESIAN_POINT ( 'NONE',  ( 18.35167777225700192, -2.962063834667000073, 12.02051524900000068 ) ) ;
#47338=B_SPLINE_CURVE_WITH_KNOTS ( 'NONE', 3,
 ( #21818, #58888, #54678, #44207, #39293, #50468, #60961, #55372, #55028, #17629, #28821, #33709, #2570, #1891 ),
 .UNSPECIFIED., .F., .F.,
 ( 4, 2, 2, 2, 2, 2, 4 ),
 ( 0.000000000000000000, 0.1250000000000011380, 0.2500000000000022760, 0.5000000000000034417, 0.6250000000000025535, 0.7500000000000016653, 1.000000000000000000 ),
 .UNSPECIFIED. ) ;
#47345=CARTESIAN_POINT ( 'NONE',  ( 12.79999999202000005, -11.41069016990000051, 4.623987642516999230 ) ) ;
#47351=CARTESIAN_POINT ( 'NONE',  ( 16.13937158902900393, -3.642730659064999710, -11.02533040164999889 ) ) ;
#47355=CARTESIAN_POINT ( 'NONE',  ( 13.67059379716000045, 8.916337866955000635, 7.720150512555999711 ) ) ;
#47359=CARTESIAN_POINT ( 'NONE',  ( 24.30000000000000071, -11.85420044612000012, -3.901016762742000488 ) ) ;
#47384=VERTEX_POINT ( 'NONE', #28744 ) ;
#47391=DIRECTION ( 'NONE',  ( -1.000000000000000000, 0.000000000000000000, 0.000000000000000000 ) ) ;
#47393=EDGE_LOOP ( 'NONE', ( #18924, #48892, #50513, #59859, #67494, #64233 ) ) ;
#47396=VERTEX_POINT ( 'NONE', #39219 ) ;
#47397=CARTESIAN_POINT ( 'NONE',  ( 23.60581810200095276, -10.13726319729669001, 9.615401152371266136 ) ) ;
#47401=DIRECTION ( 'NONE',  ( 1.000000000000000000, 0.000000000000000000, 0.000000000000000000 ) ) ;
#47404=EDGE_CURVE ( 'NONE', #40252, #46507, #18019, .T. ) ;
#47406=ORIENTED_EDGE ( 'NONE', *, *, #66914, .T. ) ;
#47416=ORIENTED_EDGE ( 'NONE', *, *, #56671, .T. ) ;
#47419=CARTESIAN_POINT ( 'NONE',  ( 21.72233714749290101, 0.000000000000000000, 0.000000000000000000 ) ) ;
#47423=CARTESIAN_POINT ( 'NONE',  ( 23.89320776801300283, -3.288740538451999651, -12.20874841473999872 ) ) ;
#47424=VECTOR ( 'NONE', #67472, 1000.000000000000227 ) ;
#47430=CARTESIAN_POINT ( 'NONE',  ( 18.41194552103540261, -3.255591973356615210, 12.09481971601743844 ) ) ;
#47434=ADVANCED_FACE ( 'NONE', ( #13006 ), #29990, .F. ) ;
#47437=CARTESIAN_POINT ( 'NONE',  ( 23.60000000000000142, -11.77655473258999841, -4.190794510628000680 ) ) ;
#47445=CARTESIAN_POINT ( 'NONE',  ( 23.60001133530950668, -1.983597864821140026E-14, -13.89477126879791058 ) ) ;
#47450=EDGE_LOOP ( 'NONE', ( #17926, #5322, #24842, #4306 ) ) ;
#47457=FACE_OUTER_BOUND ( 'NONE', #57903, .T. ) ;
#47458=CARTESIAN_POINT ( 'NONE',  ( 11.26375800691000073, 11.80847110903000186, 1.384521730739000089 ) ) ;
#47460=EDGE_CURVE ( 'NONE', #40087, #23714, #19939, .T. ) ;
#47461=CARTESIAN_POINT ( 'NONE',  ( 11.50029455687000102, -11.56505190006999939, -1.404305717648999918 ) ) ;
#47462=CARTESIAN_POINT ( 'NONE',  ( 18.50001572531400029, -2.908166856580999937, 12.18270046149000052 ) ) ;
#47463=VERTEX_POINT ( 'NONE', #39567 ) ;
#47476=CARTESIAN_POINT ( 'NONE',  ( 24.53429011008099891, 3.614318944477000084, -12.31267538233000103 ) ) ;
#47481=CARTESIAN_POINT ( 'NONE',  ( 18.22968849645936729, 3.214251582955409692, 11.19784508593241235 ) ) ;
#47483=CARTESIAN_POINT ( 'NONE',  ( 23.56664678325900297, -13.31363270032999857, -4.296980171176000063 ) ) ;
#47498=CARTESIAN_POINT ( 'NONE',  ( 23.55671020924400239, -13.49865072242999986, 4.025359669029000109 ) ) ;
#47500=B_SPLINE_CURVE_WITH_KNOTS ( 'NONE', 3,
 ( #60578, #54642, #44854, #6735, #65463, #1850 ),
 .UNSPECIFIED., .F., .F.,
 ( 4, 2, 4 ),
 ( 0.000000000000000000, 0.5000000000000000000, 1.000000000000000000 ),
 .UNSPECIFIED. ) ;
#47501=ORIENTED_EDGE ( 'NONE', *, *, #41706, .T. ) ;
#47505=CARTESIAN_POINT ( 'NONE',  ( 23.66004879239100234, -9.998910854163000295, -9.691527647852998584 ) ) ;
#47520=CARTESIAN_POINT ( 'NONE',  ( 24.30001694391200218, -12.21047201246000036, 3.271805662802000025 ) ) ;
#47521=CARTESIAN_POINT ( 'NONE',  ( 18.29999999997147242, 11.00695868226823215, -3.817556993356255202 ) ) ;
#47522=FACE_OUTER_BOUND ( 'NONE', #62535, .T. ) ;
#47540=ORIENTED_EDGE ( 'NONE', *, *, #66686, .F. ) ;
#47548=CARTESIAN_POINT ( 'NONE',  ( 23.73547087796200117, 3.554272179136999998, 13.41695213092000039 ) ) ;
#47549=EDGE_LOOP ( 'NONE', ( #30466, #62570, #64960, #49030 ) ) ;
#47552=EDGE_CURVE ( 'NONE', #17060, #7930, #65691, .T. ) ;
#47554=AXIS2_PLACEMENT_3D ( 'NONE', #45318, #60351, #60695 ) ;
#47557=CARTESIAN_POINT ( 'NONE',  ( 23.61437543478880485, -3.070577605751717787, 13.52804441183152484 ) ) ;
#47561=CARTESIAN_POINT ( 'NONE',  ( 24.30000000000000071, -2.548720605937000006, 12.21654710926000220 ) ) ;
#47566=DIRECTION ( 'NONE',  ( -1.000000000000000000, 0.000000000000000000, 0.000000000000000000 ) ) ;
#47584=EDGE_CURVE ( 'NONE', #49775, #32306, #59011, .T. ) ;
#47585=CARTESIAN_POINT ( 'NONE',  ( 17.80000000005199823, 3.345268251980999974, 11.86064071431999878 ) ) ;
#47591=CARTESIAN_POINT ( 'NONE',  ( 24.51228084553499897, 8.787217699239999291, 8.912727655930000381 ) ) ;
#47598=DIRECTION ( 'NONE',  ( 0.000000000000000000, 0.000000000000000000, -1.000000000000000000 ) ) ;
#47609=ORIENTED_EDGE ( 'NONE', *, *, #21909, .F. ) ;
#47610=EDGE_CURVE ( 'NONE', #27264, #6697, #39683, .T. ) ;
#47611=CARTESIAN_POINT ( 'NONE',  ( 23.60000000000000142, 9.517611874540000017, -8.103398312166000039 ) ) ;
#47623=FACE_OUTER_BOUND ( 'NONE', #39783, .T. ) ;
#47624=CARTESIAN_POINT ( 'NONE',  ( 25.59994555223599733, -2.024003533649000097, 11.01554633311000053 ) ) ;
#47627=CARTESIAN_POINT ( 'NONE',  ( 23.60000000000000142, -2.548720605937000006, 12.21654710926000220 ) ) ;
#47628=CIRCLE ( 'NONE', #30858, 0.2999999999999993228 ) ;
#47635=CARTESIAN_POINT ( 'NONE',  ( 24.53002386606100060, 12.09082868768999930, 3.147845687315999896 ) ) ;
#47642=VERTEX_POINT ( 'NONE', #39022 ) ;
#47643=CARTESIAN_POINT ( 'NONE',  ( 13.69996357384220609, 12.28513767539633861, 2.441259368857655154 ) ) ;
#47647=CARTESIAN_POINT ( 'NONE',  ( 18.36030550606429657, 3.088870463281629064, -11.23311224736100833 ) ) ;
#47652=CARTESIAN_POINT ( 'NONE',  ( 13.43176382712000105, 11.67665677335000041, 2.247227628037000269 ) ) ;
#47653=VERTEX_POINT ( 'NONE', #18044 ) ;
#47655=VERTEX_POINT ( 'NONE', #45646 ) ;
#47660=B_SPLINE_CURVE_WITH_KNOTS ( 'NONE', 3,
 ( #387, #43038, #50614, #66682 ),
 .UNSPECIFIED., .F., .F.,
 ( 4, 4 ),
 ( 0.000000000000000000, 1.000000000000000000 ),
 .UNSPECIFIED. ) ;
#47665=ADVANCED_FACE ( 'NONE', ( #58182 ), #56777, .T. ) ;
#47668=CARTESIAN_POINT ( 'NONE',  ( 12.79272103475300071, 12.16747052068999935, -3.133256626080000107 ) ) ;
#47669=CARTESIAN_POINT ( 'NONE',  ( 18.07302322422999907, 11.50538345640999971, -4.553133914476999777 ) ) ;
#47672=CARTESIAN_POINT ( 'NONE',  ( 18.29983863916000075, -2.861762957209999847, 11.98830831200999825 ) ) ;
#47674=CARTESIAN_POINT ( 'NONE',  ( 12.37336427446135367, -11.82897199538900068, 3.432444870275719762 ) ) ;
#47676=CARTESIAN_POINT ( 'NONE',  ( 17.71545033449769235, 12.11985731843603098, -3.159854994125695704 ) ) ;
#47680=FACE_OUTER_BOUND ( 'NONE', #26206, .T. ) ;
#47698=CARTESIAN_POINT ( 'NONE',  ( 15.90542051561399894, -3.482376784026000038, -11.36410125839000074 ) ) ;
#47699=DIRECTION ( 'NONE',  ( -1.000000000000000000, 0.000000000000000000, 0.000000000000000000 ) ) ;
#47706=CARTESIAN_POINT ( 'NONE',  ( 18.36457177586861533, -3.090900475969966088, -11.23268385209002851 ) ) ;
#47709=CARTESIAN_POINT ( 'NONE',  ( 23.60000000000000497, 12.52449950949405277, 6.096395182155569081 ) ) ;
#47711=CYLINDRICAL_SURFACE ( 'NONE', #7448, 11.50000000000000178 ) ;
#47720=CARTESIAN_POINT ( 'NONE',  ( 12.99046541331000171, 12.43411100708999939, 1.799680151465999911 ) ) ;
#47725=ORIENTED_EDGE ( 'NONE', *, *, #44282, .T. ) ;
#47749=CARTESIAN_POINT ( 'NONE',  ( 24.00938301694239740, 12.69723756695836236, 3.467595816675521636 ) ) ;
#47750=EDGE_CURVE ( 'NONE', #57964, #38892, #44650, .T. ) ;
#47763=CARTESIAN_POINT ( 'NONE',  ( 25.48370073006200087, 2.675502271624000006, 11.27075336431999908 ) ) ;
#47767=CARTESIAN_POINT ( 'NONE',  ( 24.44496264144000364, 8.810483598181999554, -8.810508341310001157 ) ) ;
#47771=DIRECTION ( 'NONE',  ( -1.000000000000000000, 0.000000000000000000, 0.000000000000000000 ) ) ;
#47774=CARTESIAN_POINT ( 'NONE',  ( 13.99999999485600277, 9.471999751521998689, 8.194948195317001804 ) ) ;
#47775=CARTESIAN_POINT ( 'NONE',  ( 13.50018479229300006, 11.60142623882999935, 2.415183939829000259 ) ) ;
#47778=CIRCLE ( 'NONE', #17633, 12.52500000000000036 ) ;
#47784=CARTESIAN_POINT ( 'NONE',  ( 24.25969109951400071, 8.928491667350998640, 8.811171947794999681 ) ) ;
#47785=ORIENTED_EDGE ( 'NONE', *, *, #25219, .F. ) ;
#47789=FACE_OUTER_BOUND ( 'NONE', #53803, .T. ) ;
#47791=AXIS2_PLACEMENT_3D ( 'NONE', #21217, #68757, #51990 ) ;
#47798=CONICAL_SURFACE ( 'NONE', #22127, 1.150081764678999585, 0.7854598963975319981 ) ;
#47804=ORIENTED_EDGE ( 'NONE', *, *, #47584, .F. ) ;
#47805=CARTESIAN_POINT ( 'NONE',  ( 11.26396921949000074, -3.857819209177999920, 11.66658462090000015 ) ) ;
#47816=ORIENTED_EDGE ( 'NONE', *, *, #18006, .T. ) ;
#47817=DIRECTION ( 'NONE',  ( 1.000000000000000000, 1.063144863253999899E-13, 0.000000000000000000 ) ) ;
#47833=AXIS2_PLACEMENT_3D ( 'NONE', #8647, #17771, #44348 ) ;
#47835=CARTESIAN_POINT ( 'NONE',  ( 18.15060209887481690, 3.510419631054046530, 12.02305644365588400 ) ) ;
#47838=VERTEX_POINT ( 'NONE', #44795 ) ;
#47840=ORIENTED_EDGE ( 'NONE', *, *, #57765, .T. ) ;
#47845=CARTESIAN_POINT ( 'NONE',  ( 18.23777283046813125, 3.105167776281879899, -11.92942829619371103 ) ) ;
#47847=CARTESIAN_POINT ( 'NONE',  ( 23.99071456098100086, -13.00908790436000118, 3.384982717025000198 ) ) ;
#47848=CARTESIAN_POINT ( 'NONE',  ( 17.79999999998900151, 3.595165934733000057, 11.99793354950999991 ) ) ;
#47856=CARTESIAN_POINT ( 'NONE',  ( 18.02410434383600091, 3.285250940561000199, -11.23276246309000115 ) ) ;
#47877=CARTESIAN_POINT ( 'NONE',  ( 24.96666885022127857, -10.83443035760302386, 3.855530939604538965 ) ) ;
#47895=CARTESIAN_POINT ( 'NONE',  ( 11.49977531252999974, 12.43119799159999950, 1.530013559959999991 ) ) ;
#47898=B_SPLINE_SURFACE_WITH_KNOTS ( 'NONE', 3, 3, ( 
 ( #21471, #26735, #31984, #54673 ),
 ( #16228, #6770, #49421, #53296 ),
 ( #42807, #58882, #11666, #10988 ),
 ( #59222, #53639, #5734, #33007 ),
 ( #11323, #48392, #499, #32664 ),
 ( #53974, #6079, #50814, #7815 ),
 ( #18311, #13072, #60268, #3256 ),
 ( #18992, #2907, #28462, #7463 ) ),
 .UNSPECIFIED., .F., .F., .F.,
 ( 4, 1, 1, 1, 1, 4 ),
 ( 4, 4 ),
 ( 0.7453249619866000319, 0.7647058823529000460, 0.8235294117646999590, 0.8823529411764999830, 0.9411764705882000870, 0.9905820749711999884 ),
 ( -0.1830924788703000017, 1.182948957423999969 ),
 .UNSPECIFIED. ) ;
#47902=B_SPLINE_CURVE_WITH_KNOTS ( 'NONE', 3,
 ( #63243, #42966, #16045, #37376, #48903, #32145 ),
 .UNSPECIFIED., .F., .F.,
 ( 4, 2, 4 ),
 ( 0.000000000000000000, 0.5000000000000000000, 1.000000000000000000 ),
 .UNSPECIFIED. ) ;
#47903=CARTESIAN_POINT ( 'NONE',  ( 25.52344528808500002, -2.888780152759999886, -11.27718479156999898 ) ) ;
#47904=CARTESIAN_POINT ( 'NONE',  ( 25.46373029971899982, -8.354610197568000274, -8.148451206582999262 ) ) ;
#47912=DIRECTION ( 'NONE',  ( 0.000000000000000000, 0.000000000000000000, -1.000000000000000000 ) ) ;
#47922=CARTESIAN_POINT ( 'NONE',  ( 13.50003721581400029, 9.159934378815998812, 7.517910889891000537 ) ) ;
#47923=CARTESIAN_POINT ( 'NONE',  ( 11.79999998400527161, -11.58088844914904314, -1.772255231651884477 ) ) ;
#47930=CARTESIAN_POINT ( 'NONE',  ( 24.46580263708699832, 8.828315330680998940, 8.953816637776000675 ) ) ;
#47947=CARTESIAN_POINT ( 'NONE',  ( 18.28136615179828794, -11.72522190381090823, 3.796555440338472032 ) ) ;
#47960=ORIENTED_EDGE ( 'NONE', *, *, #62176, .F. ) ;
#47974=CARTESIAN_POINT ( 'NONE',  ( 24.08742282057739104, 9.230907236166416396, -9.184803071643798944 ) ) ;
#47976=CARTESIAN_POINT ( 'NONE',  ( 23.95226698060700343, 12.88010722568999888, -3.487952265340000135 ) ) ;
#47981=CARTESIAN_POINT ( 'NONE',  ( 13.42725895570834460, 12.36922847561466732, 1.970373770725430518 ) ) ;
#47985=CARTESIAN_POINT ( 'NONE',  ( 24.30001694968100168, 3.271769180623000040, -12.21048179117000032 ) ) ;
#47986=CARTESIAN_POINT ( 'NONE',  ( 17.86871151025999893, -3.252328409732000214, 11.33729656921000029 ) ) ;
#47998=EDGE_CURVE ( 'NONE', #31887, #65107, #29825, .T. ) ;
#47999=ORIENTED_EDGE ( 'NONE', *, *, #50235, .F. ) ;
#48002=CARTESIAN_POINT ( 'NONE',  ( 13.49980696792482959, 11.86896009962647724, 3.468589882356392540 ) ) ;
#48007=CARTESIAN_POINT ( 'NONE',  ( 18.26357047620399854, 11.66478987891999886, -3.865847705614000152 ) ) ;
#48012=CARTESIAN_POINT ( 'NONE',  ( 18.38480835425833249, 11.99871668716868989, -3.594320732042694644 ) ) ;
#48017=FACE_OUTER_BOUND ( 'NONE', #13236, .T. ) ;
#48026=ORIENTED_EDGE ( 'NONE', *, *, #50851, .F. ) ;
#48033=CARTESIAN_POINT ( 'NONE',  ( 16.22809631267600139, -3.350750460640000039, -11.21314580301999797 ) ) ;
#48043=ADVANCED_FACE ( 'NONE', ( #24208 ), #48459, .F. ) ;
#48047=CARTESIAN_POINT ( 'NONE',  ( 21.60000000000000142, 0.000000000000000000, 0.000000000000000000 ) ) ;
#48048=DIRECTION ( 'NONE',  ( 0.000000000000000000, -0.9630775332544029288, 0.2692241908533009043 ) ) ;
#48050=ORIENTED_EDGE ( 'NONE', *, *, #46572, .F. ) ;
#48051=CARTESIAN_POINT ( 'NONE',  ( 11.29996927726999978, -12.23272628844000032, -1.505586261403999870 ) ) ;
#48052=EDGE_CURVE ( 'NONE', #67920, #54071, #51312, .T. ) ;
#48063=CARTESIAN_POINT ( 'NONE',  ( 13.18179592083890483, 11.52326738618035940, 1.714065324702974458 ) ) ;
#48073=CARTESIAN_POINT ( 'NONE',  ( 24.46225035397799985, 11.93532144209000023, -3.254112264712999636 ) ) ;
#48075=ORIENTED_EDGE ( 'NONE', *, *, #24617, .T. ) ;
#48083=AXIS2_PLACEMENT_3D ( 'NONE', #41644, #58406, #5602 ) ;
#48085=FACE_OUTER_BOUND ( 'NONE', #28192, .T. ) ;
#48089=CARTESIAN_POINT ( 'NONE',  ( 13.60806600681794087, -12.33328427344383016, -2.183404734278298509 ) ) ;
#48090=VERTEX_POINT ( 'NONE', #31523 ) ;
#48102=B_SPLINE_CURVE_WITH_KNOTS ( 'NONE', 3,
 ( #27833, #49139, #42863, #16286, #11049, #16631, #37959, #11381, #27475, #50523 ),
 .UNSPECIFIED., .F., .F.,
 ( 4, 2, 2, 2, 4 ),
 ( 0.4999999998130718604, 0.6249999998598039230, 0.7499999999065358747, 0.8749999999532679373, 1.000000000000000000 ),
 .UNSPECIFIED. ) ;
#48105=CARTESIAN_POINT ( 'NONE',  ( 12.65912070212100105, -11.49976653515000002, 4.814127980893999847 ) ) ;
#48112=CARTESIAN_POINT ( 'NONE',  ( 25.40548364110799895, -11.40418634689999955, 3.013945778314000012 ) ) ;
#48116=CARTESIAN_POINT ( 'NONE',  ( 18.46577960219898173, -3.126461091541029358, 12.12859619074140838 ) ) ;
#48128=EDGE_CURVE ( 'NONE', #5569, #33837, #42364, .T. ) ;
#48135=ORIENTED_EDGE ( 'NONE', *, *, #5842, .F. ) ;
#48141=CARTESIAN_POINT ( 'NONE',  ( 11.53154461883053017, -12.41096831814673251, -1.687237690270050994 ) ) ;
#48143=CARTESIAN_POINT ( 'NONE',  ( 15.95279538704000366, -3.847565940079000324, -11.76597731123000123 ) ) ;
#48144=CARTESIAN_POINT ( 'NONE',  ( 11.75761329816000078, 11.49411629629000053, 1.653020190619000074 ) ) ;
#48146=CARTESIAN_POINT ( 'NONE',  ( 25.29989948031900227, 2.596966625103000137, -11.35305524894999962 ) ) ;
#48164=DIRECTION ( 'NONE',  ( 0.000000000000000000, 0.7614089499631907509, 0.6482718649732928107 ) ) ;
#48165=CARTESIAN_POINT ( 'NONE',  ( 23.89320776801300283, -8.283889223723997830, 7.778387373039001851 ) ) ;
#48169=CARTESIAN_POINT ( 'NONE',  ( 18.30000000000000071, 7.694584455362999620, -1.879999999999999893 ) ) ;
#48178=CARTESIAN_POINT ( 'NONE',  ( 17.92628954468417390, 3.345291551440209954, -11.86067033211894106 ) ) ;
#48181=CARTESIAN_POINT ( 'NONE',  ( 23.81910887196500326, -12.91783950482999899, 3.708435756594000043 ) ) ;
#48183=AXIS2_PLACEMENT_3D ( 'NONE', #19979, #9819, #41985 ) ;
#48184=EDGE_LOOP ( 'NONE', ( #54681, #5079, #34688, #43161, #60001, #38994, #63150, #53662, #5420, #42572, #65454, #45760, #2746, #57106, #46578, #20990, #63624, #8420, #1915, #60522, #38452, #8161, #39216, #55580, #2137, #39770, #64106 ) ) ;
#48198=DIRECTION ( 'NONE',  ( 1.000000000000000000, 0.000000000000000000, 0.000000000000000000 ) ) ;
#48201=CARTESIAN_POINT ( 'NONE',  ( 24.43231275843400141, 8.806084858360998524, -8.751970408576999816 ) ) ;
#48207=CARTESIAN_POINT ( 'NONE',  ( 17.60000001287599858, 11.53033693765999779, -4.891431908114999949 ) ) ;
#48208=CARTESIAN_POINT ( 'NONE',  ( 25.59997295081500113, -11.07537799752999952, 3.096069084855000320 ) ) ;
#48209=VERTEX_POINT ( 'NONE', #32222 ) ;
#48217=EDGE_CURVE ( 'NONE', #56420, #36190, #64694, .T. ) ;
#48223=CARTESIAN_POINT ( 'NONE',  ( 24.02092352968800171, 3.259160059610999749, 12.61376570420999954 ) ) ;
#48224=ORIENTED_EDGE ( 'NONE', *, *, #68111, .T. ) ;
#48236=ORIENTED_EDGE ( 'NONE', *, *, #19334, .F. ) ;
#48239=ORIENTED_EDGE ( 'NONE', *, *, #26439, .T. ) ;
#48252=CARTESIAN_POINT ( 'NONE',  ( 24.87149173865001472, -3.035096352711473600, 11.66330508788991516 ) ) ;
#48254=CARTESIAN_POINT ( 'NONE',  ( 11.64585080655600002, 12.33238363550000116, 1.848877788567000024 ) ) ;
#48260=EDGE_CURVE ( 'NONE', #60537, #29347, #11184, .T. ) ;
#48263=ORIENTED_EDGE ( 'NONE', *, *, #63645, .F. ) ;
#48270=AXIS2_PLACEMENT_3D ( 'NONE', #434, #32600, #59503 ) ;
#48282=CARTESIAN_POINT ( 'NONE',  ( 12.80000000000000071, -43.96540072520999587, 14.96704326274999985 ) ) ;
#48285=LINE ( 'NONE', #7016, #44193 ) ;
#48297=EDGE_CURVE ( 'NONE', #26090, #48851, #48977, .T. ) ;
#48300=CARTESIAN_POINT ( 'NONE',  ( 25.46371819568200223, 2.879482785682999868, 11.30954024936000124 ) ) ;
#48301=CARTESIAN_POINT ( 'NONE',  ( 18.02331223754164924, -3.318306765102383871, 11.16743751352547420 ) ) ;
#48311=CARTESIAN_POINT ( 'NONE',  ( 23.59999441188499958, 10.30760541648000128, -9.317696302454001156 ) ) ;
#48312=DIRECTION ( 'NONE',  ( 0.000000000000000000, 0.2588190451024934835, 0.9659258262890757507 ) ) ;
#48313=EDGE_CURVE ( 'NONE', #15051, #56866, #29543, .T. ) ;
#48322=EDGE_CURVE ( 'NONE', #8116, #36015, #33741, .T. ) ;
#48326=CARTESIAN_POINT ( 'NONE',  ( 18.44503807197100187, -2.664600154114999953, 11.39639460691000039 ) ) ;
#48329=CARTESIAN_POINT ( 'NONE',  ( 15.90018573812399971, 8.493548356068000516, 8.263529029821000904 ) ) ;
#48330=CARTESIAN_POINT ( 'NONE',  ( 13.09162860438300058, 11.49399796109000071, 1.653788228654999859 ) ) ;
#48334=AXIS2_PLACEMENT_3D ( 'NONE', #35021, #50401, #61918 ) ;
#48342=FACE_OUTER_BOUND ( 'NONE', #40093, .T. ) ;
#48345=CARTESIAN_POINT ( 'NONE',  ( 12.68129448069100107, 12.04903608036000051, -3.200077553391999619 ) ) ;
#48346=CARTESIAN_POINT ( 'NONE',  ( 18.28867698203100289, 11.62873132690000055, -4.501748577889000735 ) ) ;
#48350=CARTESIAN_POINT ( 'NONE',  ( 18.53493609108600282, -3.035043098171999798, 12.19104765307000093 ) ) ;
#48372=CARTESIAN_POINT ( 'NONE',  ( 11.29998578400000042, -3.824193979571000046, 11.71675423233000046 ) ) ;
#48376=ADVANCED_FACE ( 'NONE', ( #919 ), #16980, .T. ) ;
#48380=ADVANCED_FACE ( 'NONE', ( #64867 ), #12967, .T. ) ;
#48385=VERTEX_POINT ( 'NONE', #55088 ) ;
#48392=CARTESIAN_POINT ( 'NONE',  ( 24.98214874725099932, -11.60529347923999843, -3.133086993850000113 ) ) ;
#48396=CARTESIAN_POINT ( 'NONE',  ( 25.44993821361100217, -11.77655473258999841, -4.190794510628000680 ) ) ;
#48397=DIRECTION ( 'NONE',  ( 1.000000000000000000, 0.000000000000000000, 0.000000000000000000 ) ) ;
#48406=CARTESIAN_POINT ( 'NONE',  ( 15.39518154839200115, 8.837017240434999366, 7.949877004991000362 ) ) ;
#48407=EDGE_LOOP ( 'NONE', ( #30383, #39440, #67146, #59676, #38816, #5549 ) ) ;
#48412=VERTEX_POINT ( 'NONE', #39356 ) ;
#48419=CARTESIAN_POINT ( 'NONE',  ( 11.29998636608000062, -3.695122995756999984, 11.25914041192000070 ) ) ;
#48422=CARTESIAN_POINT ( 'NONE',  ( 24.30000000000000071, 3.224868684338999980, 12.03537377768999939 ) ) ;
#48427=CARTESIAN_POINT ( 'NONE',  ( 16.27269624719400198, 3.670072847095000146, 12.01573327568000060 ) ) ;
#48429=DIRECTION ( 'NONE',  ( 0.000000000000000000, -0.9421243786071877846, -0.3352635608502959608 ) ) ;
#48436=CARTESIAN_POINT ( 'NONE',  ( 17.82402932260216133, -11.54140372737312425, 4.865356140869725898 ) ) ;
#48438=CARTESIAN_POINT ( 'NONE',  ( 21.60000000000000142, 0.000000000000000000, 0.000000000000000000 ) ) ;
#48439=B_SPLINE_CURVE_WITH_KNOTS ( 'NONE', 3,
 ( #13699, #67848, #66475, #18599 ),
 .UNSPECIFIED., .F., .F.,
 ( 4, 4 ),
 ( 0.000000000000000000, 1.000000000000000000 ),
 .UNSPECIFIED. ) ;
#48456=CARTESIAN_POINT ( 'NONE',  ( 24.51228084553499897, -8.787217699239999291, -8.912727655930000381 ) ) ;
#48459=B_SPLINE_SURFACE_WITH_KNOTS ( 'NONE', 3, 3, ( 
 ( #35062, #8137, #39960, #51130 ),
 ( #24899, #40295, #61277, #67536 ),
 ( #62303, #3564, #45551, #61614 ),
 ( #19660, #28788, #55341, #46229 ),
 ( #13395, #44862, #40629, #66856 ),
 ( #34717, #56028, #3233, #45883 ),
 ( #61963, #35399, #40980, #14421 ),
 ( #50099, #2208, #4593, #58091 ),
 ( #25929, #46915, #5287, #26629 ),
 ( #63665, #57389, #47, #53189 ) ),
 .UNSPECIFIED., .F., .F., .F.,
 ( 4, 1, 1, 1, 1, 1, 1, 4 ),
 ( 4, 4 ),
 ( 0.04183311431308000400, 0.1428571428570999946, 0.2857142857143000203, 0.4285714285713999594, 0.5714285714286000406, 0.7142857142856999797, 0.8571428571429000609, 0.9292981235707000742 ),
 ( -0.1917799910644999994, 1.191756862851000021 ),
 .UNSPECIFIED. ) ;
#48460=AXIS2_PLACEMENT_3D ( 'NONE', #36835, #15510, #25304 ) ;
#48462=CARTESIAN_POINT ( 'NONE',  ( 18.36021383541356400, -3.331512994333476030, 12.07398673550533630 ) ) ;
#48463=ORIENTED_EDGE ( 'NONE', *, *, #59342, .F. ) ;
#48466=EDGE_CURVE ( 'NONE', #58398, #23213, #4484, .T. ) ;
#48470=EDGE_CURVE ( 'NONE', #23714, #62083, #52014, .T. ) ;
#48471=CARTESIAN_POINT ( 'NONE',  ( 13.49980696792482959, -11.86896009962648613, -3.468589882356420073 ) ) ;
#48474=ORIENTED_EDGE ( 'NONE', *, *, #66377, .T. ) ;
#48480=ORIENTED_EDGE ( 'NONE', *, *, #19012, .F. ) ;
#48486=EDGE_LOOP ( 'NONE', ( #30873, #20052, #12930, #26910, #59841 ) ) ;
#48487=CARTESIAN_POINT ( 'NONE',  ( 16.07476513888299863, -3.720976809451999934, -11.90233817890000090 ) ) ;
#48488=CARTESIAN_POINT ( 'NONE',  ( 11.84802180303800156, 11.72322844712000034, 1.964617572541000001 ) ) ;
#48495=ORIENTED_EDGE ( 'NONE', *, *, #50970, .F. ) ;
#48496=CARTESIAN_POINT ( 'NONE',  ( 15.96457203294418470, -8.635839794705725936, -7.819790491317134773 ) ) ;
#48499=CARTESIAN_POINT ( 'NONE',  ( 11.53935385204242436, 3.267863779230346211, -11.38835623221634741 ) ) ;
#48503=ORIENTED_EDGE ( 'NONE', *, *, #64818, .F. ) ;
#48505=FACE_OUTER_BOUND ( 'NONE', #59729, .T. ) ;
#48509=CARTESIAN_POINT ( 'NONE',  ( 16.10004050617000004, -3.886235259787000018, -11.90683839252000098 ) ) ;
#48518=ORIENTED_EDGE ( 'NONE', *, *, #4916, .F. ) ;
#48523=B_SPLINE_CURVE_WITH_KNOTS ( 'NONE', 3,
 ( #20086, #35825, #67283, #8569 ),
 .UNSPECIFIED., .F., .F.,
 ( 4, 4 ),
 ( 0.000000000000000000, 1.000000000000000000 ),
 .UNSPECIFIED. ) ;
#48525=CARTESIAN_POINT ( 'NONE',  ( 24.30000000000000071, 12.03537377768999939, -3.224868684338999980 ) ) ;
#48531=CARTESIAN_POINT ( 'NONE',  ( 18.26001156276199922, 2.811979134698999960, 11.55266638147999991 ) ) ;
#48542=CARTESIAN_POINT ( 'NONE',  ( 23.61700687049500047, -10.26325659442000138, -9.294095019069999353 ) ) ;
#48543=CARTESIAN_POINT ( 'NONE',  ( 24.21981597650900042, -9.186995683914000566, 9.646844606695998081 ) ) ;
#48544=CARTESIAN_POINT ( 'NONE',  ( 23.59999999999999787, -12.52456686791425966, 6.096434097048058831 ) ) ;
#48552=VERTEX_POINT ( 'NONE', #3317 ) ;
#48559=B_SPLINE_CURVE_WITH_KNOTS ( 'NONE', 3,
 ( #60044, #59012, #11115, #12154 ),
 .UNSPECIFIED., .F., .F.,
 ( 4, 4 ),
 ( 0.5000000000000044409, 1.000000000000000000 ),
 .UNSPECIFIED. ) ;
#48567=CARTESIAN_POINT ( 'NONE',  ( 24.46225079000999969, 12.39903786276999931, -3.098987673317000091 ) ) ;
#48568=CARTESIAN_POINT ( 'NONE',  ( 12.18555568849200021, -11.56145208044000050, 4.416819796118000241 ) ) ;
#48573=ORIENTED_EDGE ( 'NONE', *, *, #24217, .F. ) ;
#48589=CARTESIAN_POINT ( 'NONE',  ( 23.61437340957948194, 10.18034756477473124, 9.423219428857132485 ) ) ;
#48592=AXIS2_PLACEMENT_3D ( 'NONE', #26287, #20693, #62977 ) ;
#48598=CARTESIAN_POINT ( 'NONE',  ( 13.73732479921000049, 9.700721122729000001, 7.982825098500999417 ) ) ;
#48607=CARTESIAN_POINT ( 'NONE',  ( 11.80877518040099972, 12.11591042788000117, 2.033719807695000270 ) ) ;
#48615=AXIS2_PLACEMENT_3D ( 'NONE', #12907, #55206, #23390 ) ;
#48627=CARTESIAN_POINT ( 'NONE',  ( 17.84552287012977700, -3.595130221969362605, -11.99794414424696676 ) ) ;
#48642=CARTESIAN_POINT ( 'NONE',  ( 12.21312755196904298, -11.61418968116107386, 4.689146002353852261 ) ) ;
#48646=CARTESIAN_POINT ( 'NONE',  ( 24.38581055541800069, 3.342338751372999628, -12.19042545898000185 ) ) ;
#48650=CARTESIAN_POINT ( 'NONE',  ( 17.80000000009400196, -3.216307036143000175, 11.40341376487999980 ) ) ;
#48653=LINE ( 'NONE', #53554, #65590 ) ;
#48655=DIRECTION ( 'NONE',  ( -0.9999999999997783995, 6.656251822948856315E-07, -7.419225572296834004E-10 ) ) ;
#48671=CARTESIAN_POINT ( 'NONE',  ( 23.97710144266886090, 3.345395384879282119, -12.79000143593332695 ) ) ;
#48672=AXIS2_PLACEMENT_3D ( 'NONE', #48719, #50102, #2210 ) ;
#48673=CARTESIAN_POINT ( 'NONE',  ( 18.26087544840899923, -2.716371057353000218, 11.57326339378999869 ) ) ;
#48678=CARTESIAN_POINT ( 'NONE',  ( 13.38404792230800133, 11.55332361678999931, 1.871151989399000071 ) ) ;
#48686=B_SPLINE_CURVE_WITH_KNOTS ( 'NONE', 3,
 ( #45363, #39425, #60404, #12509 ),
 .UNSPECIFIED., .F., .F.,
 ( 4, 4 ),
 ( 0.000000000000000000, 1.000000000000000000 ),
 .UNSPECIFIED. ) ;
#48690=CARTESIAN_POINT ( 'NONE',  ( 21.00000012402669824, -12.42499880353999941, 0.000000000000000000 ) ) ;
#48698=ORIENTED_EDGE ( 'NONE', *, *, #38391, .F. ) ;
#48700=CARTESIAN_POINT ( 'NONE',  ( 18.53712219996399924, 11.93788271774999998, -3.912105503483000124 ) ) ;
#48704=CARTESIAN_POINT ( 'NONE',  ( 18.30830001818700126, -3.300182612895000478, 12.02694835946000040 ) ) ;
#48706=B_SPLINE_CURVE_WITH_KNOTS ( 'NONE', 3,
 ( #7305, #35265, #56239, #40167 ),
 .UNSPECIFIED., .F., .F.,
 ( 4, 4 ),
 ( 0.000000000000000000, 1.000000000000000000 ),
 .UNSPECIFIED. ) ;
#48707=EDGE_LOOP ( 'NONE', ( #40810, #12325, #35930, #60148 ) ) ;
#48713=CARTESIAN_POINT ( 'NONE',  ( 24.59180579038299896, 8.769928687672001288, -9.082967714861000630 ) ) ;
#48719=CARTESIAN_POINT ( 'NONE',  ( 23.56665676678700194, 0.000000000000000000, -3.819167204710999951E-13 ) ) ;
#48729=CARTESIAN_POINT ( 'NONE',  ( 16.42348875342600323, -3.378076265369000186, -11.11016813414000204 ) ) ;
#48731=AXIS2_PLACEMENT_3D ( 'NONE', #39888, #40908, #13325 ) ;
#48734=DIRECTION ( 'NONE',  ( 0.000000000000000000, -0.1807154286439995039, 0.9835354258236027603 ) ) ;
#48744=CARTESIAN_POINT ( 'NONE',  ( 25.44994642811700203, 2.930988785009999904E-14, 1.731947918414999972E-14 ) ) ;
#48745=DIRECTION ( 'NONE',  ( 0.000000000000000000, 0.9659258262890757507, -0.2588190451024927063 ) ) ;
#48752=CARTESIAN_POINT ( 'NONE',  ( 18.29999744860993616, 2.794302574217389701, 11.51706234583376087 ) ) ;
#48762=CARTESIAN_POINT ( 'NONE',  ( 25.31135467044800080, 11.20186433212000132, -3.316420822239999566 ) ) ;
#48766=AXIS2_PLACEMENT_3D ( 'NONE', #9973, #14879, #4714 ) ;
#48768=DIRECTION ( 'NONE',  ( 0.9999999999999762412, -2.179566601840950490E-07, 9.624126031003771506E-10 ) ) ;
#48773=FACE_OUTER_BOUND ( 'NONE', #62928, .T. ) ;
#48775=B_SPLINE_CURVE_WITH_KNOTS ( 'NONE', 3,
 ( #31900, #53213, #5995, #5315 ),
 .UNSPECIFIED., .F., .F.,
 ( 4, 4 ),
 ( 0.000000000000000000, 1.000000000000000000 ),
 .UNSPECIFIED. ) ;
#48776=AXIS2_PLACEMENT_3D ( 'NONE', #44632, #1968, #28546 ) ;
#48779=EDGE_CURVE ( 'NONE', #67055, #28653, #45371, .T. ) ;
#48786=CARTESIAN_POINT ( 'NONE',  ( 24.30000000000000071, 2.258942858049999725, -12.29419282279000036 ) ) ;
#48789=CARTESIAN_POINT ( 'NONE',  ( 25.08549383408500333, -2.791071255704999921, 11.47627186989000059 ) ) ;
#48791=ORIENTED_EDGE ( 'NONE', *, *, #53763, .F. ) ;
#48792=AXIS2_PLACEMENT_3D ( 'NONE', #16495, #28035, #58457 ) ;
#48803=CARTESIAN_POINT ( 'NONE',  ( 24.46225079000999969, -8.883320982495000351, -9.188387934989000527 ) ) ;
#48807=CARTESIAN_POINT ( 'NONE',  ( 18.14797787939609464, -3.506662021210539049, 12.02412632936538905 ) ) ;
#48811=B_SPLINE_CURVE_WITH_KNOTS ( 'NONE', 3,
 ( #38343, #11769, #54426, #6528 ),
 .UNSPECIFIED., .F., .F.,
 ( 4, 4 ),
 ( 0.000000000000000000, 1.000000000000000000 ),
 .UNSPECIFIED. ) ;
#48814=AXIS2_PLACEMENT_3D ( 'NONE', #810, #1500, #28074 ) ;
#48815=CARTESIAN_POINT ( 'NONE',  ( 13.49994651945300284, -12.07042783918999795, -2.492331243371999960 ) ) ;
#48833=DIRECTION ( 'NONE',  ( 0.000000000000000000, -0.8765967884314782577, -0.4812255921203881792 ) ) ;
#48836=CARTESIAN_POINT ( 'NONE',  ( 24.63611025208533789, 3.161149086942907527, -11.86231087104421356 ) ) ;
#48837=CARTESIAN_POINT ( 'NONE',  ( 25.22251911269240665, -8.509543809242357426, -8.058442543228641952 ) ) ;
#48841=ORIENTED_EDGE ( 'NONE', *, *, #33481, .T. ) ;
#48851=VERTEX_POINT ( 'NONE', #39273 ) ;
#48864=ORIENTED_EDGE ( 'NONE', *, *, #42524, .F. ) ;
#48865=FACE_OUTER_BOUND ( 'NONE', #54851, .T. ) ;
#48868=CARTESIAN_POINT ( 'NONE',  ( 11.71271957899600125, -12.11624328427999941, -2.031646723569000113 ) ) ;
#48874=DIRECTION ( 'NONE',  ( 0.000000000000000000, -0.2588190451024934835, -0.9659258262890757507 ) ) ;
#48875=CARTESIAN_POINT ( 'NONE',  ( 24.02034026765100094, 12.55451516185999949, 3.484863126418999979 ) ) ;
#48877=ORIENTED_EDGE ( 'NONE', *, *, #32625, .T. ) ;
#48887=CARTESIAN_POINT ( 'NONE',  ( 24.08772785482500112, -9.257913837711999605, -9.301533136437999616 ) ) ;
#48889=AXIS2_PLACEMENT_3D ( 'NONE', #66365, #18486, #38775 ) ;
#48891=B_SPLINE_SURFACE_WITH_KNOTS ( 'NONE', 3, 3, ( 
 ( #60135, #12244, #12588, #61171 ),
 ( #54890, #6990, #28321, #45098 ),
 ( #2104, #55585, #55236, #34617 ),
 ( #2436, #7688, #7333, #23763 ),
 ( #39502, #60825, #66407, #39851 ),
 ( #4141, #24108, #62868, #56953 ),
 ( #67091, #25135, #57630, #62532 ),
 ( #19203, #30062, #46467, #45441 ),
 ( #30392, #20233, #3798, #14651 ),
 ( #9733, #14986, #50685, #35968 ) ),
 .UNSPECIFIED., .F., .F., .F.,
 ( 4, 1, 1, 1, 1, 1, 1, 4 ),
 ( 4, 4 ),
 ( 0.04111222701784000150, 0.1428571428570999946, 0.2857142857143000203, 0.4285714285713999594, 0.5714285714286000406, 0.7142857142856999797, 0.8571428571429000609, 0.9278613184711000939 ),
 ( -0.1900620218102000158, 1.190128522698000069 ),
 .UNSPECIFIED. ) ;
#48892=ORIENTED_EDGE ( 'NONE', *, *, #67402, .F. ) ;
#48899=CARTESIAN_POINT ( 'NONE',  ( 25.19214439740800060, 2.891371816527999794, -11.44528675289000041 ) ) ;
#48903=CARTESIAN_POINT ( 'NONE',  ( 25.37957165016208450, 11.36922881883540803, -3.069087598897670244 ) ) ;
#48904=ORIENTED_EDGE ( 'NONE', *, *, #7422, .T. ) ;
#48912=CARTESIAN_POINT ( 'NONE',  ( 24.40628504395400000, 12.24027098590999962, -3.187905388597000123 ) ) ;
#48913=CARTESIAN_POINT ( 'NONE',  ( 11.91753023736700179, -11.77475711121000224, 4.379243463657999769 ) ) ;
#48917=CARTESIAN_POINT ( 'NONE',  ( 23.62017948775300269, 2.980885128520999849, 13.51681883505999870 ) ) ;
#48923=VERTEX_POINT ( 'NONE', #11654 ) ;
#48924=EDGE_CURVE ( 'NONE', #20236, #65247, #64531, .T. ) ;
#48927=CIRCLE ( 'NONE', #16526, 5.760713961201000544 ) ;
#48928=EDGE_CURVE ( 'NONE', #63789, #16959, #61223, .T. ) ;
#48931=ORIENTED_EDGE ( 'NONE', *, *, #49385, .F. ) ;
#48933=CARTESIAN_POINT ( 'NONE',  ( 24.63002439619599926, 0.000000000000000000, 0.000000000000000000 ) ) ;
#48936=CARTESIAN_POINT ( 'NONE',  ( 17.80000000005199823, 3.345268251980999974, 11.86064071431999878 ) ) ;
#48942=CARTESIAN_POINT ( 'NONE',  ( 27.25811388278000180, 0.000000000000000000, 0.000000000000000000 ) ) ;
#48944=CARTESIAN_POINT ( 'NONE',  ( 13.64506009312500190, 9.630614656729999723, 7.923290881757000470 ) ) ;
#48946=CIRCLE ( 'NONE', #66806, 1.000000000000000444 ) ;
#48953=CARTESIAN_POINT ( 'NONE',  ( 11.72764643456600098, 12.22218869479000070, 1.954421350659000023 ) ) ;
#48959=EDGE_LOOP ( 'NONE', ( #15210, #16206, #30244, #46764 ) ) ;
#48963=CARTESIAN_POINT ( 'NONE',  ( 30.60000000000000142, 0.000000000000000000, 0.000000000000000000 ) ) ;
#48972=ORIENTED_EDGE ( 'NONE', *, *, #1177, .T. ) ;
#48975=DIRECTION ( 'NONE',  ( 1.000000000000000000, 0.000000000000000000, 0.000000000000000000 ) ) ;
#48976=DIRECTION ( 'NONE',  ( 1.000000000000000000, 0.000000000000000000, 0.000000000000000000 ) ) ;
#48977=LINE ( 'NONE', #16461, #14063 ) ;
#48979=CARTESIAN_POINT ( 'NONE',  ( 11.53926573058028282, 12.16827677310549660, 1.947218181066149745 ) ) ;
#48982=CARTESIAN_POINT ( 'NONE',  ( 18.29983863916000075, -2.861762957209999847, 11.98830831200999825 ) ) ;
#48986=CARTESIAN_POINT ( 'NONE',  ( 11.30000285318000230, 11.76356368987999979, 1.428410073821000159 ) ) ;
#48989=CARTESIAN_POINT ( 'NONE',  ( 12.80000000000000071, 11.23412379136000006, -3.084957477885999833 ) ) ;
#48993=CARTESIAN_POINT ( 'NONE',  ( 18.41067102831979341, -3.015843532943014438, 11.25293825121027780 ) ) ;
#48998=CARTESIAN_POINT ( 'NONE',  ( 15.89994436294300151, 8.847904542234999781, 8.580301953175000662 ) ) ;
#49006=B_SPLINE_CURVE_WITH_KNOTS ( 'NONE', 3,
 ( #19649, #36064, #24199, #14065 ),
 .UNSPECIFIED., .F., .F.,
 ( 4, 4 ),
 ( 0.000000000000000000, 1.000000000000000000 ),
 .UNSPECIFIED. ) ;
#49013=ORIENTED_EDGE ( 'NONE', *, *, #30867, .T. ) ;
#49016=CARTESIAN_POINT ( 'NONE',  ( 24.09353084724989813, 3.337595895983183958, -12.57553257596956975 ) ) ;
#49017=CARTESIAN_POINT ( 'NONE',  ( 18.31386961183700279, -3.086648833569000328, 11.29009770192999973 ) ) ;
#49019=DIRECTION ( 'NONE',  ( 1.000000000000000000, 0.000000000000000000, 0.000000000000000000 ) ) ;
#49021=AXIS2_PLACEMENT_3D ( 'NONE', #41498, #62811, #14929 ) ;
#49024=VERTEX_POINT ( 'NONE', #19315 ) ;
#49030=ORIENTED_EDGE ( 'NONE', *, *, #67100, .F. ) ;
#49035=B_SPLINE_SURFACE_WITH_KNOTS ( 'NONE', 3, 3, ( 
 ( #39274, #65483, #65131, #38575 ),
 ( #49760, #59899, #44535, #33344 ),
 ( #49407, #54306, #60596, #17608 ),
 ( #22489, #55352, #7450, #49068 ),
 ( #28802, #50112, #44185, #3154 ),
 ( #45809, #67120, #6409, #27757 ),
 ( #1176, #14682, #25512, #20262 ),
 ( #20955, #42291, #47183, #10118 ),
 ( #15709, #67458, #52070, #36344 ) ),
 .UNSPECIFIED., .F., .F., .F.,
 ( 4, 1, 1, 1, 1, 1, 4 ),
 ( 4, 4 ),
 ( 0.05182816266979999725, 0.1666666666667000196, 0.3333333333333000081, 0.5000000000000000000, 0.6666666666667000474, 0.8333333333333000637, 0.9772240888782000034 ),
 ( -0.1900389547208000129, 1.190219847277000031 ),
 .UNSPECIFIED. ) ;
#49037=DIRECTION ( 'NONE',  ( 0.000000000000000000, 1.000000000000000000, -1.290201028711000169E-14 ) ) ;
#49052=DIRECTION ( 'NONE',  ( 0.000000000000000000, -0.2588190451024934280, -0.9659258262890756397 ) ) ;
#49053=DIRECTION ( 'NONE',  ( 1.000000000000000000, 0.000000000000000000, 4.770489558936215471E-13 ) ) ;
#49068=CARTESIAN_POINT ( 'NONE',  ( 11.56571517796000137, 3.339665324758999798, -11.82228365027999928 ) ) ;
#49070=CARTESIAN_POINT ( 'NONE',  ( 11.43344776364301474, -11.63114020343308752, -1.412330517650108197 ) ) ;
#49077=CARTESIAN_POINT ( 'NONE',  ( 25.52344582623700120, -8.321938514753998817, 8.140348312953999965 ) ) ;
#49085=FACE_OUTER_BOUND ( 'NONE', #47450, .T. ) ;
#49088=CARTESIAN_POINT ( 'NONE',  ( 13.55500032369700136, 12.12437004458000089, 2.498522620030000141 ) ) ;
#49090=CARTESIAN_POINT ( 'NONE',  ( 23.60205915885299888, 9.230633470673003771, 8.204162215335996322 ) ) ;
#49113=CARTESIAN_POINT ( 'NONE',  ( 15.95563772304700301, 3.878390400849000219, 11.75631652949000205 ) ) ;
#49116=CARTESIAN_POINT ( 'NONE',  ( 13.09019624054849551, -12.38961571551778640, -1.836606440307318788 ) ) ;
#49117=ORIENTED_EDGE ( 'NONE', *, *, #30747, .F. ) ;
#49120=CARTESIAN_POINT ( 'NONE',  ( 18.49944584006882309, -11.81600967868165775, 4.156020558874723214 ) ) ;
#49126=CARTESIAN_POINT ( 'NONE',  ( 24.37898897380600260, -3.167411416339000141, 12.03697664498000108 ) ) ;
#49127=ORIENTED_EDGE ( 'NONE', *, *, #49921, .T. ) ;
#49130=EDGE_CURVE ( 'NONE', #58398, #40087, #52793, .T. ) ;
#49139=CARTESIAN_POINT ( 'NONE',  ( 18.30000000002853255, 11.04996330603946930, -3.691231741019871837 ) ) ;
#49147=CARTESIAN_POINT ( 'NONE',  ( 23.85395670473670648, -3.593170000430095712, 13.20269580752050054 ) ) ;
#49148=CARTESIAN_POINT ( 'NONE',  ( 17.60000000000000142, 10.78295181803999903, -4.410266442048000002 ) ) ;
#49152=CARTESIAN_POINT ( 'NONE',  ( 23.89320776801300283, 8.928716006355012169, -8.952507060126997374 ) ) ;
#49164=EDGE_CURVE ( 'NONE', #21413, #1641, #42026, .T. ) ;
#49177=CARTESIAN_POINT ( 'NONE',  ( 16.39947726215000046, 3.188035298175999621, 11.45126509954999960 ) ) ;
#49180=CARTESIAN_POINT ( 'NONE',  ( 16.09997386696500143, -8.350085070477001992, -8.123950967096998710 ) ) ;
#49190=DIRECTION ( 'NONE',  ( 0.000000000000000000, 0.7614089499631908620, -0.6482718649732928107 ) ) ;
#49192=EDGE_LOOP ( 'NONE', ( #59119, #21065, #8069, #36374, #26938 ) ) ;
#49206=CARTESIAN_POINT ( 'NONE',  ( 11.84785375340600133, -12.11644693747000012, -2.030267990277999868 ) ) ;
#49214=CARTESIAN_POINT ( 'NONE',  ( 13.00000000001300116, -11.52577654661000039, -1.696746661728000038 ) ) ;
#49218=FACE_OUTER_BOUND ( 'NONE', #35683, .T. ) ;
#49222=CARTESIAN_POINT ( 'NONE',  ( 24.02105235195200095, -9.294045785069000587, -9.129243723463000393 ) ) ;
#49223=CARTESIAN_POINT ( 'NONE',  ( 23.64693289005300159, -10.02912268983000033, 9.634668899592000457 ) ) ;
#49225=CARTESIAN_POINT ( 'NONE',  ( 11.64596081258699911, -3.342173145742999729, 11.21570452027999920 ) ) ;
#49230=CARTESIAN_POINT ( 'NONE',  ( 15.90003771078200145, -3.695138809391000034, -11.25918926437999978 ) ) ;
#49233=CARTESIAN_POINT ( 'NONE',  ( 24.59232953626900198, 3.480949472584999871, -12.13588208332000029 ) ) ;
#49239=EDGE_LOOP ( 'NONE', ( #38621, #13364, #38680, #21173 ) ) ;
#49249=CARTESIAN_POINT ( 'NONE',  ( 11.95406170795600076, -11.84685177148000079, 3.896686237526999719 ) ) ;
#49256=EDGE_CURVE ( 'NONE', #7350, #45182, #5236, .T. ) ;
#49262=CARTESIAN_POINT ( 'NONE',  ( 23.66588327052700080, 13.24635834669000012, -3.906781946131000716 ) ) ;
#49265=ORIENTED_EDGE ( 'NONE', *, *, #31405, .F. ) ;
#49268=ORIENTED_EDGE ( 'NONE', *, *, #29423, .F. ) ;
#49269=CARTESIAN_POINT ( 'NONE',  ( 24.35365242081700288, 11.54878985765998500, 2.979915831562000239 ) ) ;
#49279=CARTESIAN_POINT ( 'NONE',  ( 13.64647714749800045, 9.589793698018000967, 7.972185502806999224 ) ) ;
#49285=VERTEX_POINT ( 'NONE', #17160 ) ;
#49288=CARTESIAN_POINT ( 'NONE',  ( 11.26490954471000094, 12.17992731521000138, 1.606774076355000025 ) ) ;
#49295=ORIENTED_EDGE ( 'NONE', *, *, #49256, .T. ) ;
#49298=CARTESIAN_POINT ( 'NONE',  ( 24.31006797060300073, -3.215953369236999926, -12.14991815011999954 ) ) ;
#49299=LINE ( 'NONE', #22728, #54409 ) ;
#49303=EDGE_CURVE ( 'NONE', #29214, #57373, #34990, .T. ) ;
#49308=ORIENTED_EDGE ( 'NONE', *, *, #1590, .T. ) ;
#49309=CARTESIAN_POINT ( 'NONE',  ( 18.40806533024301572, -3.252985697207277038, -12.09525697359445218 ) ) ;
#49313=CARTESIAN_POINT ( 'NONE',  ( 24.81043930399565056, 11.68078854696337920, 3.195146919645313943 ) ) ;
#49318=CARTESIAN_POINT ( 'NONE',  ( 24.07541249139060824, -9.249162196257124435, -9.196989795079192120 ) ) ;
#49321=CARTESIAN_POINT ( 'NONE',  ( 24.54687940532700097, -12.52318695592999909, 3.000795290450999797 ) ) ;
#49324=CARTESIAN_POINT ( 'NONE',  ( 24.51193165880900082, 3.518222998965000237, -12.24296030234999932 ) ) ;
#49335=CARTESIAN_POINT ( 'NONE',  ( 17.60000001072100062, -11.41073498373000028, 4.623967591968000335 ) ) ;
#49349=ORIENTED_EDGE ( 'NONE', *, *, #59134, .F. ) ;
#49355=CARTESIAN_POINT ( 'NONE',  ( 24.44496412535000118, -8.810486166165000910, -8.810507954003998776 ) ) ;
#49361=ORIENTED_EDGE ( 'NONE', *, *, #49797, .F. ) ;
#49368=CARTESIAN_POINT ( 'NONE',  ( 24.53428985367600390, -3.614319203926000146, 12.31267510079000083 ) ) ;
#49373=CARTESIAN_POINT ( 'NONE',  ( 13.99999999485600277, -9.471999751521998689, -8.194948195317001804 ) ) ;
#49385=EDGE_CURVE ( 'NONE', #40403, #29347, #29754, .T. ) ;
#49391=EDGE_CURVE ( 'NONE', #49620, #50564, #62801, .T. ) ;
#49393=CARTESIAN_POINT ( 'NONE',  ( 11.79999999550100220, 11.52577121388000059, 1.696750555870000010 ) ) ;
#49407=CARTESIAN_POINT ( 'NONE',  ( 11.75744248190100016, 3.642994321184000128, -12.02392698342999999 ) ) ;
#49419=CARTESIAN_POINT ( 'NONE',  ( 25.25777540049900338, -8.562684835218000501, 7.910837537672998465 ) ) ;
#49421=CARTESIAN_POINT ( 'NONE',  ( 25.47112424053799984, -11.11940461786000078, -3.299559200952000282 ) ) ;
#49423=CARTESIAN_POINT ( 'NONE',  ( 13.94806348789000161, -8.812672976752997656, -7.562028778248000016 ) ) ;
#49425=DIRECTION ( 'NONE',  ( 0.000000000000000000, 0.000000000000000000, -1.000000000000000000 ) ) ;
#49432=ORIENTED_EDGE ( 'NONE', *, *, #66052, .T. ) ;
#49435=EDGE_CURVE ( 'NONE', #10933, #8116, #35322, .T. ) ;
#49436=CARTESIAN_POINT ( 'NONE',  ( 15.36427412810700055, 8.819457004710999470, 7.692809699200999773 ) ) ;
#49442=CARTESIAN_POINT ( 'NONE',  ( 18.30003129334700063, 2.732683817159999862, -11.53064095410000078 ) ) ;
#49443=PLANE ( 'NONE',  #56336 ) ;
#49456=CARTESIAN_POINT ( 'NONE',  ( 11.80432898647400108, -11.49396319796999855, -1.654000935039000142 ) ) ;
#49462=CARTESIAN_POINT ( 'NONE',  ( 13.49994651945300284, 12.07042783918999795, 2.492331243371999960 ) ) ;
#49464=AXIS2_PLACEMENT_3D ( 'NONE', #48282, #39175, #17507 ) ;
#49467=CARTESIAN_POINT ( 'NONE',  ( 24.63407876950900288, 3.094019437545999729, 11.81700057174999863 ) ) ;
#49469=CARTESIAN_POINT ( 'NONE',  ( 24.85113725905400273, -3.384275653315000021, 11.84838802887999876 ) ) ;
#49471=EDGE_LOOP ( 'NONE', ( #4945, #56728, #67634, #20033 ) ) ;
#49498=DIRECTION ( 'NONE',  ( 0.000000000000000000, 0.9516614099929482373, -0.3071490855109836327 ) ) ;
#49505=CARTESIAN_POINT ( 'NONE',  ( 24.15442778489675035, -12.45811728158824749, -3.353956205876204688 ) ) ;
#49518=CARTESIAN_POINT ( 'NONE',  ( 23.60000000000000142, -9.305479840184000651, -8.315530346521999405 ) ) ;
#49519=CARTESIAN_POINT ( 'NONE',  ( 16.04649313145500145, 3.595593625533999749, 11.13765277391999931 ) ) ;
#49525=ADVANCED_FACE ( 'NONE', ( #34649 ), #55959, .F. ) ;
#49530=CARTESIAN_POINT ( 'NONE',  ( 23.85292906093700083, -13.16237798046000051, -3.534274979399000038 ) ) ;
#49533=CARTESIAN_POINT ( 'NONE',  ( 15.95309301929700219, -8.865091978629999758, -8.639514276306002216 ) ) ;
#49534=ORIENTED_EDGE ( 'NONE', *, *, #59257, .F. ) ;
#49536=AXIS2_PLACEMENT_3D ( 'NONE', #28747, #65779, #33986 ) ;
#49538=DIRECTION ( 'NONE',  ( -1.000000000000000000, 0.000000000000000000, 0.000000000000000000 ) ) ;
#49548=CARTESIAN_POINT ( 'NONE',  ( 11.25951067610000145, -12.19482939020999979, -1.501993453007000046 ) ) ;
#49554=CARTESIAN_POINT ( 'NONE',  ( 23.83530392115299890, 13.04092488338999978, 3.622230473245000137 ) ) ;
#49568=DIRECTION ( 'NONE',  ( 0.000000000000000000, -0.7418296051989918816, -0.6705884258248929752 ) ) ;
#49570=CARTESIAN_POINT ( 'NONE',  ( 24.25970375769299991, -8.928473527296000967, -8.811154394041999183 ) ) ;
#49572=CARTESIAN_POINT ( 'NONE',  ( 24.23190313298700360, -9.065335089760999665, 9.162789734983000756 ) ) ;
#49580=VERTEX_POINT ( 'NONE', #66107 ) ;
#49581=CARTESIAN_POINT ( 'NONE',  ( 25.25798305592800119, 2.569270360355000005, -11.37081726145000005 ) ) ;
#49597=CARTESIAN_POINT ( 'NONE',  ( 11.95023821374600104, -11.77429045505000005, 4.110796463462000006 ) ) ;
#49604=CARTESIAN_POINT ( 'NONE',  ( 23.79457325321444827, -9.731831237395766721, 9.426946816267429696 ) ) ;
#49608=ORIENTED_EDGE ( 'NONE', *, *, #38593, .T. ) ;
#49611=CARTESIAN_POINT ( 'NONE',  ( 24.03158892672100322, 13.13525790609000055, -3.279774679148000249 ) ) ;
#49616=CIRCLE ( 'NONE', #62973, 0.2000000000000004274 ) ;
#49618=CARTESIAN_POINT ( 'NONE',  ( 23.89320776801300283, 10.87822567738999346, 3.284864823361000941 ) ) ;
#49620=VERTEX_POINT ( 'NONE', #17532 ) ;
#49625=CARTESIAN_POINT ( 'NONE',  ( 23.89320776801300283, 2.594336453560998734, -11.06325219636999435 ) ) ;
#49627=CARTESIAN_POINT ( 'NONE',  ( 18.29840632282400037, -11.61484981121999915, 4.280299090734999368 ) ) ;
#49635=AXIS2_PLACEMENT_3D ( 'NONE', #18663, #39995, #13430 ) ;
#49639=CARTESIAN_POINT ( 'NONE',  ( 23.62003957313999791, -2.980470172838999954, 13.51719708605000037 ) ) ;
#49645=EDGE_CURVE ( 'NONE', #29376, #67920, #32002, .T. ) ;
#49650=CARTESIAN_POINT ( 'NONE',  ( 24.36958145701300182, -3.196690648311999894, -12.07804156775000060 ) ) ;
#49651=AXIS2_PLACEMENT_3D ( 'NONE', #61148, #26149, #31056 ) ;
#49659=ORIENTED_EDGE ( 'NONE', *, *, #1367, .T. ) ;
#49667=EDGE_LOOP ( 'NONE', ( #51876, #61574, #27822, #9901 ) ) ;
#49670=ADVANCED_FACE ( 'NONE', ( #65760 ), #64712, .T. ) ;
#49671=CARTESIAN_POINT ( 'NONE',  ( 24.17202345320177059, -9.108252266928689167, -9.092754609100827778 ) ) ;
#49674=CARTESIAN_POINT ( 'NONE',  ( 24.26682857568000173, -12.18233728966999863, 3.303852351893000083 ) ) ;
#49678=CARTESIAN_POINT ( 'NONE',  ( 13.55500032369700136, -12.12437004458000089, -2.498522620030000141 ) ) ;
#49679=ORIENTED_EDGE ( 'NONE', *, *, #51605, .T. ) ;
#49681=CARTESIAN_POINT ( 'NONE',  ( 17.60000000000000142, 10.78295181803999903, -4.410266442048000002 ) ) ;
#49683=CARTESIAN_POINT ( 'NONE',  ( 17.89269116643194479, -3.351202196788405807, -11.15759579123230338 ) ) ;
#49685=VERTEX_POINT ( 'NONE', #65411 ) ;
#49695=DIRECTION ( 'NONE',  ( -1.000000000000000000, 0.000000000000000000, 0.000000000000000000 ) ) ;
#49705=DIRECTION ( 'NONE',  ( 0.000000000000000000, 1.000000000000000000, 0.000000000000000000 ) ) ;
#49707=CARTESIAN_POINT ( 'NONE',  ( 18.50003594170800270, 2.686563649653999963, -11.33603604535000109 ) ) ;
#49708=EDGE_CURVE ( 'NONE', #33837, #63101, #56661, .T. ) ;
#49709=CARTESIAN_POINT ( 'NONE',  ( 24.44496488041000148, -12.03536727282999941, 3.224852091355999928 ) ) ;
#49712=CARTESIAN_POINT ( 'NONE',  ( 11.55275411606000269, 3.402594452619000176, -11.19752650018000040 ) ) ;
#49716=ORIENTED_EDGE ( 'NONE', *, *, #50188, .F. ) ;
#49718=EDGE_LOOP ( 'NONE', ( #45402, #38071, #9979, #43172, #54411, #31670, #59286, #44784, #61570, #63374, #69146, #15726, #4076, #43594, #52566, #1204, #28199, #33029, #31328, #8584, #25152 ) ) ;
#49722=CARTESIAN_POINT ( 'NONE',  ( 17.80000000009400196, 3.216307036143000175, 11.40341376487999980 ) ) ;
#49733=CARTESIAN_POINT ( 'NONE',  ( 23.66461408848299897, -3.237974624424999615, -13.42763586457999914 ) ) ;
#49752=EDGE_CURVE ( 'NONE', #39042, #51109, #13016, .T. ) ;
#49760=CARTESIAN_POINT ( 'NONE',  ( 11.80415302574500203, 3.641975138519000232, -12.02422332381999937 ) ) ;
#49768=AXIS2_PLACEMENT_3D ( 'NONE', #65390, #43396, #59459 ) ;
#49773=CARTESIAN_POINT ( 'NONE',  ( 25.20343629728800394, -8.548126091438000174, 7.997439774512999477 ) ) ;
#49775=VERTEX_POINT ( 'NONE', #24154 ) ;
#49778=CARTESIAN_POINT ( 'NONE',  ( 13.89314246895800231, -8.838637615320999785, -7.948101024408999571 ) ) ;
#49779=CARTESIAN_POINT ( 'NONE',  ( 24.63772188294200305, -8.684914509799000371, -8.585234952018000243 ) ) ;
#49793=CARTESIAN_POINT ( 'NONE',  ( 24.22569895090174086, -12.33866087468328132, 3.306132354845392030 ) ) ;
#49797=EDGE_CURVE ( 'NONE', #56062, #50502, #46494, .T. ) ;
#49809=DIRECTION ( 'NONE',  ( -1.000000000000000000, 0.000000000000000000, 0.000000000000000000 ) ) ;
#49810=CARTESIAN_POINT ( 'NONE',  ( 11.80890711774500090, -11.72268911462999874, -1.968096114907999628 ) ) ;
#49813=ORIENTED_EDGE ( 'NONE', *, *, #57512, .T. ) ;
#49822=CARTESIAN_POINT ( 'NONE',  ( 25.29883272499000313, -2.991636379912000265, 11.41426982500999898 ) ) ;
#49824=ORIENTED_EDGE ( 'NONE', *, *, #63215, .F. ) ;
#49843=VERTEX_POINT ( 'NONE', #19602 ) ;
#49851=CARTESIAN_POINT ( 'NONE',  ( 18.29998537156714633, -2.924732060074958007, -11.97422863287303407 ) ) ;
#49856=FACE_OUTER_BOUND ( 'NONE', #66269, .T. ) ;
#49889=CARTESIAN_POINT ( 'NONE',  ( 25.34046074233263823, 11.16058629745575814, 3.348985358652643463 ) ) ;
#49907=ORIENTED_EDGE ( 'NONE', *, *, #53316, .F. ) ;
#49912=DIRECTION ( 'NONE',  ( 0.7071058810608746859, 0.7071076813110745984, -3.975036265697858125E-09 ) ) ;
#49915=AXIS2_PLACEMENT_3D ( 'NONE', #15232, #11018, #37245 ) ;
#49919=CARTESIAN_POINT ( 'NONE',  ( 23.73668232013400115, -9.842998214831000681, 9.652221460371999129 ) ) ;
#49921=EDGE_CURVE ( 'NONE', #4160, #45907, #41156, .T. ) ;
#49933=DIRECTION ( 'NONE',  ( 0.000000000000000000, -0.9999830366945593463, -0.005824630728861762523 ) ) ;
#49935=CARTESIAN_POINT ( 'NONE',  ( 16.39999999379500295, 3.351248059343999941, 11.15756683833000018 ) ) ;
#49943=ORIENTED_EDGE ( 'NONE', *, *, #44678, .F. ) ;
#49950=ORIENTED_EDGE ( 'NONE', *, *, #6797, .F. ) ;
#49951=CARTESIAN_POINT ( 'NONE',  ( 23.60000648730661155, -10.25354231743684075, 9.380090008360967957 ) ) ;
#49953=ORIENTED_EDGE ( 'NONE', *, *, #4719, .T. ) ;
#49958=CARTESIAN_POINT ( 'NONE',  ( 24.63332959156766577, 8.756202931479766249, 7.455126439085037582 ) ) ;
#49965=ORIENTED_EDGE ( 'NONE', *, *, #18673, .T. ) ;
#49974=CARTESIAN_POINT ( 'NONE',  ( 18.26719328781100060, -11.65592881096000077, 3.892957952850000236 ) ) ;
#49991=EDGE_CURVE ( 'NONE', #35342, #32947, #9439, .T. ) ;
#49996=CARTESIAN_POINT ( 'NONE',  ( 17.80000000001300009, 3.351264566333000072, 11.15757590352999884 ) ) ;
#49998=EDGE_LOOP ( 'NONE', ( #50633, #47785, #38392 ) ) ;
#50001=CARTESIAN_POINT ( 'NONE',  ( 24.46275371508600216, -3.515554276222999874, -12.28676815851000015 ) ) ;
#50013=CARTESIAN_POINT ( 'NONE',  ( 13.49994651945300284, 12.07042783918999795, 2.492331243371999960 ) ) ;
#50014=CARTESIAN_POINT ( 'NONE',  ( 11.49999672495000169, -3.632761979779000061, 11.06912554803999882 ) ) ;
#50019=EDGE_LOOP ( 'NONE', ( #49013, #43409, #15827, #60198 ) ) ;
#50021=CARTESIAN_POINT ( 'NONE',  ( 24.22565958376758388, -9.032573813968939547, -9.032576340893927025 ) ) ;
#50023=CARTESIAN_POINT ( 'NONE',  ( 25.37956961487633833, 11.36923106309306775, 3.069084611032080190 ) ) ;
#50025=DIRECTION ( 'NONE',  ( 1.000000000000000000, 0.000000000000000000, 0.000000000000000000 ) ) ;
#50029=CARTESIAN_POINT ( 'NONE',  ( 13.46005557146100173, -12.04952288628000012, -2.412084176363999966 ) ) ;
#50045=CARTESIAN_POINT ( 'NONE',  ( 24.56046482271400322, 12.50678080147000060, 2.996392338889999785 ) ) ;
#50059=FACE_OUTER_BOUND ( 'NONE', #35960, .T. ) ;
#50060=DIRECTION ( 'NONE',  ( 1.000000000000000000, 0.000000000000000000, 0.000000000000000000 ) ) ;
#50063=CARTESIAN_POINT ( 'NONE',  ( 21.10000109091659937, 0.000000000000000000, 0.000000000000000000 ) ) ;
#50064=CARTESIAN_POINT ( 'NONE',  ( 11.48831242699000121, 3.364143239851999923, -11.30418287150000012 ) ) ;
#50067=CARTESIAN_POINT ( 'NONE',  ( 23.57776920565314427, -10.35458434377875747, 9.360247510821011474 ) ) ;
#50069=ADVANCED_FACE ( 'NONE', ( #66751 ), #3457, .T. ) ;
#50084=CARTESIAN_POINT ( 'NONE',  ( 23.83526264196600053, -3.383500917634999716, -13.10496161808000082 ) ) ;
#50088=CARTESIAN_POINT ( 'NONE',  ( 17.76396973669300294, -3.526704268670000086, 11.96114524401999901 ) ) ;
#50093=CARTESIAN_POINT ( 'NONE',  ( 13.00000000001300116, 11.52577654661000039, 1.696746661728000038 ) ) ;
#50099=CARTESIAN_POINT ( 'NONE',  ( 15.49162860438300271, -8.811474098792000831, -7.563394002770000846 ) ) ;
#50102=DIRECTION ( 'NONE',  ( -1.000000000000000000, 0.000000000000000000, 0.000000000000000000 ) ) ;
#50106=EDGE_CURVE ( 'NONE', #16959, #65259, #58598, .T. ) ;
#50112=CARTESIAN_POINT ( 'NONE',  ( 11.55259020248000112, 3.617313325735000085, -11.93403632987999963 ) ) ;
#50124=CARTESIAN_POINT ( 'NONE',  ( 25.18907900072800032, 11.36138750656000163, 3.216791237253000091 ) ) ;
#50125=ORIENTED_EDGE ( 'NONE', *, *, #75, .T. ) ;
#50128=FACE_OUTER_BOUND ( 'NONE', #52579, .T. ) ;
#50131=CARTESIAN_POINT ( 'NONE',  ( 25.40545359959300242, -8.312255038417999842, -8.369389122269998538 ) ) ;
#50135=ORIENTED_EDGE ( 'NONE', *, *, #30867, .F. ) ;
#50136=EDGE_CURVE ( 'NONE', #34308, #12604, #15675, .T. ) ;
#50143=CARTESIAN_POINT ( 'NONE',  ( 23.99449523565688125, -12.72126087833753338, 3.481288081613541419 ) ) ;
#50159=CARTESIAN_POINT ( 'NONE',  ( 23.50387503050299998, 0.000000000000000000, 0.000000000000000000 ) ) ;
#50160=CARTESIAN_POINT ( 'NONE',  ( 23.56666365135700403, 2.920993777382001166, 11.72568747150000412 ) ) ;
#50164=ORIENTED_EDGE ( 'NONE', *, *, #48466, .F. ) ;
#50175=ORIENTED_EDGE ( 'NONE', *, *, #29202, .T. ) ;
#50186=DIRECTION ( 'NONE',  ( 0.7070598748788616827, 0.000000000000000000, -0.7071536843828846175 ) ) ;
#50187=CARTESIAN_POINT ( 'NONE',  ( 23.56666365135700403, -12.07812737769999245, -3.551569042642998664 ) ) ;
#50188=EDGE_CURVE ( 'NONE', #29053, #37826, #51135, .T. ) ;
#50212=DIRECTION ( 'NONE',  ( 0.000000000000000000, -0.9421243786071880066, -0.3352635608502960718 ) ) ;
#50220=CARTESIAN_POINT ( 'NONE',  ( 16.18329442974999921, 3.298233714334000144, 11.32377282473999891 ) ) ;
#50230=CARTESIAN_POINT ( 'NONE',  ( 24.08756612923799878, -12.68456084474000001, -3.366943214815000029 ) ) ;
#50235=EDGE_CURVE ( 'NONE', #68269, #16464, #59412, .T. ) ;
#50237=FACE_OUTER_BOUND ( 'NONE', #43741, .T. ) ;
#50255=CARTESIAN_POINT ( 'NONE',  ( 18.05609597790000009, 3.343430715100999873, 11.12052764821000039 ) ) ;
#50259=CARTESIAN_POINT ( 'NONE',  ( 24.44496350777200178, -12.03536639536000052, -3.224849854974999985 ) ) ;
#50262=CARTESIAN_POINT ( 'NONE',  ( 24.67559771067699970, -12.15673408770999941, 3.025797809546999950 ) ) ;
#50265=EDGE_CURVE ( 'NONE', #66927, #35108, #29407, .T. ) ;
#50266=CARTESIAN_POINT ( 'NONE',  ( 11.40000482165000228, 7.371880883511000048E-13, 4.000966224993000022E-14 ) ) ;
#50267=CARTESIAN_POINT ( 'NONE',  ( 24.56046482271400322, 3.658438515550000325, 12.32938606307999940 ) ) ;
#50270=ORIENTED_EDGE ( 'NONE', *, *, #31881, .T. ) ;
#50273=EDGE_CURVE ( 'NONE', #30098, #13517, #14570, .T. ) ;
#50275=CARTESIAN_POINT ( 'NONE',  ( 23.59425252148539087, 3.210776961502446181, 13.60476513765082451 ) ) ;
#50283=EDGE_LOOP ( 'NONE', ( #37215, #51305, #42240, #32738 ) ) ;
#50291=B_SPLINE_CURVE_WITH_KNOTS ( 'NONE', 3,
 ( #18999, #62335, #66887, #56408, #46611, #18661 ),
 .UNSPECIFIED., .F., .F.,
 ( 4, 2, 4 ),
 ( 0.000000000000000000, 0.5000000000000000000, 1.000000000000000000 ),
 .UNSPECIFIED. ) ;
#50292=EDGE_CURVE ( 'NONE', #46963, #57158, #66106, .T. ) ;
#50294=AXIS2_PLACEMENT_3D ( 'NONE', #29751, #19231, #39885 ) ;
#50300=CARTESIAN_POINT ( 'NONE',  ( 24.72250368810516363, -11.76899691939735781, -3.190821781878062424 ) ) ;
#50305=ORIENTED_EDGE ( 'NONE', *, *, #55322, .F. ) ;
#50317=CARTESIAN_POINT ( 'NONE',  ( 25.60000000000000142, -8.527654132749999505, 7.260537518967999482 ) ) ;
#50324=CARTESIAN_POINT ( 'NONE',  ( 18.07669116111300056, -11.89294021643999955, 3.415331764990000352 ) ) ;
#50335=CARTESIAN_POINT ( 'NONE',  ( 23.55360225935400109, -3.060278671086000379, 13.69502875873999947 ) ) ;
#50336=AXIS2_PLACEMENT_3D ( 'NONE', #68198, #37771, #54190 ) ;
#50347=VECTOR ( 'NONE', #65408, 1000.000000000000000 ) ;
#50354=ORIENTED_EDGE ( 'NONE', *, *, #67687, .T. ) ;
#50357=EDGE_CURVE ( 'NONE', #61329, #64377, #1032, .T. ) ;
#50358=EDGE_CURVE ( 'NONE', #64677, #21396, #16276, .T. ) ;
#50359=CARTESIAN_POINT ( 'NONE',  ( 23.66004879239100234, 0.000000000000000000, 0.000000000000000000 ) ) ;
#50360=CARTESIAN_POINT ( 'NONE',  ( 25.30000327618300204, 10.36736154742121130, 5.168041346173475326 ) ) ;
#50361=CARTESIAN_POINT ( 'NONE',  ( 24.98034512773276816, 11.50384160472775896, 3.228646524593837608 ) ) ;
#50369=CARTESIAN_POINT ( 'NONE',  ( 24.43232361760200178, -11.98245802077999933, 3.250304477315000273 ) ) ;
#50374=ORIENTED_EDGE ( 'NONE', *, *, #31061, .T. ) ;
#50391=CARTESIAN_POINT ( 'NONE',  ( 24.44917776433500123, 12.41482580133999924, 3.103222239774000357 ) ) ;
#50397=ORIENTED_EDGE ( 'NONE', *, *, #8467, .T. ) ;
#50401=DIRECTION ( 'NONE',  ( -1.000000000000000000, 0.000000000000000000, 0.000000000000000000 ) ) ;
#50406=CARTESIAN_POINT ( 'NONE',  ( 11.35180279716000129, 3.678144743825999985, -11.20807767738999949 ) ) ;
#50412=DIRECTION ( 'NONE',  ( 3.942933415072992810E-06, -0.7070925352470988079, 0.7071210268279988220 ) ) ;
#50414=CARTESIAN_POINT ( 'NONE',  ( 23.56665676678199972, 13.31363904818000066, -4.296982115204999175 ) ) ;
#50417=VERTEX_POINT ( 'NONE', #63472 ) ;
#50421=CARTESIAN_POINT ( 'NONE',  ( 24.53428985175800037, 12.47024902693999948, -3.026245299674999778 ) ) ;
#50423=CARTESIAN_POINT ( 'NONE',  ( 23.62001255296500446, -2.979299042067999892, -13.51746985525000078 ) ) ;
#50426=CARTESIAN_POINT ( 'NONE',  ( 25.60000000000000142, 10.55164198324999880, 3.754898126455999741 ) ) ;
#50431=DIRECTION ( 'NONE',  ( 0.000000000000000000, -0.9466492601157001641, 0.3222656952305000266 ) ) ;
#50435=ADVANCED_FACE ( 'NONE', ( #15595 ), #44614, .F. ) ;
#50440=CARTESIAN_POINT ( 'NONE',  ( 23.60347242227338427, -13.39430291987660482, 3.981273882526325192 ) ) ;
#50450=EDGE_LOOP ( 'NONE', ( #7980, #59593, #25468, #37653, #41928 ) ) ;
#50453=CARTESIAN_POINT ( 'NONE',  ( 23.60000000000000142, -11.77655473258999841, 4.190794510628000680 ) ) ;
#50455=EDGE_CURVE ( 'NONE', #48923, #38467, #52159, .T. ) ;
#50457=DIRECTION ( 'NONE',  ( 0.000000000000000000, -0.7614089499631907509, 0.6482718649732929217 ) ) ;
#50462=CARTESIAN_POINT ( 'NONE',  ( 25.36444586457099959, 11.12587325612000022, 3.379815864972000039 ) ) ;
#50467=CARTESIAN_POINT ( 'NONE',  ( 25.09300670485700024, -8.442812854790998855, -8.583344465159997938 ) ) ;
#50468=CARTESIAN_POINT ( 'NONE',  ( 13.61451884198179663, -11.47057857663875424, -2.038550092594244134 ) ) ;
#50472=CONICAL_SURFACE ( 'NONE', #22566, 13.94232983116000035, 1.233427434088588903 ) ;
#50477=CARTESIAN_POINT ( 'NONE',  ( 24.79995638510570544, 3.079655890133128349, 11.72210376764452278 ) ) ;
#50494=VECTOR ( 'NONE', #28600, 1000.000000000000000 ) ;
#50498=CARTESIAN_POINT ( 'NONE',  ( 11.42387073792000152, -11.74429294849999827, -1.827310270344000065 ) ) ;
#50502=VERTEX_POINT ( 'NONE', #22034 ) ;
#50512=EDGE_LOOP ( 'NONE', ( #42625, #47609, #9631, #54328 ) ) ;
#50513=ORIENTED_EDGE ( 'NONE', *, *, #62055, .F. ) ;
#50520=CARTESIAN_POINT ( 'NONE',  ( 23.99165867875700187, 9.434723935140999274, -9.573197871853999175 ) ) ;
#50521=CARTESIAN_POINT ( 'NONE',  ( 18.44504292973000048, -2.664685748803000021, -11.39637496735000077 ) ) ;
#50523=CARTESIAN_POINT ( 'NONE',  ( 17.60000000000000142, 11.23412379136000006, -3.084957477885999833 ) ) ;
#50525=ORIENTED_EDGE ( 'NONE', *, *, #39142, .T. ) ;
#50542=CARTESIAN_POINT ( 'NONE',  ( 17.92628981779797570, -3.345291551605441782, -11.86067033226837530 ) ) ;
#50544=ORIENTED_EDGE ( 'NONE', *, *, #36134, .T. ) ;
#50561=DIRECTION ( 'NONE',  ( 0.000000000000000000, 0.000000000000000000, 1.000000000000000000 ) ) ;
#50564=VERTEX_POINT ( 'NONE', #60146 ) ;
#50569=CARTESIAN_POINT ( 'NONE',  ( 24.53428991195500330, 3.614319144953999530, 12.31267516478999902 ) ) ;
#50571=CARTESIAN_POINT ( 'NONE',  ( 24.37808886034967770, 8.911082506783134960, 9.054599869853928951 ) ) ;
#50572=CARTESIAN_POINT ( 'NONE',  ( 23.74058054779100146, -13.16199033518000050, -3.761701342105999935 ) ) ;
#50583=CARTESIAN_POINT ( 'NONE',  ( 23.84134220052430209, -3.319692114198800503, -13.04897312825259093 ) ) ;
#50585=EDGE_CURVE ( 'NONE', #13082, #1379, #49299, .T. ) ;
#50602=DIRECTION ( 'NONE',  ( -1.000000000000000000, 0.000000000000000000, 0.000000000000000000 ) ) ;
#50612=CARTESIAN_POINT ( 'NONE',  ( 25.44994642811700203, 0.000000000000000000, -2.282618538628999739E-13 ) ) ;
#50614=CARTESIAN_POINT ( 'NONE',  ( 17.60000000044533408, 11.94788429102075789, -3.252375031275762218 ) ) ;
#50629=CARTESIAN_POINT ( 'NONE',  ( 13.70003001321900271, -9.668726926528000476, -7.961868161445000425 ) ) ;
#50633=ORIENTED_EDGE ( 'NONE', *, *, #55741, .T. ) ;
#50642=CARTESIAN_POINT ( 'NONE',  ( 24.66906539831122558, -11.82198933512809802, -3.190506366364596058 ) ) ;
#50647=ORIENTED_EDGE ( 'NONE', *, *, #40876, .T. ) ;
#50650=B_SPLINE_CURVE_WITH_KNOTS ( 'NONE', 3,
 ( #37345, #41900, #15336, #21264, #58669, #53429 ),
 .UNSPECIFIED., .F., .F.,
 ( 4, 2, 4 ),
 ( 0.000000000000000000, 0.5000000000000000000, 1.000000000000000000 ),
 .UNSPECIFIED. ) ;
#50667=CARTESIAN_POINT ( 'NONE',  ( 17.56496177128000369, -11.49815673738000044, 4.817809077628999681 ) ) ;
#50669=CARTESIAN_POINT ( 'NONE',  ( 24.41555929959800153, -8.820896577839000940, 8.766783479516000455 ) ) ;
#50678=ORIENTED_EDGE ( 'NONE', *, *, #49645, .T. ) ;
#50681=CARTESIAN_POINT ( 'NONE',  ( 12.73341324600965585, -11.23412379136210681, 3.084957477879898935 ) ) ;
#50683=CARTESIAN_POINT ( 'NONE',  ( 24.08773761151700299, -3.426406091450999725, 12.66833900763000109 ) ) ;
#50685=CARTESIAN_POINT ( 'NONE',  ( 17.76910169249500271, 3.411882384414000047, -11.89794055422999897 ) ) ;
#50693=DIRECTION ( 'NONE',  ( -4.468466013035191386E-09, -0.2714605545367115846, 0.9624495661231402543 ) ) ;
#50700=ORIENTED_EDGE ( 'NONE', *, *, #54779, .F. ) ;
#50701=CARTESIAN_POINT ( 'NONE',  ( 25.57799081801000085, 8.344607266676000279, 8.013922886049000383 ) ) ;
#50715=CARTESIAN_POINT ( 'NONE',  ( 24.51228084510600169, -12.11225741719000126, 3.153589928299999734 ) ) ;
#50723=CARTESIAN_POINT ( 'NONE',  ( 23.58885776300258641, -2.922211427196971911, 13.61646868590587545 ) ) ;
#50725=VECTOR ( 'NONE', #39694, 1000.000000000000114 ) ;
#50729=CARTESIAN_POINT ( 'NONE',  ( 13.99999999270239570, -8.951333082579457923, -8.002096037671929452 ) ) ;
#50735=CARTESIAN_POINT ( 'NONE',  ( 15.89979320885400327, -3.824231472901999496, -11.71686814605000038 ) ) ;
#50736=CARTESIAN_POINT ( 'NONE',  ( 11.43328525708585630, 3.653536053513361637, -11.13242455109464046 ) ) ;
#50753=CARTESIAN_POINT ( 'NONE',  ( 11.53713315544000118, 3.620704573398000115, -11.03277391605000091 ) ) ;
#50763=CARTESIAN_POINT ( 'NONE',  ( 24.68355587878626523, 8.667372866500036466, 8.629868536354566189 ) ) ;
#50764=CARTESIAN_POINT ( 'NONE',  ( 12.79999999975700042, 11.86189249994999884, -3.298671769835999967 ) ) ;
#50768=ORIENTED_EDGE ( 'NONE', *, *, #25754, .F. ) ;
#50773=DIRECTION ( 'NONE',  ( 0.000000000000000000, -1.000000000000000000, 0.000000000000000000 ) ) ;
#50775=EDGE_CURVE ( 'NONE', #42540, #19870, #34434, .T. ) ;
#50776=CARTESIAN_POINT ( 'NONE',  ( 24.51038697288600332, -3.518813880144999739, -12.24495765776000056 ) ) ;
#50787=CARTESIAN_POINT ( 'NONE',  ( 18.29998537156716054, 2.924732060074958895, 11.97422863287303052 ) ) ;
#50798=B_SPLINE_CURVE_WITH_KNOTS ( 'NONE', 3,
 ( #12447, #50542, #60341, #18732, #2642, #55098, #49851, #1961 ),
 .UNSPECIFIED., .F., .F.,
 ( 4, 2, 2, 4 ),
 ( 0.000000000000000000, 0.5000000000000000000, 0.7500000000000000000, 1.000000000000000000 ),
 .UNSPECIFIED. ) ;
#50814=CARTESIAN_POINT ( 'NONE',  ( 24.84741819964900245, -11.95754057833999973, -2.993661166240999982 ) ) ;
#50816=CARTESIAN_POINT ( 'NONE',  ( 13.99974593105000231, -8.811008772734998828, -7.563940656188999689 ) ) ;
#50818=CARTESIAN_POINT ( 'NONE',  ( 25.47131263472500251, -8.417328722977000410, -7.979452786042999790 ) ) ;
#50821=VERTEX_POINT ( 'NONE', #39774 ) ;
#50824=ORIENTED_EDGE ( 'NONE', *, *, #7740, .F. ) ;
#50826=CARTESIAN_POINT ( 'NONE',  ( 24.44496351116800170, 3.224881296174999967, 12.03535797436000010 ) ) ;
#50828=CARTESIAN_POINT ( 'NONE',  ( 18.30003129332100187, 2.732683818840999646, 11.53064095373000164 ) ) ;
#50832=ORIENTED_EDGE ( 'NONE', *, *, #57561, .T. ) ;
#50843=DIRECTION ( 'NONE',  ( 0.000000000000000000, -0.2588190451024932059, 0.9659258262890756397 ) ) ;
#50844=CARTESIAN_POINT ( 'NONE',  ( 25.29987261392200182, 8.756202924575998026, -7.455126447192999883 ) ) ;
#50846=CARTESIAN_POINT ( 'NONE',  ( 24.25375554908000097, -12.19812635653999955, -3.308082274583000526 ) ) ;
#50851=EDGE_CURVE ( 'NONE', #12119, #5014, #55506, .T. ) ;
#50860=ORIENTED_EDGE ( 'NONE', *, *, #1062, .F. ) ;
#50863=CIRCLE ( 'NONE', #27401, 1.300177795737000874 ) ;
#50867=CARTESIAN_POINT ( 'NONE',  ( 18.44382898362900036, -2.795331802377000407, -11.36579223931000016 ) ) ;
#50878=VERTEX_POINT ( 'NONE', #50259 ) ;
#50881=DIRECTION ( 'NONE',  ( 0.000000000000000000, -0.1807154286440006141, 0.9835354258236025382 ) ) ;
#50892=DIRECTION ( 'NONE',  ( -5.700570686033077343E-06, 0.7070792536779096915, 0.7071343076006096906 ) ) ;
#50901=ORIENTED_EDGE ( 'NONE', *, *, #20787, .F. ) ;
#50904=CARTESIAN_POINT ( 'NONE',  ( 25.60000000000000142, 0.000000000000000000, 0.000000000000000000 ) ) ;
#50907=ORIENTED_EDGE ( 'NONE', *, *, #22102, .F. ) ;
#50912=CARTESIAN_POINT ( 'NONE',  ( 24.62769666370868293, 3.584151135403405242, 12.19978398757196203 ) ) ;
#50922=CARTESIAN_POINT ( 'NONE',  ( 23.59999462723899910, 13.22316330987000121, -4.267799687262000319 ) ) ;
#50925=CARTESIAN_POINT ( 'NONE',  ( 24.63328775060330855, 2.078227413906825305, 11.31065739981925766 ) ) ;
#50934=DIRECTION ( 'NONE',  ( -1.000000000000000000, 0.000000000000000000, 0.000000000000000000 ) ) ;
#50941=CARTESIAN_POINT ( 'NONE',  ( 24.96666885022796478, -8.756202917673951092, -7.455126455300256083 ) ) ;
#50946=CARTESIAN_POINT ( 'NONE',  ( 13.00000000009400303, -11.69118001589999878, -1.923222888683999932 ) ) ;
#50951=FACE_OUTER_BOUND ( 'NONE', #58910, .T. ) ;
#50954=DIRECTION ( 'NONE',  ( -1.000000000000000000, 0.000000000000000000, 0.000000000000000000 ) ) ;
#50956=CARTESIAN_POINT ( 'NONE',  ( 23.58665614796800014, 10.27456427064999822, 9.417482135191999504 ) ) ;
#50964=VECTOR ( 'NONE', #47817, 1000.000000000000000 ) ;
#50968=EDGE_CURVE ( 'NONE', #14810, #33733, #18448, .T. ) ;
#50970=EDGE_CURVE ( 'NONE', #39042, #59819, #39906, .T. ) ;
#50975=DIRECTION ( 'NONE',  ( 0.000000000000000000, 1.000000000000000000, 0.000000000000000000 ) ) ;
#50976=ORIENTED_EDGE ( 'NONE', *, *, #10420, .T. ) ;
#50977=CARTESIAN_POINT ( 'NONE',  ( 11.56571517796000137, -3.339665324758999798, 11.82228365027999928 ) ) ;
#50988=CARTESIAN_POINT ( 'NONE',  ( 17.60000000798000386, 11.41069016990000051, -4.623987642516999230 ) ) ;
#50989=EDGE_LOOP ( 'NONE', ( #37159, #7803, #38251 ) ) ;
#50992=CARTESIAN_POINT ( 'NONE',  ( 21.05000000000000426, 0.000000000000000000, 0.000000000000000000 ) ) ;
#50997=EDGE_CURVE ( 'NONE', #49024, #23104, #26033, .T. ) ;
#51002=CARTESIAN_POINT ( 'NONE',  ( 24.96666885018256821, -2.078227441565727140, 11.31065739473216070 ) ) ;
#51008=CARTESIAN_POINT ( 'NONE',  ( 17.95534550153200115, -3.277905616156999713, -11.84067279748999901 ) ) ;
#51019=DIRECTION ( 'NONE',  ( 0.000000000000000000, -0.4739929102870218958, 0.8805286599524397850 ) ) ;
#51021=CARTESIAN_POINT ( 'NONE',  ( 24.45387357698500352, -3.540473908871999864, 12.31800308314999981 ) ) ;
#51029=ORIENTED_EDGE ( 'NONE', *, *, #50273, .F. ) ;
#51039=AXIS2_PLACEMENT_3D ( 'NONE', #13943, #62842, #63181 ) ;
#51052=CARTESIAN_POINT ( 'NONE',  ( 25.26998262954836250, 11.52971071118044577, 2.996572855046998995 ) ) ;
#51053=CARTESIAN_POINT ( 'NONE',  ( 18.40015514469800095, 2.597921877622999464E-14, 2.051692149506999743E-13 ) ) ;
#51055=EDGE_CURVE ( 'NONE', #42427, #29053, #12752, .T. ) ;
#51057=CARTESIAN_POINT ( 'NONE',  ( 16.07905395910120916, 8.470000438687089073, 7.998963526368290111 ) ) ;
#51064=LINE ( 'NONE', #46164, #47424 ) ;
#51090=CARTESIAN_POINT ( 'NONE',  ( 23.56695564235076290, 13.34701990426062501, -4.193234373864223485 ) ) ;
#51096=CIRCLE ( 'NONE', #828, 11.50000000000000178 ) ;
#51097=CARTESIAN_POINT ( 'NONE',  ( 25.59997327719300131, 11.07537871057999901, 3.096068926251000164 ) ) ;
#51103=CARTESIAN_POINT ( 'NONE',  ( 24.71428570498787280, 8.651876458988047247, 8.603903068042686897 ) ) ;
#51109=VERTEX_POINT ( 'NONE', #41484 ) ;
#51114=CARTESIAN_POINT ( 'NONE',  ( 24.44496482743900145, 12.03536723905999928, -3.224852005146999989 ) ) ;
#51115=CARTESIAN_POINT ( 'NONE',  ( 15.57784398236293022, 9.457709274034840519, 8.211421075710344297 ) ) ;
#51130=CARTESIAN_POINT ( 'NONE',  ( 15.86087891924500148, -8.502609378008999741, -8.308114605954999732 ) ) ;
#51135=B_SPLINE_CURVE_WITH_KNOTS ( 'NONE', 3,
 ( #58320, #20921, #10079, #47845, #63560, #53767, #48178, #31764 ),
 .UNSPECIFIED., .F., .F.,
 ( 4, 2, 2, 4 ),
 ( 0.000000000000000000, 0.2499999999999974465, 0.4999999999999948930, 1.000000000000000000 ),
 .UNSPECIFIED. ) ;
#51142=CARTESIAN_POINT ( 'NONE',  ( 23.89320776801300283, 11.54071136931999852, -2.936967729253997295 ) ) ;
#51154=CARTESIAN_POINT ( 'NONE',  ( 24.63002439619599926, 0.000000000000000000, 0.000000000000000000 ) ) ;
#51164=CARTESIAN_POINT ( 'NONE',  ( 25.60000000000000142, -9.517611874540000017, -8.103398312166000039 ) ) ;
#51184=ORIENTED_EDGE ( 'NONE', *, *, #24388, .F. ) ;
#51193=ADVANCED_FACE ( 'NONE', ( #8899 ), #57918, .F. ) ;
#51194=CARTESIAN_POINT ( 'NONE',  ( 24.56046482271400322, -12.50678080147000060, -2.996392338889999785 ) ) ;
#51210=CARTESIAN_POINT ( 'NONE',  ( 24.03127491216000067, 9.408387437348000759, -9.735706541027999705 ) ) ;
#51211=CARTESIAN_POINT ( 'NONE',  ( 18.05609597790000009, -3.343430715100999873, -11.12052764821000039 ) ) ;
#51220=AXIS2_PLACEMENT_3D ( 'NONE', #42621, #63930, #52765 ) ;
#51221=CARTESIAN_POINT ( 'NONE',  ( 11.49977531252999974, 12.43119799159999950, 1.530013559959999991 ) ) ;
#51225=EDGE_CURVE ( 'NONE', #37494, #21235, #1844, .T. ) ;
#51233=CARTESIAN_POINT ( 'NONE',  ( 16.09997386696500143, 6.963621661623434989, 9.386500412226205015 ) ) ;
#51235=CARTESIAN_POINT ( 'NONE',  ( 17.92913687483821406, -3.216295279492294767, -11.40344415251901289 ) ) ;
#51236=EDGE_LOOP ( 'NONE', ( #36666, #20732, #20372, #4312 ) ) ;
#51254=B_SPLINE_CURVE_WITH_KNOTS ( 'NONE', 3,
 ( #43064, #64370, #16493, #10906 ),
 .UNSPECIFIED., .F., .F.,
 ( 4, 4 ),
 ( 0.000000000000000000, 1.000000000000000000 ),
 .UNSPECIFIED. ) ;
#51267=CARTESIAN_POINT ( 'NONE',  ( 23.91319693356835430, -3.340393349183891747, -12.90999628518435038 ) ) ;
#51282=CARTESIAN_POINT ( 'NONE',  ( 25.30000327618300204, -10.36736154742122018, 5.168041346173460227 ) ) ;
#51286=CARTESIAN_POINT ( 'NONE',  ( 15.39403162610500075, 9.133592062008998980, 8.216350050208999889 ) ) ;
#51287=CARTESIAN_POINT ( 'NONE',  ( 18.29991931957795259, -1.031823913341759950E-13, -12.32514597914127563 ) ) ;
#51291=CARTESIAN_POINT ( 'NONE',  ( 25.46375152665800101, -2.879425814940999917, -11.30951176145000048 ) ) ;
#51295=CARTESIAN_POINT ( 'NONE',  ( 24.62773497368900166, 3.462213745051000213, 12.08749688049000071 ) ) ;
#51305=ORIENTED_EDGE ( 'NONE', *, *, #45145, .T. ) ;
#51312=B_SPLINE_CURVE_WITH_KNOTS ( 'NONE', 3,
 ( #4251, #15782, #47947, #36769, #37112, #58426, #25589, #63316, #31871, #21367 ),
 .UNSPECIFIED., .F., .F.,
 ( 4, 2, 2, 2, 4 ),
 ( 0.5015528379108959989, 0.6261646284331719992, 0.7507764189554479994, 0.8753882094777239997, 1.000000000000000000 ),
 .UNSPECIFIED. ) ;
#51313=DIRECTION ( 'NONE',  ( 0.7070979648104197546, 0.000000000000000000, -0.7071155974527518762 ) ) ;
#51316=CARTESIAN_POINT ( 'NONE',  ( 17.10000000000000142, -3.470217030164000072, -11.92928724693999953 ) ) ;
#51350=CARTESIAN_POINT ( 'NONE',  ( 18.44495723965300016, -2.860707309908000262, -12.13834028902000028 ) ) ;
#51356=EDGE_LOOP ( 'NONE', ( #65680, #38709, #58159, #19983 ) ) ;
#51382=EDGE_CURVE ( 'NONE', #25292, #15838, #47660, .T. ) ;
#51383=ADVANCED_FACE ( 'NONE', ( #45375 ), #40133, .F. ) ;
#51390=EDGE_LOOP ( 'NONE', ( #69050, #35168, #64472, #23255 ) ) ;
#51396=CARTESIAN_POINT ( 'NONE',  ( 13.64731601457200050, -9.647116713587001513, -7.903424745186999445 ) ) ;
#51398=CARTESIAN_POINT ( 'NONE',  ( 15.49269116706029514, 8.815195450845969560, 7.616746626196044367 ) ) ;
#51404=CARTESIAN_POINT ( 'NONE',  ( 23.59999468372399889, -2.915558691838999739, 13.58549495651999983 ) ) ;
#51408=ORIENTED_EDGE ( 'NONE', *, *, #18509, .F. ) ;
#51419=B_SPLINE_CURVE_WITH_KNOTS ( 'NONE', 3,
 ( #54844, #55187, #66011, #32491, #7291, #6940 ),
 .UNSPECIFIED., .F., .F.,
 ( 4, 1, 1, 4 ),
 ( 0.000000000000000000, 0.2305484669808168796, 0.8346924774243514866, 1.000000000000000000 ),
 .UNSPECIFIED. ) ;
#51421=ORIENTED_EDGE ( 'NONE', *, *, #65073, .T. ) ;
#51426=CARTESIAN_POINT ( 'NONE',  ( 25.05004217274195000, -2.896626469317051811, -11.52364839812445396 ) ) ;
#51447=EDGE_CURVE ( 'NONE', #20805, #35599, #40457, .T. ) ;
#51455=CARTESIAN_POINT ( 'NONE',  ( 13.99999999308669629, 9.069400206872137105, 8.107642827045808076 ) ) ;
#51469=CARTESIAN_POINT ( 'NONE',  ( 23.61968394240093616, -13.40114650748445335, 3.921251161824122367 ) ) ;
#51471=EDGE_CURVE ( 'NONE', #68067, #59819, #14360, .T. ) ;
#51484=ADVANCED_FACE ( 'NONE', ( #36595 ), #25412, .T. ) ;
#51494=CARTESIAN_POINT ( 'NONE',  ( 23.61768885478876356, 13.40073015714643923, 3.927800159012043490 ) ) ;
#51502=EDGE_LOOP ( 'NONE', ( #33190, #331, #25514, #42651 ) ) ;
#51509=CARTESIAN_POINT ( 'NONE',  ( 11.35393384239835690, -12.19578912391865444, -1.764073091440432561 ) ) ;
#51510=ORIENTED_EDGE ( 'NONE', *, *, #45479, .F. ) ;
#51521=ADVANCED_FACE ( 'NONE', ( #25413 ), #10478, .F. ) ;
#51526=ADVANCED_FACE ( 'NONE', ( #53019 ), #15951, .T. ) ;
#51527=CARTESIAN_POINT ( 'NONE',  ( 13.99999999231800096, -8.833253877201999060, -7.896562762484000686 ) ) ;
#51534=CARTESIAN_POINT ( 'NONE',  ( 17.79229341877100268, 3.377812583009999869, 11.11021646535000151 ) ) ;
#51542=CARTESIAN_POINT ( 'NONE',  ( 24.98216315915700036, 8.515971576431999424, -8.483917917255999086 ) ) ;
#51543=CARTESIAN_POINT ( 'NONE',  ( 24.25866889917200098, 8.929925749802000823, -8.812657214412999096 ) ) ;
#51544=CARTESIAN_POINT ( 'NONE',  ( 18.35481756226800343, -2.723642650930000020, -11.47750709399999991 ) ) ;
#51555=CARTESIAN_POINT ( 'NONE',  ( 25.59997384872700010, 11.07537887597999848, -3.096069522331000190 ) ) ;
#51566=EDGE_CURVE ( 'NONE', #60441, #29347, #45190, .T. ) ;
#51575=CARTESIAN_POINT ( 'NONE',  ( 13.32922381500400100, -11.63215034022999994, -1.960198572322999988 ) ) ;
#51578=VERTEX_POINT ( 'NONE', #20856 ) ;
#51585=ORIENTED_EDGE ( 'NONE', *, *, #45927, .F. ) ;
#51586=CARTESIAN_POINT ( 'NONE',  ( 23.57244473461747702, 10.28737204536955119, 9.478197202474877514 ) ) ;
#51589=CARTESIAN_POINT ( 'NONE',  ( 16.39999997324030900, -3.261216865579173341, -11.32142606715090416 ) ) ;
#51593=DIRECTION ( 'NONE',  ( -1.000000000000000000, 0.000000000000000000, 0.000000000000000000 ) ) ;
#51600=CARTESIAN_POINT ( 'NONE',  ( 25.46373185538400463, 11.23406899464000119, 3.161078463958999496 ) ) ;
#51605=EDGE_CURVE ( 'NONE', #13349, #12119, #56082, .T. ) ;
#51613=CARTESIAN_POINT ( 'NONE',  ( 23.60000000000000142, -9.305479840184000651, -8.315530346521999405 ) ) ;
#51618=CARTESIAN_POINT ( 'NONE',  ( 25.30000327618300204, -9.659335867304687184, 6.394377797198702140 ) ) ;
#51619=ORIENTED_EDGE ( 'NONE', *, *, #35996, .T. ) ;
#51622=B_SPLINE_CURVE_WITH_KNOTS ( 'NONE', 3,
 ( #61073, #34166, #55484, #13191, #34521, #24698 ),
 .UNSPECIFIED., .F., .F.,
 ( 4, 1, 1, 4 ),
 ( 0.000000000000000000, 0.1550125199478044891, 0.7488612388459089386, 1.000000000000000000 ),
 .UNSPECIFIED. ) ;
#51623=CARTESIAN_POINT ( 'NONE',  ( 16.04718133169100014, 8.956716759973000208, 8.677900031540000114 ) ) ;
#51631=VECTOR ( 'NONE', #13555, 1000.000000000000114 ) ;
#51634=CARTESIAN_POINT ( 'NONE',  ( 24.70869262301700076, 3.610540981815000272, 12.15034266584999934 ) ) ;
#51636=CARTESIAN_POINT ( 'NONE',  ( 23.73963774284500161, 9.840645693113000192, 9.517990711560001316 ) ) ;
#51639=PLANE ( 'NONE',  #61744 ) ;
#51642=ORIENTED_EDGE ( 'NONE', *, *, #26275, .F. ) ;
#51653=DIRECTION ( 'NONE',  ( 0.000000000000000000, -0.9979288589194759140, 0.06432723012591848311 ) ) ;
#51660=ORIENTED_EDGE ( 'NONE', *, *, #65478, .T. ) ;
#51661=AXIS2_PLACEMENT_3D ( 'NONE', #30411, #57305, #36685 ) ;
#51684=CARTESIAN_POINT ( 'NONE',  ( 17.79165415090800195, -3.528207907415000122, -11.96069611418000100 ) ) ;
#51685=CARTESIAN_POINT ( 'NONE',  ( 24.43231275843600159, -8.806084858358998346, 8.751970408574999638 ) ) ;
#51696=CARTESIAN_POINT ( 'NONE',  ( 23.50387503050299998, 0.000000000000000000, 0.000000000000000000 ) ) ;
#51701=CARTESIAN_POINT ( 'NONE',  ( 25.55308368780314510, 2.866379683385739785, -11.19759676586897257 ) ) ;
#51714=EDGE_CURVE ( 'NONE', #63300, #12790, #48523, .T. ) ;
#51715=CARTESIAN_POINT ( 'NONE',  ( 24.95781766713999872, 8.510855470215000551, 8.989990260059000704 ) ) ;
#51719=CARTESIAN_POINT ( 'NONE',  ( 11.31919037786000182, -3.456300244116000453, 11.37193521011000108 ) ) ;
#51723=CARTESIAN_POINT ( 'NONE',  ( 24.37808886002350306, -12.29705476218489046, 3.189923891270713074 ) ) ;
#51733=CARTESIAN_POINT ( 'NONE',  ( 14.04809435262700035, -9.134678144910999720, -8.215103563399999587 ) ) ;
#51740=VERTEX_POINT ( 'NONE', #51221 ) ;
#51742=( BOUNDED_SURFACE ( )  B_SPLINE_SURFACE ( 3, 3, ( 
 ( #40051, #66599, #50187, #45970 ),
 ( #29217, #56810, #55433, #40378 ),
 ( #3313, #62046, #19051, #8566 ),
 ( #67279, #45637, #56463, #13482 ) ),
 .UNSPECIFIED., .F., .F., .T. ) 
 B_SPLINE_SURFACE_WITH_KNOTS ( ( 4, 4 ),
 ( 4, 4 ),
 ( 0.000000000000000000, 1.000000000000000000 ),
 ( 0.000000000000000000, 1.000000000000000000 ),
 .UNSPECIFIED. ) 
 GEOMETRIC_REPRESENTATION_ITEM ( )  RATIONAL_B_SPLINE_SURFACE ( (
 ( 1.512182578520000042, 1.160176301760999840, 1.160176301760999840, 1.512182578520000042),
 ( 1.111288591041000196, 0.8526025270081000196, 0.8526025270081000196, 1.111288591041000196),
 ( 1.111288591041000196, 0.8526025270081000196, 0.8526025270081000196, 1.111288591041000196),
 ( 1.512182578520000042, 1.160176301760999840, 1.160176301760999840, 1.512182578520000042) ) ) 
 REPRESENTATION_ITEM ( '' )  SURFACE ( )  );
#51756=CARTESIAN_POINT ( 'NONE',  ( 17.97872601847937801, 3.578425380680016588, -12.00298730842260930 ) ) ;
#51759=ORIENTED_EDGE ( 'NONE', *, *, #7477, .T. ) ;
#51760=CIRCLE ( 'NONE', #21612, 11.50000000000000533 ) ;
#51765=DIRECTION ( 'NONE',  ( 0.000000000000000000, 0.2588190451024934835, -0.9659258262890757507 ) ) ;
#51780=CIRCLE ( 'NONE', #28383, 1.300165623000000270 ) ;
#51783=CARTESIAN_POINT ( 'NONE',  ( 24.94500410606760710, 8.558268712512990817, 8.385800952028061417 ) ) ;
#51791=ORIENTED_EDGE ( 'NONE', *, *, #58641, .T. ) ;
#51793=CARTESIAN_POINT ( 'NONE',  ( 23.59999172237900211, -2.915589696762999949, -13.58550518520000061 ) ) ;
#51798=CARTESIAN_POINT ( 'NONE',  ( 17.60000000649198171, -11.44336891997908090, 3.156190330102982333 ) ) ;
#51808=CARTESIAN_POINT ( 'NONE',  ( 23.57258086761195415, -13.35170972070031681, 4.170319815648626083 ) ) ;
#51809=ORIENTED_EDGE ( 'NONE', *, *, #24869, .F. ) ;
#51811=PLANE ( 'NONE',  #19929 ) ;
#51816=DIRECTION ( 'NONE',  ( 0.000000000000000000, 0.000000000000000000, 1.000000000000000000 ) ) ;
#51818=CARTESIAN_POINT ( 'NONE',  ( 24.30001122380595291, 3.256147833935072899, 12.15210915319683060 ) ) ;
#51834=CIRCLE ( 'NONE', #7176, 1.000000000000000666 ) ;
#51836=CARTESIAN_POINT ( 'NONE',  ( 13.55563472374800149, -9.144188282469000839, -7.452974878633000344 ) ) ;
#51837=LINE ( 'NONE', #14786, #36507 ) ;
#51851=CARTESIAN_POINT ( 'NONE',  ( 11.79999999771000141, -12.39026187696000036, -1.832249219479999969 ) ) ;
#51855=EDGE_CURVE ( 'NONE', #18634, #33492, #11861, .T. ) ;
#51863=CARTESIAN_POINT ( 'NONE',  ( 16.24418116638901921, 3.625803901486591929, 11.98884806668391256 ) ) ;
#51864=FACE_OUTER_BOUND ( 'NONE', #19084, .T. ) ;
#51874=CARTESIAN_POINT ( 'NONE',  ( 18.04399228544049905, 11.57290723012127032, -4.790145353825725927 ) ) ;
#51876=ORIENTED_EDGE ( 'NONE', *, *, #35531, .T. ) ;
#51881=CARTESIAN_POINT ( 'NONE',  ( 24.95401031917199930, 8.513686805178998895, -8.994139667403999283 ) ) ;
#51888=EDGE_LOOP ( 'NONE', ( #10731, #42212, #60705, #35605 ) ) ;
#51894=CARTESIAN_POINT ( 'NONE',  ( 11.79999998109720849, 11.63601885445003425, 1.847750289993329131 ) ) ;
#51897=CARTESIAN_POINT ( 'NONE',  ( 13.73869549901200315, 8.889050979574999900, 7.612322772148999661 ) ) ;
#51904=ADVANCED_FACE ( 'NONE', ( #61705 ), #13822, .F. ) ;
#51911=EDGE_LOOP ( 'NONE', ( #12772, #45102, #19195, #65945 ) ) ;
#51935=DIRECTION ( 'NONE',  ( 5.839779914975694033E-06, 0.7070792670853635054, -0.7071342941930635062 ) ) ;
#51951=DIRECTION ( 'NONE',  ( -3.759177529598868022E-06, -0.7070924869988756134, -0.7071210750752756624 ) ) ;
#51956=CARTESIAN_POINT ( 'NONE',  ( 15.90000000000000036, 8.729799320959164888, 8.474717466972236934 ) ) ;
#51957=CARTESIAN_POINT ( 'NONE',  ( 23.61707908624700281, 13.18052050803000164, 4.240820030121000173 ) ) ;
#51978=EDGE_LOOP ( 'NONE', ( #33396, #13987, #45277, #15962, #66969 ) ) ;
#51982=ORIENTED_EDGE ( 'NONE', *, *, #9709, .T. ) ;
#51989=EDGE_LOOP ( 'NONE', ( #43254, #43943, #29666, #66758, #37724 ) ) ;
#51990=DIRECTION ( 'NONE',  ( 1.000000000000000000, 0.000000000000000000, 0.000000000000000000 ) ) ;
#52014=CIRCLE ( 'NONE', #21873, 13.98989063587000281 ) ;
#52019=AXIS2_PLACEMENT_3D ( 'NONE', #64228, #53414, #4816 ) ;
#52023=CARTESIAN_POINT ( 'NONE',  ( 18.35309301929700254, -2.844470671424999875, -12.04740840676999802 ) ) ;
#52029=VERTEX_POINT ( 'NONE', #9505 ) ;
#52030=EDGE_LOOP ( 'NONE', ( #26065, #6866, #63749, #48518 ) ) ;
#52036=EDGE_CURVE ( 'NONE', #38268, #28175, #29349, .T. ) ;
#52038=CARTESIAN_POINT ( 'NONE',  ( 23.61990947728800094, -13.19621614317000002, 4.178973957053000454 ) ) ;
#52041=ADVANCED_FACE ( 'NONE', ( #30847 ), #56652, .F. ) ;
#52045=CARTESIAN_POINT ( 'NONE',  ( 13.50007192468515704, 9.074936576711696290, 7.617865797329646860 ) ) ;
#52058=CARTESIAN_POINT ( 'NONE',  ( 23.60000000000000142, -2.548720605937000006, -12.21654710926000220 ) ) ;
#52070=CARTESIAN_POINT ( 'NONE',  ( 11.35564217374000329, 3.878722322503999731, -11.75620894677000017 ) ) ;
#52081=EDGE_CURVE ( 'NONE', #64580, #30607, #35156, .T. ) ;
#52093=CARTESIAN_POINT ( 'NONE',  ( 24.30000000000000071, -9.517611874540000017, 8.103398312166998352 ) ) ;
#52094=DIRECTION ( 'NONE',  ( 0.000000000000000000, 0.000000000000000000, -1.000000000000000000 ) ) ;
#52096=EDGE_CURVE ( 'NONE', #46284, #48412, #13492, .T. ) ;
#52099=CARTESIAN_POINT ( 'NONE',  ( 24.51039984485900192, -12.36383375972000209, -3.075091620974999884 ) ) ;
#52101=ORIENTED_EDGE ( 'NONE', *, *, #1524, .F. ) ;
#52104=CARTESIAN_POINT ( 'NONE',  ( 11.40010796094000334, 0.000000000000000000, -5.373479439185999994E-14 ) ) ;
#52105=EDGE_LOOP ( 'NONE', ( #36826, #66398, #10469, #25785, #21982 ) ) ;
#52120=CARTESIAN_POINT ( 'NONE',  ( 24.95270871331634410, -2.977372476727536466, 11.59851889212190024 ) ) ;
#52121=CARTESIAN_POINT ( 'NONE',  ( 24.67921321731900264, -3.567517257907000250, -12.13750614118000115 ) ) ;
#52127=CIRCLE ( 'NONE', #6358, 0.3000000000000000444 ) ;
#52131=ORIENTED_EDGE ( 'NONE', *, *, #32364, .T. ) ;
#52148=FACE_OUTER_BOUND ( 'NONE', #30121, .T. ) ;
#52150=VERTEX_POINT ( 'NONE', #68572 ) ;
#52158=CARTESIAN_POINT ( 'NONE',  ( 11.49999144015000319, 3.886253129992999877, -11.90689313971000018 ) ) ;
#52159=CIRCLE ( 'NONE', #23119, 7.720759220056002903 ) ;
#52161=CARTESIAN_POINT ( 'NONE',  ( 23.61661350339327115, -3.308521622829082354, 13.56940557538989545 ) ) ;
#52162=CARTESIAN_POINT ( 'NONE',  ( 23.55339688456600200, 3.057948053973999603, -13.69581934054999905 ) ) ;
#52165=ADVANCED_FACE ( 'NONE', ( #31534 ), #15455, .T. ) ;
#52177=CARTESIAN_POINT ( 'NONE',  ( 12.79999999975700042, -11.86189249994999884, 3.298671769835999967 ) ) ;
#52181=CARTESIAN_POINT ( 'NONE',  ( 13.60249209530700121, -8.943624754334001281, -7.827978252961999672 ) ) ;
#52187=EDGE_LOOP ( 'NONE', ( #17316, #58202, #67299, #29828 ) ) ;
#52188=CARTESIAN_POINT ( 'NONE',  ( 13.63045347340495539, 12.32568024774173310, 2.226002549926721308 ) ) ;
#52195=CARTESIAN_POINT ( 'NONE',  ( 17.80000000009400196, 3.216307036143000175, -11.40341376487999980 ) ) ;
#52200=CARTESIAN_POINT ( 'NONE',  ( 13.89309513285500230, 9.135233488911998379, 8.214486393748998694 ) ) ;
#52203=AXIS2_PLACEMENT_3D ( 'NONE', #45233, #7126, #55370 ) ;
#52208=CARTESIAN_POINT ( 'NONE',  ( 11.44750515593000095, -11.62256912479000093, -1.379235499629000161 ) ) ;
#52210=CARTESIAN_POINT ( 'NONE',  ( 24.51327040776200050, -12.11106229541000090, -3.153269560843000363 ) ) ;
#52211=CARTESIAN_POINT ( 'NONE',  ( 24.30000000000000071, -3.224868684338999980, 12.03537377768999939 ) ) ;
#52213=CARTESIAN_POINT ( 'NONE',  ( 12.52995381683800247, 11.92229088141000126, -3.300664210127000064 ) ) ;
#52216=AXIS2_PLACEMENT_3D ( 'NONE', #43137, #59212, #48734 ) ;
#52219=CARTESIAN_POINT ( 'NONE',  ( 17.79421883851900077, 3.253172350820999981, 11.33701189166999868 ) ) ;
#52222=ORIENTED_EDGE ( 'NONE', *, *, #22330, .F. ) ;
#52227=DIRECTION ( 'NONE',  ( 0.000000000000000000, 4.343333852296999816E-12, -1.000000000000000000 ) ) ;
#52228=CARTESIAN_POINT ( 'NONE',  ( 25.29571535093799994, 8.389559371064001070, -8.302794996009000172 ) ) ;
#52249=ADVANCED_FACE ( 'NONE', ( #20413 ), #62708, .T. ) ;
#52252=CARTESIAN_POINT ( 'NONE',  ( 25.46372189163300348, -2.879475976718999686, 11.30953721564000070 ) ) ;
#52259=CIRCLE ( 'NONE', #24425, 0.6999999999999992895 ) ;
#52260=CARTESIAN_POINT ( 'NONE',  ( 24.44496487975900223, 3.224879802562000464, -12.03535984693000138 ) ) ;
#52276=CARTESIAN_POINT ( 'NONE',  ( 23.60453139207830375, 10.14142216786711259, 9.612068792943430751 ) ) ;
#52290=CARTESIAN_POINT ( 'NONE',  ( 23.60224675149267881, -10.14893003115017223, 9.606056460203635794 ) ) ;
#52293=DIRECTION ( 'NONE',  ( 1.000000000000000000, 0.000000000000000000, 0.000000000000000000 ) ) ;
#52300=VERTEX_POINT ( 'NONE', #64078 ) ;
#52307=AXIS2_PLACEMENT_3D ( 'NONE', #30472, #10173, #62281 ) ;
#52312=EDGE_LOOP ( 'NONE', ( #6800, #48698, #44409, #58526 ) ) ;
#52313=CIRCLE ( 'NONE', #69077, 12.42499880353999941 ) ;
#52317=CARTESIAN_POINT ( 'NONE',  ( 15.64816728597000228, 9.503848651356001653, 8.217120907884000403 ) ) ;
#52322=CARTESIAN_POINT ( 'NONE',  ( 24.98632742932199946, -11.60054869656999976, 3.134150456063999890 ) ) ;
#52326=CARTESIAN_POINT ( 'NONE',  ( 24.30000000000000071, -9.289189189551001036, -7.908916752675001050 ) ) ;
#52328=ORIENTED_EDGE ( 'NONE', *, *, #59302, .T. ) ;
#52332=ORIENTED_EDGE ( 'NONE', *, *, #57512, .F. ) ;
#52338=ORIENTED_EDGE ( 'NONE', *, *, #56460, .F. ) ;
#52342=DIRECTION ( 'NONE',  ( 0.000000000000000000, 0.4815106998112011483, -0.8764402124317022258 ) ) ;
#52344=ORIENTED_EDGE ( 'NONE', *, *, #52081, .F. ) ;
#52345=CARTESIAN_POINT ( 'NONE',  ( 24.84554778200963909, -12.09423845806785103, -2.925021800096165414 ) ) ;
#52346=CARTESIAN_POINT ( 'NONE',  ( 15.89999719559887659, 8.538166969133406781, 8.218914602276583992 ) ) ;
#52349=ORIENTED_EDGE ( 'NONE', *, *, #49797, .T. ) ;
#52353=EDGE_CURVE ( 'NONE', #18634, #63477, #20900, .T. ) ;
#52354=CARTESIAN_POINT ( 'NONE',  ( 16.09997386696500143, -6.963621661623434100, -9.386500412226212120 ) ) ;
#52371=CARTESIAN_POINT ( 'NONE',  ( 18.46714228074024078, 2.893782244576861729, 11.28496185859599699 ) ) ;
#52372=CARTESIAN_POINT ( 'NONE',  ( 23.56666365135700403, -8.673757318211000822, 7.881093921744994901 ) ) ;
#52378=EDGE_LOOP ( 'NONE', ( #28038, #51619, #19942, #21618 ) ) ;
#52382=FACE_OUTER_BOUND ( 'NONE', #26839, .T. ) ;
#52387=CARTESIAN_POINT ( 'NONE',  ( 24.13682939974800234, -12.33401113332000065, 3.394273003449000292 ) ) ;
#52388=ADVANCED_FACE ( 'NONE', ( #48017 ), #52570, .F. ) ;
#52394=EDGE_CURVE ( 'NONE', #12823, #16567, #11633, .T. ) ;
#52407=ORIENTED_EDGE ( 'NONE', *, *, #50106, .F. ) ;
#52417=CARTESIAN_POINT ( 'NONE',  ( 11.36660992314014784, -3.674321412135250764, 11.19575788941673444 ) ) ;
#52419=CARTESIAN_POINT ( 'NONE',  ( 13.99944283128300171, -9.262889243704000464, -8.209791536961999370 ) ) ;
#52430=DIRECTION ( 'NONE',  ( 1.000000000000000000, 0.000000000000000000, 0.000000000000000000 ) ) ;
#52439=CARTESIAN_POINT ( 'NONE',  ( 11.79999999771000141, 12.39026187696000036, 1.832249219479999969 ) ) ;
#52443=CARTESIAN_POINT ( 'NONE',  ( 23.99446449805473947, -3.345746341642283017, 12.75763603700710291 ) ) ;
#52444=ADVANCED_FACE ( 'NONE', ( #11987 ), #27739, .F. ) ;
#52447=CARTESIAN_POINT ( 'NONE',  ( 25.57778428390800229, -2.768507693251000212, -11.23374941714000030 ) ) ;
#52454=ORIENTED_EDGE ( 'NONE', *, *, #26589, .T. ) ;
#52465=ORIENTED_EDGE ( 'NONE', *, *, #35553, .T. ) ;
#52470=B_SPLINE_CURVE_WITH_KNOTS ( 'NONE', 3,
 ( #48815, #48471, #37625, #924, #59991, #12101 ),
 .UNSPECIFIED., .F., .F.,
 ( 4, 2, 4 ),
 ( 0.000000000000000000, 0.5000000000000000000, 1.000000000000000000 ),
 .UNSPECIFIED. ) ;
#52471=DIRECTION ( 'NONE',  ( 0.000000000000000000, 1.000000000000000000, 0.000000000000000000 ) ) ;
#52478=VERTEX_POINT ( 'NONE', #50093 ) ;
#52493=B_SPLINE_CURVE_WITH_KNOTS ( 'NONE', 3,
 ( #27675, #59471, #33612, #22411, #64357, #1101, #22063, #59131, #11234, #32914 ),
 .UNSPECIFIED., .F., .F.,
 ( 4, 2, 2, 2, 4 ),
 ( 0.000000000000000000, 0.1249999999532679928, 0.2499999999065359857, 0.3749999998598039785, 0.4999999998130725265 ),
 .UNSPECIFIED. ) ;
#52495=EDGE_CURVE ( 'NONE', #35879, #49285, #33308, .T. ) ;
#52499=CARTESIAN_POINT ( 'NONE',  ( 11.30000000000000071, -11.91995122273334751, -1.454135469681903547 ) ) ;
#52514=AXIS2_PLACEMENT_3D ( 'NONE', #60909, #7074, #49037 ) ;
#52516=CARTESIAN_POINT ( 'NONE',  ( 11.50001436749000128, 11.64999275565999959, 4.104571566060999824E-10 ) ) ;
#52525=CARTESIAN_POINT ( 'NONE',  ( 13.46222979673600051, -9.132942286732999904, -7.608635239113000104 ) ) ;
#52528=CIRCLE ( 'NONE', #50294, 13.89999856298999958 ) ;
#52533=CARTESIAN_POINT ( 'NONE',  ( 13.60806600682073153, 12.33328427344333811, 2.183404734281086501 ) ) ;
#52535=VERTEX_POINT ( 'NONE', #54643 ) ;
#52537=CARTESIAN_POINT ( 'NONE',  ( 17.84632887396263001, 3.351233551899029717, -11.15758637348134208 ) ) ;
#52546=ORIENTED_EDGE ( 'NONE', *, *, #34689, .F. ) ;
#52549=ORIENTED_EDGE ( 'NONE', *, *, #66686, .T. ) ;
#52553=CARTESIAN_POINT ( 'NONE',  ( 24.35365242081699932, -8.885108761891000739, -7.331500822262997374 ) ) ;
#52558=CARTESIAN_POINT ( 'NONE',  ( 12.83560584653800163, 12.04942283913000090, -3.198386977700000244 ) ) ;
#52559=CARTESIAN_POINT ( 'NONE',  ( 18.22487142087599921, 11.55078329699999884, -4.188961560869000067 ) ) ;
#52563=CARTESIAN_POINT ( 'NONE',  ( 12.09999922233642522, -11.66744139996562701, 3.971920075675145156 ) ) ;
#52564=CARTESIAN_POINT ( 'NONE',  ( 18.26004861284300063, -2.925574202914999589, 11.93524904697000011 ) ) ;
#52566=ORIENTED_EDGE ( 'NONE', *, *, #22358, .T. ) ;
#52568=AXIS2_PLACEMENT_3D ( 'NONE', #29649, #56883, #40128 ) ;
#52570=PLANE ( 'NONE',  #69022 ) ;
#52572=CARTESIAN_POINT ( 'NONE',  ( 24.15442797605639669, 3.324447313803516213, 12.46602381067075527 ) ) ;
#52574=EDGE_CURVE ( 'NONE', #57654, #12746, #26620, .T. ) ;
#52579=EDGE_LOOP ( 'NONE', ( #15301, #50976, #58633, #69118, #35249 ) ) ;
#52588=CARTESIAN_POINT ( 'NONE',  ( 13.73849254682300192, 8.874722368053999944, 7.906926164786999500 ) ) ;
#52591=CARTESIAN_POINT ( 'NONE',  ( 17.80000000001300009, -3.351264566333000072, 11.15757590352999884 ) ) ;
#52599=CARTESIAN_POINT ( 'NONE',  ( 25.60000000000000142, 0.000000000000000000, 0.000000000000000000 ) ) ;
#52607=CARTESIAN_POINT ( 'NONE',  ( 13.08018231457700153, -11.57028798436999928, -1.758177683552999859 ) ) ;
#52615=CARTESIAN_POINT ( 'NONE',  ( 16.13712493497300215, 8.294738329384999886, 8.125890082391000746 ) ) ;
#52618=CARTESIAN_POINT ( 'NONE',  ( 23.61131147273417241, 10.12055327194686427, 9.627973054067471281 ) ) ;
#52621=DIRECTION ( 'NONE',  ( 0.000000000000000000, -0.9659258262890757507, 0.2588190451024934835 ) ) ;
#52630=CARTESIAN_POINT ( 'NONE',  ( 23.60956155030027759, -10.12579905328778374, 9.624114175715389408 ) ) ;
#52634=CARTESIAN_POINT ( 'NONE',  ( 11.79999999771000141, -12.39026187696000036, -1.832249219479999969 ) ) ;
#52639=ORIENTED_EDGE ( 'NONE', *, *, #26802, .F. ) ;
#52647=ADVANCED_FACE ( 'NONE', ( #66850 ), #60924, .F. ) ;
#52648=DIRECTION ( 'NONE',  ( 0.000000000000000000, 1.000000000000000000, 0.000000000000000000 ) ) ;
#52650=CARTESIAN_POINT ( 'NONE',  ( 23.50387503050299998, 0.000000000000000000, 0.000000000000000000 ) ) ;
#52657=CARTESIAN_POINT ( 'NONE',  ( 15.47616489729399980, 9.395071224208001226, 8.199988963223999505 ) ) ;
#52663=CARTESIAN_POINT ( 'NONE',  ( 25.58980682296600051, -11.09071036895000084, 3.239368791882000220 ) ) ;
#52669=CARTESIAN_POINT ( 'NONE',  ( 24.45366905783700062, 8.897659148319000622, 9.225340520377001141 ) ) ;
#52673=LINE ( 'NONE', #26109, #65066 ) ;
#52674=DIRECTION ( 'NONE',  ( 0.000000000000000000, -0.2588190451024934280, 0.9659258262890756397 ) ) ;
#52676=CARTESIAN_POINT ( 'NONE',  ( 18.26005557146100244, 2.925549590147000334, 11.93525498079000080 ) ) ;
#52687=CARTESIAN_POINT ( 'NONE',  ( 11.35194303199000032, -3.840151595817999919, 11.76830449990999838 ) ) ;
#52692=CARTESIAN_POINT ( 'NONE',  ( 16.29309513285500088, -3.300500509464999954, -11.83372189959999865 ) ) ;
#52698=CARTESIAN_POINT ( 'NONE',  ( 13.50000000000000178, 0.000000000000000000, 0.000000000000000000 ) ) ;
#52726=ORIENTED_EDGE ( 'NONE', *, *, #50997, .T. ) ;
#52731=EDGE_CURVE ( 'NONE', #4160, #48090, #11727, .T. ) ;
#52736=CARTESIAN_POINT ( 'NONE',  ( 23.91179595127900015, -12.75400041561000108, 3.592921910965999999 ) ) ;
#52747=CARTESIAN_POINT ( 'NONE',  ( 24.85114852451900092, 8.568860018262000722, 8.855052040836000060 ) ) ;
#52753=ORIENTED_EDGE ( 'NONE', *, *, #6797, .T. ) ;
#52756=B_SPLINE_CURVE_WITH_KNOTS ( 'NONE', 3,
 ( #35002, #22846, #60262, #59908, #28103, #64793 ),
 .UNSPECIFIED., .F., .F.,
 ( 4, 2, 4 ),
 ( 0.000000000000000000, 0.5000000000000000000, 1.000000000000000000 ),
 .UNSPECIFIED. ) ;
#52758=DIRECTION ( 'NONE',  ( -1.000000000000000000, 0.000000000000000000, 0.000000000000000000 ) ) ;
#52763=CIRCLE ( 'NONE', #21459, 11.85002173638999778 ) ;
#52765=DIRECTION ( 'NONE',  ( -1.000000000000000000, 0.000000000000000000, 0.000000000000000000 ) ) ;
#52768=CARTESIAN_POINT ( 'NONE',  ( 14.02341781689399980, -9.526752659074999130, -8.190681853965998016 ) ) ;
#52774=CARTESIAN_POINT ( 'NONE',  ( 24.70910065716694959, -11.78226157761774751, 3.190800174812568724 ) ) ;
#52783=CARTESIAN_POINT ( 'NONE',  ( 23.74058065684300090, 3.323266457502000115, 13.27946843520000009 ) ) ;
#52784=ORIENTED_EDGE ( 'NONE', *, *, #7137, .T. ) ;
#52785=CARTESIAN_POINT ( 'NONE',  ( 23.66004879239100234, 13.39256428908000096, 3.813547978107000080 ) ) ;
#52788=CARTESIAN_POINT ( 'NONE',  ( 11.53154451118193258, 12.41096832478124057, 1.687237643085517158 ) ) ;
#52790=ORIENTED_EDGE ( 'NONE', *, *, #36299, .T. ) ;
#52793=B_SPLINE_CURVE_WITH_KNOTS ( 'NONE', 3,
 ( #26641, #25941, #52161, #10204, #46928, #53198 ),
 .UNSPECIFIED., .F., .F.,
 ( 4, 2, 4 ),
 ( 0.000000000000000000, 0.5000000000000000000, 1.000000000000000000 ),
 .UNSPECIFIED. ) ;
#52794=CARTESIAN_POINT ( 'NONE',  ( 23.60000336544893074, -2.996612530978001843, 13.56986086524380930 ) ) ;
#52795=ADVANCED_FACE ( 'NONE', ( #36331 ), #26687, .F. ) ;
#52804=CARTESIAN_POINT ( 'NONE',  ( 13.00000000005200107, -12.15994572112000149, -2.000334444851999738 ) ) ;
#52806=DIRECTION ( 'NONE',  ( -0.000000000000000000, 0.5895247755844827964, 0.8077502949377767250 ) ) ;
#52807=CARTESIAN_POINT ( 'NONE',  ( 15.90003771078200145, 3.695138809391000034, 11.25918926437999978 ) ) ;
#52810=CARTESIAN_POINT ( 'NONE',  ( 25.59994555223600088, 0.6783951095376320461, -11.19994871957817573 ) ) ;
#52819=B_SPLINE_CURVE_WITH_KNOTS ( 'NONE', 3,
 ( #64206, #16666, #38337, #48836, #53048, #17364, #37990, #26828, #6521, #27510, #69119, #11417, #11083, #6169, #63865, #15979, #54072, #5493, #32759, #16321, #48146 ),
 .UNSPECIFIED., .F., .F.,
 ( 4, 2, 2, 1, 1, 2, 2, 2, 1, 2, 2, 4 ),
 ( 0.000000000000000000, 0.1249999999999699685, 0.1874999999999563127, 0.2187499999999506228, 0.2343749999999491240, 0.2421874999999520106, 0.2499999999999548694, 0.3749999999999629186, 0.4374999999999693023, 0.4687499999999714118, 0.4999999999999735767, 1.000000000000000000 ),
 .UNSPECIFIED. ) ;
#52828=CARTESIAN_POINT ( 'NONE',  ( 24.72545694048200104, 8.702406706990998941, 9.187175443698999189 ) ) ;
#52834=EDGE_CURVE ( 'NONE', #20902, #67055, #8402, .T. ) ;
#52840=CARTESIAN_POINT ( 'NONE',  ( 25.29987654162099986, -9.517611874540000017, -8.103398312166000039 ) ) ;
#52842=CARTESIAN_POINT ( 'NONE',  ( 12.57536348657924385, 11.53887048480315691, -4.871543742293567902 ) ) ;
#52852=FACE_OUTER_BOUND ( 'NONE', #43649, .T. ) ;
#52854=DIRECTION ( 'NONE',  ( 0.000000000000000000, -0.06400262754467088422, -0.9979497300302145879 ) ) ;
#52857=CARTESIAN_POINT ( 'NONE',  ( 23.68244710019300214, 3.146849026561000073, -13.35211358126000114 ) ) ;
#52863=CARTESIAN_POINT ( 'NONE',  ( 23.60000000000000142, -9.289189189551001036, -7.908916752675001050 ) ) ;
#52865=CARTESIAN_POINT ( 'NONE',  ( 25.60000000000000142, 8.527654132752997995, -7.260537518969999660 ) ) ;
#52872=EDGE_CURVE ( 'NONE', #22245, #61548, #48927, .T. ) ;
#52875=CARTESIAN_POINT ( 'NONE',  ( 24.03569645326925297, 9.310050201079944188, -9.237031074784450624 ) ) ;
#52877=CARTESIAN_POINT ( 'NONE',  ( 23.58681904253500150, 13.29342458620000045, -4.187351535191000451 ) ) ;
#52881=ORIENTED_EDGE ( 'NONE', *, *, #52872, .T. ) ;
#52882=CARTESIAN_POINT ( 'NONE',  ( 24.96666885024123417, 10.83443035737135851, -3.855530940255541772 ) ) ;
#52887=CARTESIAN_POINT ( 'NONE',  ( 17.79319863334400154, -3.315493116453000155, 11.22361396466000016 ) ) ;
#52891=CARTESIAN_POINT ( 'NONE',  ( 12.97447410014400226, 11.72278459482000024, 1.967342116188999679 ) ) ;
#52892=VERTEX_POINT ( 'NONE', #22307 ) ;
#52896=EDGE_CURVE ( 'NONE', #18236, #14432, #834, .T. ) ;
#52903=CARTESIAN_POINT ( 'NONE',  ( 18.30002258771995471, 11.69706282806914288, -3.884923957652766102 ) ) ;
#52907=CONICAL_SURFACE ( 'NONE', #31701, 12.42518024156999878, 0.7854126340177727261 ) ;
#52908=ORIENTED_EDGE ( 'NONE', *, *, #47610, .F. ) ;
#52909=CARTESIAN_POINT ( 'NONE',  ( 12.13343030045100157, 11.60886806805999960, -4.031065632098000506 ) ) ;
#52910=CARTESIAN_POINT ( 'NONE',  ( 17.61515110739400214, 11.44262809724999919, -4.698133467368000638 ) ) ;
#52915=CARTESIAN_POINT ( 'NONE',  ( 18.17677363193000062, -3.419785592864999835, 11.99291007725999947 ) ) ;
#52918=VERTEX_POINT ( 'NONE', #33505 ) ;
#52919=DIRECTION ( 'NONE',  ( 0.000000000000000000, 1.000000000000000000, 0.000000000000000000 ) ) ;
#52920=EDGE_CURVE ( 'NONE', #43147, #35517, #45594, .T. ) ;
#52937=CARTESIAN_POINT ( 'NONE',  ( 16.00249209530700156, -3.346223412964000055, -11.40475585647000045 ) ) ;
#52939=CARTESIAN_POINT ( 'NONE',  ( 25.59994555223599733, 10.55174472786000095, -3.754934689065000164 ) ) ;
#52943=DIRECTION ( 'NONE',  ( 2.186552006505935969E-10, 0.9979498542811704453, -0.06400069015401811667 ) ) ;
#52945=CARTESIAN_POINT ( 'NONE',  ( 11.79999999771000141, 12.39026187696000036, 1.832249219479999969 ) ) ;
#52958=DIRECTION ( 'NONE',  ( 0.3139086814191160424, 2.556637375876062946E-07, -0.9494531793246292484 ) ) ;
#52963=CARTESIAN_POINT ( 'NONE',  ( 25.60000000000000142, 9.517611874540000017, -8.103398312166000039 ) ) ;
#52965=ORIENTED_EDGE ( 'NONE', *, *, #21601, .T. ) ;
#52966=CARTESIAN_POINT ( 'NONE',  ( 13.09269116697131885, 11.52576810756814751, 1.696811579065023556 ) ) ;
#52968=CARTESIAN_POINT ( 'NONE',  ( 15.95296092448800174, 8.433319028468000411, 8.247373098099998856 ) ) ;
#52970=CARTESIAN_POINT ( 'NONE',  ( 16.39999999347100257, 3.345256695718999751, 11.86066175541999890 ) ) ;
#52972=CARTESIAN_POINT ( 'NONE',  ( 23.56665676678700194, 0.000000000000000000, -3.819167204710999951E-13 ) ) ;
#52976=CARTESIAN_POINT ( 'NONE',  ( 25.08549704953700044, 11.33427520304999980, -3.320998664874999839 ) ) ;
#52990=CARTESIAN_POINT ( 'NONE',  ( 24.03543903504724355, 12.65494737823116012, 3.444447339656595553 ) ) ;
#52996=DIRECTION ( 'NONE',  ( 1.000000000000000000, 0.000000000000000000, 0.000000000000000000 ) ) ;
#52998=LINE ( 'NONE', #51613, #44526 ) ;
#53001=CARTESIAN_POINT ( 'NONE',  ( 25.52346828417099900, 2.888732412976000141, 11.27716578594000119 ) ) ;
#53014=CARTESIAN_POINT ( 'NONE',  ( 15.40000000001299973, -8.815237407733999220, -7.616696375847999967 ) ) ;
#53019=FACE_OUTER_BOUND ( 'NONE', #60129, .T. ) ;
#53023=CARTESIAN_POINT ( 'NONE',  ( 21.72233714749290101, 0.000000000000000000, 0.000000000000000000 ) ) ;
#53028=CIRCLE ( 'NONE', #54170, 11.65000000000000036 ) ;
#53033=CARTESIAN_POINT ( 'NONE',  ( 24.30000564989370204, 3.240508264636430713, -12.09374148597397891 ) ) ;
#53039=EDGE_CURVE ( 'NONE', #8953, #47157, #12092, .T. ) ;
#53040=EDGE_CURVE ( 'NONE', #5919, #60348, #17689, .T. ) ;
#53046=CARTESIAN_POINT ( 'NONE',  ( 11.82333928233100018, 11.49420271256999904, 1.652349626741000055 ) ) ;
#53048=CARTESIAN_POINT ( 'NONE',  ( 24.65659773182258974, 3.152267499950374141, -11.84443715742482084 ) ) ;
#53049=CARTESIAN_POINT ( 'NONE',  ( 16.39999999347100257, -3.345256695718999751, -11.86066175541999890 ) ) ;
#53060=LINE ( 'NONE', #58298, #30685 ) ;
#53067=CARTESIAN_POINT ( 'NONE',  ( 17.89269116643086122, 3.351202196788891197, 11.15759579123215950 ) ) ;
#53081=VECTOR ( 'NONE', #55968, 1000.000000000000114 ) ;
#53097=CARTESIAN_POINT ( 'NONE',  ( 18.43329219593509549, -2.701919656448346974, -11.40083085748004876 ) ) ;
#53103=CARTESIAN_POINT ( 'NONE',  ( 17.60000000798000386, 11.41069016990000051, -4.623987642516999230 ) ) ;
#53114=ORIENTED_EDGE ( 'NONE', *, *, #58433, .F. ) ;
#53122=EDGE_CURVE ( 'NONE', #57489, #25637, #32544, .T. ) ;
#53129=ORIENTED_EDGE ( 'NONE', *, *, #2276, .T. ) ;
#53130=CARTESIAN_POINT ( 'NONE',  ( 25.60000000000000142, 0.000000000000000000, 0.000000000000000000 ) ) ;
#53131=EDGE_CURVE ( 'NONE', #12705, #10297, #52259, .T. ) ;
#53134=AXIS2_PLACEMENT_3D ( 'NONE', #57532, #9637, #30984 ) ;
#53140=CARTESIAN_POINT ( 'NONE',  ( 25.59037377391700119, -2.738633770010999502, -11.22408586312000089 ) ) ;
#53145=ORIENTED_EDGE ( 'NONE', *, *, #58642, .F. ) ;
#53158=B_SPLINE_CURVE_WITH_KNOTS ( 'NONE', 3,
 ( #63856, #62823, #10380, #41511, #52345, #25432 ),
 .UNSPECIFIED., .F., .F.,
 ( 4, 2, 4 ),
 ( 0.000000000000000000, 0.5000000000000000000, 1.000000000000000000 ),
 .UNSPECIFIED. ) ;
#53167=DIRECTION ( 'NONE',  ( 0.000000000000000000, 0.000000000000000000, -1.000000000000000000 ) ) ;
#53168=ORIENTED_EDGE ( 'NONE', *, *, #32364, .F. ) ;
#53186=CARTESIAN_POINT ( 'NONE',  ( 12.49459120399991896, 12.10614746208231551, -3.212001293532309454 ) ) ;
#53189=CARTESIAN_POINT ( 'NONE',  ( 15.37447410014400084, -8.836271409840000146, -7.950749727554001112 ) ) ;
#53191=CARTESIAN_POINT ( 'NONE',  ( 11.29996927726999978, -12.23272628844000032, -1.505586261403999870 ) ) ;
#53192=ORIENTED_EDGE ( 'NONE', *, *, #13975, .T. ) ;
#53198=CARTESIAN_POINT ( 'NONE',  ( 23.56665676678100141, -2.935523947847999970, 13.67844066972000050 ) ) ;
#53200=EDGE_LOOP ( 'NONE', ( #34231, #46213, #58705, #45123 ) ) ;
#53203=CARTESIAN_POINT ( 'NONE',  ( 25.00266768346542889, 3.413762979258133878, 11.76148390993455628 ) ) ;
#53204=CARTESIAN_POINT ( 'NONE',  ( 24.63002439619599926, 0.000000000000000000, 0.000000000000000000 ) ) ;
#53213=CARTESIAN_POINT ( 'NONE',  ( 24.30000564890097081, 8.853233220944831672, 8.853233220944831672 ) ) ;
#53214=CARTESIAN_POINT ( 'NONE',  ( 24.15442946601968188, 9.133667536019347111, -9.112066069742461139 ) ) ;
#53216=CARTESIAN_POINT ( 'NONE',  ( 24.51195772155200103, 12.36179148984999898, -3.074600399797000172 ) ) ;
#53223=FACE_OUTER_BOUND ( 'NONE', #31804, .T. ) ;
#53225=ORIENTED_EDGE ( 'NONE', *, *, #1823, .T. ) ;
#53226=DIRECTION ( 'NONE',  ( 0.000000000000000000, -0.1807154286440006141, -0.9835354258236025382 ) ) ;
#53228=CARTESIAN_POINT ( 'NONE',  ( 24.17206213204222820, 3.320420788054297745, -12.43428578304583354 ) ) ;
#53229=CARTESIAN_POINT ( 'NONE',  ( 17.96012107570599881, -3.168891391480999520, 11.45723209283999999 ) ) ;
#53247=CARTESIAN_POINT ( 'NONE',  ( 17.72554598058900055, 11.44503420830000096, -4.692817581925999626 ) ) ;
#53249=CARTESIAN_POINT ( 'NONE',  ( 18.30003129334700063, -2.732683817159999862, 11.53064095410000078 ) ) ;
#53253=CARTESIAN_POINT ( 'NONE',  ( 18.14390421667115305, 12.07230385407727447, -3.337096842113823847 ) ) ;
#53260=VECTOR ( 'NONE', #4828, 1000.000000000000000 ) ;
#53261=DIRECTION ( 'NONE',  ( 1.000000000000000000, 0.000000000000000000, 0.000000000000000000 ) ) ;
#53263=ADVANCED_FACE ( 'NONE', ( #46234 ), #51811, .F. ) ;
#53272=VERTEX_POINT ( 'NONE', #2545 ) ;
#53273=CIRCLE ( 'NONE', #13116, 12.52500000000000036 ) ;
#53281=CARTESIAN_POINT ( 'NONE',  ( 15.99015267864900203, -3.493241607194999876, -11.26524960718000123 ) ) ;
#53283=CARTESIAN_POINT ( 'NONE',  ( 19.89999890908300273, 0.000000000000000000, 0.000000000000000000 ) ) ;
#53292=FACE_OUTER_BOUND ( 'NONE', #50450, .T. ) ;
#53296=CARTESIAN_POINT ( 'NONE',  ( 25.57779415553899938, -11.11294835904000067, -3.219291969928999908 ) ) ;
#53302=CARTESIAN_POINT ( 'NONE',  ( 12.97415039705200179, 12.11604096695999999, 2.033011318524000188 ) ) ;
#53311=CARTESIAN_POINT ( 'NONE',  ( 16.04382898362900178, 8.457859886528000359, 8.090718092504999959 ) ) ;
#53316=EDGE_CURVE ( 'NONE', #68518, #27264, #40969, .T. ) ;
#53322=CARTESIAN_POINT ( 'NONE',  ( 21.60000012424471194, 3.970157536060000036E-13, 1.776356839399999796E-13 ) ) ;
#53326=CARTESIAN_POINT ( 'NONE',  ( 11.79999999471800010, -3.216299622513999701, 11.40340969442000052 ) ) ;
#53329=CARTESIAN_POINT ( 'NONE',  ( 23.58407651006106676, -10.21953228476464837, 9.544199785307510453 ) ) ;
#53336=B_SPLINE_SURFACE_WITH_KNOTS ( 'NONE', 3, 3, ( 
 ( #53982, #31638, #31299, #53302 ),
 ( #47720, #69033, #6084, #42471 ),
 ( #22168, #63082, #36533, #15207 ),
 ( #57858, #6778, #11673, #7469 ),
 ( #59920, #18319, #64805, #1893 ),
 ( #27778, #23212, #65152, #2239 ),
 ( #54680, #7825, #39642, #55725 ),
 ( #17976, #16916, #44209, #34059 ),
 ( #38957, #44893, #49088, #60274 ),
 ( #38247, #59574, #43851, #38597 ) ),
 .UNSPECIFIED., .F., .F., .F.,
 ( 4, 1, 1, 1, 1, 1, 1, 4 ),
 ( 4, 4 ),
 ( 0.07203983506772999867, 0.1428571428570999946, 0.2857142857143000203, 0.4285714285713999594, 0.5714285714286000406, 0.7142857142856999797, 0.8571428571429000609, 0.9589780836993999635 ),
 ( -0.1900620218102000158, 1.190128522698000069 ),
 .UNSPECIFIED. ) ;
#53339=ORIENTED_EDGE ( 'NONE', *, *, #44161, .F. ) ;
#53342=CARTESIAN_POINT ( 'NONE',  ( 18.32080262064242504, -12.02611605606520584, 3.500834971663305595 ) ) ;
#53344=CARTESIAN_POINT ( 'NONE',  ( 24.67921321864300310, 12.29514728640000065, 2.979192498689000157 ) ) ;
#53348=ORIENTED_EDGE ( 'NONE', *, *, #33142, .T. ) ;
#53349=CARTESIAN_POINT ( 'NONE',  ( 14.30000961100051704, 12.52500000000000036, 1.148724466519551595E-10 ) ) ;
#53363=CARTESIAN_POINT ( 'NONE',  ( 24.21998667016800155, 9.186813646192000249, 9.646745715273000954 ) ) ;
#53370=DIRECTION ( 'NONE',  ( -1.000000000000000000, 0.000000000000000000, 0.000000000000000000 ) ) ;
#53376=ORIENTED_EDGE ( 'NONE', *, *, #51714, .F. ) ;
#53378=AXIS2_PLACEMENT_3D ( 'NONE', #17882, #25529, #61557 ) ;
#53388=AXIS2_PLACEMENT_3D ( 'NONE', #11636, #816, #37184 ) ;
#53390=CARTESIAN_POINT ( 'NONE',  ( 15.95458079702100029, -3.771493919207000278, -11.78965436225000118 ) ) ;
#53393=ORIENTED_EDGE ( 'NONE', *, *, #63113, .T. ) ;
#53395=CARTESIAN_POINT ( 'NONE',  ( 24.63612635734461875, -8.692478787479979374, -8.668777295098667679 ) ) ;
#53397=ORIENTED_EDGE ( 'NONE', *, *, #68833, .T. ) ;
#53401=EDGE_CURVE ( 'NONE', #25637, #16938, #39977, .T. ) ;
#53408=CARTESIAN_POINT ( 'NONE',  ( 15.76350100824699929, -9.023747925888001120, -8.341981946770999912 ) ) ;
#53410=VERTEX_POINT ( 'NONE', #10883 ) ;
#53413=CARTESIAN_POINT ( 'NONE',  ( 23.60000000000000497, 0.9826074340704106236, 13.89473237476927459 ) ) ;
#53414=DIRECTION ( 'NONE',  ( 1.000000000000000000, 0.000000000000000000, 0.000000000000000000 ) ) ;
#53427=CARTESIAN_POINT ( 'NONE',  ( 23.57774090764768005, -10.35460453196024311, -9.360197169778087911 ) ) ;
#53429=CARTESIAN_POINT ( 'NONE',  ( 15.90003771078200145, 3.695138809391000034, 11.25918926437999978 ) ) ;
#53436=EDGE_CURVE ( 'NONE', #28950, #33864, #28883, .T. ) ;
#53439=CARTESIAN_POINT ( 'NONE',  ( 18.35295676019000055, 2.690485605734000085, -11.48482900035000043 ) ) ;
#53444=CARTESIAN_POINT ( 'NONE',  ( 11.83178351958400043, -3.316209711830000018, 11.22342786695999983 ) ) ;
#53446=DIRECTION ( 'NONE',  ( 0.000000000000000000, -0.9466492601157000530, 0.3222656952305000266 ) ) ;
#53451=B_SPLINE_CURVE_WITH_KNOTS ( 'NONE', 3,
 ( #30123, #18589, #39564, #60888, #24169, #35020 ),
 .UNSPECIFIED., .F., .F.,
 ( 4, 2, 4 ),
 ( 0.000000000000000000, 0.5000000000000000000, 1.000000000000000000 ),
 .UNSPECIFIED. ) ;
#53487=ORIENTED_EDGE ( 'NONE', *, *, #34379, .T. ) ;
#53494=CARTESIAN_POINT ( 'NONE',  ( 24.30000000000000071, -8.756202924575998026, 7.455126447192999883 ) ) ;
#53504=B_SPLINE_CURVE_WITH_KNOTS ( 'NONE', 3,
 ( #43911, #6489, #33768, #59978, #64516, #17330, #43562, #27480 ),
 .UNSPECIFIED., .F., .F.,
 ( 4, 2, 2, 4 ),
 ( 0.000000000000000000, 0.2500000000000018319, 0.5000000000000036637, 1.000000000000000000 ),
 .UNSPECIFIED. ) ;
#53518=EDGE_CURVE ( 'NONE', #43577, #25042, #41703, .T. ) ;
#53520=CARTESIAN_POINT ( 'NONE',  ( 11.36669567114815749, 11.69740569349575843, 1.420376822756192592 ) ) ;
#53523=EDGE_CURVE ( 'NONE', #66927, #30301, #68303, .T. ) ;
#53532=CARTESIAN_POINT ( 'NONE',  ( 12.74229120054512343, 12.11986439831269635, -3.159827838237255992 ) ) ;
#53535=CARTESIAN_POINT ( 'NONE',  ( 12.65361178023557009, 10.78680294140104046, -4.401676341640982315 ) ) ;
#53539=ORIENTED_EDGE ( 'NONE', *, *, #31188, .T. ) ;
#53542=CARTESIAN_POINT ( 'NONE',  ( 15.90000000000360991, 3.781197540827905712, 11.56430939782970668 ) ) ;
#53547=CARTESIAN_POINT ( 'NONE',  ( 24.45366336996499967, 3.540551434415999843, -12.31827634870000132 ) ) ;
#53550=DIRECTION ( 'NONE',  ( -1.000000000000000000, 0.000000000000000000, 0.000000000000000000 ) ) ;
#53554=CARTESIAN_POINT ( 'NONE',  ( 17.60000000000000142, -11.23412379136000006, 3.084957477885999833 ) ) ;
#53560=CARTESIAN_POINT ( 'NONE',  ( 24.56500367226799852, 12.27494567759000077, 3.065703875465999761 ) ) ;
#53562=ORIENTED_EDGE ( 'NONE', *, *, #22869, .F. ) ;
#53566=CARTESIAN_POINT ( 'NONE',  ( 13.55676532396020484, 12.34669046015806337, 2.106274408591566338 ) ) ;
#53571=CARTESIAN_POINT ( 'NONE',  ( 23.67740124563481174, 3.195736743838564209, -13.38333689704936091 ) ) ;
#53573=CARTESIAN_POINT ( 'NONE',  ( 18.38722619340700248, -3.117741388420999904, 11.18549237633000004 ) ) ;
#53578=DIRECTION ( 'NONE',  ( -1.000000000000000000, 0.000000000000000000, 0.000000000000000000 ) ) ;
#53579=CARTESIAN_POINT ( 'NONE',  ( 13.19211270977099915, 11.64284154253999937, 1.888701237101999997 ) ) ;
#53580=ORIENTED_EDGE ( 'NONE', *, *, #31205, .T. ) ;
#53583=CIRCLE ( 'NONE', #15652, 6.772075922005999615 ) ;
#53584=CARTESIAN_POINT ( 'NONE',  ( 24.54174074949149897, -12.46120270595140234, 3.023779783212969363 ) ) ;
#53589=CARTESIAN_POINT ( 'NONE',  ( 24.77780260647635657, -8.621837834250825949, 8.548044453014501443 ) ) ;
#53594=CARTESIAN_POINT ( 'NONE',  ( 12.27593309678900191, 11.75515418280000013, -3.561236062516000000 ) ) ;
#53595=CARTESIAN_POINT ( 'NONE',  ( 17.56813469587400434, 11.44347843772000139, -4.696234928490000904 ) ) ;
#53600=CARTESIAN_POINT ( 'NONE',  ( 18.04816728597000264, -3.610133590554000182, 12.03375048192000207 ) ) ;
#53613=B_SPLINE_CURVE_WITH_KNOTS ( 'NONE', 3,
 ( #47345, #57823, #57138, #19743 ),
 .UNSPECIFIED., .F., .F.,
 ( 4, 4 ),
 ( 0.000000000000000000, 1.000000000000000000 ),
 .UNSPECIFIED. ) ;
#53629=B_SPLINE_SURFACE_WITH_KNOTS ( 'NONE', 3, 3, ( 
 ( #9925, #20415, #9573, #24291 ),
 ( #3977, #62710, #35138, #62378 ),
 ( #56451, #62035, #29904, #40709 ),
 ( #8556, #35480, #52228, #8898 ),
 ( #30237, #51542, #41057, #25317 ),
 ( #57131, #41743, #9228, #51881 ),
 ( #30567, #63044, #46653, #59193 ),
 ( #27385, #10960, #48713, #58165 ) ),
 .UNSPECIFIED., .F., .F., .F.,
 ( 4, 1, 1, 1, 1, 4 ),
 ( 4, 4 ),
 ( 0.7452945369162999878, 0.7647058823529000460, 0.8235294117646999590, 0.8823529411764999830, 0.9411764705882000870, 0.9905759319504999771 ),
 ( -0.1831087563478999980, 1.182948900798000080 ),
 .UNSPECIFIED. ) ;
#53632=ORIENTED_EDGE ( 'NONE', *, *, #8103, .T. ) ;
#53637=DIRECTION ( 'NONE',  ( 1.000000000000000000, 0.000000000000000000, 0.000000000000000000 ) ) ;
#53639=CARTESIAN_POINT ( 'NONE',  ( 25.18910272528800220, -11.36135965050999985, -3.216800270569000197 ) ) ;
#53643=CARTESIAN_POINT ( 'NONE',  ( 11.49999672495000524, -7.851643750443679792, 8.692270414123820288 ) ) ;
#53651=CARTESIAN_POINT ( 'NONE',  ( 15.48018231457700189, 8.819832297131000587, 7.692419064155999742 ) ) ;
#53652=EDGE_CURVE ( 'NONE', #35693, #59934, #46662, .T. ) ;
#53656=EDGE_CURVE ( 'NONE', #60101, #26192, #52313, .T. ) ;
#53662=ORIENTED_EDGE ( 'NONE', *, *, #16250, .T. ) ;
#53669=CARTESIAN_POINT ( 'NONE',  ( 11.50001258332000020, 11.56502147876000031, 1.404302031979000054 ) ) ;
#53671=CARTESIAN_POINT ( 'NONE',  ( 24.39664234077866567, 3.224866613683543992, 12.03536604998859083 ) ) ;
#53675=CARTESIAN_POINT ( 'NONE',  ( 16.22798078375900133, 3.564332247067999671, 11.94996243427999971 ) ) ;
#53678=AXIS2_PLACEMENT_3D ( 'NONE', #61603, #46564, #25579 ) ;
#53698=CARTESIAN_POINT ( 'NONE',  ( 12.71479700542668922, -11.41062399033360819, 4.624005385416206870 ) ) ;
#53700=CARTESIAN_POINT ( 'NONE',  ( 24.53003472522700434, -8.771519074185000875, -8.897032352648000852 ) ) ;
#53705=EDGE_CURVE ( 'NONE', #33649, #45386, #43309, .T. ) ;
#53706=CARTESIAN_POINT ( 'NONE',  ( 24.02042701938200153, 9.295092309749000137, 9.129993563720001148 ) ) ;
#53707=ORIENTED_EDGE ( 'NONE', *, *, #49303, .F. ) ;
#53711=DIRECTION ( 'NONE',  ( 0.000000000000000000, -0.9466492601157001641, 0.3222656952305000266 ) ) ;
#53712=CARTESIAN_POINT ( 'NONE',  ( 25.46372779695100164, -11.23407511953000082, -3.161075425950000017 ) ) ;
#53721=CARTESIAN_POINT ( 'NONE',  ( 15.89999719559888369, -8.538166969133412110, -8.218914602276569781 ) ) ;
#53723=EDGE_LOOP ( 'NONE', ( #22287, #33033, #1981, #50525 ) ) ;
#53728=EDGE_LOOP ( 'NONE', ( #11268, #32679, #34849, #41197, #52222 ) ) ;
#53729=CARTESIAN_POINT ( 'NONE',  ( 16.15930817923600316, -3.787151970053999950, -11.97924296128000066 ) ) ;
#53730=CARTESIAN_POINT ( 'NONE',  ( 11.61719580513100247, 11.50344080059000085, 1.587150035090999722 ) ) ;
#53741=ADVANCED_FACE ( 'NONE', ( #63589 ), #4858, .T. ) ;
#53750=ORIENTED_EDGE ( 'NONE', *, *, #53401, .F. ) ;
#53753=CARTESIAN_POINT ( 'NONE',  ( 23.60205915885299888, -9.223492163361996177, 8.025915643364996299 ) ) ;
#53754=CARTESIAN_POINT ( 'NONE',  ( 25.60000000000000142, 0.000000000000000000, 0.000000000000000000 ) ) ;
#53757=CARTESIAN_POINT ( 'NONE',  ( 13.69997185827400266, -11.40547114375999982, -2.374390024598000082 ) ) ;
#53763=EDGE_CURVE ( 'NONE', #15051, #66838, #9131, .T. ) ;
#53764=CARTESIAN_POINT ( 'NONE',  ( 25.29989948031900227, 2.596966625103000137, -11.35305524894999962 ) ) ;
#53767=CARTESIAN_POINT ( 'NONE',  ( 18.05828166255868084, 3.296090596061254541, -11.87625419658844983 ) ) ;
#53773=CARTESIAN_POINT ( 'NONE',  ( 18.26087891924500184, 2.716433685251999908, 11.57325030293000090 ) ) ;
#53777=CARTESIAN_POINT ( 'NONE',  ( 18.31802873821099809, 2.927761598026000112, -11.42873208727000112 ) ) ;
#53780=CONICAL_SURFACE ( 'NONE', #62703, 11.34994642770999818, 0.7853934433896081480 ) ;
#53783=CARTESIAN_POINT ( 'NONE',  ( 19.89999890908300273, 0.000000000000000000, -12.52499975980204816 ) ) ;
#53789=CARTESIAN_POINT ( 'NONE',  ( 24.46275371508600216, 8.882876217567000410, -9.187943390846999847 ) ) ;
#53803=EDGE_LOOP ( 'NONE', ( #19100, #29871, #20552, #38555 ) ) ;
#53805=CARTESIAN_POINT ( 'NONE',  ( 12.46445792838400024, -11.52135921566999954, 4.763665720747999544 ) ) ;
#53809=CARTESIAN_POINT ( 'NONE',  ( 24.51040166152899857, 3.518808723585000298, 12.24493758046000025 ) ) ;
#53811=AXIS2_PLACEMENT_3D ( 'NONE', #55722, #12725, #39638 ) ;
#53812=CARTESIAN_POINT ( 'NONE',  ( 24.32158544041289261, 12.72716532455095972, 3.095239629920860214 ) ) ;
#53813=B_SPLINE_CURVE_WITH_KNOTS ( 'NONE', 3,
 ( #37043, #68151, #31122, #9423, #4180, #24832, #63597, #52774, #31456, #36702, #19588, #67808, #3832, #4869, #46159, #62231, #62905, #9089, #35672, #47191, #56986 ),
 .UNSPECIFIED., .F., .F.,
 ( 4, 2, 2, 1, 1, 2, 2, 2, 1, 2, 2, 4 ),
 ( 0.000000000000000000, 0.1250000000000654754, 0.1875000000000969225, 0.2187500000001172396, 0.2343750000001220968, 0.2421875000001264266, 0.2500000000001307288, 0.3750000000001184608, 0.4375000000001083578, 0.4687500000001048051, 0.5000000000001012523, 1.000000000000000000 ),
 .UNSPECIFIED. ) ;
#53816=ORIENTED_EDGE ( 'NONE', *, *, #32163, .T. ) ;
#53818=CARTESIAN_POINT ( 'NONE',  ( 24.34833249973733516, 12.15210535428998284, 3.256146816021051382 ) ) ;
#53821=ADVANCED_FACE ( 'NONE', ( #19143 ), #21651, .F. ) ;
#53824=DIRECTION ( 'NONE',  ( 1.000000000000000000, 0.000000000000000000, 0.000000000000000000 ) ) ;
#53825=ORIENTED_EDGE ( 'NONE', *, *, #50358, .T. ) ;
#53828=ORIENTED_EDGE ( 'NONE', *, *, #2992, .F. ) ;
#53836=CARTESIAN_POINT ( 'NONE',  ( 13.99944283128300171, 9.262889243704000464, 8.209791536961999370 ) ) ;
#53842=ADVANCED_FACE ( 'NONE', ( #63503 ), #41844, .T. ) ;
#53851=FACE_OUTER_BOUND ( 'NONE', #16856, .T. ) ;
#53862=CARTESIAN_POINT ( 'NONE',  ( 24.30000000000000071, -10.83443035398000021, -3.855530949778000149 ) ) ;
#53864=CARTESIAN_POINT ( 'NONE',  ( 18.49997192701553317, -2.999031289802028155, -12.16100995559911446 ) ) ;
#53886=CARTESIAN_POINT ( 'NONE',  ( 18.43276988671243544, -2.975106096554608559, 11.26378872113905238 ) ) ;
#53890=CARTESIAN_POINT ( 'NONE',  ( 21.60000000000000142, -12.52500000000000036, 0.000000000000000000 ) ) ;
#53895=CARTESIAN_POINT ( 'NONE',  ( 24.16198684513495110, 9.122969203443838992, -9.103568285634533908 ) ) ;
#53902=EDGE_LOOP ( 'NONE', ( #23111, #43871, #24613, #35710 ) ) ;
#53911=CARTESIAN_POINT ( 'NONE',  ( 18.53574650668400281, -2.786976374009999535, 11.27236326136999978 ) ) ;
#53915=DIRECTION ( 'NONE',  ( 0.000000000000000000, 1.099932324123999872E-09, -1.000000000000000000 ) ) ;
#53920=CARTESIAN_POINT ( 'NONE',  ( 24.62620337148488048, -12.35920179360042681, 2.996409964397301451 ) ) ;
#53924=EDGE_CURVE ( 'NONE', #60029, #31626, #52470, .T. ) ;
#53925=CARTESIAN_POINT ( 'NONE',  ( 24.92847981667748769, -8.562973297442058040, 8.403437224533664818 ) ) ;
#53926=CARTESIAN_POINT ( 'NONE',  ( 18.30000077768849565, 11.66744147158535405, -3.971919865264926575 ) ) ;
#53930=VERTEX_POINT ( 'NONE', #22236 ) ;
#53932=CARTESIAN_POINT ( 'NONE',  ( 17.93529619513299878, 12.15408297959000095, -3.184072412108000183 ) ) ;
#53937=CARTESIAN_POINT ( 'NONE',  ( 18.35499787466299892, -2.879071536379000040, 12.03968120189999880 ) ) ;
#53939=ORIENTED_EDGE ( 'NONE', *, *, #19735, .F. ) ;
#53940=PLANE ( 'NONE',  #5807 ) ;
#53942=DIRECTION ( 'NONE',  ( -1.000000000000000000, 0.000000000000000000, 0.000000000000000000 ) ) ;
#53954=EDGE_CURVE ( 'NONE', #15615, #49620, #64953, .T. ) ;
#53957=CARTESIAN_POINT ( 'NONE',  ( 17.60000001994400165, -11.53041320601000130, 4.891397783926000109 ) ) ;
#53960=CARTESIAN_POINT ( 'NONE',  ( 16.32975648157900039, -3.316681689484000106, -11.22330675696999869 ) ) ;
#53961=CONICAL_SURFACE ( 'NONE', #55129, 11.75016914289000169, 0.7854125553233202162 ) ;
#53965=AXIS2_PLACEMENT_3D ( 'NONE', #60988, #19631, #49809 ) ;
#53966=CARTESIAN_POINT ( 'NONE',  ( 24.36453968238300050, -3.372832729159999765, 12.24475767785000002 ) ) ;
#53971=CARTESIAN_POINT ( 'NONE',  ( 24.59181004102800117, -8.769933227510000151, 9.082960305682000524 ) ) ;
#53974=CARTESIAN_POINT ( 'NONE',  ( 24.63407836964800168, -11.78083276143999925, -3.229000863272000199 ) ) ;
#53980=CARTESIAN_POINT ( 'NONE',  ( 23.50387503050299998, 3.715991115242999921E-06, -13.79999999999999893 ) ) ;
#53982=CARTESIAN_POINT ( 'NONE',  ( 12.95870478550200211, 12.43384127863000010, 1.801469962976000039 ) ) ;
#53989=CARTESIAN_POINT ( 'NONE',  ( 16.00000000429200142, 11.53036813819577411, -4.891445144093894193 ) ) ;
#53990=CARTESIAN_POINT ( 'NONE',  ( 25.21376180238323528, 8.515659051923003986, -8.063054907511679303 ) ) ;
#53991=CARTESIAN_POINT ( 'NONE',  ( 15.39325612864500137, 8.820489328074000213, 7.691617095226000345 ) ) ;
#53993=CARTESIAN_POINT ( 'NONE',  ( 23.67741840186891622, -13.18815814536682751, 3.924039949733880928 ) ) ;
#54001=VECTOR ( 'NONE', #13206, 1000.000000000000000 ) ;
#54006=CARTESIAN_POINT ( 'NONE',  ( 24.30001683613300045, -12.21047198529999989, -3.271805531187999883 ) ) ;
#54010=CARTESIAN_POINT ( 'NONE',  ( 24.69607688207488749, 11.79509585809828742, -3.190917141363150744 ) ) ;
#54016=CIRCLE ( 'NONE', #24980, 1.000000000000000666 ) ;
#54017=CARTESIAN_POINT ( 'NONE',  ( 24.30000000000000071, 9.305479840184000651, 8.315530346521999405 ) ) ;
#54034=CYLINDRICAL_SURFACE ( 'NONE', #18339, 0.6999999999999992895 ) ;
#54041=B_SPLINE_SURFACE_WITH_KNOTS ( 'NONE', 3, 3, ( 
 ( #48201, #38049, #64265, #306 ),
 ( #59374, #11823, #42283, #21622 ),
 ( #37710, #33162, #16036, #27568 ),
 ( #37031, #11474, #63925, #59038 ),
 ( #10446, #31786, #53789, #5204 ),
 ( #27226, #32814, #6228, #61109 ) ),
 .UNSPECIFIED., .F., .F., .F.,
 ( 4, 1, 1, 4 ),
 ( 4, 4 ),
 ( 0.1423941366080999915, 0.3333333333333000081, 0.6666666666667000474, 0.8219462302419999755 ),
 ( -0.1256563615234000120, 1.125656361508000192 ),
 .UNSPECIFIED. ) ;
#54043=B_SPLINE_CURVE_WITH_KNOTS ( 'NONE', 3,
 ( #6457, #37933, #59252, #59603, #54354, #11359, #54010, #11702, #6112, #43876, #64835, #27451, #883, #16944, #65182, #12058, #14393, #66568, #36047, #25562, #45263 ),
 .UNSPECIFIED., .F., .F.,
 ( 4, 2, 2, 1, 1, 2, 2, 2, 1, 2, 2, 4 ),
 ( 0.000000000000000000, 0.1249999999999492073, 0.1874999999999213685, 0.2187499999999089617, 0.2343749999999027445, 0.2421874999999015232, 0.2499999999999003575, 0.3749999999999252265, 0.4374999999999350520, 0.4687499999999401035, 0.4999999999999450440, 1.000000000000000000 ),
 .UNSPECIFIED. ) ;
#54044=CARTESIAN_POINT ( 'NONE',  ( 24.63805661103100064, 8.801154613476001032, 9.346935862444000875 ) ) ;
#54069=DIRECTION ( 'NONE',  ( 1.000000000000000000, 0.000000000000000000, 0.000000000000000000 ) ) ;
#54070=CARTESIAN_POINT ( 'NONE',  ( 11.53970701685000222, 11.52114570934000071, 1.450082077858000140 ) ) ;
#54071=VERTEX_POINT ( 'NONE', #34478 ) ;
#54072=CARTESIAN_POINT ( 'NONE',  ( 24.94501239293118644, 2.983176329050218012, -11.60457232061659205 ) ) ;
#54073=CARTESIAN_POINT ( 'NONE',  ( 16.44832727683000329, 3.192413998985999868, 11.44999110620999794 ) ) ;
#54074=AXIS2_PLACEMENT_3D ( 'NONE', #46695, #15211, #30958 ) ;
#54076=EDGE_LOOP ( 'NONE', ( #14890, #27505, #20817, #49716 ) ) ;
#54078=CARTESIAN_POINT ( 'NONE',  ( 24.30001682246400208, -8.938702682732001747, -8.938676171235998780 ) ) ;
#54081=DIRECTION ( 'NONE',  ( -1.000000000000000000, 0.000000000000000000, 0.000000000000000000 ) ) ;
#54086=FILL_AREA_STYLE_COLOUR ( '', #25092 ) ;
#54091=EDGE_CURVE ( 'NONE', #9579, #10089, #20768, .T. ) ;
#54093=DIRECTION ( 'NONE',  ( -5.691941604301808236E-06, -0.9659358920123676251, 0.2587814763267914375 ) ) ;
#54096=ADVANCED_FACE ( 'NONE', ( #7538 ), #2302, .F. ) ;
#54109=CARTESIAN_POINT ( 'NONE',  ( 23.73952188783414741, -13.33635550666453540, -3.648248442822538351 ) ) ;
#54117=CARTESIAN_POINT ( 'NONE',  ( 17.79416955086200147, 3.253172910778000304, -11.33701170283999993 ) ) ;
#54122=CARTESIAN_POINT ( 'NONE',  ( 23.61814126825800031, -10.28285508195000020, -9.267271738533999326 ) ) ;
#54124=CARTESIAN_POINT ( 'NONE',  ( 24.22012566761399910, -8.984033207697999401, 8.868613826359998953 ) ) ;
#54125=ORIENTED_EDGE ( 'NONE', *, *, #42342, .T. ) ;
#54128=EDGE_CURVE ( 'NONE', #43538, #55462, #33286, .T. ) ;
#54134=CARTESIAN_POINT ( 'NONE',  ( 25.41799978389900261, 2.807552223335999741, -11.31775031636999884 ) ) ;
#54148=CARTESIAN_POINT ( 'NONE',  ( 12.70688507812400125, -11.81408563393000044, 3.326099274546999940 ) ) ;
#54170=AXIS2_PLACEMENT_3D ( 'NONE', #68305, #14503, #26715 ) ;
#54184=CARTESIAN_POINT ( 'NONE',  ( 23.60205915885299888, -11.72032963058999400, 3.891881970957998593 ) ) ;
#54186=CARTESIAN_POINT ( 'NONE',  ( 11.48828127163000268, 12.23964378314000001, 1.839251152677999990 ) ) ;
#54190=DIRECTION ( 'NONE',  ( 0.000000000000000000, -0.9439966912222074180, -0.3299549165591025846 ) ) ;
#54191=CARTESIAN_POINT ( 'NONE',  ( 25.46372189163300348, -2.879475976718999686, 11.30953721564000070 ) ) ;
#54210=FACE_OUTER_BOUND ( 'NONE', #64989, .T. ) ;
#54213=CARTESIAN_POINT ( 'NONE',  ( 11.66883611569390489, 12.15999240567520268, 2.000270994069734964 ) ) ;
#54214=VERTEX_POINT ( 'NONE', #52591 ) ;
#54217=CARTESIAN_POINT ( 'NONE',  ( 18.29983863915591158, 0.9627070266348703997, 12.32514598389175831 ) ) ;
#54218=AXIS2_PLACEMENT_3D ( 'NONE', #66624, #22938, #50212 ) ;
#54223=CARTESIAN_POINT ( 'NONE',  ( 24.42335332038400253, 3.752413731090000315, -12.53707314549000174 ) ) ;
#54226=CARTESIAN_POINT ( 'NONE',  ( 12.10000669845703847, 11.02846243759400124, -3.754394857303852362 ) ) ;
#54238=CARTESIAN_POINT ( 'NONE',  ( 24.31006797060300073, 12.13011445653000031, 3.289861759914999517 ) ) ;
#54243=ORIENTED_EDGE ( 'NONE', *, *, #42695, .F. ) ;
#54244=B_SPLINE_CURVE_WITH_KNOTS ( 'NONE', 3,
 ( #11432, #17733, #33814, #56159, #28927, #28569 ),
 .UNSPECIFIED., .F., .F.,
 ( 4, 2, 4 ),
 ( 0.000000000000000000, 0.5000000000000000000, 1.000000000000000000 ),
 .UNSPECIFIED. ) ;
#54251=AXIS2_PLACEMENT_3D ( 'NONE', #10196, #25931, #26282 ) ;
#54252=CARTESIAN_POINT ( 'NONE',  ( 17.77441288034700051, -3.189751316310999840, 11.45074679932000095 ) ) ;
#54259=ORIENTED_EDGE ( 'NONE', *, *, #60451, .T. ) ;
#54261=ORIENTED_EDGE ( 'NONE', *, *, #12878, .T. ) ;
#54275=ORIENTED_EDGE ( 'NONE', *, *, #10088, .T. ) ;
#54277=CARTESIAN_POINT ( 'NONE',  ( 18.30003129332100187, 2.732683818840999646, 11.53064095373000164 ) ) ;
#54284=DIRECTION ( 'NONE',  ( -1.000000000000000000, 0.000000000000000000, 0.000000000000000000 ) ) ;
#54300=AXIS2_PLACEMENT_3D ( 'NONE', #67314, #63446, #30963 ) ;
#54305=CARTESIAN_POINT ( 'NONE',  ( 24.45625626939792951, 12.38367859507303415, 3.108175842103299669 ) ) ;
#54306=CARTESIAN_POINT ( 'NONE',  ( 11.74249537357300177, 3.528133194209999601, -11.96072866431000037 ) ) ;
#54308=APPLICATION_CONTEXT ( 'automotive_design' ) ;
#54312=EDGE_CURVE ( 'NONE', #62750, #26055, #38219, .T. ) ;
#54318=CARTESIAN_POINT ( 'NONE',  ( 25.08881512370800237, -8.444445702635000828, 8.588598710570000350 ) ) ;
#54321=CARTESIAN_POINT ( 'NONE',  ( 25.59994555223600088, 9.407310119912997592, -6.227539428020409495 ) ) ;
#54324=FACE_OUTER_BOUND ( 'NONE', #28485, .T. ) ;
#54325=CARTESIAN_POINT ( 'NONE',  ( 17.60000003185799855, -12.11983897296999935, 3.159727888982000188 ) ) ;
#54328=ORIENTED_EDGE ( 'NONE', *, *, #55535, .F. ) ;
#54329=CARTESIAN_POINT ( 'NONE',  ( 24.35365242081699932, 8.885108761891000739, 7.331500822262997374 ) ) ;
#54333=CARTESIAN_POINT ( 'NONE',  ( 24.66912214958201233, 8.674026130943369495, -8.642841412892551034 ) ) ;
#54339=FACE_OUTER_BOUND ( 'NONE', #52312, .T. ) ;
#54354=CARTESIAN_POINT ( 'NONE',  ( 24.65657919783774332, 11.83373535527700504, -3.192275918523050482 ) ) ;
#54359=B_SPLINE_CURVE_WITH_KNOTS ( 'NONE', 3,
 ( #8750, #25515, #47188, #9086 ),
 .UNSPECIFIED., .F., .F.,
 ( 4, 4 ),
 ( 0.000000000000000000, 1.000000000000000000 ),
 .UNSPECIFIED. ) ;
#54360=B_SPLINE_CURVE_WITH_KNOTS ( 'NONE', 3,
 ( #19013, #67580, #51509, #57436, #62346, #40337 ),
 .UNSPECIFIED., .F., .F.,
 ( 4, 2, 4 ),
 ( 0.000000000000000000, 0.5000000000000000000, 1.000000000000000000 ),
 .UNSPECIFIED. ) ;
#54364=CARTESIAN_POINT ( 'NONE',  ( 13.39991752512754530, 12.13029446165148961, 2.190571078338882760 ) ) ;
#54367=CARTESIAN_POINT ( 'NONE',  ( 24.98214774730800158, 3.089314405311999856, 11.61702339075000090 ) ) ;
#54383=CARTESIAN_POINT ( 'NONE',  ( 12.80000000000000071, -43.96540072520999587, 14.96704326274999985 ) ) ;
#54385=ADVANCED_FACE ( 'NONE', ( #60092 ), #6028, .F. ) ;
#54391=ORIENTED_EDGE ( 'NONE', *, *, #2991, .T. ) ;
#54395=( BOUNDED_SURFACE ( )  B_SPLINE_SURFACE ( 3, 3, ( 
 ( #4815, #38012, #11102, #47138 ),
 ( #20905, #5511, #41885, #26852 ),
 ( #68439, #48165, #52372, #53753 ),
 ( #27190, #26157, #269, #31750 ) ),
 .UNSPECIFIED., .F., .F., .T. ) 
 B_SPLINE_SURFACE_WITH_KNOTS ( ( 4, 4 ),
 ( 4, 4 ),
 ( 0.000000000000000000, 1.000000000000000000 ),
 ( 0.000000000000000000, 1.000000000000000000 ),
 .UNSPECIFIED. ) 
 GEOMETRIC_REPRESENTATION_ITEM ( )  RATIONAL_B_SPLINE_SURFACE ( (
 ( 1.512182578520000042, 1.160176301760999840, 1.160176301760999840, 1.512182578520000042),
 ( 1.111288591041000196, 0.8526025270081000196, 0.8526025270081000196, 1.111288591041000196),
 ( 1.111288591041000196, 0.8526025270081000196, 0.8526025270081000196, 1.111288591041000196),
 ( 1.512182578520000042, 1.160176301760999840, 1.160176301760999840, 1.512182578520000042) ) ) 
 REPRESENTATION_ITEM ( '' )  SURFACE ( )  );
#54398=CONICAL_SURFACE ( 'NONE', #24262, 11.34994642770999818, 0.7853934433896081480 ) ;
#54400=EDGE_CURVE ( 'NONE', #7379, #28950, #44063, .T. ) ;
#54406=CARTESIAN_POINT ( 'NONE',  ( 24.30001685126999789, 8.938702716825000394, -8.938676159935001309 ) ) ;
#54409=VECTOR ( 'NONE', #50693, 1000.000000000000227 ) ;
#54411=ORIENTED_EDGE ( 'NONE', *, *, #15312, .T. ) ;
#54419=FACE_OUTER_BOUND ( 'NONE', #25744, .T. ) ;
#54422=CARTESIAN_POINT ( 'NONE',  ( 25.29996559941400136, -2.596925179230000325, -11.35302181744000016 ) ) ;
#54426=CARTESIAN_POINT ( 'NONE',  ( 17.60000002360358096, -11.94788428419862747, 3.252375034948150390 ) ) ;
#54435=CARTESIAN_POINT ( 'NONE',  ( 15.98069952315600162, -9.346107076637000688, -8.395568570714997847 ) ) ;
#54439=CARTESIAN_POINT ( 'NONE',  ( 16.10004050617000004, -5.773856762095680217, -11.16084031980687108 ) ) ;
#54444=EDGE_CURVE ( 'NONE', #61665, #41305, #14821, .T. ) ;
#54451=B_SPLINE_CURVE_WITH_KNOTS ( 'NONE', 3,
 ( #21389, #759, #38866, #16489, #12292, #58797, #43420, #48998 ),
 .UNSPECIFIED., .F., .F.,
 ( 4, 2, 2, 4 ),
 ( 0.000000000000000000, 0.4999999999999953371, 0.7499999999999976685, 1.000000000000000000 ),
 .UNSPECIFIED. ) ;
#54452=CARTESIAN_POINT ( 'NONE',  ( 11.80727443316700231, -12.22191286342000005, -1.956148154176999832 ) ) ;
#54462=FACE_OUTER_BOUND ( 'NONE', #26077, .T. ) ;
#54465=CARTESIAN_POINT ( 'NONE',  ( 18.30003129334700063, -2.732683817159999862, 11.53064095410000078 ) ) ;
#54466=CARTESIAN_POINT ( 'NONE',  ( 18.38722619340700248, 3.117741388420999904, -11.18549237633000004 ) ) ;
#54471=CARTESIAN_POINT ( 'NONE',  ( 23.55359760295800342, -10.33014718151000189, -9.497754714104001295 ) ) ;
#54472=CARTESIAN_POINT ( 'NONE',  ( 24.02992999001800101, -9.410060158574999889, 9.736248058902001290 ) ) ;
#54473=CIRCLE ( 'NONE', #33274, 13.98989069973999477 ) ;
#54474=CARTESIAN_POINT ( 'NONE',  ( 11.68610928851700237, -3.397019518052000198, 11.10441497445000003 ) ) ;
#54475=ORIENTED_EDGE ( 'NONE', *, *, #33330, .F. ) ;
#54482=CARTESIAN_POINT ( 'NONE',  ( 24.56892813840100231, 3.303732449835000029, -12.00214075350999821 ) ) ;
#54495=CARTESIAN_POINT ( 'NONE',  ( 24.56351374471499938, 12.27674503263999917, -3.066186501856999591 ) ) ;
#54497=CARTESIAN_POINT ( 'NONE',  ( 12.03709034744600181, -11.69601057336999972, 4.586677359659000253 ) ) ;
#54502=VERTEX_POINT ( 'NONE', #23258 ) ;
#54503=CARTESIAN_POINT ( 'NONE',  ( 24.19055608310253191, -9.082956471743646176, 9.070969611592573756 ) ) ;
#54506=FACE_OUTER_BOUND ( 'NONE', #65656, .T. ) ;
#54511=AXIS2_PLACEMENT_3D ( 'NONE', #60236, #49052, #34020 ) ;
#54516=CARTESIAN_POINT ( 'NONE',  ( 23.56664676942400050, 2.935522432666999748, 13.67843419499999946 ) ) ;
#54520=CARTESIAN_POINT ( 'NONE',  ( 23.89320776801300283, 12.21745654481001075, 3.256241354617000816 ) ) ;
#54522=ORIENTED_EDGE ( 'NONE', *, *, #58059, .T. ) ;
#54527=CARTESIAN_POINT ( 'NONE',  ( 18.39711792013700276, -11.90291294758000085, 3.720230460285999907 ) ) ;
#54529=CARTESIAN_POINT ( 'NONE',  ( 12.79999999038796510, 11.45060587895086002, -4.713120762395663910 ) ) ;
#54530=CARTESIAN_POINT ( 'NONE',  ( 13.78326532032400031, 9.295717737520000412, 8.172239456948000580 ) ) ;
#54542=CARTESIAN_POINT ( 'NONE',  ( 11.60578299225600141, 12.22760809526000081, 1.919009911369000010 ) ) ;
#54544=CARTESIAN_POINT ( 'NONE',  ( 13.00000000009400303, 11.69118001589999878, 1.923222888683999932 ) ) ;
#54548=VERTEX_POINT ( 'NONE', #66929 ) ;
#54554=B_SPLINE_CURVE_WITH_KNOTS ( 'NONE', 3,
 ( #33536, #54855, #1368, #50988 ),
 .UNSPECIFIED., .F., .F.,
 ( 4, 4 ),
 ( 0.000000000000000000, 1.000000000000000000 ),
 .UNSPECIFIED. ) ;
#54565=DIRECTION ( 'NONE',  ( 0.000000000000000000, 0.000000000000000000, 1.000000000000000000 ) ) ;
#54573=ADVANCED_FACE ( 'NONE', ( #7870 ), #46651, .T. ) ;
#54580=CARTESIAN_POINT ( 'NONE',  ( 18.90826270587400160, 11.65000000000000036, 0.000000000000000000 ) ) ;
#54581=CARTESIAN_POINT ( 'NONE',  ( 12.96900185986900134, -12.22197440418000092, -1.955830866674999946 ) ) ;
#54592=DIRECTION ( 'NONE',  ( 1.000000000000000000, 0.000000000000000000, 0.000000000000000000 ) ) ;
#54605=CARTESIAN_POINT ( 'NONE',  ( 23.72388938462524877, 3.247317956399220051, -13.28503071072038288 ) ) ;
#54608=CARTESIAN_POINT ( 'NONE',  ( 17.80000000005199823, -3.345268251980999974, -11.86064071431999878 ) ) ;
#54609=CARTESIAN_POINT ( 'NONE',  ( 11.42387073792000152, 3.325692027085000113, -11.41083924281000073 ) ) ;
#54613=ORIENTED_EDGE ( 'NONE', *, *, #61960, .T. ) ;
#54622=CARTESIAN_POINT ( 'NONE',  ( 17.33333333083533390, 3.216308279608388609, 11.40341444610950461 ) ) ;
#54625=B_SPLINE_SURFACE_WITH_KNOTS ( 'NONE', 3, 3, ( 
 ( #32831, #28275, #11490, #64967 ),
 ( #21983, #6244, #48567, #65669 ),
 ( #59737, #48912, #12197, #11838 ),
 ( #1703, #33178, #54495, #37725 ),
 ( #27937, #39110, #33525, #12541 ),
 ( #43324, #64628, #6596, #44370 ) ),
 .UNSPECIFIED., .F., .F., .F.,
 ( 4, 1, 1, 4 ),
 ( 4, 4 ),
 ( 0.1811037619699999990, 0.3333333333333000081, 0.6666666666667000474, 0.8725156331704999602 ),
 ( -0.1256563615239000009, 1.125656361510000147 ),
 .UNSPECIFIED. ) ;
#54627=CARTESIAN_POINT ( 'NONE',  ( 23.56666365135700403, -8.694246338441999455, -8.392498551189996547 ) ) ;
#54635=B_SPLINE_CURVE_WITH_KNOTS ( 'NONE', 3,
 ( #26950, #16783, #5951, #54191 ),
 .UNSPECIFIED., .F., .F.,
 ( 4, 4 ),
 ( 0.000000000000000000, 1.000000000000000000 ),
 .UNSPECIFIED. ) ;
#54638=CARTESIAN_POINT ( 'NONE',  ( 25.29986325275000070, 2.078227429405999693, 11.31065739696999906 ) ) ;
#54642=CARTESIAN_POINT ( 'NONE',  ( 24.32155075627094831, 3.683040026163987957, 12.56970858062822849 ) ) ;
#54643=CARTESIAN_POINT ( 'NONE',  ( 24.30001680216799897, -3.271769318036999774, 12.21048166890999909 ) ) ;
#54645=DIRECTION ( 'NONE',  ( -1.000000000000000000, 0.000000000000000000, 0.000000000000000000 ) ) ;
#54659=CARTESIAN_POINT ( 'NONE',  ( 13.50003721581400029, 9.159934378815998812, 7.517910889891000537 ) ) ;
#54661=ORIENTED_EDGE ( 'NONE', *, *, #22950, .T. ) ;
#54667=CARTESIAN_POINT ( 'NONE',  ( 24.44496351116800170, 3.224881296174999967, 12.03535797436000010 ) ) ;
#54673=CARTESIAN_POINT ( 'NONE',  ( 25.59037099084400069, -11.08966619523999952, -3.240309866392999893 ) ) ;
#54677=VECTOR ( 'NONE', #31897, 1000.000000000000114 ) ;
#54678=CARTESIAN_POINT ( 'NONE',  ( 13.69586690835513565, -11.42311322218530556, -2.288407577486363920 ) ) ;
#54680=CARTESIAN_POINT ( 'NONE',  ( 13.68724299200000161, 12.36060503258000054, 2.247042498203000171 ) ) ;
#54681=ORIENTED_EDGE ( 'NONE', *, *, #36607, .F. ) ;
#54691=DIRECTION ( 'NONE',  ( -1.000000000000000000, 0.000000000000000000, 0.000000000000000000 ) ) ;
#54696=EDGE_CURVE ( 'NONE', #26192, #60622, #37838, .T. ) ;
#54698=CARTESIAN_POINT ( 'NONE',  ( 25.55274092379240258, 8.264541415825529924, -8.081433428414696252 ) ) ;
#54699=ORIENTED_EDGE ( 'NONE', *, *, #63956, .F. ) ;
#54700=CARTESIAN_POINT ( 'NONE',  ( 13.69997185827400266, 11.40547114375999982, 2.374390024598000082 ) ) ;
#54706=CARTESIAN_POINT ( 'NONE',  ( 16.13732479921000262, 3.901986904155000158, 11.94169104666999992 ) ) ;
#54711=ORIENTED_EDGE ( 'NONE', *, *, #16561, .F. ) ;
#54715=DIRECTION ( 'NONE',  ( 0.000000000000000000, -0.1807154286440003366, -0.9835354258236024272 ) ) ;
#54721=CARTESIAN_POINT ( 'NONE',  ( 25.20468240883799993, -2.650152599392000319, 11.40088862747000142 ) ) ;
#54731=CARTESIAN_POINT ( 'NONE',  ( 25.46373024410000241, -11.23407150414000100, 3.161076981347000103 ) ) ;
#54736=B_SPLINE_CURVE_WITH_KNOTS ( 'NONE', 3,
 ( #59757, #23042, #33197, #54516 ),
 .UNSPECIFIED., .F., .F.,
 ( 4, 4 ),
 ( 0.000000000000000000, 1.000000000000000000 ),
 .UNSPECIFIED. ) ;
#54737=CARTESIAN_POINT ( 'NONE',  ( 24.56351374471499938, -8.793767919668001198, -9.098879823118998900 ) ) ;
#54744=CARTESIAN_POINT ( 'NONE',  ( 18.01246087681401775, 10.82907928505076711, -4.296547899031908813 ) ) ;
#54754=CARTESIAN_POINT ( 'NONE',  ( 24.17809223743226710, -12.41828058357439346, -3.338452890154027575 ) ) ;
#54759=FACE_OUTER_BOUND ( 'NONE', #42768, .T. ) ;
#54763=CARTESIAN_POINT ( 'NONE',  ( 23.60000000000000142, 0.000000000000000000, 0.000000000000000000 ) ) ;
#54764=CARTESIAN_POINT ( 'NONE',  ( 17.80000000009400196, 3.216307036143000175, 11.40341376487999980 ) ) ;
#54768=CARTESIAN_POINT ( 'NONE',  ( 15.99015267864900203, 3.493241607194999876, 11.26524960718000123 ) ) ;
#54771=CARTESIAN_POINT ( 'NONE',  ( 15.40000000001299973, -8.815237407733999220, -7.616696375847999967 ) ) ;
#54779=EDGE_CURVE ( 'NONE', #23104, #63538, #69057, .T. ) ;
#54783=CARTESIAN_POINT ( 'NONE',  ( 15.86005557146100209, -8.873324881979000267, -8.501367972259000538 ) ) ;
#54785=B_SPLINE_SURFACE_WITH_KNOTS ( 'NONE', 3, 3, ( 
 ( #46388, #20846, #57908, #10006 ),
 ( #14914, #35892, #57208, #51286 ),
 ( #68040, #52657, #31343, #9310 ),
 ( #52317, #19469, #3383, #35219 ),
 ( #24718, #4753, #8636, #26095 ),
 ( #67350, #56877, #68728, #46043 ),
 ( #40792, #14233, #62114, #20156 ),
 ( #35561, #56532, #30316, #13892 ),
 ( #20500, #51623, #29986, #25749 ),
 ( #67692, #3719, #4063, #25057 ) ),
 .UNSPECIFIED., .F., .F., .F.,
 ( 4, 1, 1, 1, 1, 1, 1, 4 ),
 ( 4, 4 ),
 ( 0.07203983506773999068, 0.1428571428570999946, 0.2857142857143000203, 0.4285714285713999594, 0.5714285714286000406, 0.7142857142856999797, 0.8571428571429000609, 0.9589780836993999635 ),
 ( -0.1900620218102000158, 1.190128522698000069 ),
 .UNSPECIFIED. ) ;
#54794=VERTEX_POINT ( 'NONE', #40897 ) ;
#54796=ORIENTED_EDGE ( 'NONE', *, *, #4416, .F. ) ;
#54797=CARTESIAN_POINT ( 'NONE',  ( 11.26395919764000197, -12.20155262497000059, -1.453968487665999954 ) ) ;
#54802=CARTESIAN_POINT ( 'NONE',  ( 24.63332959156760182, -8.756202931479764473, -7.455126439085038470 ) ) ;
#54803=CARTESIAN_POINT ( 'NONE',  ( 24.22012832183300191, 12.17245628853000028, 3.346092709831000267 ) ) ;
#54806=CARTESIAN_POINT ( 'NONE',  ( 18.53712493497300073, 2.638811780578999677, 11.30793729956000071 ) ) ;
#54807=AXIS2_PLACEMENT_3D ( 'NONE', #57828, #41414, #31273 ) ;
#54810=CARTESIAN_POINT ( 'NONE',  ( 18.49996808500599954, -0.9036517542723243590, -11.65000000000000213 ) ) ;
#54812=CARTESIAN_POINT ( 'NONE',  ( 18.35481935287100086, 2.723593151845999927, -11.47751840123000022 ) ) ;
#54818=CARTESIAN_POINT ( 'NONE',  ( 23.83659698888000023, -9.655115511098998127, -9.481980187101999746 ) ) ;
#54819=CARTESIAN_POINT ( 'NONE',  ( 23.73946058743000265, -9.841007807744000857, 9.518031540355998743 ) ) ;
#54821=CARTESIAN_POINT ( 'NONE',  ( 25.60000000000000142, 0.000000000000000000, 0.000000000000000000 ) ) ;
#54826=CARTESIAN_POINT ( 'NONE',  ( 24.35365242081700288, -3.193712117489998281, 11.49150331539999215 ) ) ;
#54829=CARTESIAN_POINT ( 'NONE',  ( 24.30000565690453840, -8.853233224111329847, 8.853233224111329847 ) ) ;
#54843=ORIENTED_EDGE ( 'NONE', *, *, #33144, .F. ) ;
#54844=CARTESIAN_POINT ( 'NONE',  ( 24.67921321864300310, 12.29514728640000065, 2.979192498689000157 ) ) ;
#54845=CARTESIAN_POINT ( 'NONE',  ( 12.27593309678900191, -11.75515418280000013, 3.561236062516000000 ) ) ;
#54849=CARTESIAN_POINT ( 'NONE',  ( 23.51693421199300360, 2.933245738859999729, 13.82474819291000045 ) ) ;
#54851=EDGE_LOOP ( 'NONE', ( #16195, #67759, #41052, #63799, #59547 ) ) ;
#54852=CARTESIAN_POINT ( 'NONE',  ( 23.80953379775873557, -9.702200433909665023, 9.418729782999628597 ) ) ;
#54854=ORIENTED_EDGE ( 'NONE', *, *, #17611, .F. ) ;
#54855=CARTESIAN_POINT ( 'NONE',  ( 17.60000000266004960, 10.99220013531737372, -4.481500379774075782 ) ) ;
#54856=ORIENTED_EDGE ( 'NONE', *, *, #58556, .F. ) ;
#54858=CARTESIAN_POINT ( 'NONE',  ( 23.51508276455100344, 13.45797239394999956, -4.320681590166000063 ) ) ;
#54862=VERTEX_POINT ( 'NONE', #21966 ) ;
#54864=B_SPLINE_CURVE_WITH_KNOTS ( 'NONE', 3,
 ( #17630, #34408, #13760, #34747, #41360, #35771, #67566, #46263, #14106, #8167 ),
 .UNSPECIFIED., .F., .F.,
 ( 4, 2, 2, 2, 4 ),
 ( 0.4999999998130725265, 0.6249999998598043671, 0.7499999999065363188, 0.8749999999532681594, 1.000000000000000000 ),
 .UNSPECIFIED. ) ;
#54865=EDGE_CURVE ( 'NONE', #48385, #63101, #43305, .T. ) ;
#54868=CARTESIAN_POINT ( 'NONE',  ( 23.60000648950287427, 10.25354916021784746, 9.380079597658479429 ) ) ;
#54874=CARTESIAN_POINT ( 'NONE',  ( 18.35889944991900435, -11.74562277640000119, 3.912379265303000508 ) ) ;
#54882=ORIENTED_EDGE ( 'NONE', *, *, #17719, .T. ) ;
#54883=CARTESIAN_POINT ( 'NONE',  ( 24.35365242081699932, -12.20235406293000935, 3.288253180433003298 ) ) ;
#54890=CARTESIAN_POINT ( 'NONE',  ( 18.53935907712300235, 2.923447147946000246, -12.21821814482000157 ) ) ;
#54897=CARTESIAN_POINT ( 'NONE',  ( 24.44917776433500123, -3.519943607436000210, -12.30316564740000196 ) ) ;
#54906=CARTESIAN_POINT ( 'NONE',  ( 25.31133098161000206, 8.473030475148000562, 8.042931544829999169 ) ) ;
#54914=ORIENTED_EDGE ( 'NONE', *, *, #42149, .F. ) ;
#54917=CARTESIAN_POINT ( 'NONE',  ( 23.94495875478589753, -9.457063741204379426, -9.320448346922830751 ) ) ;
#54922=CARTESIAN_POINT ( 'NONE',  ( 24.56351374521100439, -12.27674503203999912, 3.066186501695999933 ) ) ;
#54928=ADVANCED_FACE ( 'NONE', ( #47522 ), #54041, .F. ) ;
#54939=CIRCLE ( 'NONE', #15846, 1.000000000000000222 ) ;
#54954=DIRECTION ( 'NONE',  ( -1.000000000000000000, 0.000000000000000000, 0.000000000000000000 ) ) ;
#54963=DIRECTION ( 'NONE',  ( 1.000000000000000000, 0.000000000000000000, 0.000000000000000000 ) ) ;
#54969=CARTESIAN_POINT ( 'NONE',  ( 25.12926781546009636, -8.519457660519075048, 8.174621111370402815 ) ) ;
#54978=VERTEX_POINT ( 'NONE', #33510 ) ;
#54980=CARTESIAN_POINT ( 'NONE',  ( 17.56849549447199976, 11.93188800409999928, -3.261574020045000299 ) ) ;
#54983=CIRCLE ( 'NONE', #42703, 1.000000000000001332 ) ;
#54991=CARTESIAN_POINT ( 'NONE',  ( 18.30000000000000071, 2.818726571106858980, 11.83569999720589294 ) ) ;
#54993=CARTESIAN_POINT ( 'NONE',  ( 24.53428985175800037, 12.47024902693999948, -3.026245299674999778 ) ) ;
#55004=EDGE_CURVE ( 'NONE', #52029, #56220, #46528, .T. ) ;
#55008=VERTEX_POINT ( 'NONE', #65994 ) ;
#55009=EDGE_CURVE ( 'NONE', #28289, #52029, #59028, .T. ) ;
#55010=EDGE_CURVE ( 'NONE', #62083, #11162, #10729, .T. ) ;
#55016=CARTESIAN_POINT ( 'NONE',  ( 24.44916829770000177, -3.519946668155999880, 12.30317708153000034 ) ) ;
#55020=CARTESIAN_POINT ( 'NONE',  ( 24.95409909025299910, -8.513620944989998662, 8.994042707941998671 ) ) ;
#55026=CARTESIAN_POINT ( 'NONE',  ( 25.31131545028100049, -8.473030824119000215, -8.042950951552001015 ) ) ;
#55028=CARTESIAN_POINT ( 'NONE',  ( 13.42968832854747241, -11.50414049279774176, -1.837906235105113861 ) ) ;
#55029=FACE_OUTER_BOUND ( 'NONE', #16161, .T. ) ;
#55031=VERTEX_POINT ( 'NONE', #6925 ) ;
#55035=FACE_OUTER_BOUND ( 'NONE', #7017, .T. ) ;
#55042=ORIENTED_EDGE ( 'NONE', *, *, #9776, .F. ) ;
#55062=CARTESIAN_POINT ( 'NONE',  ( 24.30000561709021412, 8.853233208361997342, -8.853233208361997342 ) ) ;
#55064=AXIS2_PLACEMENT_3D ( 'NONE', #47611, #11559, #63669 ) ;
#55065=CARTESIAN_POINT ( 'NONE',  ( 16.86666666323366925, -3.595157417866057248, -11.99793599502774200 ) ) ;
#55080=VECTOR ( 'NONE', #66141, 1000.000000000000114 ) ;
#55083=CARTESIAN_POINT ( 'NONE',  ( 18.02449637307654129, 11.46556595593859562, -4.499409268768501668 ) ) ;
#55088=CARTESIAN_POINT ( 'NONE',  ( 12.99999999998900080, -12.39025855408000076, -1.832244667012999928 ) ) ;
#55091=EDGE_CURVE ( 'NONE', #43802, #23570, #60076, .T. ) ;
#55092=EDGE_CURVE ( 'NONE', #43147, #62317, #57954, .T. ) ;
#55093=FACE_OUTER_BOUND ( 'NONE', #48184, .T. ) ;
#55094=CARTESIAN_POINT ( 'NONE',  ( 23.59999196693599899, 2.915561532799999966, -13.58550759281999909 ) ) ;
#55098=CARTESIAN_POINT ( 'NONE',  ( 18.28771851938396154, -2.987294196519939327, -11.95930572916780399 ) ) ;
#55100=ORIENTED_EDGE ( 'NONE', *, *, #52353, .F. ) ;
#55108=ADVANCED_FACE ( 'NONE', ( #39438 ), #63774, .F. ) ;
#55110=CARTESIAN_POINT ( 'NONE',  ( 24.54223752976283635, -8.848832083081973110, 9.279389144537915968 ) ) ;
#55113=CIRCLE ( 'NONE', #55064, 0.3000000000000004330 ) ;
#55118=CARTESIAN_POINT ( 'NONE',  ( 16.13763077846600069, 3.625006537420000008, 11.03132468648999875 ) ) ;
#55128=CARTESIAN_POINT ( 'NONE',  ( 23.73547072523399848, -13.39655754821999878, -3.630386468378000053 ) ) ;
#55129=AXIS2_PLACEMENT_3D ( 'NONE', #40072, #35506, #39721 ) ;
#55133=CARTESIAN_POINT ( 'NONE',  ( 23.76527359064235512, 13.07191039515678987, -3.759479379680037425 ) ) ;
#55144=CARTESIAN_POINT ( 'NONE',  ( 11.83148568236900111, -12.32826180562000040, -1.876276850727000012 ) ) ;
#55156=TOROIDAL_SURFACE ( 'NONE', #64067, 12.20000000000000107, 0.6999999999999999556 ) ;
#55157=CARTESIAN_POINT ( 'NONE',  ( 21.60000052036195584, 13.89999947951999992, 2.298222147633000150E-09 ) ) ;
#55163=CARTESIAN_POINT ( 'NONE',  ( 24.38452337929200198, -8.887488439818000074, 8.991265583227999514 ) ) ;
#55171=CARTESIAN_POINT ( 'NONE',  ( 23.61755490549040459, 3.309897709845488478, 13.56828019137976504 ) ) ;
#55174=CARTESIAN_POINT ( 'NONE',  ( 25.52466892626799932, 2.886236140895999558, -11.27617498557999909 ) ) ;
#55187=CARTESIAN_POINT ( 'NONE',  ( 24.66807826201145204, 12.30863159257428485, 2.982840176812266542 ) ) ;
#55194=CARTESIAN_POINT ( 'NONE',  ( 23.61708149841600246, 2.918613252417999515, 13.53488618919000075 ) ) ;
#55196=EDGE_LOOP ( 'NONE', ( #35433, #14013, #58242, #28996 ) ) ;
#55197=CARTESIAN_POINT ( 'NONE',  ( 23.71897706907673964, -9.886090438455083174, 9.463268644442225153 ) ) ;
#55199=ORIENTED_EDGE ( 'NONE', *, *, #54128, .F. ) ;
#55201=LINE ( 'NONE', #12553, #61863 ) ;
#55206=DIRECTION ( 'NONE',  ( 0.000000000000000000, 0.9835354258236025382, 0.1807154286440004198 ) ) ;
#55210=AXIS2_PLACEMENT_3D ( 'NONE', #25590, #24561, #30838 ) ;
#55220=CARTESIAN_POINT ( 'NONE',  ( 18.38280243546500259, -11.68827787447999889, 4.347381705584999700 ) ) ;
#55228=AXIS2_PLACEMENT_3D ( 'NONE', #53322, #47391, #37573 ) ;
#55232=CARTESIAN_POINT ( 'NONE',  ( 24.15441502362300241, -3.593679633234999837, 12.72319232787999965 ) ) ;
#55236=CARTESIAN_POINT ( 'NONE',  ( 18.35167777225700192, 2.962063834667000073, -12.02051524900000068 ) ) ;
#55237=ADVANCED_FACE ( 'NONE', ( #62130 ), #8992, .T. ) ;
#55245=CARTESIAN_POINT ( 'NONE',  ( 24.53002386606100060, -3.319300011433999664, -12.04488764000000067 ) ) ;
#55250=B_SPLINE_CURVE_WITH_KNOTS ( 'NONE', 3,
 ( #32370, #6119, #22545, #33399 ),
 .UNSPECIFIED., .F., .F.,
 ( 4, 4 ),
 ( 0.000000000000000000, 1.000000000000000000 ),
 .UNSPECIFIED. ) ;
#55254=ORIENTED_EDGE ( 'NONE', *, *, #22214, .T. ) ;
#55255=CARTESIAN_POINT ( 'NONE',  ( 25.26979906455200009, 8.566782599371000728, 7.890677837420999374 ) ) ;
#55257=EDGE_CURVE ( 'NONE', #21413, #26398, #4426, .T. ) ;
#55267=CARTESIAN_POINT ( 'NONE',  ( 18.29983863915590803, 1.925365864301426200, 12.21183829863293724 ) ) ;
#55280=LINE ( 'NONE', #52945, #50347 ) ;
#55284=ADVANCED_FACE ( 'NONE', ( #35578 ), #20170, .F. ) ;
#55289=CARTESIAN_POINT ( 'NONE',  ( 18.50001572531400029, -2.908166856580999937, 12.18270046149000052 ) ) ;
#55291=CARTESIAN_POINT ( 'NONE',  ( 21.60000000000000142, 12.52500000000000036, 0.000000000000000000 ) ) ;
#55296=EDGE_LOOP ( 'NONE', ( #34003, #9473, #46626, #56390 ) ) ;
#55299=VERTEX_POINT ( 'NONE', #22234 ) ;
#55300=CARTESIAN_POINT ( 'NONE',  ( 24.83136278930371432, -3.060660479504548892, -11.69612704205236398 ) ) ;
#55321=CARTESIAN_POINT ( 'NONE',  ( 24.35365242081700288, -8.355077740067001102, -8.511587483820997946 ) ) ;
#55322=EDGE_CURVE ( 'NONE', #47655, #29725, #56427, .T. ) ;
#55326=CARTESIAN_POINT ( 'NONE',  ( 18.50003594167399967, 2.686563651857999613, 11.33603604486000016 ) ) ;
#55327=CARTESIAN_POINT ( 'NONE',  ( 24.42274717983899990, -3.752455261644000117, -12.53779156268999984 ) ) ;
#55330=AXIS2_PLACEMENT_3D ( 'NONE', #27324, #53550, #43414 ) ;
#55334=DIRECTION ( 'NONE',  ( 0.000000000000000000, 0.7455306007789014311, 0.6664713972124013397 ) ) ;
#55341=CARTESIAN_POINT ( 'NONE',  ( 15.91802873821099951, -8.603382153815999800, -8.072764124688998066 ) ) ;
#55345=ADVANCED_FACE ( 'NONE', ( #47789 ), #575, .F. ) ;
#55352=CARTESIAN_POINT ( 'NONE',  ( 11.64585080655600002, 3.555558855182999967, -11.95257446901999998 ) ) ;
#55362=CARTESIAN_POINT ( 'NONE',  ( 11.49999672495000524, 10.70720904779669524, -4.749689352253906982 ) ) ;
#55370=DIRECTION ( 'NONE',  ( 0.000000000000000000, 0.9421243786071877846, 0.3352635608502961828 ) ) ;
#55371=CARTESIAN_POINT ( 'NONE',  ( 23.66004879239100234, 0.000000000000000000, 0.000000000000000000 ) ) ;
#55372=CARTESIAN_POINT ( 'NONE',  ( 13.46547102624232117, -11.49951335169909683, -1.866756745165379483 ) ) ;
#55387=CARTESIAN_POINT ( 'NONE',  ( 11.30000000000000071, -11.28618258042000022, -10.08934826511999994 ) ) ;
#55388=ORIENTED_EDGE ( 'NONE', *, *, #12418, .F. ) ;
#55399=CARTESIAN_POINT ( 'NONE',  ( 19.89999966725400071, 12.52499966719000035, 3.709624234311000015E-10 ) ) ;
#55400=CARTESIAN_POINT ( 'NONE',  ( 11.83979429613600232, -11.64688653560999931, -1.860528257274000064 ) ) ;
#55414=CARTESIAN_POINT ( 'NONE',  ( 24.77999297203200157, 3.612935283031999845, 12.08260076442999953 ) ) ;
#55418=EDGE_LOOP ( 'NONE', ( #52726, #47116, #8464, #62859, #48224 ) ) ;
#55427=LINE ( 'NONE', #44944, #35995 ) ;
#55433=CARTESIAN_POINT ( 'NONE',  ( 23.56666365135700403, -11.61524011585000160, -3.333188920242000197 ) ) ;
#55435=CARTESIAN_POINT ( 'NONE',  ( 25.44994642811700203, 0.000000000000000000, 2.140509991476999645E-13 ) ) ;
#55441=FACE_BOUND ( 'NONE', #60304, .T. ) ;
#55443=CARTESIAN_POINT ( 'NONE',  ( 13.50003721581400029, -9.159934378815998812, -7.517910889891000537 ) ) ;
#55450=ADVANCED_FACE ( 'NONE', ( #10023 ), #64525, .F. ) ;
#55451=CARTESIAN_POINT ( 'NONE',  ( 24.01983190392353151, -12.68029376182448864, -3.458225379361195007 ) ) ;
#55462=VERTEX_POINT ( 'NONE', #16299 ) ;
#55463=CARTESIAN_POINT ( 'NONE',  ( 16.39999999485600313, -3.595156957901000094, -11.99794989424000136 ) ) ;
#55465=VECTOR ( 'NONE', #48768, 1000.000000000000000 ) ;
#55473=CARTESIAN_POINT ( 'NONE',  ( 24.57937622052009985, 3.599767751968668161, 12.25814915835329266 ) ) ;
#55476=CARTESIAN_POINT ( 'NONE',  ( 23.54917057566099814, -13.36598973949000069, -4.292165629430000351 ) ) ;
#55484=CARTESIAN_POINT ( 'NONE',  ( 24.57788509278177003, 12.41755320330292989, -3.012067450446723083 ) ) ;
#55489=EDGE_CURVE ( 'NONE', #37319, #41440, #15533, .T. ) ;
#55506=LINE ( 'NONE', #65637, #28730 ) ;
#55513=DIRECTION ( 'NONE',  ( 0.000000000000000000, 0.000000000000000000, -1.000000000000000000 ) ) ;
#55514=CARTESIAN_POINT ( 'NONE',  ( 30.60000000000000142, 0.000000000000000000, 0.000000000000000000 ) ) ;
#55520=CARTESIAN_POINT ( 'NONE',  ( 15.90018573812067615, -7.083264066697359418, -9.547770387689276106 ) ) ;
#55524=CARTESIAN_POINT ( 'NONE',  ( 17.79165415090800195, 3.528207907415000122, 11.96069611418000100 ) ) ;
#55527=CARTESIAN_POINT ( 'NONE',  ( 16.24412496488759317, 3.380981662632266183, 11.14874627148169672 ) ) ;
#55530=B_SPLINE_CURVE_WITH_KNOTS ( 'NONE', 3,
 ( #59498, #6010, #60201, #38523, #53571, #11951, #54605, #43077, #65430, #32940, #6352, #44132, #87, #31913, #5666, #10919, #27700, #48671, #6703, #37487, #776, #17553, #21405, #49016, #38879, #28044, #38168, #64043, #16846, #53228, #22091, #47985 ),
 .UNSPECIFIED., .F., .F.,
 ( 4, 2, 2, 2, 2, 2, 2, 2, 1, 2, 2, 2, 1, 1, 1, 2, 2, 4 ),
 ( 0.000000000000000000, 0.2500000000000330291, 0.3750000000000466294, 0.4375000000000535683, 0.4687500000000569544, 0.5000000000000602851, 0.6250000000000622835, 0.6875000000000632827, 0.7187500000000637268, 0.7343750000000640599, 0.7500000000000642819, 0.8125000000000637268, 0.8437500000000613953, 0.8593750000000611733, 0.8671875000000591749, 0.8710937500000600631, 0.8750000000000608402, 1.000000000000000000 ),
 .UNSPECIFIED. ) ;
#55535=EDGE_CURVE ( 'NONE', #46507, #54548, #60206, .T. ) ;
#55538=ORIENTED_EDGE ( 'NONE', *, *, #53523, .T. ) ;
#55539=CARTESIAN_POINT ( 'NONE',  ( 11.53943995709000170, -3.847421095330999741, 11.95976051375000004 ) ) ;
#55540=CARTESIAN_POINT ( 'NONE',  ( 13.99999997735699608, 8.821177874197267954, 7.709989353259445011 ) ) ;
#55549=CARTESIAN_POINT ( 'NONE',  ( 19.99999987597299977, 12.42499880353999941, 0.000000000000000000 ) ) ;
#55554=CARTESIAN_POINT ( 'NONE',  ( 13.49994651945300284, 12.07042783918999795, 2.492331243371999960 ) ) ;
#55558=ORIENTED_EDGE ( 'NONE', *, *, #41187, .T. ) ;
#55560=VECTOR ( 'NONE', #66537, 1000.000000000000000 ) ;
#55561=ORIENTED_EDGE ( 'NONE', *, *, #26944, .F. ) ;
#55568=CARTESIAN_POINT ( 'NONE',  ( 23.60205915885299888, 2.338900754078999444, -12.00073634674999212 ) ) ;
#55570=CARTESIAN_POINT ( 'NONE',  ( 18.12304911038100030, -11.48572971900999917, 4.352322683670000636 ) ) ;
#55574=AXIS2_PLACEMENT_3D ( 'NONE', #22229, #43566, #27142 ) ;
#55580=ORIENTED_EDGE ( 'NONE', *, *, #64949, .F. ) ;
#55581=DIRECTION ( 'NONE',  ( 0.000000000000000000, 0.000000000000000000, -1.000000000000000000 ) ) ;
#55583=CARTESIAN_POINT ( 'NONE',  ( 23.73832292375600161, -3.439035004086000047, 13.34772648052000044 ) ) ;
#55585=CARTESIAN_POINT ( 'NONE',  ( 18.44330693167099966, 2.998553466420000202, -12.10578145104000036 ) ) ;
#55590=ORIENTED_EDGE ( 'NONE', *, *, #33330, .T. ) ;
#55594=ADVANCED_FACE ( 'NONE', ( #1263 ), #16007, .F. ) ;
#55618=CARTESIAN_POINT ( 'NONE',  ( 24.40628504445000146, -12.24027098532000046, 3.187905388436000464 ) ) ;
#55624=ORIENTED_EDGE ( 'NONE', *, *, #2665, .T. ) ;
#55626=CARTESIAN_POINT ( 'NONE',  ( 23.57774091470277611, -2.928866170651173384, 13.64744915248744306 ) ) ;
#55633=CARTESIAN_POINT ( 'NONE',  ( 14.00000000000000178, 50.50083396221999976, 44.47484963936999947 ) ) ;
#55636=CIRCLE ( 'NONE', #39970, 1.000000000000000666 ) ;
#55639=CARTESIAN_POINT ( 'NONE',  ( 11.72005178113508173, 3.595543782877861805, -11.99782022136548143 ) ) ;
#55643=ORIENTED_EDGE ( 'NONE', *, *, #29770, .F. ) ;
#55647=ORIENTED_EDGE ( 'NONE', *, *, #55004, .T. ) ;
#55651=CARTESIAN_POINT ( 'NONE',  ( 23.61662973629609752, 13.40571813662669776, -3.919378641685453246 ) ) ;
#55658=EDGE_CURVE ( 'NONE', #55031, #12730, #64827, .T. ) ;
#55660=EDGE_CURVE ( 'NONE', #46963, #47396, #33777, .T. ) ;
#55664=LINE ( 'NONE', #29106, #2371 ) ;
#55666=CONICAL_SURFACE ( 'NONE', #31113, 12.42515511468000078, 0.7854106315584118425 ) ;
#55671=ORIENTED_EDGE ( 'NONE', *, *, #27755, .F. ) ;
#55673=CARTESIAN_POINT ( 'NONE',  ( 23.89320776801300283, -8.313844348291002717, -8.526065358951003148 ) ) ;
#55676=CARTESIAN_POINT ( 'NONE',  ( 24.32155364739020342, 12.72720341677420741, -3.095246424363175652 ) ) ;
#55678=CARTESIAN_POINT ( 'NONE',  ( 23.64071596919400164, -3.067373287554000072, -13.45661305457000090 ) ) ;
#55686=DIRECTION ( 'NONE',  ( 1.000000000000000000, 0.000000000000000000, 0.000000000000000000 ) ) ;
#55696=CARTESIAN_POINT ( 'NONE',  ( 23.59082918485488278, -13.38373040019899918, 4.039796375151918362 ) ) ;
#55711=DIRECTION ( 'NONE',  ( -5.233425451124840269E-15, 2.123563019594860353E-14, 1.000000000000000000 ) ) ;
#55717=CARTESIAN_POINT ( 'NONE',  ( 25.08881572089300249, 11.66016675852999818, 3.018805299122000019 ) ) ;
#55722=CARTESIAN_POINT ( 'NONE',  ( 23.60000000000000142, 9.517611874540000017, 8.103398312166000039 ) ) ;
#55725=CARTESIAN_POINT ( 'NONE',  ( 13.43019412026600179, 12.07125412582999857, 2.305633000807000066 ) ) ;
#55731=CARTESIAN_POINT ( 'NONE',  ( 25.05002146819219178, 2.896643222720280519, 11.52366225513116937 ) ) ;
#55737=EDGE_LOOP ( 'NONE', ( #34993, #52549 ) ) ;
#55741=EDGE_CURVE ( 'NONE', #35662, #47463, #60637, .T. ) ;
#55744=B_SPLINE_CURVE_WITH_KNOTS ( 'NONE', 3,
 ( #44134, #32942, #2170, #49709 ),
 .UNSPECIFIED., .F., .F.,
 ( 4, 4 ),
 ( 0.000000000000000000, 1.000000000000000000 ),
 .UNSPECIFIED. ) ;
#55746=ADVANCED_FACE ( 'NONE', ( #36088 ), #47272, .F. ) ;
#55762=ADVANCED_FACE ( 'NONE', ( #9168 ), #60790, .F. ) ;
#55772=FACE_OUTER_BOUND ( 'NONE', #42953, .T. ) ;
#55774=CARTESIAN_POINT ( 'NONE',  ( 16.39999997735698756, 3.306214596137839745, 11.23948664129755137 ) ) ;
#55776=ORIENTED_EDGE ( 'NONE', *, *, #44597, .T. ) ;
#55782=VERTEX_POINT ( 'NONE', #54580 ) ;
#55810=FACE_OUTER_BOUND ( 'NONE', #35384, .T. ) ;
#55819=CARTESIAN_POINT ( 'NONE',  ( 25.30000327618300204, 2.078227429405999693, -11.31065739696999906 ) ) ;
#55820=CARTESIAN_POINT ( 'NONE',  ( 17.80000000005199823, -3.345268251980999974, 11.86064071431999878 ) ) ;
#55821=ORIENTED_EDGE ( 'NONE', *, *, #38593, .F. ) ;
#55825=SURFACE_SIDE_STYLE ('',( #12481 ) ) ;
#55827=EDGE_LOOP ( 'NONE', ( #8107, #32569, #29585, #52790 ) ) ;
#55831=CARTESIAN_POINT ( 'NONE',  ( 24.01967453583397472, -3.345244851302060063, -12.71086981538412708 ) ) ;
#55837=ORIENTED_EDGE ( 'NONE', *, *, #19012, .T. ) ;
#55838=CARTESIAN_POINT ( 'NONE',  ( 24.30000000000000071, -12.80696435099000041, -50.50083396221000243 ) ) ;
#55849=B_SPLINE_CURVE_WITH_KNOTS ( 'NONE', 3,
 ( #55326, #29116, #38905, #54277 ),
 .UNSPECIFIED., .F., .F.,
 ( 4, 4 ),
 ( 0.000000000000000000, 1.000000000000000000 ),
 .UNSPECIFIED. ) ;
#55851=LINE ( 'NONE', #45705, #51631 ) ;
#55856=CARTESIAN_POINT ( 'NONE',  ( 25.29995758267499895, -11.13046986584000031, -3.427500733308000314 ) ) ;
#55862=ORIENTED_EDGE ( 'NONE', *, *, #6826, .T. ) ;
#55867=ORIENTED_EDGE ( 'NONE', *, *, #1617, .F. ) ;
#55877=CARTESIAN_POINT ( 'NONE',  ( 13.56663763856171734, -9.565814837444753138, -7.877123307579370071 ) ) ;
#55884=EDGE_CURVE ( 'NONE', #65259, #64287, #60860, .T. ) ;
#55892=CARTESIAN_POINT ( 'NONE',  ( 24.30001697071400457, -8.938702858184001343, 8.938676113071998941 ) ) ;
#55894=VERTEX_POINT ( 'NONE', #61209 ) ;
#55897=CARTESIAN_POINT ( 'NONE',  ( 18.49985170088394426, -7.837663500889314729E-14, -12.52499999999998792 ) ) ;
#55900=DIRECTION ( 'NONE',  ( 0.000000000000000000, -0.7455306007789014311, -0.6664713972124013397 ) ) ;
#55905=ORIENTED_EDGE ( 'NONE', *, *, #43168, .T. ) ;
#55910=EDGE_LOOP ( 'NONE', ( #65990, #5142, #20183, #32408 ) ) ;
#55927=AXIS2_PLACEMENT_3D ( 'NONE', #12932, #34258, #55581 ) ;
#55955=DIRECTION ( 'NONE',  ( 0.000000000000000000, -0.2714570858282905341, -0.9624505444715651947 ) ) ;
#55957=CARTESIAN_POINT ( 'NONE',  ( 24.35145719007200071, -12.30648751194999946, 3.205655321895999776 ) ) ;
#55958=CARTESIAN_POINT ( 'NONE',  ( 16.01451879247772681, 8.585242134253062929, 7.875498515383617892 ) ) ;
#55959=CYLINDRICAL_SURFACE ( 'NONE', #19694, 1.000000000000000000 ) ;
#55965=ADVANCED_FACE ( 'NONE', ( #35334 ), #8701, .F. ) ;
#55968=DIRECTION ( 'NONE',  ( 2.887756364189944304E-10, 0.4812251768484908099, -0.8765970164032835799 ) ) ;
#55979=CARTESIAN_POINT ( 'NONE',  ( 11.53926831409257403, 3.396912098314702977, -11.84566400435341649 ) ) ;
#55989=CARTESIAN_POINT ( 'NONE',  ( 29.60000000000000142, -2.052090822757999903E-07, 7.720759220056000238 ) ) ;
#55999=DIRECTION ( 'NONE',  ( 0.000000000000000000, 0.000000000000000000, -1.000000000000000000 ) ) ;
#56001=CARTESIAN_POINT ( 'NONE',  ( 23.58888327362420867, -10.33109198681894902, 9.338987663515077031 ) ) ;
#56004=CARTESIAN_POINT ( 'NONE',  ( 24.44496488009700030, 8.810487470433001178, 8.810507756548000557 ) ) ;
#56012=ORIENTED_EDGE ( 'NONE', *, *, #4071, .F. ) ;
#56014=CARTESIAN_POINT ( 'NONE',  ( 24.39664321829268800, 12.03536693101104049, -3.224866849775587241 ) ) ;
#56015=CARTESIAN_POINT ( 'NONE',  ( 23.61264779926599999, -3.132474875089000133, -13.53881878004999884 ) ) ;
#56017=CARTESIAN_POINT ( 'NONE',  ( 24.44496350777200178, -12.03536639536000052, -3.224849854974999985 ) ) ;
#56021=CARTESIAN_POINT ( 'NONE',  ( 23.59999445750599989, -13.22316420035999940, -4.267800004853000040 ) ) ;
#56022=DIRECTION ( 'NONE',  ( -1.000000000000000000, 0.000000000000000000, 0.000000000000000000 ) ) ;
#56028=CARTESIAN_POINT ( 'NONE',  ( 15.78404792230800346, -8.744893293839998805, -7.778646260181000471 ) ) ;
#56031=ORIENTED_EDGE ( 'NONE', *, *, #16561, .T. ) ;
#56039=VERTEX_POINT ( 'NONE', #3161 ) ;
#56045=DIRECTION ( 'NONE',  ( 5.026600068074292105E-17, 0.6482718649732923666, 0.7614089499631913061 ) ) ;
#56053=CARTESIAN_POINT ( 'NONE',  ( 13.91144947526900033, -8.829982735797999638, -7.819410275689000045 ) ) ;
#56058=VERTEX_POINT ( 'NONE', #45814 ) ;
#56062=VERTEX_POINT ( 'NONE', #23798 ) ;
#56067=CARTESIAN_POINT ( 'NONE',  ( 24.44496264144000364, 8.810483598181999554, -8.810508341310001157 ) ) ;
#56078=CARTESIAN_POINT ( 'NONE',  ( 25.29987667925500361, 10.83443035398000021, 3.855530949778000149 ) ) ;
#56082=B_SPLINE_CURVE_WITH_KNOTS ( 'NONE', 3,
 ( #26105, #16978, #26451, #32729, #48116, #47430, #48462, #42194, #27483, #48807, #68739, #570, #16294, #43214 ),
 .UNSPECIFIED., .F., .F.,
 ( 4, 2, 2, 2, 2, 2, 4 ),
 ( 0.000000000000000000, 0.1250000000000025813, 0.2500000000000051625, 0.5000000000000103251, 0.6250000000000096589, 0.7500000000000089928, 1.000000000000000000 ),
 .UNSPECIFIED. ) ;
#56086=CARTESIAN_POINT ( 'NONE',  ( 24.56500367226799852, -12.27494567759000077, -3.065703875465999761 ) ) ;
#56105=CARTESIAN_POINT ( 'NONE',  ( 23.63066106396900068, 10.04550756903999975, -9.752170026777999823 ) ) ;
#56106=CARTESIAN_POINT ( 'NONE',  ( 17.75917414208900169, -3.376094807733999836, -11.11072694497999969 ) ) ;
#56117=VERTEX_POINT ( 'NONE', #39538 ) ;
#56118=DIRECTION ( 'NONE',  ( -1.000000000000000000, 0.000000000000000000, 0.000000000000000000 ) ) ;
#56124=AXIS2_PLACEMENT_3D ( 'NONE', #7813, #19684, #35424 ) ;
#56133=CARTESIAN_POINT ( 'NONE',  ( 23.84129557661856680, -12.96064935002960539, -3.649606885852778593 ) ) ;
#56136=EDGE_LOOP ( 'NONE', ( #12759, #13168, #67581, #55671 ) ) ;
#56144=ORIENTED_EDGE ( 'NONE', *, *, #52394, .T. ) ;
#56146=CARTESIAN_POINT ( 'NONE',  ( 25.60000000000000142, 0.000000000000000000, 0.000000000000000000 ) ) ;
#56154=CARTESIAN_POINT ( 'NONE',  ( 17.92628954468417746, -3.345291551440210398, 11.86067033211894284 ) ) ;
#56159=CARTESIAN_POINT ( 'NONE',  ( 16.10004050617000004, 5.773856762095636697, 11.16084031980689417 ) ) ;
#56181=CARTESIAN_POINT ( 'NONE',  ( 24.53428991195500330, 3.614319144953999530, 12.31267516478999902 ) ) ;
#56182=AXIS2_PLACEMENT_3D ( 'NONE', #68193, #57709, #40953 ) ;
#56191=CARTESIAN_POINT ( 'NONE',  ( 18.29983863915590447, 0.9627071077475295446, -12.32514597913991850 ) ) ;
#56194=B_SPLINE_CURVE_WITH_KNOTS ( 'NONE', 3,
 ( #38715, #33474, #6889, #7936 ),
 .UNSPECIFIED., .F., .F.,
 ( 4, 4 ),
 ( 0.000000000000000000, 1.000000000000000000 ),
 .UNSPECIFIED. ) ;
#56199=CARTESIAN_POINT ( 'NONE',  ( 24.51327040776200050, 3.324719603035999782, 12.06512239505999950 ) ) ;
#56206=CARTESIAN_POINT ( 'NONE',  ( 23.56666365135700403, -2.009474831861002286, 11.63289034805000277 ) ) ;
#56214=VERTEX_POINT ( 'NONE', #25858 ) ;
#56219=DIRECTION ( 'NONE',  ( -1.000000000000000000, 0.000000000000000000, 0.000000000000000000 ) ) ;
#56220=VERTEX_POINT ( 'NONE', #41253 ) ;
#56232=EDGE_CURVE ( 'NONE', #51578, #33943, #53813, .T. ) ;
#56233=CARTESIAN_POINT ( 'NONE',  ( 16.24412496488131552, -3.380981662633991913, -11.14874627148116559 ) ) ;
#56234=CIRCLE ( 'NONE', #64042, 12.52500000000000036 ) ;
#56235=ORIENTED_EDGE ( 'NONE', *, *, #34906, .T. ) ;
#56236=CARTESIAN_POINT ( 'NONE',  ( 18.49993212792200126, -2.908182645667999999, -12.18276646858999968 ) ) ;
#56239=CARTESIAN_POINT ( 'NONE',  ( 14.46666666157666903, -8.833279249958291501, -7.896561128163722465 ) ) ;
#56240=CARTESIAN_POINT ( 'NONE',  ( 15.40000000000000036, 43.28911730077999920, 38.02789377380999980 ) ) ;
#56247=B_SPLINE_CURVE_WITH_KNOTS ( 'NONE', 3,
 ( #67943, #63381, #15156, #52211 ),
 .UNSPECIFIED., .F., .F.,
 ( 4, 4 ),
 ( 0.000000000000000000, 1.000000000000000000 ),
 .UNSPECIFIED. ) ;
#56248=CARTESIAN_POINT ( 'NONE',  ( 24.09354145009956838, 9.221916985538504363, 9.178197973474382820 ) ) ;
#56254=CARTESIAN_POINT ( 'NONE',  ( 18.23019412026500063, -3.031170125296999807, -11.90979123982999965 ) ) ;
#56262=ORIENTED_EDGE ( 'NONE', *, *, #31509, .T. ) ;
#56266=CARTESIAN_POINT ( 'NONE',  ( 23.85322410408000238, -3.520566476961000113, 13.16563783490999917 ) ) ;
#56267=CARTESIAN_POINT ( 'NONE',  ( 13.12913653430047134, 11.69120254989820573, 1.923246422712991066 ) ) ;
#56281=CIRCLE ( 'NONE', #40644, 11.26964301940000013 ) ;
#56284=AXIS2_PLACEMENT_3D ( 'NONE', #60968, #13083, #7474 ) ;
#56300=CARTESIAN_POINT ( 'NONE',  ( 12.09997738314739912, 11.69706276465918116, -3.884924152321057367 ) ) ;
#56301=CARTESIAN_POINT ( 'NONE',  ( 17.79999999998900151, 3.595165934733000057, -11.99793354950999991 ) ) ;
#56302=FACE_OUTER_BOUND ( 'NONE', #30430, .T. ) ;
#56315=EDGE_LOOP ( 'NONE', ( #24594, #42985, #54914, #39588 ) ) ;
#56318=CARTESIAN_POINT ( 'NONE',  ( 23.60000000000000142, 11.77655473258999841, -4.190794510628000680 ) ) ;
#56320=EDGE_CURVE ( 'NONE', #26090, #29376, #26333, .T. ) ;
#56326=CARTESIAN_POINT ( 'NONE',  ( 18.41194552102802007, 3.255591973369043934, -12.09481971601418415 ) ) ;
#56332=ORIENTED_EDGE ( 'NONE', *, *, #28904, .F. ) ;
#56334=CARTESIAN_POINT ( 'NONE',  ( 24.98034594679068121, -2.955830752047062138, -11.57694219477421704 ) ) ;
#56336=AXIS2_PLACEMENT_3D ( 'NONE', #55387, #60286, #1551 ) ;
#56347=VERTEX_POINT ( 'NONE', #3748 ) ;
#56357=EDGE_CURVE ( 'NONE', #30294, #60176, #32161, .T. ) ;
#56359=EDGE_CURVE ( 'NONE', #42844, #20915, #57149, .T. ) ;
#56361=CARTESIAN_POINT ( 'NONE',  ( 17.80000000001300009, -3.351264566333000072, 11.15757590352999884 ) ) ;
#56362=CARTESIAN_POINT ( 'NONE',  ( 24.67921570607400383, -3.567514742249000115, 12.13750887372000165 ) ) ;
#56363=CARTESIAN_POINT ( 'NONE',  ( 23.51521078797799902, -2.987649840005000001, -13.81502094324000041 ) ) ;
#56372=CARTESIAN_POINT ( 'NONE',  ( 24.30000000000000071, -10.83443035398000021, 3.855530949778000149 ) ) ;
#56374=CARTESIAN_POINT ( 'NONE',  ( 18.19991756629438484, 3.160410836633246845, 11.91446384612377862 ) ) ;
#56380=CARTESIAN_POINT ( 'NONE',  ( 23.59527583324263134, -13.38802479761197972, 4.017745927562742736 ) ) ;
#56388=CARTESIAN_POINT ( 'NONE',  ( 13.50018479229300006, 11.60142623882999935, 2.415183939829000259 ) ) ;
#56390=ORIENTED_EDGE ( 'NONE', *, *, #32163, .F. ) ;
#56396=B_SPLINE_CURVE_WITH_KNOTS ( 'NONE', 3,
 ( #66128, #60548, #65434, #54608 ),
 .UNSPECIFIED., .F., .F.,
 ( 4, 4 ),
 ( 0.000000000000000000, 1.000000000000000000 ),
 .UNSPECIFIED. ) ;
#56399=CARTESIAN_POINT ( 'NONE',  ( 25.46373029971899982, -8.354610197568000274, -8.148451206582999262 ) ) ;
#56401=ORIENTED_EDGE ( 'NONE', *, *, #66914, .F. ) ;
#56404=CARTESIAN_POINT ( 'NONE',  ( 23.59718018307008336, 13.38963915723865306, 4.008749883956627791 ) ) ;
#56408=CARTESIAN_POINT ( 'NONE',  ( 16.13886389318898651, 3.397126321181335395, 11.84561170022415766 ) ) ;
#56420=VERTEX_POINT ( 'NONE', #57580 ) ;
#56423=CARTESIAN_POINT ( 'NONE',  ( 25.59994555223700274, -9.407310119912859037, 6.227539428020667955 ) ) ;
#56424=ORIENTED_EDGE ( 'NONE', *, *, #23279, .F. ) ;
#56427=B_SPLINE_CURVE_WITH_KNOTS ( 'NONE', 3,
 ( #53712, #68745, #16645, #20861 ),
 .UNSPECIFIED., .F., .F.,
 ( 4, 4 ),
 ( 0.000000000000000000, 1.000000000000000000 ),
 .UNSPECIFIED. ) ;
#56428=VERTEX_POINT ( 'NONE', #9336 ) ;
#56431=CIRCLE ( 'NONE', #27377, 11.79499999999999993 ) ;
#56432=CARTESIAN_POINT ( 'NONE',  ( 11.53937873044000106, -11.52961813267000046, -1.376592384073999975 ) ) ;
#56437=ORIENTED_EDGE ( 'NONE', *, *, #44195, .F. ) ;
#56451=CARTESIAN_POINT ( 'NONE',  ( 25.20341525953400108, 8.548126993989999534, -7.997462102762000313 ) ) ;
#56452=CARTESIAN_POINT ( 'NONE',  ( 25.37958977069655475, -3.026682599187875855, -11.38056660099664086 ) ) ;
#56453=ADVANCED_FACE ( 'NONE', ( #41852 ), #31034, .T. ) ;
#56460=EDGE_CURVE ( 'NONE', #43730, #60967, #23856, .T. ) ;
#56463=CARTESIAN_POINT ( 'NONE',  ( 23.56666365135700403, -11.07911597678999271, -4.076188921308005142 ) ) ;
#56470=B_SPLINE_CURVE_WITH_KNOTS ( 'NONE', 3,
 ( #28102, #60261, #34047, #837 ),
 .UNSPECIFIED., .F., .F.,
 ( 4, 4 ),
 ( 0.000000000000000000, 1.000000000000000000 ),
 .UNSPECIFIED. ) ;
#56472=CARTESIAN_POINT ( 'NONE',  ( 18.49996808500599954, 0.9036517535198380635, -11.64999999999999858 ) ) ;
#56478=CARTESIAN_POINT ( 'NONE',  ( 24.26682857475500299, 3.229948578041999863, -12.20213974738999951 ) ) ;
#56484=CARTESIAN_POINT ( 'NONE',  ( 13.43176382712000105, -11.67665677335000041, -2.247227628037000269 ) ) ;
#56491=CARTESIAN_POINT ( 'NONE',  ( 16.13937158902900393, 3.642730659064999710, 11.02533040164999889 ) ) ;
#56503=B_SPLINE_CURVE_WITH_KNOTS ( 'NONE', 3,
 ( #36963, #20876, #37299, #14942, #47109, #26820, #42547, #42213, #36614, #41855 ),
 .UNSPECIFIED., .F., .F.,
 ( 4, 2, 2, 2, 4 ),
 ( 0.000000000000000000, 0.2500000000000000000, 0.5000000000000000000, 0.7500000000000000000, 1.000000000000000000 ),
 .UNSPECIFIED. ) ;
#56504=DIRECTION ( 'NONE',  ( 0.000000000000000000, 0.000000000000000000, -1.000000000000000000 ) ) ;
#56507=ORIENTED_EDGE ( 'NONE', *, *, #46031, .T. ) ;
#56511=CARTESIAN_POINT ( 'NONE',  ( 24.14319218954479851, -3.327217583210993812, -12.48607456098757318 ) ) ;
#56516=EDGE_CURVE ( 'NONE', #56220, #7173, #63832, .T. ) ;
#56521=CARTESIAN_POINT ( 'NONE',  ( 25.46373024410000241, -11.23407150414000100, 3.161076981347000103 ) ) ;
#56527=CARTESIAN_POINT ( 'NONE',  ( 23.73393238974700026, 13.39775320304000061, 3.632760668476999744 ) ) ;
#56529=ORIENTED_EDGE ( 'NONE', *, *, #12672, .T. ) ;
#56532=CARTESIAN_POINT ( 'NONE',  ( 16.04331666222400088, 9.026410239312001593, 8.606113518243997618 ) ) ;
#56535=CARTESIAN_POINT ( 'NONE',  ( 23.56666365135700403, -2.009474831917003268, -11.63289034803000455 ) ) ;
#56537=EDGE_CURVE ( 'NONE', #58094, #5174, #41078, .T. ) ;
#56541=CARTESIAN_POINT ( 'NONE',  ( 24.53002386606100060, 3.319300011433999664, 12.04488764000000067 ) ) ;
#56543=CARTESIAN_POINT ( 'NONE',  ( 23.64712440262699999, 10.02868315663000054, 9.634752534433001614 ) ) ;
#56549=ORIENTED_EDGE ( 'NONE', *, *, #12563, .T. ) ;
#56552=CARTESIAN_POINT ( 'NONE',  ( 17.79046541331000242, 3.643254180937999909, 12.02383733079000017 ) ) ;
#56561=CARTESIAN_POINT ( 'NONE',  ( 17.60000001072100062, -11.41073498373000028, 4.623967591968000335 ) ) ;
#56564=CARTESIAN_POINT ( 'NONE',  ( 11.31944011432000075, -3.562654288336999819, 11.75631193234000094 ) ) ;
#56567=B_SPLINE_CURVE_WITH_KNOTS ( 'NONE', 3,
 ( #8472, #24890, #9484, #35728, #61267, #40620 ),
 .UNSPECIFIED., .F., .F.,
 ( 4, 2, 4 ),
 ( 0.000000000000000000, 0.5000000000000000000, 1.000000000000000000 ),
 .UNSPECIFIED. ) ;
#56572=VERTEX_POINT ( 'NONE', #21552 ) ;
#56576=CARTESIAN_POINT ( 'NONE',  ( 16.39999999379500295, -3.351248059343999941, -11.15756683833000018 ) ) ;
#56583=CARTESIAN_POINT ( 'NONE',  ( 19.39373726536100051, 11.26964301940000013, 9.577061366172998945E-14 ) ) ;
#56591=CARTESIAN_POINT ( 'NONE',  ( 24.22569962767899199, 9.032524208146405442, 9.032526752365093614 ) ) ;
#56596=CARTESIAN_POINT ( 'NONE',  ( 14.93333333127366735, 8.815235367372475039, 7.616700428521842703 ) ) ;
#56597=CARTESIAN_POINT ( 'NONE',  ( 18.40156003475500057, -3.148349829928000165, -12.06792178657999948 ) ) ;
#56606=DIRECTION ( 'NONE',  ( 1.000000000000000000, 0.000000000000000000, 0.000000000000000000 ) ) ;
#56608=ADVANCED_FACE ( 'NONE', ( #49856 ), #39369, .F. ) ;
#56613=CARTESIAN_POINT ( 'NONE',  ( 23.55075186166400059, -13.34760076072000068, 4.341130030273000706 ) ) ;
#56635=CARTESIAN_POINT ( 'NONE',  ( 25.30000327618300204, 9.659335867304680079, 6.394377797198711910 ) ) ;
#56644=CARTESIAN_POINT ( 'NONE',  ( 11.79999999684100054, -3.345264396959000130, 11.86064773189999855 ) ) ;
#56647=CARTESIAN_POINT ( 'NONE',  ( 24.30001131568331729, -3.256147847238520132, -12.15210920284597407 ) ) ;
#56652=( BOUNDED_SURFACE ( )  B_SPLINE_SURFACE ( 3, 3, ( 
 ( #3574, #14084, #2549, #9165 ),
 ( #23876, #66518, #35071, #29494 ),
 ( #46240, #51142, #35409, #56736 ),
 ( #14429, #35748, #57066, #21040 ) ),
 .UNSPECIFIED., .F., .F., .T. ) 
 B_SPLINE_SURFACE_WITH_KNOTS ( ( 4, 4 ),
 ( 4, 4 ),
 ( 0.000000000000000000, 1.000000000000000000 ),
 ( 0.000000000000000000, 1.000000000000000000 ),
 .UNSPECIFIED. ) 
 GEOMETRIC_REPRESENTATION_ITEM ( )  RATIONAL_B_SPLINE_SURFACE ( (
 ( 1.512182578520000042, 1.160176301760999840, 1.160176301760999840, 1.512182578520000042),
 ( 1.111288591041000196, 0.8526025270081000196, 0.8526025270081000196, 1.111288591041000196),
 ( 1.111288591041000196, 0.8526025270081000196, 0.8526025270081000196, 1.111288591041000196),
 ( 1.512182578520000042, 1.160176301760999840, 1.160176301760999840, 1.512182578520000042) ) ) 
 REPRESENTATION_ITEM ( '' )  SURFACE ( )  );
#56653=CARTESIAN_POINT ( 'NONE',  ( 24.44496356267099912, -8.810485190366000197, 8.810508100388000585 ) ) ;
#56655=AXIS2_PLACEMENT_3D ( 'NONE', #19674, #40310, #67209 ) ;
#56661=LINE ( 'NONE', #45142, #28636 ) ;
#56670=B_SPLINE_CURVE_WITH_KNOTS ( 'NONE', 3,
 ( #19333, #35092, #20368, #41356, #40659, #56754, #51494, #9525, #14103, #56404, #25268, #9182, #8506, #41009, #41692, #62331 ),
 .UNSPECIFIED., .F., .F.,
 ( 4, 2, 2, 2, 2, 2, 2, 4 ),
 ( 0.000000000000000000, 0.1249999999999919509, 0.1874999999999888978, 0.2499999999999858447, 0.3749999999999896749, 0.4374999999999915623, 0.4999999999999935607, 1.000000000000000000 ),
 .UNSPECIFIED. ) ;
#56671=EDGE_CURVE ( 'NONE', #30666, #34183, #38841, .T. ) ;
#56673=CARTESIAN_POINT ( 'NONE',  ( 16.10004050617000004, -3.886235259787000018, -11.90683839252000098 ) ) ;
#56680=EDGE_LOOP ( 'NONE', ( #33725, #16950, #63166, #23946 ) ) ;
#56694=CARTESIAN_POINT ( 'NONE',  ( 11.79999999471800010, 3.216299622513999701, -11.40340969442000052 ) ) ;
#56702=ORIENTED_EDGE ( 'NONE', *, *, #68407, .T. ) ;
#56704=CIRCLE ( 'NONE', #14285, 1.000000000000000666 ) ;
#56705=CARTESIAN_POINT ( 'NONE',  ( 25.26999686867947759, 8.359966454775140221, 8.486712842816988456 ) ) ;
#56706=ORIENTED_EDGE ( 'NONE', *, *, #7743, .F. ) ;
#56728=ORIENTED_EDGE ( 'NONE', *, *, #56516, .T. ) ;
#56734=CARTESIAN_POINT ( 'NONE',  ( 23.55075821821200321, -2.914207289901999953, 13.72993041849000129 ) ) ;
#56736=CARTESIAN_POINT ( 'NONE',  ( 23.60205915885299888, 11.72032963058999400, -3.891881970957998593 ) ) ;
#56738=CARTESIAN_POINT ( 'NONE',  ( 23.56666365135700403, 9.069641144872004901, -7.556701426719000025 ) ) ;
#56746=CARTESIAN_POINT ( 'NONE',  ( 24.70770306079000278, -3.610860736573000107, 12.15153796058999980 ) ) ;
#56754=CARTESIAN_POINT ( 'NONE',  ( 23.62146722581017144, 13.40161425103470805, 3.915220144369890853 ) ) ;
#56755=CARTESIAN_POINT ( 'NONE',  ( 24.44496356267099912, -8.810485190366000197, 8.810508100388000585 ) ) ;
#56764=CYLINDRICAL_SURFACE ( 'NONE', #16739, 1.000000000000000666 ) ;
#56777=CONICAL_SURFACE ( 'NONE', #44509, 13.94232984211000037, 1.233427423210649021 ) ;
#56782=CARTESIAN_POINT ( 'NONE',  ( 11.26375800691000073, -11.80847110903000186, -1.384521730739000089 ) ) ;
#56785=CARTESIAN_POINT ( 'NONE',  ( 13.73895793914714680, -8.868838256396809783, -7.856013393113983945 ) ) ;
#56793=CARTESIAN_POINT ( 'NONE',  ( 18.24051303026600124, 3.055556278716000218, 11.39470302754000031 ) ) ;
#56798=EDGE_CURVE ( 'NONE', #26237, #60415, #10471, .T. ) ;
#56801=CARTESIAN_POINT ( 'NONE',  ( 24.14113419639268798, 3.327735694157559099, 12.48984860408194031 ) ) ;
#56802=CARTESIAN_POINT ( 'NONE',  ( 23.86947024834200093, 9.628432572233000641, -9.781540490154000622 ) ) ;
#56803=CARTESIAN_POINT ( 'NONE',  ( 18.53959992722300143, -2.682146997965999979, -11.29770844980000000 ) ) ;
#56810=CARTESIAN_POINT ( 'NONE',  ( 23.89320776801300283, -11.54071136943000297, -2.936967729234000402 ) ) ;
#56817=CARTESIAN_POINT ( 'NONE',  ( 16.10004050617000004, -3.886235259787000018, -11.90683839252000098 ) ) ;
#56819=CARTESIAN_POINT ( 'NONE',  ( 24.67921570607400383, -3.567514742249000115, 12.13750887372000165 ) ) ;
#56829=EDGE_CURVE ( 'NONE', #46546, #61230, #19647, .T. ) ;
#56831=ADVANCED_FACE ( 'NONE', ( #3330 ), #9600, .T. ) ;
#56834=CARTESIAN_POINT ( 'NONE',  ( 13.43887202961200167, -11.47449689335000045, -1.782105406474000064 ) ) ;
#56853=EDGE_CURVE ( 'NONE', #62750, #12534, #60505, .T. ) ;
#56858=ADVANCED_FACE ( 'NONE', ( #35165 ), #67296, .T. ) ;
#56866=VERTEX_POINT ( 'NONE', #35503 ) ;
#56873=CARTESIAN_POINT ( 'NONE',  ( 23.58436998763100334, 13.25821845536999888, 4.304235178824000307 ) ) ;
#56877=CARTESIAN_POINT ( 'NONE',  ( 15.90830001818700090, 9.238654026387999707, 8.377706362734000933 ) ) ;
#56881=DIRECTION ( 'NONE',  ( -0.9999999999991096011, 6.425037516353057767E-07, 1.169597258120009531E-06 ) ) ;
#56883=DIRECTION ( 'NONE',  ( 1.000000000000000000, 0.000000000000000000, 0.000000000000000000 ) ) ;
#56887=CARTESIAN_POINT ( 'NONE',  ( 24.44917776433500123, 3.519943607436000210, 12.30316564740000196 ) ) ;
#56892=CARTESIAN_POINT ( 'NONE',  ( 23.60000000000000142, -11.49391741900999975, -4.090215442373000165 ) ) ;
#56896=CARTESIAN_POINT ( 'NONE',  ( 18.35309301929700254, 2.844470671424999875, 12.04740840676999802 ) ) ;
#56906=CARTESIAN_POINT ( 'NONE',  ( 11.68591862085600219, -3.663505620393999962, 12.01771987839999944 ) ) ;
#56931=CARTESIAN_POINT ( 'NONE',  ( 25.50736871274565232, -8.309691349922452730, -8.116382010822352555 ) ) ;
#56933=B_SPLINE_SURFACE_WITH_KNOTS ( 'NONE', 3, 3, ( 
 ( #24957, #67592, #19367, #25299 ),
 ( #35121, #52210, #40352, #66912 ),
 ( #18690, #20056, #56086, #41384 ),
 ( #29544, #8195, #62694, #3287 ),
 ( #35460, #30217, #29886, #51194 ),
 ( #50846, #14814, #40689, #36135 ) ),
 .UNSPECIFIED., .F., .F., .F.,
 ( 4, 1, 1, 4 ),
 ( 4, 4 ),
 ( 0.1423941366080999915, 0.3333333333333000081, 0.6666666666667000474, 0.8219462302418999444 ),
 ( -0.1256563615234000120, 1.125656361508000192 ),
 .UNSPECIFIED. ) ;
#56939=CARTESIAN_POINT ( 'NONE',  ( 17.85446786537200126, -3.297647132553999771, -11.83458225989999946 ) ) ;
#56940=CARTESIAN_POINT ( 'NONE',  ( 24.36958145734899972, -8.861545501181000262, 8.807436093055001081 ) ) ;
#56945=ORIENTED_EDGE ( 'NONE', *, *, #50265, .F. ) ;
#56948=CARTESIAN_POINT ( 'NONE',  ( 12.80000000000000071, -11.23412379136000006, 3.084957477885999833 ) ) ;
#56953=CARTESIAN_POINT ( 'NONE',  ( 18.06944243593800081, 3.222040310929999762, -11.85748006108999952 ) ) ;
#56968=CARTESIAN_POINT ( 'NONE',  ( 11.40156680346000151, -3.471758886279999956, 11.27177987500999912 ) ) ;
#56977=ORIENTED_EDGE ( 'NONE', *, *, #19128, .T. ) ;
#56981=CARTESIAN_POINT ( 'NONE',  ( 13.60261247405900242, -9.239907047945001395, -8.094831983377998696 ) ) ;
#56985=CARTESIAN_POINT ( 'NONE',  ( 17.60000000000000142, 10.78295181803999903, -4.410266442048000002 ) ) ;
#56986=CARTESIAN_POINT ( 'NONE',  ( 25.29995823066400362, -11.13046982544999963, 3.427501264366999756 ) ) ;
#56988=EDGE_LOOP ( 'NONE', ( #38765, #54882, #32655, #52101 ) ) ;
#57006=CARTESIAN_POINT ( 'NONE',  ( 11.30000000000000071, 0.000000000000000000, 0.000000000000000000 ) ) ;
#57009=EDGE_LOOP ( 'NONE', ( #6823, #7591, #37306, #51421, #28616 ) ) ;
#57014=CARTESIAN_POINT ( 'NONE',  ( 23.58888331804951122, 13.25334641141371073, 4.277494313177894192 ) ) ;
#57040=CARTESIAN_POINT ( 'NONE',  ( 24.52301464528887465, -3.339127113045694095, 12.06936612931750297 ) ) ;
#57041=CARTESIAN_POINT ( 'NONE',  ( 15.61911349846455899, 9.449623925638377386, 8.220739594287655549 ) ) ;
#57044=EDGE_CURVE ( 'NONE', #23400, #1871, #58035, .T. ) ;
#57046=CARTESIAN_POINT ( 'NONE',  ( 25.50740514701198336, 11.18379543759817984, -3.138198361856242347 ) ) ;
#57058=CARTESIAN_POINT ( 'NONE',  ( 23.58414895174732351, -13.37550325405040397, 4.077674481848631238 ) ) ;
#57065=AXIS2_PLACEMENT_3D ( 'NONE', #3048, #24380, #7959 ) ;
#57066=CARTESIAN_POINT ( 'NONE',  ( 23.56666365135700403, 12.07812737763999955, -3.551569042617998662 ) ) ;
#57068=DIRECTION ( 'NONE',  ( -1.000000000000000000, 0.000000000000000000, 0.000000000000000000 ) ) ;
#57080=CARTESIAN_POINT ( 'NONE',  ( 23.56665676678199972, 13.31363904818000066, -4.296982115204999175 ) ) ;
#57090=ORIENTED_EDGE ( 'NONE', *, *, #60693, .T. ) ;
#57094=CARTESIAN_POINT ( 'NONE',  ( 18.43276988671242123, 2.975106096549898549, -11.26378872114027274 ) ) ;
#57095=CARTESIAN_POINT ( 'NONE',  ( 13.55370778485685435, 9.344737785247383854, 8.032732227356667920 ) ) ;
#57100=ORIENTED_EDGE ( 'NONE', *, *, #21053, .F. ) ;
#57105=FILL_AREA_STYLE ('',( #19711 ) ) ;
#57106=ORIENTED_EDGE ( 'NONE', *, *, #45145, .F. ) ;
#57109=CARTESIAN_POINT ( 'NONE',  ( 12.10000669845703847, 11.02846243759400124, -3.754394857303852362 ) ) ;
#57119=CARTESIAN_POINT ( 'NONE',  ( 18.23176382712000176, 2.916721637292999603, 11.52766586543999949 ) ) ;
#57123=EDGE_CURVE ( 'NONE', #1716, #23725, #25314, .T. ) ;
#57124=VERTEX_POINT ( 'NONE', #43144 ) ;
#57131=CARTESIAN_POINT ( 'NONE',  ( 24.63399677426199830, 8.686855860201999846, -8.588054097598998737 ) ) ;
#57132=CARTESIAN_POINT ( 'NONE',  ( 24.23232877498800164, 9.064816052010000291, -9.162332550022000532 ) ) ;
#57133=CARTESIAN_POINT ( 'NONE',  ( 18.26087891924500184, -2.716433685251999908, -11.57325030293000090 ) ) ;
#57138=CARTESIAN_POINT ( 'NONE',  ( 16.00000000448733672, -11.41071763184507759, 4.623975355603788806 ) ) ;
#57145=ADVANCED_FACE ( 'NONE', ( #26731 ), #47711, .T. ) ;
#57148=AXIS2_PLACEMENT_3D ( 'NONE', #51164, #8508, #13759 ) ;
#57149=B_SPLINE_CURVE_WITH_KNOTS ( 'NONE', 3,
 ( #14602, #9684, #36611, #25084, #46417, #62820 ),
 .UNSPECIFIED., .F., .F.,
 ( 4, 2, 4 ),
 ( 0.000000000000000000, 0.5000000000000000000, 1.000000000000000000 ),
 .UNSPECIFIED. ) ;
#57151=CARTESIAN_POINT ( 'NONE',  ( 25.00272134720554007, -3.413729871556085982, 11.76143154378893030 ) ) ;
#57158=VERTEX_POINT ( 'NONE', #21135 ) ;
#57166=ORIENTED_EDGE ( 'NONE', *, *, #69042, .F. ) ;
#57178=CARTESIAN_POINT ( 'NONE',  ( 16.39999997735699822, -3.306214596137841966, -11.23948664129755493 ) ) ;
#57188=CARTESIAN_POINT ( 'NONE',  ( 23.99446517519106692, 12.72130897981146802, -3.481316059523209105 ) ) ;
#57189=CARTESIAN_POINT ( 'NONE',  ( 11.79999999713068703, -12.23671679745269181, -1.944304699248228685 ) ) ;
#57201=CARTESIAN_POINT ( 'NONE',  ( 16.39999999231800132, -3.216285993016000155, -11.40340220863999932 ) ) ;
#57204=ORIENTED_EDGE ( 'NONE', *, *, #57207, .F. ) ;
#57207=EDGE_CURVE ( 'NONE', #59568, #16464, #42460, .T. ) ;
#57208=CARTESIAN_POINT ( 'NONE',  ( 15.39284288850700122, 9.264553731144999915, 8.207894312349999666 ) ) ;
#57214=DIRECTION ( 'NONE',  ( 1.000000000000000000, 0.000000000000000000, 0.000000000000000000 ) ) ;
#57222=CARTESIAN_POINT ( 'NONE',  ( 18.30000000000000071, -14.70300865175000027, 5.744762642578000289 ) ) ;
#57223=ADVANCED_FACE ( 'NONE', ( #53292 ), #5394, .T. ) ;
#57224=CARTESIAN_POINT ( 'NONE',  ( 17.10000000000000142, -3.283787102340999464, -11.28049554847999936 ) ) ;
#57228=CARTESIAN_POINT ( 'NONE',  ( 18.16350100824700320, 3.138009765975000143, 11.88148072165000002 ) ) ;
#57232=CARTESIAN_POINT ( 'NONE',  ( 12.99999999998900080, 12.39025855408000076, 1.832244667012999928 ) ) ;
#57235=CARTESIAN_POINT ( 'NONE',  ( 24.54223752889060961, 8.848832083880790123, -9.279389145428778463 ) ) ;
#57236=CARTESIAN_POINT ( 'NONE',  ( 15.40000000005200143, 9.187454762873001002, 8.213177997099000649 ) ) ;
#57245=DIRECTION ( 'NONE',  ( 1.000000000000000000, 0.000000000000000000, 0.000000000000000000 ) ) ;
#57267=CARTESIAN_POINT ( 'NONE',  ( 18.30830001818700126, -3.300182612895000478, -12.02694835946000040 ) ) ;
#57271=FACE_OUTER_BOUND ( 'NONE', #41843, .T. ) ;
#57273=EDGE_LOOP ( 'NONE', ( #769, #64396, #19543, #57632 ) ) ;
#57277=FACE_BOUND ( 'NONE', #18551, .T. ) ;
#57282=CARTESIAN_POINT ( 'NONE',  ( 23.61813716858800305, -13.16714277698999958, 4.271540868536000346 ) ) ;
#57289=CARTESIAN_POINT ( 'NONE',  ( 13.99999999231800096, 8.833253877201999060, 7.896562762484000686 ) ) ;
#57295=CONICAL_SURFACE ( 'NONE', #5940, 12.42510776559999996, 0.7854022111938739892 ) ;
#57297=CARTESIAN_POINT ( 'NONE',  ( 25.19214487158300031, 8.466223133107002141, 8.226644165488000482 ) ) ;
#57299=CARTESIAN_POINT ( 'NONE',  ( 25.44994642811700203, 1.048050535245999973E-13, -6.616929226765999876E-14 ) ) ;
#57301=CARTESIAN_POINT ( 'NONE',  ( 13.99999999485600277, 9.471999751521998689, 8.194948195317001804 ) ) ;
#57305=DIRECTION ( 'NONE',  ( -1.000000000000000000, 0.000000000000000000, 0.000000000000000000 ) ) ;
#57310=ORIENTED_EDGE ( 'NONE', *, *, #63680, .F. ) ;
#57317=CARTESIAN_POINT ( 'NONE',  ( 13.73854985688900143, -9.171197327466000360, -8.173482659384999849 ) ) ;
#57319=CARTESIAN_POINT ( 'NONE',  ( 12.79999998712400178, -11.53033693765999779, 4.891431908114999949 ) ) ;
#57331=ORIENTED_EDGE ( 'NONE', *, *, #2992, .T. ) ;
#57337=CARTESIAN_POINT ( 'NONE',  ( 24.22565377178775137, -3.306156338801836458, 12.33873653827660455 ) ) ;
#57338=CARTESIAN_POINT ( 'NONE',  ( 17.79999999998900151, 3.595165934733000057, -11.99793354950999991 ) ) ;
#57344=CARTESIAN_POINT ( 'NONE',  ( 15.49019623963660308, -9.469115506160978413, -8.198265202209942260 ) ) ;
#57345=CARTESIAN_POINT ( 'NONE',  ( 13.25828219467850388, -12.15323025559006531, -2.051492516881108230 ) ) ;
#57346=ORIENTED_EDGE ( 'NONE', *, *, #37310, .T. ) ;
#57360=PLANE ( 'NONE',  #26989 ) ;
#57363=CARTESIAN_POINT ( 'NONE',  ( 24.66807826201277010, -3.571100427736410676, -12.15100773339871232 ) ) ;
#57365=AXIS2_PLACEMENT_3D ( 'NONE', #13630, #67768, #34955 ) ;
#57372=EDGE_CURVE ( 'NONE', #4626, #40201, #15433, .T. ) ;
#57373=VERTEX_POINT ( 'NONE', #23543 ) ;
#57380=DIRECTION ( 'NONE',  ( 0.000000000000000000, -1.000000000000000000, 0.000000000000000000 ) ) ;
#57389=CARTESIAN_POINT ( 'NONE',  ( 15.36427412810700055, -8.819457004710999470, -7.692809699200999773 ) ) ;
#57391=CARTESIAN_POINT ( 'NONE',  ( 17.10000000000000142, 3.470217030164000072, 11.92928724693999953 ) ) ;
#57403=CARTESIAN_POINT ( 'NONE',  ( 23.62942910622400206, 3.420921953095000134, -13.57770915236000064 ) ) ;
#57404=ORIENTED_EDGE ( 'NONE', *, *, #17210, .T. ) ;
#57406=CIRCLE ( 'NONE', #44058, 9.250000000000000000 ) ;
#57413=VECTOR ( 'NONE', #27089, 1000.000000000000114 ) ;
#57418=CARTESIAN_POINT ( 'NONE',  ( 23.73953442324672025, 3.508702049063129547, -13.37373019756607739 ) ) ;
#57421=DIRECTION ( 'NONE',  ( 0.000000000000000000, 0.7071067811865475727, 0.7071067811865475727 ) ) ;
#57427=ORIENTED_EDGE ( 'NONE', *, *, #14802, .T. ) ;
#57433=EDGE_CURVE ( 'NONE', #59370, #56214, #19731, .T. ) ;
#57436=CARTESIAN_POINT ( 'NONE',  ( 11.53926573483131968, -12.16827677290229737, -1.947218182817292975 ) ) ;
#57438=CARTESIAN_POINT ( 'NONE',  ( 13.67057712374000289, 9.352787036275000077, 8.106596622149000453 ) ) ;
#57440=ORIENTED_EDGE ( 'NONE', *, *, #60927, .T. ) ;
#57446=CARTESIAN_POINT ( 'NONE',  ( 17.80000000005199823, -3.345268251980999974, 11.86064071431999878 ) ) ;
#57450=CARTESIAN_POINT ( 'NONE',  ( 12.10154284453400209, 11.81398323980999976, -3.695357857504999899 ) ) ;
#57453=LINE ( 'NONE', #46642, #3929 ) ;
#57465=CARTESIAN_POINT ( 'NONE',  ( 23.60000333944509521, 2.996291596448416694, 13.57008848946830248 ) ) ;
#57466=CARTESIAN_POINT ( 'NONE',  ( 24.63626978684600033, 8.802569683972000902, -9.348439433646998253 ) ) ;
#57468=CIRCLE ( 'NONE', #39624, 12.52500000000000036 ) ;
#57477=DIRECTION ( 'NONE',  ( 0.9999999999889699343, 2.769066798711915030E-06, 3.793722030377884974E-06 ) ) ;
#57481=CARTESIAN_POINT ( 'NONE',  ( 13.87289819560299975, 8.829573912736998764, 7.542332231507000273 ) ) ;
#57482=CARTESIAN_POINT ( 'NONE',  ( 16.24418116637980347, -3.625803901490415981, -11.98884806668273306 ) ) ;
#57487=DIRECTION ( 'NONE',  ( -1.000000000000000000, 0.000000000000000000, 0.000000000000000000 ) ) ;
#57489=VERTEX_POINT ( 'NONE', #42036 ) ;
#57499=CARTESIAN_POINT ( 'NONE',  ( 13.55192027319500170, -11.56672964510999968, -2.320600286854999972 ) ) ;
#57504=ORIENTED_EDGE ( 'NONE', *, *, #44248, .F. ) ;
#57512=EDGE_CURVE ( 'NONE', #40403, #55462, #54554, .T. ) ;
#57517=ADVANCED_FACE ( 'NONE', ( #54506 ), #39122, .F. ) ;
#57528=CARTESIAN_POINT ( 'NONE',  ( 23.61209254828138171, -10.11819938911013494, 9.629780466774583658 ) ) ;
#57529=CARTESIAN_POINT ( 'NONE',  ( 23.96071418768165628, 12.77533843076500020, -3.513734256132603928 ) ) ;
#57532=CARTESIAN_POINT ( 'NONE',  ( 21.72233714749290101, 0.000000000000000000, 0.000000000000000000 ) ) ;
#57536=CARTESIAN_POINT ( 'NONE',  ( 17.80000000005199823, 3.345268251980999974, -11.86064071431999878 ) ) ;
#57541=EDGE_CURVE ( 'NONE', #23725, #49775, #21961, .T. ) ;
#57559=CARTESIAN_POINT ( 'NONE',  ( 25.52466960993000100, -11.20857090970999970, 3.138534493961999683 ) ) ;
#57560=CIRCLE ( 'NONE', #27430, 0.9999999999999996669 ) ;
#57561=EDGE_CURVE ( 'NONE', #40252, #27371, #18641, .T. ) ;
#57565=CARTESIAN_POINT ( 'NONE',  ( 24.37816252494532421, -8.911180844771308784, 9.054574243701839720 ) ) ;
#57567=CARTESIAN_POINT ( 'NONE',  ( 24.96659818554506316, -2.078227411456102125, -11.31065740026955702 ) ) ;
#57568=ORIENTED_EDGE ( 'NONE', *, *, #13690, .F. ) ;
#57580=CARTESIAN_POINT ( 'NONE',  ( 24.60000000000000142, 0.000000000000000000, 5.000000000000000000 ) ) ;
#57589=DIRECTION ( 'NONE',  ( 0.000000000000000000, 1.000000000000000000, 0.000000000000000000 ) ) ;
#57608=CARTESIAN_POINT ( 'NONE',  ( 25.55279089809471671, -8.264493593867687338, -8.081392981407944376 ) ) ;
#57613=CARTESIAN_POINT ( 'NONE',  ( 18.50005573548403248, 2.729642361726667854, 11.32578974454715137 ) ) ;
#57614=CARTESIAN_POINT ( 'NONE',  ( 18.38069952315600020, -3.381269036354999979, -12.09968217836000015 ) ) ;
#57618=CARTESIAN_POINT ( 'NONE',  ( 13.69997185827400088, -10.10519270881757059, -5.872265061164112510 ) ) ;
#57621=ORIENTED_EDGE ( 'NONE', *, *, #21874, .F. ) ;
#57623=EDGE_CURVE ( 'NONE', #56039, #27357, #45405, .T. ) ;
#57628=CARTESIAN_POINT ( 'NONE',  ( 24.67921430886200085, -8.727631620858000261, -9.158313288899000426 ) ) ;
#57630=CARTESIAN_POINT ( 'NONE',  ( 17.98628609634500108, 3.388648274289000284, -11.90503202562999974 ) ) ;
#57632=ORIENTED_EDGE ( 'NONE', *, *, #9650, .F. ) ;
#57646=EDGE_CURVE ( 'NONE', #50417, #35693, #55201, .T. ) ;
#57654=VERTEX_POINT ( 'NONE', #55549 ) ;
#57655=CONICAL_SURFACE ( 'NONE', #66597, 1.150087858351999781, 0.7854644967339313721 ) ;
#57657=CARTESIAN_POINT ( 'NONE',  ( 13.92027728199409431, 8.815475954240564960, 7.616421984250506760 ) ) ;
#57658=UNCERTAINTY_MEASURE_WITH_UNIT (LENGTH_MEASURE( 1.000000000000000082E-05 ), #62354, 'distance_accuracy_value', 'NONE');
#57660=CARTESIAN_POINT ( 'NONE',  ( 13.46053068095500116, -9.490401724732999256, -7.804222448269000800 ) ) ;
#57661=CARTESIAN_POINT ( 'NONE',  ( 15.89979320884932967, 4.771864030974168003, 11.40757335769640513 ) ) ;
#57667=ORIENTED_EDGE ( 'NONE', *, *, #57623, .T. ) ;
#57673=CARTESIAN_POINT ( 'NONE',  ( 24.23232976021700225, 3.402404391673000017, 12.43152572969999881 ) ) ;
#57680=CARTESIAN_POINT ( 'NONE',  ( 23.74396322974578766, -3.264338234022875707, 13.24371991867584519 ) ) ;
#57704=CARTESIAN_POINT ( 'NONE',  ( 25.46373154986600085, 8.354608910739999672, 8.148450287869000164 ) ) ;
#57706=EDGE_CURVE ( 'NONE', #6268, #17363, #24595, .T. ) ;
#57709=DIRECTION ( 'NONE',  ( 1.000000000000000000, 0.000000000000000000, 0.000000000000000000 ) ) ;
#57710=CARTESIAN_POINT ( 'NONE',  ( 25.22252232637437785, 8.509544449812528555, 8.058439155819339561 ) ) ;
#57718=ORIENTED_EDGE ( 'NONE', *, *, #42524, .T. ) ;
#57719=CARTESIAN_POINT ( 'NONE',  ( 24.55996189763800075, 8.848787117368999589, 9.333438204885000644 ) ) ;
#57723=CARTESIAN_POINT ( 'NONE',  ( 16.03045494250125813, 9.206206171697990825, 8.492540761685223316 ) ) ;
#57731=CARTESIAN_POINT ( 'NONE',  ( 12.01556330254185845, 11.99897551495936909, -3.593484177663820667 ) ) ;
#57738=VECTOR ( 'NONE', #30485, 1000.000000000000227 ) ;
#57743=EDGE_CURVE ( 'NONE', #17363, #59240, #62106, .T. ) ;
#57756=CARTESIAN_POINT ( 'NONE',  ( 13.99999999393278927, -9.282302710986076733, -8.207095416277889299 ) ) ;
#57764=CARTESIAN_POINT ( 'NONE',  ( 13.55436146409600262, -9.071829816454000550, -7.538704307477999578 ) ) ;
#57765=EDGE_CURVE ( 'NONE', #50821, #40899, #6057, .T. ) ;
#57779=CARTESIAN_POINT ( 'NONE',  ( 18.29999744883402002, 2.794302572679392416, -11.51706234618142233 ) ) ;
#57782=CARTESIAN_POINT ( 'NONE',  ( 24.32155143133507380, 9.044166503376443345, -9.474459912027812791 ) ) ;
#57786=CARTESIAN_POINT ( 'NONE',  ( 13.55279538703999975, 9.560508190731999534, 7.863756665013000635 ) ) ;
#57788=EDGE_LOOP ( 'NONE', ( #39313, #64777, #21882 ) ) ;
#57794=EDGE_CURVE ( 'NONE', #27849, #29214, #38707, .T. ) ;
#57802=CARTESIAN_POINT ( 'NONE',  ( 12.46445792838400024, 11.52135921566999954, -4.763665720747999544 ) ) ;
#57805=CIRCLE ( 'NONE', #58911, 0.3000000000000000444 ) ;
#57816=CARTESIAN_POINT ( 'NONE',  ( 23.91316326678529336, 3.340384790131674109, 12.91004685077541048 ) ) ;
#57822=ORIENTED_EDGE ( 'NONE', *, *, #56537, .T. ) ;
#57823=CARTESIAN_POINT ( 'NONE',  ( 14.39999999825366750, -11.41071763166321240, 4.623975355197338821 ) ) ;
#57828=CARTESIAN_POINT ( 'NONE',  ( 29.60000000000000142, 0.000000000000000000, 0.000000000000000000 ) ) ;
#57831=CARTESIAN_POINT ( 'NONE',  ( 16.13862479881500178, -3.581551568669000041, -11.04584923442999944 ) ) ;
#57833=B_SPLINE_CURVE_WITH_KNOTS ( 'NONE', 3,
 ( #11412, #6163, #27504, #59662, #38332, #15635 ),
 .UNSPECIFIED., .F., .F.,
 ( 4, 2, 4 ),
 ( 0.000000000000000000, 0.5000000000000000000, 1.000000000000000000 ),
 .UNSPECIFIED. ) ;
#57834=CARTESIAN_POINT ( 'NONE',  ( 13.46018463513500052, 9.195629459350000090, 7.535158378801000367 ) ) ;
#57850=EDGE_LOOP ( 'NONE', ( #44502, #27380, #44295, #34412 ) ) ;
#57853=ADVANCED_FACE ( 'NONE', ( #63170 ), #14276, .T. ) ;
#57854=CARTESIAN_POINT ( 'NONE',  ( 16.39999999485600313, -3.595156957901000094, -11.99794989424000136 ) ) ;
#57855=CARTESIAN_POINT ( 'NONE',  ( 13.58722619340700177, -11.45202530529999940, -1.920069653109999885 ) ) ;
#57857=CIRCLE ( 'NONE', #47791, 1.000000000000000888 ) ;
#57858=CARTESIAN_POINT ( 'NONE',  ( 13.24816728597000193, 12.42904273309000018, 1.833878933190999927 ) ) ;
#57862=EDGE_LOOP ( 'NONE', ( #9611, #11752, #65277, #4395, #14189 ) ) ;
#57865=CARTESIAN_POINT ( 'NONE',  ( 15.91802873821099951, 8.603382153815999800, 8.072764124688998066 ) ) ;
#57877=CARTESIAN_POINT ( 'NONE',  ( 12.71479700542636060, 11.41062399033359753, -4.624005385416205982 ) ) ;
#57887=CARTESIAN_POINT ( 'NONE',  ( 15.40000000009400161, -8.833277835210999740, -7.896561221812000930 ) ) ;
#57899=CARTESIAN_POINT ( 'NONE',  ( 25.31012846324300014, 2.730838012578999940, 11.36012275232000057 ) ) ;
#57902=DIRECTION ( 'NONE',  ( 0.7808688094474018904, 0.3122742207642010270, -0.5410440956875032237 ) ) ;
#57903=EDGE_LOOP ( 'NONE', ( #22393, #43959, #13577, #39702 ) ) ;
#57908=CARTESIAN_POINT ( 'NONE',  ( 15.36900185986900169, 9.263677555280001030, 8.208910455558001473 ) ) ;
#57913=CARTESIAN_POINT ( 'NONE',  ( 25.09299657149600193, -11.65481462448000016, 3.020019921150999931 ) ) ;
#57918=B_SPLINE_SURFACE_WITH_KNOTS ( 'NONE', 3, 3, ( 
 ( #51543, #62379, #14496, #57466 ),
 ( #61354, #35814, #24640, #29209 ),
 ( #40043, #57132, #46656, #20076 ),
 ( #45285, #9229, #13474, #8216 ),
 ( #40710, #29563, #50520, #51210 ),
 ( #66933, #13810, #3639, #56802 ),
 ( #14834, #19386, #66590, #30568 ),
 ( #34794, #30238, #18710, #56105 ),
 ( #45629, #41405, #3978, #45961 ),
 ( #3306, #2963, #24976, #35141 ),
 ( #14153, #24292, #62711, #2619 ),
 ( #23951, #62038, #67271, #40371 ) ),
 .UNSPECIFIED., .F., .F., .F.,
 ( 4, 1, 1, 1, 1, 1, 1, 1, 1, 4 ),
 ( 4, 4 ),
 ( 0.01098129032804999981, 0.05000000000000000278, 0.1000000000000000056, 0.1499999999999999944, 0.2000000000000000111, 0.2500000000000000000, 0.2999999999999999889, 0.3499999999999999778, 0.4000000000000000222, 0.4470328610943000158 ),
 ( -0.2706696436996000044, 1.270788880587000014 ),
 .UNSPECIFIED. ) ;
#57929=CARTESIAN_POINT ( 'NONE',  ( 18.23590051321700400, 3.219096189435000088, 11.95421454054999977 ) ) ;
#57939=ORIENTED_EDGE ( 'NONE', *, *, #50585, .T. ) ;
#57945=CARTESIAN_POINT ( 'NONE',  ( 15.86268444654400156, -3.728894906265999509, -11.70612128528000007 ) ) ;
#57954=CIRCLE ( 'NONE', #40104, 1.300156908083999863 ) ;
#57957=CARTESIAN_POINT ( 'NONE',  ( 24.34833239334600208, -12.15210528830085757, -3.256146798339317527 ) ) ;
#57964=VERTEX_POINT ( 'NONE', #21905 ) ;
#57968=DIRECTION ( 'NONE',  ( 0.000000000000000000, -0.2714570858282905341, 0.9624505444715651947 ) ) ;
#57969=CARTESIAN_POINT ( 'NONE',  ( 23.59378684139632298, -13.38703058558571080, -4.024018919119528803 ) ) ;
#57971=EDGE_CURVE ( 'NONE', #23400, #10787, #52819, .T. ) ;
#57976=B_SPLINE_CURVE_WITH_KNOTS ( 'NONE', 3,
 ( #40089, #28562, #1637, #6873 ),
 .UNSPECIFIED., .F., .F.,
 ( 4, 4 ),
 ( 0.000000000000000000, 1.000000000000000000 ),
 .UNSPECIFIED. ) ;
#57984=CARTESIAN_POINT ( 'NONE',  ( 24.45367377732199898, -12.43820265659000057, 3.092926956713999864 ) ) ;
#57991=CARTESIAN_POINT ( 'NONE',  ( 23.57810697541089340, -10.23415488232117099, -9.534542369472955414 ) ) ;
#57996=CARTESIAN_POINT ( 'NONE',  ( 24.48566042065300152, 8.805064172929998989, 8.922039496844000439 ) ) ;
#58007=EDGE_CURVE ( 'NONE', #38892, #40442, #46132, .T. ) ;
#58016=CARTESIAN_POINT ( 'NONE',  ( 13.99932787941000178, -9.131694343880999654, -8.218494815692999111 ) ) ;
#58018=VERTEX_POINT ( 'NONE', #13514 ) ;
#58026=EDGE_CURVE ( 'NONE', #58018, #11014, #15002, .T. ) ;
#58032=CARTESIAN_POINT ( 'NONE',  ( 23.74313554628299983, 3.207763596684000351, 13.21072658733999994 ) ) ;
#58033=EDGE_LOOP ( 'NONE', ( #7748, #44995, #29390, #55100 ) ) ;
#58035=B_SPLINE_CURVE_WITH_KNOTS ( 'NONE', 3,
 ( #149, #11319, #37546, #63424 ),
 .UNSPECIFIED., .F., .F.,
 ( 4, 4 ),
 ( 0.000000000000000000, 1.000000000000000000 ),
 .UNSPECIFIED. ) ;
#58048=CARTESIAN_POINT ( 'NONE',  ( 15.95676543642413847, -9.288185316739916431, -8.402783510542167988 ) ) ;
#58051=CARTESIAN_POINT ( 'NONE',  ( 24.30001682246400208, -8.938702682732001747, -8.938676171235998780 ) ) ;
#58059=EDGE_CURVE ( 'NONE', #17363, #52029, #65309, .T. ) ;
#58064=B_SPLINE_CURVE_WITH_KNOTS ( 'NONE', 3,
 ( #39132, #51002, #34932, #60803 ),
 .UNSPECIFIED., .F., .F.,
 ( 4, 4 ),
 ( 0.000000000000000000, 1.000000000000000000 ),
 .UNSPECIFIED. ) ;
#58070=CARTESIAN_POINT ( 'NONE',  ( 13.69997185827399910, 9.599065136398388987, 6.667560658748404201 ) ) ;
#58087=CARTESIAN_POINT ( 'NONE',  ( 12.08335418496251101, 11.66230666314208264, -4.568774126650350986 ) ) ;
#58091=CARTESIAN_POINT ( 'NONE',  ( 15.45728973496400194, -8.836548693809998412, -7.950469186927999310 ) ) ;
#58093=DIRECTION ( 'NONE',  ( 0.000000000000000000, -0.4815106998112011483, 0.8764402124317022258 ) ) ;
#58094=VERTEX_POINT ( 'NONE', #18752 ) ;
#58099=CARTESIAN_POINT ( 'NONE',  ( 14.70000000000000107, -9.329726667597000755, -8.204053922562998480 ) ) ;
#58102=CARTESIAN_POINT ( 'NONE',  ( 23.61990251228100135, 2.978955071604999727, -13.51777065273999945 ) ) ;
#58107=CARTESIAN_POINT ( 'NONE',  ( 18.29999744883402002, -2.794302572679392416, 11.51706234618142055 ) ) ;
#58120=DIRECTION ( 'NONE',  ( 0.000000000000000000, -0.9659258262890757507, 0.2588190451024927063 ) ) ;
#58121=CARTESIAN_POINT ( 'NONE',  ( 23.58568869556000180, 13.39453640560000025, -4.037491894581999752 ) ) ;
#58127=CARTESIAN_POINT ( 'NONE',  ( 25.60000000000000142, 13.52296156804999860, -3.623466631435000362 ) ) ;
#58131=CARTESIAN_POINT ( 'NONE',  ( 18.23289209646694431, 3.217460216929902028, -11.19708622233978090 ) ) ;
#58137=CARTESIAN_POINT ( 'NONE',  ( 13.60429364930200080, 11.50682694388999927, 2.143319390578000139 ) ) ;
#58141=ORIENTED_EDGE ( 'NONE', *, *, #56359, .T. ) ;
#58143=EDGE_LOOP ( 'NONE', ( #10638, #42376, #62012, #51510 ) ) ;
#58144=CARTESIAN_POINT ( 'NONE',  ( 11.72006721069024593, -11.52583591982215161, -1.696350940455132239 ) ) ;
#58148=CARTESIAN_POINT ( 'NONE',  ( 15.40000000009400161, 8.833277835210999740, 7.896561221812000930 ) ) ;
#58150=CARTESIAN_POINT ( 'NONE',  ( 12.29459504890800048, 12.00990144118000025, -3.349639255392000248 ) ) ;
#58157=CARTESIAN_POINT ( 'NONE',  ( 17.86534991953400109, -3.412585803847000054, 11.89775424487000066 ) ) ;
#58159=ORIENTED_EDGE ( 'NONE', *, *, #61485, .F. ) ;
#58161=AXIS2_PLACEMENT_3D ( 'NONE', #67019, #40452, #23690 ) ;
#58165=CARTESIAN_POINT ( 'NONE',  ( 24.69847697201900161, 8.734418378053000254, -9.243512260004999703 ) ) ;
#58166=EDGE_CURVE ( 'NONE', #11014, #58018, #3809, .T. ) ;
#58173=VERTEX_POINT ( 'NONE', #49518 ) ;
#58180=CARTESIAN_POINT ( 'NONE',  ( 16.44004776902900034, -3.254301421112999915, -11.33671678219000079 ) ) ;
#58181=CARTESIAN_POINT ( 'NONE',  ( 13.50542051561400214, 9.036698429651000453, 7.720610530813999617 ) ) ;
#58182=FACE_OUTER_BOUND ( 'NONE', #8776, .T. ) ;
#58184=CARTESIAN_POINT ( 'NONE',  ( 17.60000003393297163, 11.45048720807753284, -4.713173851737514575 ) ) ;
#58185=ADVANCED_FACE ( 'NONE', ( #13171 ), #1580, .T. ) ;
#58186=FACE_OUTER_BOUND ( 'NONE', #43154, .T. ) ;
#58202=ORIENTED_EDGE ( 'NONE', *, *, #37700, .T. ) ;
#58206=CARTESIAN_POINT ( 'NONE',  ( 13.46547102623810943, 11.49951335169978606, 1.866756745161230580 ) ) ;
#58222=FACE_OUTER_BOUND ( 'NONE', #38336, .T. ) ;
#58232=ORIENTED_EDGE ( 'NONE', *, *, #10751, .T. ) ;
#58234=ORIENTED_EDGE ( 'NONE', *, *, #8547, .T. ) ;
#58237=DIRECTION ( 'NONE',  ( 0.000000000000000000, 1.000000000000000000, 0.000000000000000000 ) ) ;
#58239=DIRECTION ( 'NONE',  ( -1.000000000000000000, 0.000000000000000000, 0.000000000000000000 ) ) ;
#58241=CARTESIAN_POINT ( 'NONE',  ( 23.50387503050299998, 6.898380679426999507, -11.95208534113000098 ) ) ;
#58242=ORIENTED_EDGE ( 'NONE', *, *, #42695, .T. ) ;
#58245=DIRECTION ( 'NONE',  ( 1.000000000000000000, 0.000000000000000000, 0.000000000000000000 ) ) ;
#58246=DIRECTION ( 'NONE',  ( 1.000000000000000000, 0.000000000000000000, 0.000000000000000000 ) ) ;
#58254=CARTESIAN_POINT ( 'NONE',  ( 25.31133132558300147, -11.20189781360999959, 3.316394190663999986 ) ) ;
#58263=DIRECTION ( 'NONE',  ( 0.000000000000000000, -0.2588190451024927063, 0.9659258262890757507 ) ) ;
#58266=CARTESIAN_POINT ( 'NONE',  ( 18.44495723965300016, 2.860707309908000262, 12.13834028902000028 ) ) ;
#58267=ADVANCED_FACE ( 'NONE', ( #3343, #35177 ), #35518, .F. ) ;
#58276=VERTEX_POINT ( 'NONE', #36538 ) ;
#58282=CARTESIAN_POINT ( 'NONE',  ( 16.04731601457200085, -3.899361801049999965, -11.84592592973999992 ) ) ;
#58283=FACE_OUTER_BOUND ( 'NONE', #58033, .T. ) ;
#58284=EDGE_LOOP ( 'NONE', ( #56144, #44577, #40755, #54796 ) ) ;
#58286=CARTESIAN_POINT ( 'NONE',  ( 24.56713313357033002, -8.731543158497419910, -8.723146645339960870 ) ) ;
#58287=PLANE ( 'NONE',  #7661 ) ;
#58298=CARTESIAN_POINT ( 'NONE',  ( 15.40000000001299973, -8.815237407733999220, -7.616696375847999967 ) ) ;
#58301=ORIENTED_EDGE ( 'NONE', *, *, #54779, .T. ) ;
#58303=CARTESIAN_POINT ( 'NONE',  ( 24.67921311619700120, 3.567517360056999820, 12.13750603036999998 ) ) ;
#58304=CARTESIAN_POINT ( 'NONE',  ( 23.59999443371599881, 2.915558930973999985, 13.58549620949000136 ) ) ;
#58313=ORIENTED_EDGE ( 'NONE', *, *, #21131, .T. ) ;
#58320=CARTESIAN_POINT ( 'NONE',  ( 18.29983863916000075, 2.861762957209999847, -11.98830831200999825 ) ) ;
#58334=DIRECTION ( 'NONE',  ( 0.000000000000000000, 0.000000000000000000, -1.000000000000000000 ) ) ;
#58337=B_SPLINE_SURFACE_WITH_KNOTS ( 'NONE', 3, 3, ( 
 ( #58814, #58470, #32941, #54252 ),
 ( #38525, #52887, #21072, #31568 ),
 ( #42740, #4986, #47986, #68959 ),
 ( #6353, #15822, #27008, #53229 ),
 ( #42402, #10575, #22092, #64385 ),
 ( #53573, #49017, #1124, #37152 ),
 ( #27701, #32596, #16164, #26672 ),
 ( #53911, #22438, #63710, #5328 ),
 ( #16506, #6011, #64044, #27350 ),
 ( #32263, #48326, #431, #48673 ) ),
 .UNSPECIFIED., .F., .F., .F.,
 ( 4, 1, 1, 1, 1, 1, 1, 4 ),
 ( 4, 4 ),
 ( 0.07063076901675999220, 0.1428571428570999946, 0.2857142857143000203, 0.4285714285713999594, 0.5714285714286000406, 0.7142857142856999797, 0.8571428571429000609, 0.9582423226859000387 ),
 ( -0.1917799910644999994, 1.191756862851000021 ),
 .UNSPECIFIED. ) ;
#58352=CARTESIAN_POINT ( 'NONE',  ( 13.55458079702099994, -9.509022223680998920, -7.924557572090001223 ) ) ;
#58360=ORIENTED_EDGE ( 'NONE', *, *, #60057, .F. ) ;
#58374=CARTESIAN_POINT ( 'NONE',  ( 24.13789385032118773, -3.328480681758700488, 12.49557795887629119 ) ) ;
#58377=CARTESIAN_POINT ( 'NONE',  ( 24.95409859149600251, -3.532259266401000186, -11.87003396491999929 ) ) ;
#58380=ORIENTED_EDGE ( 'NONE', *, *, #20066, .F. ) ;
#58381=CARTESIAN_POINT ( 'NONE',  ( 16.00806624337635142, -9.235483320791386674, -8.460674029563278964 ) ) ;
#58382=CARTESIAN_POINT ( 'NONE',  ( 24.30000000000000071, 2.548720605937000006, -12.21654710926000220 ) ) ;
#58398=VERTEX_POINT ( 'NONE', #64125 ) ;
#58399=AXIS2_PLACEMENT_3D ( 'NONE', #63231, #52758, #4165 ) ;
#58402=CARTESIAN_POINT ( 'NONE',  ( 25.10987708584536904, 8.510208471453900358, 8.211061621397103494 ) ) ;
#58406=DIRECTION ( 'NONE',  ( 1.000000000000000000, 0.000000000000000000, 0.000000000000000000 ) ) ;
#58407=DIRECTION ( 'NONE',  ( 1.000000000000000000, 0.000000000000000000, 0.000000000000000000 ) ) ;
#58423=CARTESIAN_POINT ( 'NONE',  ( 25.55279130549196509, 8.264493201100965081, 8.081392654661549102 ) ) ;
#58426=CARTESIAN_POINT ( 'NONE',  ( 18.02668091122101401, -11.82887279600184272, 3.432551977438183410 ) ) ;
#58433=EDGE_CURVE ( 'NONE', #855, #52478, #11945, .T. ) ;
#58440=CARTESIAN_POINT ( 'NONE',  ( 23.58444653190300144, 2.899227940640999979, -13.63439735100000050 ) ) ;
#58447=DIRECTION ( 'NONE',  ( 0.000000000000000000, 0.007439385635787961089, 0.9999723273877941798 ) ) ;
#58450=CARTESIAN_POINT ( 'NONE',  ( 13.99999999485600277, -9.471999751521998689, -8.194948195317001804 ) ) ;
#58453=CARTESIAN_POINT ( 'NONE',  ( 24.34833292637366853, 3.256146932298328522, -12.15210578825087140 ) ) ;
#58455=CARTESIAN_POINT ( 'NONE',  ( 11.50001544675000176, -12.52500000000000213, 1.310230436065862980 ) ) ;
#58456=CARTESIAN_POINT ( 'NONE',  ( 24.26257012332692398, 8.985986007774535267, -8.985987282385920594 ) ) ;
#58457=DIRECTION ( 'NONE',  ( -1.000000000000000000, 0.000000000000000000, -5.088522196198629516E-14 ) ) ;
#58458=CARTESIAN_POINT ( 'NONE',  ( 24.22094041469999937, 12.17087951192999995, -3.345634150892999870 ) ) ;
#58470=CARTESIAN_POINT ( 'NONE',  ( 17.76418844530500252, -3.313976920866999798, 11.22406790378000174 ) ) ;
#58471=B_SPLINE_CURVE_WITH_KNOTS ( 'NONE', 3,
 ( #61693, #19387, #23952, #61013, #13131, #18711 ),
 .UNSPECIFIED., .F., .F.,
 ( 4, 2, 4 ),
 ( 0.000000000000000000, 0.5000000000000000000, 1.000000000000000000 ),
 .UNSPECIFIED. ) ;
#58475=CARTESIAN_POINT ( 'NONE',  ( 13.05728973496400336, 11.72286803092000085, 1.966956593348999860 ) ) ;
#58485=CARTESIAN_POINT ( 'NONE',  ( 17.68557836066964839, 11.86191914806434333, -3.298674357360816156 ) ) ;
#58490=CARTESIAN_POINT ( 'NONE',  ( 11.95406170795600076, 11.84685177148000079, -3.896686237526999719 ) ) ;
#58491=CARTESIAN_POINT ( 'NONE',  ( 18.26656969954900234, 11.60886806805999960, -4.031065632098000506 ) ) ;
#58497=CARTESIAN_POINT ( 'NONE',  ( 18.19046715839422035, 12.06204093805255084, -3.374120125975932805 ) ) ;
#58499=ORIENTED_EDGE ( 'NONE', *, *, #8797, .T. ) ;
#58509=LINE ( 'NONE', #25667, #62045 ) ;
#58526=ORIENTED_EDGE ( 'NONE', *, *, #17947, .F. ) ;
#58549=CARTESIAN_POINT ( 'NONE',  ( 23.56664322114200161, -2.935586410151000081, -13.67842711829000102 ) ) ;
#58552=CARTESIAN_POINT ( 'NONE',  ( 23.58333993490100156, 3.064215547964999882E-13, 1.261213355973999610E-13 ) ) ;
#58555=EDGE_CURVE ( 'NONE', #5914, #43538, #36969, .T. ) ;
#58556=EDGE_CURVE ( 'NONE', #50502, #47384, #11334, .T. ) ;
#58559=ORIENTED_EDGE ( 'NONE', *, *, #44330, .T. ) ;
#58574=B_SPLINE_CURVE_WITH_KNOTS ( 'NONE', 3,
 ( #43099, #48002, #21088, #10246, #64400, #16523 ),
 .UNSPECIFIED., .F., .F.,
 ( 4, 2, 4 ),
 ( 0.000000000000000000, 0.5000000000000000000, 1.000000000000000000 ),
 .UNSPECIFIED. ) ;
#58587=B_SPLINE_CURVE_WITH_KNOTS ( 'NONE', 3,
 ( #22629, #64584, #59348, #28587 ),
 .UNSPECIFIED., .F., .F.,
 ( 4, 4 ),
 ( 0.000000000000000000, 1.000000000000000000 ),
 .UNSPECIFIED. ) ;
#58589=CARTESIAN_POINT ( 'NONE',  ( 12.83903456837200174, -11.55258133652000119, 4.939873833509000889 ) ) ;
#58593=CARTESIAN_POINT ( 'NONE',  ( 13.99999999439439335, 9.377150629848445718, 8.201012428486359696 ) ) ;
#58596=FACE_OUTER_BOUND ( 'NONE', #49667, .T. ) ;
#58598=B_SPLINE_CURVE_WITH_KNOTS ( 'NONE', 3,
 ( #24453, #40196, #9384, #13628, #30728, #34953, #56267, #8377 ),
 .UNSPECIFIED., .F., .F.,
 ( 4, 2, 2, 4 ),
 ( 0.000000000000000000, 0.2500000000000014433, 0.5000000000000028866, 1.000000000000000000 ),
 .UNSPECIFIED. ) ;
#58605=CARTESIAN_POINT ( 'NONE',  ( 25.29987261392200182, 8.756202924575998026, -7.455126447192999883 ) ) ;
#58606=CARTESIAN_POINT ( 'NONE',  ( 17.80000000000000071, -13.72414332887999855, 50.50083396221000243 ) ) ;
#58616=CARTESIAN_POINT ( 'NONE',  ( 24.44496264144000364, 8.810483598181999554, -8.810508341310001157 ) ) ;
#58626=CARTESIAN_POINT ( 'NONE',  ( 15.90567905817900218, -3.588626488247999902, -11.74852861413999960 ) ) ;
#58633=ORIENTED_EDGE ( 'NONE', *, *, #34512, .F. ) ;
#58634=CARTESIAN_POINT ( 'NONE',  ( 15.49269116706140537, -8.815195450845674685, -7.616746626196380987 ) ) ;
#58639=ORIENTED_EDGE ( 'NONE', *, *, #55009, .F. ) ;
#58641=EDGE_CURVE ( 'NONE', #32947, #28894, #60375, .T. ) ;
#58642=EDGE_CURVE ( 'NONE', #56420, #54978, #17192, .T. ) ;
#58646=CARTESIAN_POINT ( 'NONE',  ( 16.04718133169100014, -8.956716759973000208, -8.677900031540000114 ) ) ;
#58647=DIRECTION ( 'NONE',  ( 1.000000000000000000, 0.000000000000000000, 0.000000000000000000 ) ) ;
#58648=ORIENTED_EDGE ( 'NONE', *, *, #25273, .T. ) ;
#58662=CARTESIAN_POINT ( 'NONE',  ( 25.60000000000000142, 0.000000000000000000, -10.75000000000000000 ) ) ;
#58663=DIRECTION ( 'NONE',  ( 0.000000000000000000, 0.000000000000000000, -1.000000000000000000 ) ) ;
#58669=CARTESIAN_POINT ( 'NONE',  ( 15.90007192502618238, 3.569777767583313111, 11.29792192708077181 ) ) ;
#58677=CARTESIAN_POINT ( 'NONE',  ( 18.31386961183700279, 3.086648833569000328, -11.29009770192999973 ) ) ;
#58690=VERTEX_POINT ( 'NONE', #66548 ) ;
#58699=ADVANCED_FACE ( 'NONE', ( #55035 ), #44566, .F. ) ;
#58705=ORIENTED_EDGE ( 'NONE', *, *, #24808, .F. ) ;
#58712=CARTESIAN_POINT ( 'NONE',  ( 24.45284689113699983, 3.540778225556000081, 12.31935692833000040 ) ) ;
#58713=EDGE_LOOP ( 'NONE', ( #2989, #57090, #62816, #66032 ) ) ;
#58723=CARTESIAN_POINT ( 'NONE',  ( 24.67332979692900352, -3.458637065210999673, -12.04350545405000084 ) ) ;
#58726=EDGE_LOOP ( 'NONE', ( #53339, #66614, #498, #53376 ) ) ;
#58728=CARTESIAN_POINT ( 'NONE',  ( 23.99449529258459179, 9.375514267760260978, 9.276290998956193690 ) ) ;
#58743=CARTESIAN_POINT ( 'NONE',  ( 11.40162633574000139, 12.25609765133000018, 1.727435033673999865 ) ) ;
#58754=CARTESIAN_POINT ( 'NONE',  ( 13.73140886085690582, -8.907522817021714445, -7.508769385438534449 ) ) ;
#58770=CARTESIAN_POINT ( 'NONE',  ( 12.10000669845703847, 11.02846243759400124, -3.754394857303852362 ) ) ;
#58776=CARTESIAN_POINT ( 'NONE',  ( 12.60217350508042067, -12.11433231916790376, 3.180975838886041185 ) ) ;
#58787=B_SPLINE_CURVE_WITH_KNOTS ( 'NONE', 3,
 ( #48208, #42624, #65313, #11482 ),
 .UNSPECIFIED., .F., .F.,
 ( 4, 4 ),
 ( 0.000000000000000000, 1.000000000000000000 ),
 .UNSPECIFIED. ) ;
#58797=CARTESIAN_POINT ( 'NONE',  ( 15.88771848669683351, 8.938332686942986882, 8.488529254939262358 ) ) ;
#58799=AXIS2_PLACEMENT_3D ( 'NONE', #35421, #18988, #36099 ) ;
#58809=DIRECTION ( 'NONE',  ( -1.000000000000000000, 0.000000000000000000, 0.000000000000000000 ) ) ;
#58811=ORIENTED_EDGE ( 'NONE', *, *, #44683, .T. ) ;
#58813=CARTESIAN_POINT ( 'NONE',  ( 25.30000327618300204, 2.078227429405999693, -11.31065739696999906 ) ) ;
#58814=CARTESIAN_POINT ( 'NONE',  ( 17.75907622778400352, -3.376089723145999866, 11.11072845602000037 ) ) ;
#58819=CARTESIAN_POINT ( 'NONE',  ( 13.55192027319500170, 11.56672964510999968, 2.320600286854999972 ) ) ;
#58828=CARTESIAN_POINT ( 'NONE',  ( 24.81043909399123848, -8.607472784691234224, 8.518286398806663939 ) ) ;
#58830=EDGE_CURVE ( 'NONE', #42044, #59692, #20245, .T. ) ;
#58835=CARTESIAN_POINT ( 'NONE',  ( 18.46722213196600393, 12.01216300861999997, -3.678628708156000293 ) ) ;
#58838=CIRCLE ( 'NONE', #68863, 0.3000000000000000999 ) ;
#58840=CARTESIAN_POINT ( 'NONE',  ( 18.26123302403700066, -2.828310120379999848, 11.95646042099000006 ) ) ;
#58848=FACE_BOUND ( 'NONE', #15978, .T. ) ;
#58849=DIRECTION ( 'NONE',  ( 0.000000000000000000, 0.9979288589194752479, -0.06432723012592840572 ) ) ;
#58859=CARTESIAN_POINT ( 'NONE',  ( 30.60000000000000142, 0.000000000000000000, 0.000000000000000000 ) ) ;
#58862=EDGE_CURVE ( 'NONE', #26055, #4160, #57833, .T. ) ;
#58864=CIRCLE ( 'NONE', #48792, 1.500000000000001332 ) ;
#58867=CARTESIAN_POINT ( 'NONE',  ( 25.39940118446284956, 11.19882020338194195, -3.252373299299911036 ) ) ;
#58873=DIRECTION ( 'NONE',  ( 1.000000000000000000, 0.000000000000000000, 0.000000000000000000 ) ) ;
#58874=CARTESIAN_POINT ( 'NONE',  ( 25.29987333571600061, -10.83443035398000021, -3.855530949778000149 ) ) ;
#58882=CARTESIAN_POINT ( 'NONE',  ( 25.31013104180999918, -11.20357036551999919, -3.315088882916999768 ) ) ;
#58886=DIRECTION ( 'NONE',  ( 0.000000000000000000, 0.000000000000000000, -1.000000000000000000 ) ) ;
#58888=CARTESIAN_POINT ( 'NONE',  ( 13.70006033574439286, -11.41449502534927163, -2.331043471727575422 ) ) ;
#58891=ORIENTED_EDGE ( 'NONE', *, *, #46237, .T. ) ;
#58895=EDGE_LOOP ( 'NONE', ( #14689, #41704, #39325, #18241, #60787 ) ) ;
#58896=CARTESIAN_POINT ( 'NONE',  ( 13.66714157633269444, 11.44713007569950669, 2.165075719398914966 ) ) ;
#58908=FACE_OUTER_BOUND ( 'NONE', #39172, .T. ) ;
#58910=EDGE_LOOP ( 'NONE', ( #40863, #48135, #64898, #50175 ) ) ;
#58911=AXIS2_PLACEMENT_3D ( 'NONE', #37556, #31988, #48745 ) ;
#58919=CARTESIAN_POINT ( 'NONE',  ( 16.20650642310300071, 3.719849042574000286, 12.00042637259999978 ) ) ;
#58921=CARTESIAN_POINT ( 'NONE',  ( 24.30001696810800027, 12.21047201856000086, 3.271805692349999628 ) ) ;
#58930=CARTESIAN_POINT ( 'NONE',  ( 17.82606829449534658, -12.11439310048800877, 3.181038237424487214 ) ) ;
#58935=ORIENTED_EDGE ( 'NONE', *, *, #47292, .F. ) ;
#58942=CARTESIAN_POINT ( 'NONE',  ( 12.62563329236320619, -11.41733447966565862, 4.609296053777788060 ) ) ;
#58944=CARTESIAN_POINT ( 'NONE',  ( 24.66122485234200212, -8.759220508654999904, -9.243943008462998989 ) ) ;
#58945=AXIS2_PLACEMENT_3D ( 'NONE', #35750, #57068, #68575 ) ;
#58956=CARTESIAN_POINT ( 'NONE',  ( 24.30000000000000071, 8.756202924575998026, -7.455126447192999883 ) ) ;
#58963=ORIENTED_EDGE ( 'NONE', *, *, #45927, .T. ) ;
#58973=ADVANCED_FACE ( 'NONE', ( #26394 ), #53336, .F. ) ;
#58977=ORIENTED_EDGE ( 'NONE', *, *, #44161, .T. ) ;
#58979=CARTESIAN_POINT ( 'NONE',  ( 11.68610928851700237, 11.49703662065999943, 1.632765284408000062 ) ) ;
#58980=ORIENTED_EDGE ( 'NONE', *, *, #50775, .T. ) ;
#58988=CARTESIAN_POINT ( 'NONE',  ( 24.14474118650271706, -12.92575622504552690, 3.214623506209951742 ) ) ;
#58993=EDGE_LOOP ( 'NONE', ( #23847, #48474, #61676, #60656, #5827 ) ) ;
#58995=CARTESIAN_POINT ( 'NONE',  ( 16.04331666222400088, -9.026410239312999906, -8.606113518243997618 ) ) ;
#58999=CARTESIAN_POINT ( 'NONE',  ( 16.10004050617000360, -8.286228349446556507, -9.446703038322569412 ) ) ;
#59008=VERTEX_POINT ( 'NONE', #33012 ) ;
#59011=CIRCLE ( 'NONE', #61264, 11.50000000000000178 ) ;
#59012=CARTESIAN_POINT ( 'NONE',  ( 25.30000327618300204, -0.6965695964343677771, -11.50000000000000000 ) ) ;
#59018=CARTESIAN_POINT ( 'NONE',  ( 23.62948033907000323, -13.46907223791000163, 3.826138227952000204 ) ) ;
#59025=CARTESIAN_POINT ( 'NONE',  ( 18.23887202961200060, 3.252214874110999965, -11.14733497513999971 ) ) ;
#59028=B_SPLINE_CURVE_WITH_KNOTS ( 'NONE', 3,
 ( #28968, #7275, #2039, #49230 ),
 .UNSPECIFIED., .F., .F.,
 ( 4, 4 ),
 ( 0.000000000000000000, 1.000000000000000000 ),
 .UNSPECIFIED. ) ;
#59030=CARTESIAN_POINT ( 'NONE',  ( 23.91258968280600072, -9.487094596478000241, -9.248012932198999891 ) ) ;
#59031=CARTESIAN_POINT ( 'NONE',  ( 18.50003594167399967, -2.686563651857999613, -11.33603604486000016 ) ) ;
#59038=CARTESIAN_POINT ( 'NONE',  ( 24.60320129348500018, 8.810542265399000428, -9.295223627480998729 ) ) ;
#59044=CARTESIAN_POINT ( 'NONE',  ( 27.09999999999999787, 0.000000000000000000, 0.000000000000000000 ) ) ;
#59055=CARTESIAN_POINT ( 'NONE',  ( 12.32697677577000128, -11.50538345640999971, 4.553133914476999777 ) ) ;
#59081=CARTESIAN_POINT ( 'NONE',  ( 25.60000000000000142, 0.000000000000000000, 0.000000000000000000 ) ) ;
#59089=CARTESIAN_POINT ( 'NONE',  ( 23.56666365135700403, -11.07911597677999360, 4.076188921367005058 ) ) ;
#59091=CARTESIAN_POINT ( 'NONE',  ( 11.42397234076999979, 12.13750352647000064, 1.893412522203000048 ) ) ;
#59099=EDGE_LOOP ( 'NONE', ( #17080, #45867, #61453, #60142 ) ) ;
#59109=CARTESIAN_POINT ( 'NONE',  ( 18.32727125556385417, -3.363648366948407631, -12.06493410109945152 ) ) ;
#59119=ORIENTED_EDGE ( 'NONE', *, *, #24388, .T. ) ;
#59123=CARTESIAN_POINT ( 'NONE',  ( 11.89965592520902682, -11.89526654130121841, 3.923396420608940893 ) ) ;
#59124=CARTESIAN_POINT ( 'NONE',  ( 24.45625629573268256, -3.500080033065961160, -12.27866820334083187 ) ) ;
#59131=CARTESIAN_POINT ( 'NONE',  ( 18.29058466016384443, -10.98038933998877553, 3.892884224343166721 ) ) ;
#59134=EDGE_CURVE ( 'NONE', #68518, #34052, #50291, .T. ) ;
#59143=LINE ( 'NONE', #10908, #39868 ) ;
#59152=ORIENTED_EDGE ( 'NONE', *, *, #2442, .F. ) ;
#59161=CARTESIAN_POINT ( 'NONE',  ( 13.22410434383600197, 11.56587205782000005, 1.788415454164999918 ) ) ;
#59164=EDGE_LOOP ( 'NONE', ( #5058, #8244, #19206, #57427, #35187 ) ) ;
#59182=CARTESIAN_POINT ( 'NONE',  ( 18.18731764114100358, 11.62758720635999765, -4.758865308234000224 ) ) ;
#59186=CARTESIAN_POINT ( 'NONE',  ( 18.53935907712300235, -2.923447147946000246, 12.21821814482000157 ) ) ;
#59193=CARTESIAN_POINT ( 'NONE',  ( 24.77993120524800119, 8.657413043978001710, -9.170265824677001021 ) ) ;
#59201=CARTESIAN_POINT ( 'NONE',  ( 24.30001697071400457, -8.938702858184001343, 8.938676113071998941 ) ) ;
#59206=CARTESIAN_POINT ( 'NONE',  ( 23.59999193302000364, -13.22318594659000013, 4.267778254689999606 ) ) ;
#59207=DIRECTION ( 'NONE',  ( -1.000000000000000000, 0.000000000000000000, 0.000000000000000000 ) ) ;
#59211=EDGE_CURVE ( 'NONE', #54978, #56420, #1633, .T. ) ;
#59212=DIRECTION ( 'NONE',  ( -1.000000000000000000, 0.000000000000000000, 0.000000000000000000 ) ) ;
#59219=CARTESIAN_POINT ( 'NONE',  ( 25.36444524348200247, -8.489942824528000642, 7.945382091837999816 ) ) ;
#59221=ORIENTED_EDGE ( 'NONE', *, *, #68640, .T. ) ;
#59222=CARTESIAN_POINT ( 'NONE',  ( 25.08243281028700267, -11.33758179239000086, -3.319403910104000044 ) ) ;
#59224=CARTESIAN_POINT ( 'NONE',  ( 23.60000000000000142, -2.204728229456999866, -11.99913219504999873 ) ) ;
#59226=CARTESIAN_POINT ( 'NONE',  ( 11.79999999471800010, -11.69117318561000118, -1.923227876431999883 ) ) ;
#59240=VERTEX_POINT ( 'NONE', #27519 ) ;
#59242=CARTESIAN_POINT ( 'NONE',  ( 25.29883596902100251, 11.38086143259999972, -3.116303541651999964 ) ) ;
#59252=CARTESIAN_POINT ( 'NONE',  ( 24.56710111988151013, 11.92027008148530776, -3.200169502113732189 ) ) ;
#59257=EDGE_CURVE ( 'NONE', #9710, #37068, #66921, .T. ) ;
#59265=CARTESIAN_POINT ( 'NONE',  ( 24.66807826193371511, -12.30863159266774609, -2.982840176837593837 ) ) ;
#59268=CARTESIAN_POINT ( 'NONE',  ( 25.47132987582600450, -2.701711062754999837, 11.27933522402000044 ) ) ;
#59281=CARTESIAN_POINT ( 'NONE',  ( 24.41456973790700147, -8.821771448540999927, -8.767658430047001517 ) ) ;
#59285=CARTESIAN_POINT ( 'NONE',  ( 23.95123756517200064, 9.462321155404998407, 9.411281308674000812 ) ) ;
#59286=ORIENTED_EDGE ( 'NONE', *, *, #47235, .T. ) ;
#59289=CONICAL_SURFACE ( 'NONE', #41432, 12.42511170355999894, 0.7854024644601717009 ) ;
#59294=EDGE_CURVE ( 'NONE', #25042, #60421, #32756, .T. ) ;
#59300=AXIS2_PLACEMENT_3D ( 'NONE', #1137, #22449, #43791 ) ;
#59302=EDGE_CURVE ( 'NONE', #34904, #65107, #6876, .T. ) ;
#59303=CARTESIAN_POINT ( 'NONE',  ( 15.40000000009400161, -8.833277835210999740, -7.896561221812000930 ) ) ;
#59305=ORIENTED_EDGE ( 'NONE', *, *, #41274, .T. ) ;
#59312=ORIENTED_EDGE ( 'NONE', *, *, #7827, .T. ) ;
#59315=CARTESIAN_POINT ( 'NONE',  ( 11.74267124137200113, 11.57041781403000158, 1.757356211607000063 ) ) ;
#59316=EDGE_LOOP ( 'NONE', ( #18832, #51759, #27042, #21839 ) ) ;
#59319=CLOSED_SHELL ( 'NONE', ( #8829, #41041, #68523, #34504, #3549, #59443, #42963, #24537, #10105, #34803, #36180, #32657, #41355, #39447, #1800, #41925, #48380, #24309, #39449, #35746, #27899, #10974, #7199, #55345, #3382, #25645, #27878, #61568, #50069, #34017, #30395, #44728, #61780, #25533, #58699, #56831, #59842, #68693, #18566, #15699, #47149, #64364, #17228, #13497, #21460, #32227, #68724, #31825, #51904, #18033, #21648, #8526, #53821, #66774, #63561, #33846, #2908, #49670, #14831, #38740, #58973, #30285, #23660, #19009, #31741, #26714, #65563, #40148, #25739, #20746, #21084, #61059, #25196, #40478, #11385, #25090, #57517, #54096, #22556, #39139, #26673, #63306, #62036, #39060, #45174, #46318, #26154, #55450, #20531, #32362, #6146, #10670, #32878, #28257, #20046, #21454, #47665, #65447, #27618, #52444, #32748, #22339, #41625, #13129, #6771, #41992, #16304, #13742, #52388, #62651, #34802, #43196, #55108, #40528, #60327, #52647, #11676, #27057, #4578, #22276, #16947, #4959, #65782, #1403, #34936, #12081, #50435, #30153, #20063, #34881, #25922, #31987, #47434, #272, #33455, #48376, #59562, #51521, #34889, #21098, #24409, #42865, #12625, #17355, #57145, #46718, #66753, #28905, #55746, #21403, #26441, #65612, #52041, #3681, #55594, #23836, #33981, #12960, #39415, #34888, #32243, #45593, #32459, #7340, #49525, #27954, #25054, #30535, #3303, #4776, #36079, #54928, #51193, #68960, #68241, #37014, #11340, #8148, #55762, #10918, #55284, #16082, #35585, #63707, #43169, #57853, #35225, #16642, #5902, #62096, #1337, #33813, #12331, #40643, #32135, #62832, #5608, #63762, #57223, #25331, #5120, #7592, #38659, #10958, #51484, #12707, #44281, #41971, #43490, #41904, #62946, #19816, #4127, #15915, #28752, #27958, #41006, #18934, #41353, #63507, #58185, #55965, #45230, #61671, #41573, #66152, #53263, #10865, #28091, #23534, #54385, #56608, #11062, #52795, #52249, #45846, #34528, #43716, #9680, #46983, #56858, #59649, #12586, #21599, #67041, #51383, #37736, #33704, #28322, #5517, #53842, #65278, #47099, #28096, #56453, #13463, #22473, #401, #52165, #43485, #2958, #15610, #39183, #11285, #51526, #60393, #53741, #45004, #31013, #26239, #18621, #48043, #28414, #43317, #55237, #40893, #19095, #36811, #61261, #40207, #20912, #43410, #3939, #61361, #26695, #17760, #45673, #10177, #62289, #37094, #67164, #2933, #33018, #14279, #24139, #62134, #3813, #45337, #19657, #11344, #54573, #58267 ) ) ;
#59327=EDGE_LOOP ( 'NONE', ( #27725, #670, #48236, #67082 ) ) ;
#59331=CARTESIAN_POINT ( 'NONE',  ( 15.86122879894100102, -8.802595411723000751, -8.571496522999998646 ) ) ;
#59336=CARTESIAN_POINT ( 'NONE',  ( 16.10004050617000004, -7.492404338401445152, -10.08789649943574851 ) ) ;
#59338=CARTESIAN_POINT ( 'NONE',  ( 24.16219716209097967, -3.322358446342811966, -12.45205009512240224 ) ) ;
#59342=EDGE_CURVE ( 'NONE', #10933, #8271, #23669, .T. ) ;
#59348=CARTESIAN_POINT ( 'NONE',  ( 14.30001311048500057, -12.52500000000000036, 4.931155131476459494E-11 ) ) ;
#59352=CARTESIAN_POINT ( 'NONE',  ( 24.30000000000000071, 12.03537377768999939, 3.224868684338999980 ) ) ;
#59353=CARTESIAN_POINT ( 'NONE',  ( 24.23234572864199876, -12.46720875768999903, 3.269128814187999943 ) ) ;
#59357=CARTESIAN_POINT ( 'NONE',  ( 18.49055856039300139, 2.949841519493000330, 11.23086453091999992 ) ) ;
#59367=CARTESIAN_POINT ( 'NONE',  ( 23.51706659920400355, -10.50862010217999831, -9.449478156932999084 ) ) ;
#59368=FACE_OUTER_BOUND ( 'NONE', #52105, .T. ) ;
#59370=VERTEX_POINT ( 'NONE', #61404 ) ;
#59374=CARTESIAN_POINT ( 'NONE',  ( 24.41555930013399944, 8.820896577363999569, -8.766783479041999172 ) ) ;
#59376=EDGE_LOOP ( 'NONE', ( #20193, #33366, #62158, #4176 ) ) ;
#59389=ORIENTED_EDGE ( 'NONE', *, *, #17525, .T. ) ;
#59390=FACE_OUTER_BOUND ( 'NONE', #49718, .T. ) ;
#59391=CARTESIAN_POINT ( 'NONE',  ( 12.83944380997200163, -12.16696032571000075, 3.135189167188999537 ) ) ;
#59393=B_SPLINE_CURVE_WITH_KNOTS ( 'NONE', 3,
 ( #66110, #39552, #12636, #33966, #2829, #55289 ),
 .UNSPECIFIED., .F., .F.,
 ( 4, 2, 4 ),
 ( 0.000000000000000000, 0.5000000000000000000, 1.000000000000000000 ),
 .UNSPECIFIED. ) ;
#59399=CARTESIAN_POINT ( 'NONE',  ( 24.89161184346078670, -11.59760657164508046, -3.206054533605021462 ) ) ;
#59412=B_SPLINE_CURVE_WITH_KNOTS ( 'NONE', 3,
 ( #10422, #37685, #32111, #26514 ),
 .UNSPECIFIED., .F., .F.,
 ( 4, 4 ),
 ( 0.000000000000000000, 1.000000000000000000 ),
 .UNSPECIFIED. ) ;
#59418=CARTESIAN_POINT ( 'NONE',  ( 24.96658174203286151, -8.756202942073826989, 7.455126426642118886 ) ) ;
#59420=CARTESIAN_POINT ( 'NONE',  ( 25.59994555223599733, 2.024003533649000097, -11.01554633311000053 ) ) ;
#59429=ORIENTED_EDGE ( 'NONE', *, *, #12009, .F. ) ;
#59431=CARTESIAN_POINT ( 'NONE',  ( 24.39664890229900251, 8.853228234369833416, 8.853228234369833416 ) ) ;
#59432=CARTESIAN_POINT ( 'NONE',  ( 23.60000000000000142, 11.49391741900999975, 4.090215442373000165 ) ) ;
#59443=ADVANCED_FACE ( 'NONE', ( #4375 ), #20463, .F. ) ;
#59452=CARTESIAN_POINT ( 'NONE',  ( 13.70005190196300227, 9.005348107749998832, 7.391036106496999381 ) ) ;
#59454=DIRECTION ( 'NONE',  ( 0.000000000000000000, 0.000000000000000000, -1.000000000000000000 ) ) ;
#59459=DIRECTION ( 'NONE',  ( 0.000000000000000000, 0.9624505444715647506, -0.2714570858282915333 ) ) ;
#59460=EDGE_LOOP ( 'NONE', ( #39730, #64763, #927, #14044 ) ) ;
#59461=AXIS2_PLACEMENT_3D ( 'NONE', #60381, #49538, #38713 ) ;
#59463=CARTESIAN_POINT ( 'NONE',  ( 23.65870916658217382, -10.04306394571245953, -9.454468549935667099 ) ) ;
#59468=CARTESIAN_POINT ( 'NONE',  ( 24.03012267896300003, 3.726860619367999838, -13.01722844268999957 ) ) ;
#59470=CARTESIAN_POINT ( 'NONE',  ( 16.39999999347100257, -3.345256695718999751, -11.86066175541999890 ) ) ;
#59471=CARTESIAN_POINT ( 'NONE',  ( 17.66658675203450102, -10.78295181804075398, 4.410266442045759128 ) ) ;
#59472=CARTESIAN_POINT ( 'NONE',  ( 18.15262501847808707, -3.263149105984915810, -11.18369374219367174 ) ) ;
#59478=EDGE_CURVE ( 'NONE', #31587, #9710, #41996, .T. ) ;
#59498=CARTESIAN_POINT ( 'NONE',  ( 23.59999196693599899, 2.915561532799999966, -13.58550759281999909 ) ) ;
#59500=FACE_OUTER_BOUND ( 'NONE', #8877, .T. ) ;
#59503=DIRECTION ( 'NONE',  ( 0.000000000000000000, -0.01629188381079070894, 0.9998672784534433644 ) ) ;
#59522=DIRECTION ( 'NONE',  ( -0.9999999999991096011, -6.425037516353057767E-07, -1.169597258120009531E-06 ) ) ;
#59537=CARTESIAN_POINT ( 'NONE',  ( 11.79999999684100054, -3.345264396959000130, 11.86064773189999855 ) ) ;
#59547=ORIENTED_EDGE ( 'NONE', *, *, #4563, .T. ) ;
#59559=CIRCLE ( 'NONE', #7068, 13.98989069978000188 ) ;
#59562=ADVANCED_FACE ( 'NONE', ( #37235 ), #61919, .T. ) ;
#59568=VERTEX_POINT ( 'NONE', #10658 ) ;
#59574=CARTESIAN_POINT ( 'NONE',  ( 13.64495723965300122, 12.20594327342000085, 2.556931772870000064 ) ) ;
#59578=ORIENTED_EDGE ( 'NONE', *, *, #39146, .T. ) ;
#59580=CARTESIAN_POINT ( 'NONE',  ( 24.74121292487855683, 8.638778361025718056, -8.580587272887251871 ) ) ;
#59583=CARTESIAN_POINT ( 'NONE',  ( 23.75091537440847134, -13.09198522470825132, 3.783037687685711692 ) ) ;
#59591=CARTESIAN_POINT ( 'NONE',  ( 24.69899733841000256, 12.37167067653999908, -2.942311114818999762 ) ) ;
#59593=ORIENTED_EDGE ( 'NONE', *, *, #61959, .F. ) ;
#59595=CARTESIAN_POINT ( 'NONE',  ( 16.10005255078199937, 3.632778330393000132, 11.06917548872000090 ) ) ;
#59598=ORIENTED_EDGE ( 'NONE', *, *, #54312, .T. ) ;
#59603=CARTESIAN_POINT ( 'NONE',  ( 24.63609380610749966, 11.85365310353625823, -3.193521306612203237 ) ) ;
#59608=ORIENTED_EDGE ( 'NONE', *, *, #55660, .T. ) ;
#59611=CIRCLE ( 'NONE', #60716, 1.300162295583999539 ) ;
#59631=CARTESIAN_POINT ( 'NONE',  ( 13.99999999347100044, -9.187456302440001110, -8.213201953411001455 ) ) ;
#59639=EDGE_LOOP ( 'NONE', ( #16305, #23480, #7867, #45656, #19697 ) ) ;
#59649=ADVANCED_FACE ( 'NONE', ( #39306 ), #49443, .F. ) ;
#59662=CARTESIAN_POINT ( 'NONE',  ( 13.84418086767167466, 9.492976300297533143, 8.170822042178436106 ) ) ;
#59667=CARTESIAN_POINT ( 'NONE',  ( 16.22809631267600139, 3.350750460640000039, 11.21314580301999797 ) ) ;
#59671=CARTESIAN_POINT ( 'NONE',  ( 13.50000000000339639, 9.396284335645857411, 7.729197028970922645 ) ) ;
#59676=ORIENTED_EDGE ( 'NONE', *, *, #57123, .F. ) ;
#59681=CARTESIAN_POINT ( 'NONE',  ( 15.55534550153200080, -9.119897322331999234, -8.232476562723000768 ) ) ;
#59683=ORIENTED_EDGE ( 'NONE', *, *, #64901, .T. ) ;
#59692=VERTEX_POINT ( 'NONE', #51851 ) ;
#59695=CARTESIAN_POINT ( 'NONE',  ( 11.55259020248000112, -12.34178403982000205, -1.785089783152000065 ) ) ;
#59699=EDGE_CURVE ( 'NONE', #50821, #33837, #54360, .T. ) ;
#59701=CARTESIAN_POINT ( 'NONE',  ( 24.56892806240000127, 12.57303442533000037, 2.966957253552999774 ) ) ;
#59705=CARTESIAN_POINT ( 'NONE',  ( 23.60000000000000142, 2.548720605937000006, 12.21654710926000220 ) ) ;
#59712=CARTESIAN_POINT ( 'NONE',  ( 24.53428991268900106, -12.47024905405999995, -3.026245386525999947 ) ) ;
#59714=CARTESIAN_POINT ( 'NONE',  ( 23.73577082021700235, -9.841767396222000031, -9.786596206530999709 ) ) ;
#59715=FACE_OUTER_BOUND ( 'NONE', #46352, .T. ) ;
#59729=EDGE_LOOP ( 'NONE', ( #47725, #4007, #39299, #46684 ) ) ;
#59737=CARTESIAN_POINT ( 'NONE',  ( 24.30857393632600250, 12.13191889359999998, -3.290345171646999578 ) ) ;
#59740=CARTESIAN_POINT ( 'NONE',  ( 12.10154284453400209, -11.81398323980999976, 3.695357857504999899 ) ) ;
#59752=CARTESIAN_POINT ( 'NONE',  ( 23.82002767510200414, 12.91624849431999955, -3.707179493336999698 ) ) ;
#59755=EDGE_CURVE ( 'NONE', #47838, #54862, #60823, .T. ) ;
#59757=CARTESIAN_POINT ( 'NONE',  ( 23.59999443371599881, 2.915558930973999985, 13.58549620949000136 ) ) ;
#59768=CARTESIAN_POINT ( 'NONE',  ( 18.53600088859200312, -11.84356608895999941, 4.189033083324999573 ) ) ;
#59777=DIRECTION ( 'NONE',  ( 0.9999999999777403614, -3.933702046811161244E-06, -5.389360668004222102E-06 ) ) ;
#59779=CARTESIAN_POINT ( 'NONE',  ( 11.35642168284000242, 12.27417251877000126, 1.600391102631000040 ) ) ;
#59781=CARTESIAN_POINT ( 'NONE',  ( 25.46372797112000086, -8.354608193938998895, 8.148457429720000533 ) ) ;
#59790=CARTESIAN_POINT ( 'NONE',  ( 24.35146665670700017, -3.377061749054000028, -12.26054704401999906 ) ) ;
#59812=AXIS2_PLACEMENT_3D ( 'NONE', #32975, #43816, #49053 ) ;
#59813=CARTESIAN_POINT ( 'NONE',  ( 12.08097595788930789, -12.02669421650221437, 3.498808775436077934 ) ) ;
#59818=CARTESIAN_POINT ( 'NONE',  ( 13.43019412026500170, -12.07125412582999857, -2.305633000807000066 ) ) ;
#59819=VERTEX_POINT ( 'NONE', #46962 ) ;
#59822=FACE_OUTER_BOUND ( 'NONE', #47393, .T. ) ;
#59830=CARTESIAN_POINT ( 'NONE',  ( 11.50002544571312058, -3.809924653178162313, 11.93174516965595622 ) ) ;
#59832=FACE_OUTER_BOUND ( 'NONE', #16596, .T. ) ;
#59841=ORIENTED_EDGE ( 'NONE', *, *, #61424, .F. ) ;
#59842=ADVANCED_FACE ( 'NONE', ( #40677 ), #37705, .F. ) ;
#59846=CIRCLE ( 'NONE', #25214, 1.300133550998999743 ) ;
#59859=ORIENTED_EDGE ( 'NONE', *, *, #55489, .F. ) ;
#59863=CARTESIAN_POINT ( 'NONE',  ( 23.57774079265084310, 13.28347076428885565, -4.287252149520854871 ) ) ;
#59867=DIRECTION ( 'NONE',  ( 0.000000000000000000, -0.2714570858282905341, 0.9624505444715651947 ) ) ;
#59882=DIRECTION ( 'NONE',  ( 0.9999999999999762412, 2.179566365501950425E-07, -9.624109672044771190E-10 ) ) ;
#59893=AXIS2_PLACEMENT_3D ( 'NONE', #48169, #21588, #31408 ) ;
#59899=CARTESIAN_POINT ( 'NONE',  ( 11.80561165699200110, 3.526771526455999783, -11.96112153682000034 ) ) ;
#59907=CARTESIAN_POINT ( 'NONE',  ( 24.41456973790700147, -3.182129207855000086, 12.02370739584000070 ) ) ;
#59908=CARTESIAN_POINT ( 'NONE',  ( 13.50018479229797030, -11.10053973472247790, -4.255642710877533652 ) ) ;
#59913=ORIENTED_EDGE ( 'NONE', *, *, #53656, .F. ) ;
#59917=CARTESIAN_POINT ( 'NONE',  ( 25.48313369564800368, -8.422746779740000633, -7.953667242360999978 ) ) ;
#59920=CARTESIAN_POINT ( 'NONE',  ( 13.43043922992600159, 12.41458792447999926, 1.928118222792999825 ) ) ;
#59927=CARTESIAN_POINT ( 'NONE',  ( 25.26126739128486065, 8.521553289640936057, -7.991940988076141394 ) ) ;
#59934=VERTEX_POINT ( 'NONE', #4990 ) ;
#59937=CARTESIAN_POINT ( 'NONE',  ( 25.50731759324898107, 8.309739206314244342, -8.116424455511989322 ) ) ;
#59939=TOROIDAL_SURFACE ( 'NONE', #29829, 13.79999999999999893, 0.2000000000000000111 ) ;
#59940=CARTESIAN_POINT ( 'NONE',  ( 11.35399482404720040, -3.445326802703576163, 11.33548354870907282 ) ) ;
#59948=CARTESIAN_POINT ( 'NONE',  ( 16.04506009312500225, 3.874776422117000241, 11.85383417895000058 ) ) ;
#59949=CARTESIAN_POINT ( 'NONE',  ( 23.60205915885299888, 2.171992490544001786, 12.06370038613001228 ) ) ;
#59956=CARTESIAN_POINT ( 'NONE',  ( 13.43777338887524486, 12.12041883920677243, 2.246947635350981631 ) ) ;
#59959=CARTESIAN_POINT ( 'NONE',  ( 25.18909985880100066, 2.894851937781000029, 11.44762852350000060 ) ) ;
#59978=CARTESIAN_POINT ( 'NONE',  ( 23.58017449365151208, 10.23400074257411063, -9.531361764565000172 ) ) ;
#59982=ORIENTED_EDGE ( 'NONE', *, *, #53763, .T. ) ;
#59988=CARTESIAN_POINT ( 'NONE',  ( 23.60205915885299888, 9.361474752760003071, -7.912850866705011477 ) ) ;
#59991=CARTESIAN_POINT ( 'NONE',  ( 13.49980696792483137, -10.14812545701395585, -7.065329385613733137 ) ) ;
#60001=ORIENTED_EDGE ( 'NONE', *, *, #6486, .F. ) ;
#60009=DIRECTION ( 'NONE',  ( -1.000000000000000000, 0.000000000000000000, 0.000000000000000000 ) ) ;
#60010=CARTESIAN_POINT ( 'NONE',  ( 14.80000000000000071, -3.283787102340999464, 11.28049554847999936 ) ) ;
#60011=ORIENTED_EDGE ( 'NONE', *, *, #12818, .T. ) ;
#60014=CARTESIAN_POINT ( 'NONE',  ( 16.15961700471899931, 3.514971253533999640, 11.06754630474000045 ) ) ;
#60017=CARTESIAN_POINT ( 'NONE',  ( 24.30001694968100168, 3.271769180623000040, -12.21048179117000032 ) ) ;
#60019=AXIS2_PLACEMENT_3D ( 'NONE', #46418, #51653, #56219 ) ;
#60025=CARTESIAN_POINT ( 'NONE',  ( 23.55757948181399897, -13.49847953779999976, -4.022400660198999667 ) ) ;
#60027=DIRECTION ( 'NONE',  ( -1.000000000000000000, 0.000000000000000000, 0.000000000000000000 ) ) ;
#60029=VERTEX_POINT ( 'NONE', #12311 ) ;
#60044=CARTESIAN_POINT ( 'NONE',  ( 25.30000327618300204, -6.604245036507551141E-15, -11.49994408209238017 ) ) ;
#60048=AXIS2_PLACEMENT_3D ( 'NONE', #58606, #69098, #26808 ) ;
#60049=CARTESIAN_POINT ( 'NONE',  ( 24.30001683570900184, 3.271769286791000209, 12.21048169671000139 ) ) ;
#60054=ORIENTED_EDGE ( 'NONE', *, *, #38115, .T. ) ;
#60057=EDGE_CURVE ( 'NONE', #44042, #61329, #8557, .T. ) ;
#60062=CARTESIAN_POINT ( 'NONE',  ( 17.79319863334400154, 3.315493116453000155, -11.22361396466000016 ) ) ;
#60068=CARTESIAN_POINT ( 'NONE',  ( 23.58444971190600015, -10.35811008870000016, -9.328007211334000459 ) ) ;
#60071=CARTESIAN_POINT ( 'NONE',  ( 24.66708179685902991, 3.571422468837009756, -12.15221134863278962 ) ) ;
#60076=LINE ( 'NONE', #18119, #17786 ) ;
#60082=DIRECTION ( 'NONE',  ( 0.000000000000000000, -0.007439385635786961021, -0.9999723273877941798 ) ) ;
#60092=FACE_OUTER_BOUND ( 'NONE', #48486, .T. ) ;
#60099=CARTESIAN_POINT ( 'NONE',  ( 23.95415685822884200, -9.440317297343241876, 9.313970111589597423 ) ) ;
#60101=VERTEX_POINT ( 'NONE', #27706 ) ;
#60108=CARTESIAN_POINT ( 'NONE',  ( 23.61357239562000032, 13.29063276735999999, -4.053366244155999887 ) ) ;
#60114=CARTESIAN_POINT ( 'NONE',  ( 23.56666365135700403, 11.16210620494999439, 3.571147222960000533 ) ) ;
#60115=CARTESIAN_POINT ( 'NONE',  ( 23.59999192078999997, 10.30759737717999869, 9.317725909430999209 ) ) ;
#60117=PLANE ( 'NONE',  #14903 ) ;
#60119=CARTESIAN_POINT ( 'NONE',  ( 23.56666365135700403, 2.963314674619003330, -12.23574966049000423 ) ) ;
#60129=EDGE_LOOP ( 'NONE', ( #31841, #21164, #65682, #24834 ) ) ;
#60132=CARTESIAN_POINT ( 'NONE',  ( 11.83966971788800215, 12.22235437154000159, 1.953272420501999784 ) ) ;
#60135=CARTESIAN_POINT ( 'NONE',  ( 18.53682820967700451, 2.877067450793000081, -12.22924281482000097 ) ) ;
#60142=ORIENTED_EDGE ( 'NONE', *, *, #37057, .F. ) ;
#60146=CARTESIAN_POINT ( 'NONE',  ( 24.30000000000000071, -3.224868684338999980, -12.03537377768999939 ) ) ;
#60148=ORIENTED_EDGE ( 'NONE', *, *, #68407, .F. ) ;
#60161=CARTESIAN_POINT ( 'NONE',  ( 24.45625570098342294, 8.883597759657003934, -9.170492528765944229 ) ) ;
#60164=CARTESIAN_POINT ( 'NONE',  ( 23.59999467231800097, -10.30760443253999981, -9.317695455237998914 ) ) ;
#60168=CARTESIAN_POINT ( 'NONE',  ( 12.79999999975700042, 11.86189249994999884, -3.298671769835999967 ) ) ;
#60174=CARTESIAN_POINT ( 'NONE',  ( 24.08693222998299888, 3.426481660494999915, -12.66967535867999928 ) ) ;
#60175=CARTESIAN_POINT ( 'NONE',  ( 13.64718133169100156, -12.21462133634999958, -2.516296819814999974 ) ) ;
#60176=VERTEX_POINT ( 'NONE', #27808 ) ;
#60178=CARTESIAN_POINT ( 'NONE',  ( 12.65360965087631939, 11.23193385079074957, -3.094113056604177014 ) ) ;
#60180=DIRECTION ( 'NONE',  ( 1.000000000000000000, 0.000000000000000000, 0.000000000000000000 ) ) ;
#60192=B_SPLINE_CURVE_WITH_KNOTS ( 'NONE', 3,
 ( #29239, #61039, #66962, #13503, #29931, #3332, #51235, #24665 ),
 .UNSPECIFIED., .F., .F.,
 ( 4, 2, 2, 4 ),
 ( 0.000000000000000000, 0.2500000000000022760, 0.5000000000000045519, 1.000000000000000000 ),
 .UNSPECIFIED. ) ;
#60197=CARTESIAN_POINT ( 'NONE',  ( 21.60000052036201268, -13.89999947951999992, -2.298221717064000337E-09 ) ) ;
#60198=ORIENTED_EDGE ( 'NONE', *, *, #64933, .F. ) ;
#60201=CARTESIAN_POINT ( 'NONE',  ( 23.61436141550033341, 3.070533063945404262, -13.52808024449816848 ) ) ;
#60205=CARTESIAN_POINT ( 'NONE',  ( 11.80912799980900019, 3.189026639965999443, -11.45098040807999951 ) ) ;
#60206=CIRCLE ( 'NONE', #24313, 13.98989063586999571 ) ;
#60208=CARTESIAN_POINT ( 'NONE',  ( 25.59994555223599733, -8.527741194213000142, -7.260611644044000279 ) ) ;
#60227=CARTESIAN_POINT ( 'NONE',  ( 17.69319447854400096, 11.81408139396000045, -3.326117390868000179 ) ) ;
#60228=CARTESIAN_POINT ( 'NONE',  ( 23.58312315446800156, -2.940929503173999926, -13.62839437077999882 ) ) ;
#60230=B_SPLINE_SURFACE_WITH_KNOTS ( 'NONE', 3, 3, ( 
 ( #54122, #60068, #43645, #59367 ),
 ( #48542, #42950, #12173, #33155 ),
 ( #43296, #38040, #54471, #64604 ),
 ( #38388, #22305, #16372, #6219 ),
 ( #27560, #16710, #64942, #22647 ),
 ( #33503, #6573, #37702, #59714 ),
 ( #17414, #54818, #21958, #11813 ),
 ( #59030, #11465, #32807, #43992 ),
 ( #49222, #48887, #11132, #994 ),
 ( #65298, #32466, #17055, #21615 ),
 ( #1330, #38739, #6918, #28250 ),
 ( #49570, #1680, #64258, #22996 ) ),
 .UNSPECIFIED., .F., .F., .F.,
 ( 4, 1, 1, 1, 1, 1, 1, 1, 1, 4 ),
 ( 4, 4 ),
 ( 0.5516038081316999575, 0.5999999999999999778, 0.6500000000000000222, 0.6999999999999999556, 0.7500000000000000000, 0.8000000000000000444, 0.8499999999999999778, 0.9000000000000000222, 0.9499999999999999556, 0.9893631058703999948 ),
 ( -0.2706695798834999889, 1.270788350771999919 ),
 .UNSPECIFIED. ) ;
#60236=CARTESIAN_POINT ( 'NONE',  ( 25.60000000000000142, -13.52296156804999860, 3.623466631435000362 ) ) ;
#60256=VERTEX_POINT ( 'NONE', #11360 ) ;
#60258=CARTESIAN_POINT ( 'NONE',  ( 17.60000000085000238, 12.11987927271999865, -3.159802730921999814 ) ) ;
#60261=CARTESIAN_POINT ( 'NONE',  ( 24.34833281187866660, -3.256146913723438896, 12.15210571892843916 ) ) ;
#60262=CARTESIAN_POINT ( 'NONE',  ( 13.50018479229797208, -10.27880801399731858, -5.973155204427725629 ) ) ;
#60268=CARTESIAN_POINT ( 'NONE',  ( 24.67332274059700126, -12.15930828887999837, -3.026486267162999511 ) ) ;
#60270=CARTESIAN_POINT ( 'NONE',  ( 14.04004776902899998, -8.829547661313998930, -7.819892149868999276 ) ) ;
#60271=CARTESIAN_POINT ( 'NONE',  ( 25.29878307837499918, -8.389243454266001265, -8.298034019942999606 ) ) ;
#60274=CARTESIAN_POINT ( 'NONE',  ( 13.46281931570200108, 12.03411875281000043, 2.480748420245000307 ) ) ;
#60282=CARTESIAN_POINT ( 'NONE',  ( 23.94498309455302731, -12.80023880358030475, 3.529808243006147706 ) ) ;
#60286=DIRECTION ( 'NONE',  ( 0.000000000000000000, -0.6664713972124013397, 0.7455306007789014311 ) ) ;
#60298=CARTESIAN_POINT ( 'NONE',  ( 16.31137892731300099, 3.415016125706999972, 11.89702177947000017 ) ) ;
#60299=CARTESIAN_POINT ( 'NONE',  ( 24.35365242081700288, 3.193712117558000774, 11.49150331547998860 ) ) ;
#60304=EDGE_LOOP ( 'NONE', ( #63438, #28791 ) ) ;
#60315=VERTEX_POINT ( 'NONE', #64836 ) ;
#60323=AXIS2_PLACEMENT_3D ( 'NONE', #29700, #1725, #18160 ) ;
#60327=ADVANCED_FACE ( 'NONE', ( #57271 ), #44621, .F. ) ;
#60328=CARTESIAN_POINT ( 'NONE',  ( 24.54687940532799928, -8.860358431052000938, -9.345000394951000544 ) ) ;
#60330=CARTESIAN_POINT ( 'NONE',  ( 17.60000000798000386, 11.41069016990000051, -4.623987642516999230 ) ) ;
#60335=CARTESIAN_POINT ( 'NONE',  ( 24.14469781561994211, -3.678927484064260511, 12.80140212425259705 ) ) ;
#60341=CARTESIAN_POINT ( 'NONE',  ( 18.05828223140173705, -3.296090368282506233, -11.87625427050431703 ) ) ;
#60348=VERTEX_POINT ( 'NONE', #33391 ) ;
#60351=DIRECTION ( 'NONE',  ( -1.000000000000000000, 0.000000000000000000, 0.000000000000000000 ) ) ;
#60360=CARTESIAN_POINT ( 'NONE',  ( 25.10988277031431437, -8.510211365751388257, -8.211054588496716988 ) ) ;
#60364=VERTEX_POINT ( 'NONE', #50844 ) ;
#60372=CARTESIAN_POINT ( 'NONE',  ( 24.15420937678199920, -12.81569892223000018, -3.249518417564999595 ) ) ;
#60373=AXIS2_PLACEMENT_3D ( 'NONE', #58859, #36164, #31272 ) ;
#60375=B_SPLINE_CURVE_WITH_KNOTS ( 'NONE', 3,
 ( #1898, #39647, #43856, #13433, #44899, #38962 ),
 .UNSPECIFIED., .F., .F.,
 ( 4, 2, 4 ),
 ( 0.000000000000000000, 0.5000000000000000000, 1.000000000000000000 ),
 .UNSPECIFIED. ) ;
#60378=B_SPLINE_SURFACE_WITH_KNOTS ( 'NONE', 3, 3, ( 
 ( #68311, #42448, #62394, #36863 ),
 ( #41074, #26373, #31617, #25677 ),
 ( #67627, #9243, #47010, #26023 ),
 ( #57481, #19751, #30585, #52588 ),
 ( #14510, #51897, #47355, #3995 ),
 ( #69010, #46670, #20090, #58181 ),
 ( #9588, #30933, #41760, #63060 ),
 ( #15187, #10283, #68659, #57834 ),
 ( #21123, #21438, #16199, #43473 ) ),
 .UNSPECIFIED., .F., .F., .F.,
 ( 4, 1, 1, 1, 1, 1, 4 ),
 ( 4, 4 ),
 ( 0.02209653170518000032, 0.1666666666667000196, 0.3333333333333000081, 0.5000000000000000000, 0.6666666666667000474, 0.8333333333333000637, 0.9492823795161999811 ),
 ( -0.1916656884162999952, 1.191851428473000185 ),
 .UNSPECIFIED. ) ;
#60379=CARTESIAN_POINT ( 'NONE',  ( 23.74396220697517634, 13.10156841507209613, -3.794861878603663197 ) ) ;
#60381=CARTESIAN_POINT ( 'NONE',  ( 16.00017105474300294, 1.714184350020999865E-13, 1.962874307536999842E-13 ) ) ;
#60389=EDGE_CURVE ( 'NONE', #48412, #65865, #11891, .T. ) ;
#60393=ADVANCED_FACE ( 'NONE', ( #7853 ), #68944, .F. ) ;
#60397=CARTESIAN_POINT ( 'NONE',  ( 23.74225507199300367, 13.04612777714000060, 3.828889919760000371 ) ) ;
#60399=ORIENTED_EDGE ( 'NONE', *, *, #45150, .T. ) ;
#60400=CARTESIAN_POINT ( 'NONE',  ( 23.60000000000000142, 0.000000000000000000, 0.000000000000000000 ) ) ;
#60404=CARTESIAN_POINT ( 'NONE',  ( 25.39940835236649264, -2.782819894115065029, 11.32465380471084693 ) ) ;
#60408=VECTOR ( 'NONE', #59777, 1000.000000000000114 ) ;
#60409=EDGE_CURVE ( 'NONE', #36918, #11759, #25133, .T. ) ;
#60412=CARTESIAN_POINT ( 'NONE',  ( 23.58679018630100188, -10.27406905139999971, 9.417699698887998849 ) ) ;
#60415=VERTEX_POINT ( 'NONE', #62358 ) ;
#60419=CARTESIAN_POINT ( 'NONE',  ( 23.56664676942400050, 2.935522432666999748, 13.67843419499999946 ) ) ;
#60421=VERTEX_POINT ( 'NONE', #57446 ) ;
#60422=CARTESIAN_POINT ( 'NONE',  ( 25.19966451436399879, 3.337967404952000283, -11.59330719735999971 ) ) ;
#60427=EDGE_LOOP ( 'NONE', ( #3885, #14209, #63795, #48972 ) ) ;
#60435=CARTESIAN_POINT ( 'NONE',  ( 11.85864217039400259, -11.85700164854999983, 4.150661879143999755 ) ) ;
#60439=CARTESIAN_POINT ( 'NONE',  ( 23.64132674793100364, 3.068957318205999929, 13.45500447039000136 ) ) ;
#60441=VERTEX_POINT ( 'NONE', #3961 ) ;
#60442=CARTESIAN_POINT ( 'NONE',  ( 23.81728156613312564, -9.687086922993964677, 9.414217616044480152 ) ) ;
#60450=CARTESIAN_POINT ( 'NONE',  ( 24.23279599547700158, 12.46651541951000119, -3.268895217084000215 ) ) ;
#60451=EDGE_CURVE ( 'NONE', #58276, #55894, #26009, .T. ) ;
#60452=CARTESIAN_POINT ( 'NONE',  ( 25.30000327618300204, 8.756202924575998026, 7.455126447192999883 ) ) ;
#60456=CARTESIAN_POINT ( 'NONE',  ( 12.79999998712400178, 11.53033693765999779, -4.891431908114999949 ) ) ;
#60457=ORIENTED_EDGE ( 'NONE', *, *, #6486, .T. ) ;
#60458=CARTESIAN_POINT ( 'NONE',  ( 24.35365242081700288, 10.90899669677000006, 3.315896191878997978 ) ) ;
#60459=LINE ( 'NONE', #66036, #32 ) ;
#60460=VERTEX_POINT ( 'NONE', #19366 ) ;
#60465=CARTESIAN_POINT ( 'NONE',  ( 17.60631394974399910, -11.38841897587999874, 4.575468659046999953 ) ) ;
#60478=CARTESIAN_POINT ( 'NONE',  ( 24.63807759523900032, -3.694099725974000048, 12.29546658197999953 ) ) ;
#60487=DIRECTION ( 'NONE',  ( 0.000000000000000000, 0.000000000000000000, -1.000000000000000000 ) ) ;
#60495=EDGE_LOOP ( 'NONE', ( #20469, #57504, #28384, #57568, #54475, #56262, #14951 ) ) ;
#60505=B_SPLINE_CURVE_WITH_KNOTS ( 'NONE', 3,
 ( #19413, #45984, #25687, #13835 ),
 .UNSPECIFIED., .F., .F.,
 ( 4, 4 ),
 ( 0.000000000000000000, 1.000000000000000000 ),
 .UNSPECIFIED. ) ;
#60514=CARTESIAN_POINT ( 'NONE',  ( 12.97415039705200179, -12.11604096695999999, -2.033011318525000277 ) ) ;
#60519=VECTOR ( 'NONE', #35386, 1000.000000000000000 ) ;
#60522=ORIENTED_EDGE ( 'NONE', *, *, #55092, .F. ) ;
#60529=EDGE_CURVE ( 'NONE', #12119, #60421, #47318, .T. ) ;
#60532=CARTESIAN_POINT ( 'NONE',  ( 15.89979320884932612, -5.681736459261024663, -10.98277228430214691 ) ) ;
#60534=EDGE_CURVE ( 'NONE', #44670, #22409, #56431, .T. ) ;
#60537=VERTEX_POINT ( 'NONE', #57109 ) ;
#60539=ORIENTED_EDGE ( 'NONE', *, *, #3707, .T. ) ;
#60542=EDGE_LOOP ( 'NONE', ( #62352, #14401, #56507, #52546 ) ) ;
#60545=CARTESIAN_POINT ( 'NONE',  ( 23.66004879239100234, 13.39256445865000167, -3.813547382634999483 ) ) ;
#60547=CARTESIAN_POINT ( 'NONE',  ( 24.39664275023335804, -8.810499738035991513, -8.810499738035991513 ) ) ;
#60548=CARTESIAN_POINT ( 'NONE',  ( 16.86666666233133327, -3.345268057356067359, -11.86064107292373571 ) ) ;
#60549=CARTESIAN_POINT ( 'NONE',  ( 11.25913761803000135, 3.706864829039000053, -11.29572955805999968 ) ) ;
#60552=DIRECTION ( 'NONE',  ( 1.000000000000000000, 0.000000000000000000, 0.000000000000000000 ) ) ;
#60565=CARTESIAN_POINT ( 'NONE',  ( 24.35365242081700288, -8.326148686889998984, -7.789520173161003314 ) ) ;
#60567=VERTEX_POINT ( 'NONE', #24616 ) ;
#60570=CARTESIAN_POINT ( 'NONE',  ( 24.02990352322499845, -3.726800819761000305, -13.01750903018000116 ) ) ;
#60578=CARTESIAN_POINT ( 'NONE',  ( 24.53428991195500330, 3.614319144953999530, 12.31267516478999902 ) ) ;
#60596=CARTESIAN_POINT ( 'NONE',  ( 11.72754826524499983, 3.413272067235999963, -11.89753034518999897 ) ) ;
#60599=AXIS2_PLACEMENT_3D ( 'NONE', #1262, #22576, #27488 ) ;
#60602=CARTESIAN_POINT ( 'NONE',  ( 23.60000000000000142, 0.000000000000000000, 0.000000000000000000 ) ) ;
#60603=CARTESIAN_POINT ( 'NONE',  ( 11.49999672495000524, 11.45771900890041728, -2.434039779711009821 ) ) ;
#60615=CARTESIAN_POINT ( 'NONE',  ( 24.95773344659900062, -8.510917023874998932, -8.990083141738999473 ) ) ;
#60622=VERTEX_POINT ( 'NONE', #48690 ) ;
#60637=B_SPLINE_CURVE_WITH_KNOTS ( 'NONE', 3,
 ( #4608, #51818, #25942, #36431 ),
 .UNSPECIFIED., .F., .F.,
 ( 4, 4 ),
 ( 0.000000000000000000, 1.000000000000000000 ),
 .UNSPECIFIED. ) ;
#60643=CARTESIAN_POINT ( 'NONE',  ( 23.89320776801300283, 3.288740538451999651, 12.20874841473999872 ) ) ;
#60647=DIRECTION ( 'NONE',  ( 0.000000000000000000, -0.7071067811865475727, 0.7071067811865475727 ) ) ;
#60656=ORIENTED_EDGE ( 'NONE', *, *, #27615, .F. ) ;
#60662=CARTESIAN_POINT ( 'NONE',  ( 23.56697384540236939, 3.042303125952126486, -13.65541767842539933 ) ) ;
#60666=CARTESIAN_POINT ( 'NONE',  ( 16.39999999231800132, 3.216285993016000155, 11.40340220863999932 ) ) ;
#60677=CARTESIAN_POINT ( 'NONE',  ( 23.66004879239100234, -3.393653467490999720, 13.50507469661999949 ) ) ;
#60687=CARTESIAN_POINT ( 'NONE',  ( 24.60109543021109602, -12.20853568610929329, 3.061026903515568165 ) ) ;
#60688=CARTESIAN_POINT ( 'NONE',  ( 24.05250961456292913, -12.62704480724583078, -3.430091672397665103 ) ) ;
#60690=ORIENTED_EDGE ( 'NONE', *, *, #13282, .T. ) ;
#60693=EDGE_CURVE ( 'NONE', #12534, #24760, #58574, .T. ) ;
#60695=DIRECTION ( 'NONE',  ( 0.000000000000000000, -0.7614089499631907509, -0.6482718649732928107 ) ) ;
#60703=CARTESIAN_POINT ( 'NONE',  ( 25.34044016535778354, -2.679925846854998905, -11.33984901862687167 ) ) ;
#60705=ORIENTED_EDGE ( 'NONE', *, *, #11448, .F. ) ;
#60707=CARTESIAN_POINT ( 'NONE',  ( 18.30017264560542145, -0.9191760148722679657, 11.85014035458664772 ) ) ;
#60712=CARTESIAN_POINT ( 'NONE',  ( 24.53429010490700080, 8.855930189872001534, 9.286429716155000236 ) ) ;
#60716=AXIS2_PLACEMENT_3D ( 'NONE', #35932, #57245, #14950 ) ;
#60723=CARTESIAN_POINT ( 'NONE',  ( 24.30000000000000071, -10.83443035398000021, -3.855530949778000149 ) ) ;
#60728=ORIENTED_EDGE ( 'NONE', *, *, #14218, .T. ) ;
#60736=CARTESIAN_POINT ( 'NONE',  ( 25.29987667925500361, 10.83443035398000021, 3.855530949778000149 ) ) ;
#60750=EDGE_CURVE ( 'NONE', #67010, #15838, #62652, .T. ) ;
#60752=CARTESIAN_POINT ( 'NONE',  ( 23.51521052042600246, -10.47031424384000076, 9.494913483761999728 ) ) ;
#60758=CARTESIAN_POINT ( 'NONE',  ( 24.35365242081699932, -1.906711579001001189, 11.36048031431998595 ) ) ;
#60770=CARTESIAN_POINT ( 'NONE',  ( 25.46375345652300126, 2.879422156700999658, -11.30951020355999859 ) ) ;
#60774=ORIENTED_EDGE ( 'NONE', *, *, #22329, .F. ) ;
#60775=CARTESIAN_POINT ( 'NONE',  ( 11.61689913334100055, -3.709679022145000005, 12.00356807880999988 ) ) ;
#60787=ORIENTED_EDGE ( 'NONE', *, *, #62564, .T. ) ;
#60788=CARTESIAN_POINT ( 'NONE',  ( 18.49993212792200126, -2.908182645667999999, -12.18276646858999968 ) ) ;
#60790=B_SPLINE_SURFACE_WITH_KNOTS ( 'NONE', 3, 3, ( 
 ( #3916, #58440, #63328, #62648 ),
 ( #36780, #25602, #15793, #25250 ),
 ( #58102, #10205, #52162, #31538 ),
 ( #4265, #14771, #37124, #46589 ),
 ( #52857, #20014, #67896, #57403 ),
 ( #4956, #9508, #46929, #20352 ),
 ( #41676, #65046, #38494, #32909 ),
 ( #38142, #22408, #7026, #59468 ),
 ( #38851, #60174, #17161, #28017 ),
 ( #33606, #11566, #32234, #54223 ),
 ( #1439, #6321, #53547, #27672 ),
 ( #12280, #48646, #49324, #1097 ) ),
 .UNSPECIFIED., .F., .F., .F.,
 ( 4, 1, 1, 1, 1, 1, 1, 1, 1, 4 ),
 ( 4, 4 ),
 ( 0.5527776740318000037, 0.5999999999999999778, 0.6500000000000000222, 0.6999999999999999556, 0.7500000000000000000, 0.8000000000000000444, 0.8499999999999999778, 0.9000000000000000222, 0.9499999999999999556, 0.9893859725818999751 ),
 ( -0.2706685848836000163, 1.270789706183999890 ),
 .UNSPECIFIED. ) ;
#60803=CARTESIAN_POINT ( 'NONE',  ( 24.30000000000000071, -2.078227429405999693, 11.31065739696999906 ) ) ;
#60805=B_SPLINE_SURFACE_WITH_KNOTS ( 'NONE', 3, 3, ( 
 ( #5605, #36402, #4234, #25574 ),
 ( #47243, #10179, #30819, #57719 ),
 ( #15077, #19988, #9477, #10858 ),
 ( #36755, #47930, #25912, #31854 ),
 ( #9827, #47591, #10514, #37430 ),
 ( #63649, #68546, #68897, #52828 ) ),
 .UNSPECIFIED., .F., .F., .F.,
 ( 4, 1, 1, 4 ),
 ( 4, 4 ),
 ( 0.1811037619699999990, 0.3333333333333000081, 0.6666666666667000474, 0.8725156331704999602 ),
 ( -0.1256563615239000009, 1.125656361510000147 ),
 .UNSPECIFIED. ) ;
#60810=CARTESIAN_POINT ( 'NONE',  ( 18.15645116484899901, -11.61859527604000064, 4.781095881906999523 ) ) ;
#60819=FACE_OUTER_BOUND ( 'NONE', #1906, .T. ) ;
#60822=CARTESIAN_POINT ( 'NONE',  ( 24.33740572418300019, -3.364255348473000229, 12.26555798179999890 ) ) ;
#60823=CIRCLE ( 'NONE', #18410, 14.00000000000000000 ) ;
#60825=CARTESIAN_POINT ( 'NONE',  ( 18.30830001818700126, 3.300182612895000478, -12.02694835946000040 ) ) ;
#60826=B_SPLINE_CURVE_WITH_KNOTS ( 'NONE', 3,
 ( #15186, #37887, #58867, #42789 ),
 .UNSPECIFIED., .F., .F.,
 ( 4, 4 ),
 ( 0.000000000000000000, 1.000000000000000000 ),
 .UNSPECIFIED. ) ;
#60834=CIRCLE ( 'NONE', #37368, 9.250000000000000000 ) ;
#60838=EDGE_CURVE ( 'NONE', #47384, #46507, #15970, .T. ) ;
#60854=FACE_OUTER_BOUND ( 'NONE', #65799, .T. ) ;
#60857=DIRECTION ( 'NONE',  ( 0.000000000000000000, 0.000000000000000000, -1.000000000000000000 ) ) ;
#60860=LINE ( 'NONE', #18905, #46674 ) ;
#60861=CARTESIAN_POINT ( 'NONE',  ( 13.64495723965300122, -12.20594327342000085, -2.556931772870000064 ) ) ;
#60865=CARTESIAN_POINT ( 'NONE',  ( 30.60000000000000142, 2.052081123290000139E-07, -7.720759220056000238 ) ) ;
#60871=EDGE_CURVE ( 'NONE', #54548, #25005, #53504, .T. ) ;
#60879=CARTESIAN_POINT ( 'NONE',  ( 24.54688887196200042, 12.52317552374000087, 3.000792222368999784 ) ) ;
#60888=CARTESIAN_POINT ( 'NONE',  ( 18.49996808500599599, 0.9036517550248718278, 11.64999999991244017 ) ) ;
#60909=CARTESIAN_POINT ( 'NONE',  ( 21.60000012424471194, 3.970157536060000036E-13, 1.776356839399999796E-13 ) ) ;
#60924=CYLINDRICAL_SURFACE ( 'NONE', #41086, 0.6999999999999992895 ) ;
#60927=EDGE_CURVE ( 'NONE', #55462, #67010, #46815, .T. ) ;
#60930=B_SPLINE_CURVE_WITH_KNOTS ( 'NONE', 3,
 ( #44098, #65397, #1090, #58776, #32230, #22404, #17516, #65042, #38490, #59813, #64350, #37800, #59123, #11915, #5976, #27316, #33257, #48642, #742, #64700, #6670, #16811, #38137, #34986, #66785, #1781 ),
 .UNSPECIFIED., .F., .F.,
 ( 4, 2, 2, 2, 2, 2, 2, 2, 2, 2, 2, 2, 4 ),
 ( 0.000000000000000000, 0.06249999999999833467, 0.09374999999999844569, 0.1249999999999985567, 0.2499999999999987788, 0.3749999999999990008, 0.4999999999999992228, 0.6249999999999994449, 0.7499999999999996669, 0.8124999999999995559, 0.8437500000000000000, 0.8750000000000005551, 1.000000000000000000 ),
 .UNSPECIFIED. ) ;
#60960=CARTESIAN_POINT ( 'NONE',  ( 25.19211255715600117, -8.466231870115001001, -8.226678917617000764 ) ) ;
#60961=CARTESIAN_POINT ( 'NONE',  ( 13.56457200097585591, -11.48338024779226707, -1.964390585072006257 ) ) ;
#60967=VERTEX_POINT ( 'NONE', #6837 ) ;
#60968=CARTESIAN_POINT ( 'NONE',  ( 24.60000000000000142, 0.000000000000000000, 0.000000000000000000 ) ) ;
#60969=CARTESIAN_POINT ( 'NONE',  ( 16.10005255078199937, -3.632778330393000132, -11.06917548872000090 ) ) ;
#60988=CARTESIAN_POINT ( 'NONE',  ( 24.30000000000000071, -9.305479840184000651, -8.315530346521999405 ) ) ;
#60989=CARTESIAN_POINT ( 'NONE',  ( 11.72772918458500158, -11.64671933177000085, -1.861692232596000141 ) ) ;
#60995=CARTESIAN_POINT ( 'NONE',  ( 24.30001123418010778, 8.895961323370999096, -8.895961323370999096 ) ) ;
#61013=CARTESIAN_POINT ( 'NONE',  ( 15.95377458853735853, -3.445704530244193098, -11.33538647441605640 ) ) ;
#61024=ORIENTED_EDGE ( 'NONE', *, *, #13586, .T. ) ;
#61028=CARTESIAN_POINT ( 'NONE',  ( 24.63329222613833380, 10.83443034969673846, 3.855530961822280833 ) ) ;
#61034=ORIENTED_EDGE ( 'NONE', *, *, #31325, .F. ) ;
#61039=CARTESIAN_POINT ( 'NONE',  ( 18.29999744860992905, -2.794302574217387924, -11.51706234583375732 ) ) ;
#61053=CIRCLE ( 'NONE', #32018, 1.000000000000000222 ) ;
#61059=ADVANCED_FACE ( 'NONE', ( #13137 ), #51742, .F. ) ;
#61060=CARTESIAN_POINT ( 'NONE',  ( 24.63333006944293402, 2.078227422262555635, -11.31065739827893779 ) ) ;
#61065=CARTESIAN_POINT ( 'NONE',  ( 23.64132706837899889, -13.18685377439000028, -4.069706785829999340 ) ) ;
#61073=CARTESIAN_POINT ( 'NONE',  ( 24.53428985175800037, 12.47024902693999948, -3.026245299674999778 ) ) ;
#61074=CARTESIAN_POINT ( 'NONE',  ( 24.39664795268166841, 3.240506188470991145, 12.09373373761089177 ) ) ;
#61081=FACE_BOUND ( 'NONE', #42631, .T. ) ;
#61109=CARTESIAN_POINT ( 'NONE',  ( 24.54688887196200042, 8.860350057919001543, -9.344992028423000363 ) ) ;
#61114=EDGE_CURVE ( 'NONE', #55782, #57373, #53028, .T. ) ;
#61134=CARTESIAN_POINT ( 'NONE',  ( 17.80000000005199823, 3.345268251980999974, -11.86064071431999878 ) ) ;
#61138=ORIENTED_EDGE ( 'NONE', *, *, #62564, .F. ) ;
#61141=DIRECTION ( 'NONE',  ( -1.000000000000000000, 0.000000000000000000, 0.000000000000000000 ) ) ;
#61148=CARTESIAN_POINT ( 'NONE',  ( 25.60000000000000142, 0.000000000000000000, 0.000000000000000000 ) ) ;
#61152=ORIENTED_EDGE ( 'NONE', *, *, #36578, .F. ) ;
#61158=CARTESIAN_POINT ( 'NONE',  ( 17.69476807989700262, -11.38964709781999929, 4.572869473993000256 ) ) ;
#61166=CIRCLE ( 'NONE', #36602, 0.6999999999999992895 ) ;
#61167=CARTESIAN_POINT ( 'NONE',  ( 23.60000000000000142, 1.954456641860109256, -13.79170062071063008 ) ) ;
#61169=CARTESIAN_POINT ( 'NONE',  ( 24.03158564178600187, -3.727259782881000127, 13.01535860997999983 ) ) ;
#61171=CARTESIAN_POINT ( 'NONE',  ( 18.26123302403700066, 2.828310120379999848, -11.95646042099000006 ) ) ;
#61177=ORIENTED_EDGE ( 'NONE', *, *, #17117, .F. ) ;
#61190=CARTESIAN_POINT ( 'NONE',  ( 25.40548315682400116, 8.312246831039999506, 8.369343040493999908 ) ) ;
#61205=CARTESIAN_POINT ( 'NONE',  ( 24.46580263758400164, -12.16839033388000146, 3.168637029940999827 ) ) ;
#61209=CARTESIAN_POINT ( 'NONE',  ( 16.39999999485600313, 3.595156957901000094, 11.99794989424000136 ) ) ;
#61210=CARTESIAN_POINT ( 'NONE',  ( 13.07616489729400122, -12.32806027643999869, -1.877794484342000025 ) ) ;
#61223=B_SPLINE_CURVE_WITH_KNOTS ( 'NONE', 3,
 ( #54659, #8491, #30173, #18980, #29495, #56388 ),
 .UNSPECIFIED., .F., .F.,
 ( 4, 2, 4 ),
 ( 0.000000000000000000, 0.5000000000000000000, 1.000000000000000000 ),
 .UNSPECIFIED. ) ;
#61226=CARTESIAN_POINT ( 'NONE',  ( 15.89979320884932967, -4.771864030974223958, -11.40757335769646552 ) ) ;
#61230=VERTEX_POINT ( 'NONE', #11647 ) ;
#61235=CARTESIAN_POINT ( 'NONE',  ( 24.72675015352175620, -3.119025593723015355, -11.78403009279797864 ) ) ;
#61243=CARTESIAN_POINT ( 'NONE',  ( 11.84006751466700180, 3.254324250158000087, -11.33670592834999979 ) ) ;
#61247=EDGE_LOOP ( 'NONE', ( #30008, #28695, #64877, #57667 ) ) ;
#61249=CARTESIAN_POINT ( 'NONE',  ( 24.51106053578591926, 8.765536724423055759, 8.765535773142982379 ) ) ;
#61260=CARTESIAN_POINT ( 'NONE',  ( 24.14470051247585403, 12.92580021110792643, -3.214654389895091224 ) ) ;
#61261=ADVANCED_FACE ( 'NONE', ( #52852 ), #40986, .T. ) ;
#61263=CARTESIAN_POINT ( 'NONE',  ( 23.91164119559400092, -3.265432764442000035, -12.84207651524999960 ) ) ;
#61264=AXIS2_PLACEMENT_3D ( 'NONE', #18931, #61577, #35022 ) ;
#61267=CARTESIAN_POINT ( 'NONE',  ( 23.60000000000000497, 12.92119138974382864, -5.203241264448742243 ) ) ;
#61277=CARTESIAN_POINT ( 'NONE',  ( 15.95481756226799952, -8.457314961363000094, -8.223455601337001042 ) ) ;
#61280=CARTESIAN_POINT ( 'NONE',  ( 23.66004879239100234, -13.39256420742000131, 3.813548264891000183 ) ) ;
#61287=B_SPLINE_CURVE_WITH_KNOTS ( 'NONE', 3,
 ( #17368, #59671, #64555, #5836 ),
 .UNSPECIFIED., .F., .F.,
 ( 4, 4 ),
 ( 0.000000000000000000, 1.000000000000000000 ),
 .UNSPECIFIED. ) ;
#61300=CARTESIAN_POINT ( 'NONE',  ( 25.29574884316900096, 11.38516889222999851, 3.114186424562000344 ) ) ;
#61304=DIRECTION ( 'NONE',  ( -1.000000000000000000, 0.000000000000000000, 0.000000000000000000 ) ) ;
#61313=CARTESIAN_POINT ( 'NONE',  ( 24.72250568140215421, 3.121164773874959497, 11.78765955954131606 ) ) ;
#61329=VERTEX_POINT ( 'NONE', #22748 ) ;
#61333=CARTESIAN_POINT ( 'NONE',  ( 24.30000000000000071, -8.756202924575998026, -7.455126447192999883 ) ) ;
#61334=CARTESIAN_POINT ( 'NONE',  ( 23.89320776801300283, 1.894218448865001792, 11.32736289216000536 ) ) ;
#61339=CARTESIAN_POINT ( 'NONE',  ( 24.54174074851747989, -3.611931245578916094, 12.30360799784193837 ) ) ;
#61348=ORIENTED_EDGE ( 'NONE', *, *, #67496, .T. ) ;
#61349=ORIENTED_EDGE ( 'NONE', *, *, #48260, .F. ) ;
#61354=CARTESIAN_POINT ( 'NONE',  ( 24.22025221778200077, 8.983854323373000383, -8.868431746691999962 ) ) ;
#61361=ADVANCED_FACE ( 'NONE', ( #5633 ), #11561, .T. ) ;
#61367=ORIENTED_EDGE ( 'NONE', *, *, #66052, .F. ) ;
#61370=CARTESIAN_POINT ( 'NONE',  ( 24.44496356299600137, 12.03536643057000077, 3.224849944858999784 ) ) ;
#61371=DIRECTION ( 'NONE',  ( 0.000000000000000000, 0.000000000000000000, -1.000000000000000000 ) ) ;
#61372=AXIS2_PLACEMENT_3D ( 'NONE', #40578, #45147, #17888 ) ;
#61381=CARTESIAN_POINT ( 'NONE',  ( 23.80948493899275675, -13.00802406696185543, -3.693054094325271652 ) ) ;
#61382=CARTESIAN_POINT ( 'NONE',  ( 24.43232361759900328, 3.176382763002000509, -12.00226528444000174 ) ) ;
#61396=B_SPLINE_CURVE_WITH_KNOTS ( 'NONE', 3,
 ( #37069, #4207, #57344, #41282, #42324, #30791, #26583, #62591, #58048, #58381, #25545, #46870, #16073, #68177 ),
 .UNSPECIFIED., .F., .F.,
 ( 4, 2, 2, 2, 2, 2, 4 ),
 ( 0.000000000000000000, 0.1250000000000009159, 0.2500000000000018319, 0.5000000000000023315, 0.6250000000000025535, 0.7500000000000026645, 1.000000000000000000 ),
 .UNSPECIFIED. ) ;
#61400=CARTESIAN_POINT ( 'NONE',  ( 25.59997255263800042, -11.07537722176000017, -3.096069202785999952 ) ) ;
#61402=CARTESIAN_POINT ( 'NONE',  ( 25.29995734509200034, 8.533537492639000632, -7.925519463018001254 ) ) ;
#61404=CARTESIAN_POINT ( 'NONE',  ( 23.60000000000000142, 2.204728229456999866, 11.99913219504999873 ) ) ;
#61410=( NAMED_UNIT ( * ) PLANE_ANGLE_UNIT ( ) SI_UNIT ( $, .RADIAN. ) );
#61411=B_SPLINE_CURVE_WITH_KNOTS ( 'NONE', 3,
 ( #33548, #16757, #5925, #48936 ),
 .UNSPECIFIED., .F., .F.,
 ( 4, 4 ),
 ( 0.000000000000000000, 1.000000000000000000 ),
 .UNSPECIFIED. ) ;
#61414=CARTESIAN_POINT ( 'NONE',  ( 23.66004879239100234, -3.393652723963000106, -13.50507488346000073 ) ) ;
#61418=CARTESIAN_POINT ( 'NONE',  ( 11.49999672495000169, -3.632761979779000061, 11.06912554803999882 ) ) ;
#61424=EDGE_CURVE ( 'NONE', #68269, #252, #60930, .T. ) ;
#61425=AXIS2_PLACEMENT_3D ( 'NONE', #20886, #15980, #11084 ) ;
#61430=DIRECTION ( 'NONE',  ( 0.000000000000000000, -0.7071067811865475727, -0.7071067811865475727 ) ) ;
#61431=CARTESIAN_POINT ( 'NONE',  ( 23.64073796900200364, 13.18743409422000035, 4.071803983738000454 ) ) ;
#61435=CARTESIAN_POINT ( 'NONE',  ( 25.30000327618300204, -10.36736154742121130, -5.168041346173475326 ) ) ;
#61444=FACE_OUTER_BOUND ( 'NONE', #17672, .T. ) ;
#61448=ORIENTED_EDGE ( 'NONE', *, *, #24242, .F. ) ;
#61453=ORIENTED_EDGE ( 'NONE', *, *, #52394, .F. ) ;
#61464=PLANE ( 'NONE',  #65602 ) ;
#61466=CARTESIAN_POINT ( 'NONE',  ( 11.80852891948700290, -3.296364302329999774, 11.83491796280999964 ) ) ;
#61474=ORIENTED_EDGE ( 'NONE', *, *, #9775, .T. ) ;
#61479=ORIENTED_EDGE ( 'NONE', *, *, #37255, .F. ) ;
#61483=CARTESIAN_POINT ( 'NONE',  ( 18.30008632280270930, 2.887848135250621385E-14, -11.85014035451981762 ) ) ;
#61485=EDGE_CURVE ( 'NONE', #48209, #35693, #33442, .T. ) ;
#61488=EDGE_CURVE ( 'NONE', #10241, #2158, #3467, .T. ) ;
#61492=CARTESIAN_POINT ( 'NONE',  ( 24.07543051757465946, 9.249134803097012636, 9.196971017846948371 ) ) ;
#61498=CARTESIAN_POINT ( 'NONE',  ( 17.97370160627000146, -12.15014996206000042, 3.198998983672000307 ) ) ;
#61501=CARTESIAN_POINT ( 'NONE',  ( 18.50001572531400029, 2.908166856580999937, -12.18270046149000052 ) ) ;
#61531=CARTESIAN_POINT ( 'NONE',  ( 25.48313734979400280, 8.422747986984999713, 7.953661500581000965 ) ) ;
#61534=CARTESIAN_POINT ( 'NONE',  ( 11.72003495739535595, -3.351648276372030555, 11.15746180793239795 ) ) ;
#61541=LINE ( 'NONE', #56301, #14018 ) ;
#61542=CARTESIAN_POINT ( 'NONE',  ( 11.79999999771000141, -3.595163221087000149, 11.99793848941000007 ) ) ;
#61543=CARTESIAN_POINT ( 'NONE',  ( 24.30857393682200041, -12.13191889299999815, 3.290345171485999920 ) ) ;
#61544=CARTESIAN_POINT ( 'NONE',  ( 15.40000000001299973, 8.815237407733999220, 7.616696375847999967 ) ) ;
#61548=VERTEX_POINT ( 'NONE', #2467 ) ;
#61550=( BOUNDED_SURFACE ( )  B_SPLINE_SURFACE ( 3, 3, ( 
 ( #41486, #47423, #47081, #15262 ),
 ( #36585, #9314, #4066, #68731 ),
 ( #40795, #62118, #20850, #14236 ),
 ( #8979, #42183, #56535, #67695 ) ),
 .UNSPECIFIED., .F., .F., .T. ) 
 B_SPLINE_SURFACE_WITH_KNOTS ( ( 4, 4 ),
 ( 4, 4 ),
 ( 0.000000000000000000, 1.000000000000000000 ),
 ( 0.000000000000000000, 1.000000000000000000 ),
 .UNSPECIFIED. ) 
 GEOMETRIC_REPRESENTATION_ITEM ( )  RATIONAL_B_SPLINE_SURFACE ( (
 ( 1.512182578520000042, 1.160176301760999840, 1.160176301760999840, 1.512182578520000042),
 ( 1.111288591041000196, 0.8526025270081000196, 0.8526025270081000196, 1.111288591041000196),
 ( 1.111288591041000196, 0.8526025270081000196, 0.8526025270081000196, 1.111288591041000196),
 ( 1.512182578520000042, 1.160176301760999840, 1.160176301760999840, 1.512182578520000042) ) ) 
 REPRESENTATION_ITEM ( '' )  SURFACE ( )  );
#61552=DIRECTION ( 'NONE',  ( 0.000000000000000000, -1.000000000000000000, 0.000000000000000000 ) ) ;
#61557=DIRECTION ( 'NONE',  ( 0.000000000000000000, 0.000000000000000000, -1.000000000000000000 ) ) ;
#61565=CARTESIAN_POINT ( 'NONE',  ( 18.47825479160223239, 3.085175724107807493, -12.13916519603725419 ) ) ;
#61568=ADVANCED_FACE ( 'NONE', ( #60854 ), #34645, .T. ) ;
#61570=ORIENTED_EDGE ( 'NONE', *, *, #2747, .T. ) ;
#61572=DIRECTION ( 'NONE',  ( 0.000000000000000000, 0.000000000000000000, -1.000000000000000000 ) ) ;
#61574=ORIENTED_EDGE ( 'NONE', *, *, #46799, .T. ) ;
#61577=DIRECTION ( 'NONE',  ( 1.000000000000000000, 0.000000000000000000, 0.000000000000000000 ) ) ;
#61586=ORIENTED_EDGE ( 'NONE', *, *, #14716, .T. ) ;
#61600=CARTESIAN_POINT ( 'NONE',  ( 18.49993212792200126, 2.908182645667999999, 12.18276646858999968 ) ) ;
#61601=CARTESIAN_POINT ( 'NONE',  ( 24.23189443787899933, -3.402543883684999937, -12.43221920717999929 ) ) ;
#61603=CARTESIAN_POINT ( 'NONE',  ( 24.30000000000000071, -2.258942858049999725, -12.29419282279000036 ) ) ;
#61609=CARTESIAN_POINT ( 'NONE',  ( 18.29995268966800026, 2.861739928647000220, 11.98821236628000086 ) ) ;
#61611=CARTESIAN_POINT ( 'NONE',  ( 18.28771851938432036, 2.987294196519939327, 11.95930572916780754 ) ) ;
#61614=CARTESIAN_POINT ( 'NONE',  ( 15.86001156276200064, -8.572187346067000391, -8.239473968622000655 ) ) ;
#61616=CARTESIAN_POINT ( 'NONE',  ( 23.57927802539584405, -13.36787453502657819, 4.109736056796153392 ) ) ;
#61619=AXIS2_PLACEMENT_3D ( 'NONE', #38368, #21591, #6894 ) ;
#61621=EDGE_CURVE ( 'NONE', #19330, #37826, #61541, .T. ) ;
#61625=CARTESIAN_POINT ( 'NONE',  ( 24.44496482743900145, 12.03536723905999928, -3.224852005146999989 ) ) ;
#61627=DIRECTION ( 'NONE',  ( -8.952907862884472301E-11, -0.2714597137497840040, -0.9624498032681421122 ) ) ;
#61628=ORIENTED_EDGE ( 'NONE', *, *, #34023, .F. ) ;
#61631=B_SPLINE_CURVE_WITH_KNOTS ( 'NONE', 3,
 ( #58450, #62990, #57756, #15803 ),
 .UNSPECIFIED., .F., .F.,
 ( 4, 4 ),
 ( 0.000000000000000000, 1.000000000000000000 ),
 .UNSPECIFIED. ) ;
#61641=CARTESIAN_POINT ( 'NONE',  ( 13.59015267864900345, -8.992820872206999994, -7.631366745126000772 ) ) ;
#61661=ORIENTED_EDGE ( 'NONE', *, *, #15554, .F. ) ;
#61665=VERTEX_POINT ( 'NONE', #39100 ) ;
#61671=ADVANCED_FACE ( 'NONE', ( #23705 ), #25185, .F. ) ;
#61673=CARTESIAN_POINT ( 'NONE',  ( 11.53713099069000059, -11.52702260260000067, -1.399766873409999945 ) ) ;
#61676=ORIENTED_EDGE ( 'NONE', *, *, #68079, .F. ) ;
#61686=ORIENTED_EDGE ( 'NONE', *, *, #13825, .T. ) ;
#61691=CARTESIAN_POINT ( 'NONE',  ( 23.59999443371599881, 2.915558930973999985, 13.58549620949000136 ) ) ;
#61692=CARTESIAN_POINT ( 'NONE',  ( 25.46375152665800101, -2.879425814940999917, -11.30951176145000048 ) ) ;
#61693=CARTESIAN_POINT ( 'NONE',  ( 16.39999999231800132, -3.216285993016000155, -11.40340220863999932 ) ) ;
#61705=FACE_OUTER_BOUND ( 'NONE', #59099, .T. ) ;
#61716=CARTESIAN_POINT ( 'NONE',  ( 24.44496356267099912, -8.810485190366000197, 8.810508100388000585 ) ) ;
#61729=CARTESIAN_POINT ( 'NONE',  ( 21.72233714749290101, 0.000000000000000000, 0.000000000000000000 ) ) ;
#61744=AXIS2_PLACEMENT_3D ( 'NONE', #57222, #9324, #17338 ) ;
#61748=CARTESIAN_POINT ( 'NONE',  ( 23.65871028981190349, 13.20934072687480310, -3.970311354682951155 ) ) ;
#61752=CARTESIAN_POINT ( 'NONE',  ( 24.11212198533107909, -3.334560347335004948, -12.54180816139383126 ) ) ;
#61753=CARTESIAN_POINT ( 'NONE',  ( 11.79999999550100220, 3.351258778187000242, -11.15757272551999968 ) ) ;
#61756=EDGE_LOOP ( 'NONE', ( #53825, #19454, #16675, #13816 ) ) ;
#61761=CARTESIAN_POINT ( 'NONE',  ( 25.34480240682214003, -11.16380505725911298, 3.340444239295249584 ) ) ;
#61777=CYLINDRICAL_SURFACE ( 'NONE', #57065, 0.6999999999999992895 ) ;
#61780=ADVANCED_FACE ( 'NONE', ( #5985 ), #37810, .T. ) ;
#61782=DIRECTION ( 'NONE',  ( -1.000000000000000000, 0.000000000000000000, 0.000000000000000000 ) ) ;
#61784=CARTESIAN_POINT ( 'NONE',  ( 23.64081946308400362, 10.11970730052999912, 9.384831229972000699 ) ) ;
#61788=EDGE_CURVE ( 'NONE', #26090, #53272, #52493, .T. ) ;
#61817=CONICAL_SURFACE ( 'NONE', #27231, 5.886037960926999268, 0.3217505543965463732 ) ;
#61822=CARTESIAN_POINT ( 'NONE',  ( 25.44993977744900349, 9.517611874540000017, 8.103398312166998352 ) ) ;
#61829=CARTESIAN_POINT ( 'NONE',  ( 24.17206818058083329, 9.108188618978893203, 9.092704695918069291 ) ) ;
#61836=CARTESIAN_POINT ( 'NONE',  ( 17.56813658992500393, -11.93194907420999940, 3.261335586771000106 ) ) ;
#61845=ORIENTED_EDGE ( 'NONE', *, *, #9775, .F. ) ;
#61846=CIRCLE ( 'NONE', #16070, 0.6999999999999992895 ) ;
#61863=VECTOR ( 'NONE', #66368, 1000.000000000000227 ) ;
#61878=B_SPLINE_CURVE_WITH_KNOTS ( 'NONE', 3,
 ( #5132, #47107, #32407, #10718 ),
 .UNSPECIFIED., .F., .F.,
 ( 4, 4 ),
 ( 0.000000000000000000, 1.000000000000000000 ),
 .UNSPECIFIED. ) ;
#61885=CARTESIAN_POINT ( 'NONE',  ( 11.79999999116810727, -3.511856242852832377, 11.95218832016636945 ) ) ;
#61894=CARTESIAN_POINT ( 'NONE',  ( 13.43979992210467067, -11.65095899958523340, -2.173573044049637470 ) ) ;
#61900=CARTESIAN_POINT ( 'NONE',  ( 23.56665657357900301, 3.064215547964999882E-13, 1.261213355973999610E-13 ) ) ;
#61908=CARTESIAN_POINT ( 'NONE',  ( 11.36660992314014784, 3.674321412135251652, -11.19575788941673267 ) ) ;
#61917=CARTESIAN_POINT ( 'NONE',  ( 24.89163398232695812, -3.022263450368753990, -11.64683128245694554 ) ) ;
#61918=DIRECTION ( 'NONE',  ( 0.000000000000000000, 0.9659258262890756397, -0.2588190451024932059 ) ) ;
#61919=CONICAL_SURFACE ( 'NONE', #45211, 13.94232985059000107, 1.233427423217456464 ) ;
#61932=CARTESIAN_POINT ( 'NONE',  ( 25.60000000000000142, -2.976419018679000050, -11.10814700232000085 ) ) ;
#61934=CARTESIAN_POINT ( 'NONE',  ( 24.69609520272172176, 8.660953915096069267, 8.619378635578760495 ) ) ;
#61935=B_SPLINE_CURVE_WITH_KNOTS ( 'NONE', 3,
 ( #63662, #58423, #25926, #32218 ),
 .UNSPECIFIED., .F., .F.,
 ( 4, 4 ),
 ( 0.000000000000000000, 1.000000000000000000 ),
 .UNSPECIFIED. ) ;
#61942=CARTESIAN_POINT ( 'NONE',  ( 24.67921580255100267, 8.727633792449999817, 9.158312800479000870 ) ) ;
#61953=CARTESIAN_POINT ( 'NONE',  ( 25.46373329105799854, 11.23406619596999967, -3.161081784610999978 ) ) ;
#61959=EDGE_CURVE ( 'NONE', #54862, #33733, #15153, .T. ) ;
#61960=EDGE_CURVE ( 'NONE', #57124, #46963, #24149, .T. ) ;
#61963=CARTESIAN_POINT ( 'NONE',  ( 15.65609597790000151, -8.788746246889001412, -7.589637905006999752 ) ) ;
#61965=CARTESIAN_POINT ( 'NONE',  ( 23.56934271467462594, -13.33981148175788434, 4.212069331298350150 ) ) ;
#61972=CARTESIAN_POINT ( 'NONE',  ( 23.61814127931500096, -2.884265323764000133, 13.53884956573999965 ) ) ;
#61976=ORIENTED_EDGE ( 'NONE', *, *, #49435, .T. ) ;
#61987=CARTESIAN_POINT ( 'NONE',  ( 25.27036577661199956, 11.11618949463999861, 3.474359096894000132 ) ) ;
#62007=CARTESIAN_POINT ( 'NONE',  ( 13.73712493497300180, 11.35980872612999804, 2.405726353896999736 ) ) ;
#62012=ORIENTED_EDGE ( 'NONE', *, *, #57623, .F. ) ;
#62028=CARTESIAN_POINT ( 'NONE',  ( 17.89162860438300129, 3.376692001085000339, 11.11057855219999979 ) ) ;
#62035=CARTESIAN_POINT ( 'NONE',  ( 25.31008644117000372, 8.472729765048999440, -8.045102513582000014 ) ) ;
#62036=ADVANCED_FACE ( 'NONE', ( #54759 ), #18057, .T. ) ;
#62038=CARTESIAN_POINT ( 'NONE',  ( 23.58435503226500174, 10.35630177538000041, -9.330313185629002248 ) ) ;
#62039=CARTESIAN_POINT ( 'NONE',  ( 18.23176382712000176, -2.916721637292999603, -11.52766586543999949 ) ) ;
#62045=VECTOR ( 'NONE', #128, 1000.000000000000114 ) ;
#62046=CARTESIAN_POINT ( 'NONE',  ( 23.89320776801300283, -10.87822567738999346, -3.284864823361000941 ) ) ;
#62049=CARTESIAN_POINT ( 'NONE',  ( 11.30000000000000071, 0.000000000000000000, 0.000000000000000000 ) ) ;
#62050=CARTESIAN_POINT ( 'NONE',  ( 23.56665676678100141, 1.192379528446999839E-13, -4.982680934517999418E-13 ) ) ;
#62055=EDGE_CURVE ( 'NONE', #41440, #12705, #12918, .T. ) ;
#62058=ORIENTED_EDGE ( 'NONE', *, *, #62349, .F. ) ;
#62062=DIRECTION ( 'NONE',  ( 0.000000000000000000, -0.8075584957945176612, 0.5897874836499127360 ) ) ;
#62077=ORIENTED_EDGE ( 'NONE', *, *, #11448, .T. ) ;
#62082=CARTESIAN_POINT ( 'NONE',  ( 24.60115017391931502, 3.453285473742774947, 12.10347684623337550 ) ) ;
#62083=VERTEX_POINT ( 'NONE', #1623 ) ;
#62085=DIRECTION ( 'NONE',  ( 0.000000000000000000, 1.000000000000000000, 0.000000000000000000 ) ) ;
#62086=CARTESIAN_POINT ( 'NONE',  ( 12.37550370467830696, 11.46556593385748357, -4.499409319921212180 ) ) ;
#62093=EDGE_CURVE ( 'NONE', #32306, #25573, #65349, .T. ) ;
#62094=CARTESIAN_POINT ( 'NONE',  ( 23.60000657692131654, -2.996625413523755110, -13.56987347963171686 ) ) ;
#62096=ADVANCED_FACE ( 'NONE', ( #12811 ), #2313, .F. ) ;
#62099=EDGE_LOOP ( 'NONE', ( #56945, #21962, #52753, #27660 ) ) ;
#62103=DIRECTION ( 'NONE',  ( 0.000000000000000000, -0.9659258262890757507, -0.2588190451024934835 ) ) ;
#62106=B_SPLINE_CURVE_WITH_KNOTS ( 'NONE', 3,
 ( #9699, #67392, #19514, #52354, #63527, #25786 ),
 .UNSPECIFIED., .F., .F.,
 ( 4, 2, 4 ),
 ( 0.000000000000000000, 0.5000000000000000000, 1.000000000000000000 ),
 .UNSPECIFIED. ) ;
#62113=DIRECTION ( 'NONE',  ( 0.000000000000000000, -0.3118250626419980520, 0.9501395320205942019 ) ) ;
#62114=CARTESIAN_POINT ( 'NONE',  ( 15.91587707751000025, 9.040653309694000939, 8.458480061295000851 ) ) ;
#62118=CARTESIAN_POINT ( 'NONE',  ( 23.89320776801300283, -2.594336453666000075, -11.06325219639999347 ) ) ;
#62121=CARTESIAN_POINT ( 'NONE',  ( 24.56892856850300078, -12.04602458699000067, 3.139954038541999726 ) ) ;
#62124=CARTESIAN_POINT ( 'NONE',  ( 24.36958145701300182, 3.196690648311999894, 12.07804156775000060 ) ) ;
#62130=FACE_OUTER_BOUND ( 'NONE', #43708, .T. ) ;
#62131=CARTESIAN_POINT ( 'NONE',  ( 24.30001682246400208, -8.938702682732001747, -8.938676171235998780 ) ) ;
#62134=ADVANCED_FACE ( 'NONE', ( #58848, #6390 ), #42771, .T. ) ;
#62140=DIRECTION ( 'NONE',  ( 2.186053604475938581E-10, -0.8077514394224775129, 0.5895232074404836986 ) ) ;
#62144=CARTESIAN_POINT ( 'NONE',  ( 17.60000000357355532, -10.99221148292035544, 4.481504242813237227 ) ) ;
#62153=ORIENTED_EDGE ( 'NONE', *, *, #55322, .T. ) ;
#62157=CARTESIAN_POINT ( 'NONE',  ( 11.30000000000000071, 3.090860900556000105E-13, -1.000866056699999936E-13 ) ) ;
#62158=ORIENTED_EDGE ( 'NONE', *, *, #49991, .F. ) ;
#62169=CARTESIAN_POINT ( 'NONE',  ( 11.79999998956225937, 3.428554832065389135, -11.90642801602077228 ) ) ;
#62176=EDGE_CURVE ( 'NONE', #38467, #41893, #17397, .T. ) ;
#62177=CARTESIAN_POINT ( 'NONE',  ( 24.62773497369100184, -8.736972494141998169, 9.042113496788999782 ) ) ;
#62182=EDGE_CURVE ( 'NONE', #52150, #56420, #31947, .T. ) ;
#62204=AXIS2_PLACEMENT_3D ( 'NONE', #38404, #38056, #64618 ) ;
#62225=CARTESIAN_POINT ( 'NONE',  ( 13.67476513888300005, -9.526862765824999357, -8.046751417967000108 ) ) ;
#62227=CARTESIAN_POINT ( 'NONE',  ( 17.60000001994400165, -11.53041320601000130, 4.891397783926000109 ) ) ;
#62231=CARTESIAN_POINT ( 'NONE',  ( 24.92745128319736736, -11.55994776411245262, 3.214489235262763867 ) ) ;
#62233=ORIENTED_EDGE ( 'NONE', *, *, #23440, .F. ) ;
#62248=CARTESIAN_POINT ( 'NONE',  ( 24.17201600611014101, -3.320432398031667898, 12.43436857130917161 ) ) ;
#62252=ORIENTED_EDGE ( 'NONE', *, *, #49752, .T. ) ;
#62253=CIRCLE ( 'NONE', #27676, 0.9999999999999993339 ) ;
#62273=ORIENTED_EDGE ( 'NONE', *, *, #27643, .T. ) ;
#62276=CARTESIAN_POINT ( 'NONE',  ( 24.57937622054645033, -3.599767751962166251, -12.25814915832331842 ) ) ;
#62281=DIRECTION ( 'NONE',  ( 0.000000000000000000, 0.9925108176925445669, 0.1221567712543053380 ) ) ;
#62287=CARTESIAN_POINT ( 'NONE',  ( 25.49994615423647204, 2.042074767856997042, -11.11389836053589875 ) ) ;
#62288=CARTESIAN_POINT ( 'NONE',  ( 18.36651216305128997, 2.877244130631058106, 12.05316132863762846 ) ) ;
#62289=ADVANCED_FACE ( 'NONE', ( #65465 ), #38915, .F. ) ;
#62303=CARTESIAN_POINT ( 'NONE',  ( 16.13573769406199787, -8.400696156758000299, -8.016340154447000543 ) ) ;
#62306=VERTEX_POINT ( 'NONE', #56372 ) ;
#62317=VERTEX_POINT ( 'NONE', #29820 ) ;
#62328=CARTESIAN_POINT ( 'NONE',  ( 24.84742972624900403, 11.95752699856999968, 2.993660429748000062 ) ) ;
#62331=CARTESIAN_POINT ( 'NONE',  ( 23.56664311700400205, 13.31365802054999925, 4.296923094388999331 ) ) ;
#62335=CARTESIAN_POINT ( 'NONE',  ( 15.90006914250094461, 3.698856701507908795, 11.75540275481943020 ) ) ;
#62341=CARTESIAN_POINT ( 'NONE',  ( 24.83134246164797787, 3.060673188834726499, 11.69614408486561352 ) ) ;
#62346=CARTESIAN_POINT ( 'NONE',  ( 11.66883611783287655, -12.15999240571540696, -2.000270994041519756 ) ) ;
#62348=CARTESIAN_POINT ( 'NONE',  ( 25.30000327618300204, -6.604245036507551141E-15, -11.49994408209238017 ) ) ;
#62349=EDGE_CURVE ( 'NONE', #68412, #43577, #17459, .T. ) ;
#62350=CARTESIAN_POINT ( 'NONE',  ( 24.34832162680337575, -12.03537037244042374, 3.224867771903811242 ) ) ;
#62352=ORIENTED_EDGE ( 'NONE', *, *, #2747, .F. ) ;
#62354=( LENGTH_UNIT ( ) NAMED_UNIT ( * ) SI_UNIT ( .MILLI., .METRE. ) );
#62358=CARTESIAN_POINT ( 'NONE',  ( 16.09997386696500143, 8.350085070477001992, 8.123950967096998710 ) ) ;
#62359=AXIS2_PLACEMENT_3D ( 'NONE', #39229, #60552, #3201 ) ;
#62363=CARTESIAN_POINT ( 'NONE',  ( 24.66708179678231261, -3.571422468857847310, 12.15221134872180997 ) ) ;
#62367=CARTESIAN_POINT ( 'NONE',  ( 19.89999890908300273, 0.000000000000000000, 0.000000000000000000 ) ) ;
#62371=CARTESIAN_POINT ( 'NONE',  ( 17.87778689823928246, 11.54766097721278229, -4.850486155499411645 ) ) ;
#62374=ORIENTED_EDGE ( 'NONE', *, *, #52096, .T. ) ;
#62378=CARTESIAN_POINT ( 'NONE',  ( 25.57777390266700124, 8.344452479015000534, -8.014498661339999330 ) ) ;
#62379=CARTESIAN_POINT ( 'NONE',  ( 24.38453586173000076, 8.887473727858999695, -8.991251287490998223 ) ) ;
#62380=CARTESIAN_POINT ( 'NONE',  ( 18.49055856039300139, -2.949841519493000330, -11.23086453091999992 ) ) ;
#62385=CARTESIAN_POINT ( 'NONE',  ( 25.46373024410000241, -11.23407150414000100, 3.161076981347000103 ) ) ;
#62394=CARTESIAN_POINT ( 'NONE',  ( 14.04004776902899998, 8.829547661313998930, 7.819892149868999276 ) ) ;
#62403=CARTESIAN_POINT ( 'NONE',  ( 24.50399615158200106, 3.502219942208999903, -12.23695409027999936 ) ) ;
#62409=CARTESIAN_POINT ( 'NONE',  ( 12.96427412810700197, -11.57018092489999894, -1.758708699944000031 ) ) ;
#62417=CARTESIAN_POINT ( 'NONE',  ( 15.83176382712000319, 8.647155996545000889, 8.162171193140999037 ) ) ;
#62427=EDGE_CURVE ( 'NONE', #54502, #44042, #57560, .T. ) ;
#62435=DIRECTION ( 'NONE',  ( 0.000000000000000000, -0.9466492601157000530, 0.3222656952305000266 ) ) ;
#62449=CARTESIAN_POINT ( 'NONE',  ( 17.33333333083533390, -3.216308279608389054, -11.40341444610950283 ) ) ;
#62451=CARTESIAN_POINT ( 'NONE',  ( 23.54916660312699861, 13.36550856414000066, 4.293655460768000864 ) ) ;
#62457=VECTOR ( 'NONE', #48655, 1000.000000000000227 ) ;
#62464=FACE_OUTER_BOUND ( 'NONE', #2278, .T. ) ;
#62466=CARTESIAN_POINT ( 'NONE',  ( 23.81909306311399988, 9.670551759768001077, 9.332972164518999136 ) ) ;
#62467=ORIENTED_EDGE ( 'NONE', *, *, #12009, .T. ) ;
#62472=CARTESIAN_POINT ( 'NONE',  ( 18.17677363193000062, 3.419785592864999835, 11.99291007725999947 ) ) ;
#62476=ORIENTED_EDGE ( 'NONE', *, *, #3881, .F. ) ;
#62481=DIRECTION ( 'NONE',  ( -1.000000000000000000, 0.000000000000000000, 0.000000000000000000 ) ) ;
#62485=CARTESIAN_POINT ( 'NONE',  ( 15.88832047282411075, 8.582214862760459084, 8.173711952084858012 ) ) ;
#62488=ORIENTED_EDGE ( 'NONE', *, *, #64336, .T. ) ;
#62490=B_SPLINE_CURVE_WITH_KNOTS ( 'NONE', 3,
 ( #4000, #41763, #56472, #36515 ),
 .UNSPECIFIED., .F., .F.,
 ( 4, 4 ),
 ( 0.000000000000000000, 0.4999999997918080918 ),
 .UNSPECIFIED. ) ;
#62491=CARTESIAN_POINT ( 'NONE',  ( 13.49980696793000057, -9.514462421839999351, -7.834836582454001608 ) ) ;
#62492=VERTEX_POINT ( 'NONE', #24894 ) ;
#62507=EDGE_CURVE ( 'NONE', #5914, #60441, #66744, .T. ) ;
#62510=ORIENTED_EDGE ( 'NONE', *, *, #2276, .F. ) ;
#62516=CARTESIAN_POINT ( 'NONE',  ( 17.72467941260600099, -11.93112142875000004, 3.264904591444000026 ) ) ;
#62517=CARTESIAN_POINT ( 'NONE',  ( 24.56500367260400353, -8.792450275132999593, 9.097562848838000704 ) ) ;
#62532=CARTESIAN_POINT ( 'NONE',  ( 17.95534550153200115, 3.277905616156999713, -11.84067279748999901 ) ) ;
#62535=EDGE_LOOP ( 'NONE', ( #2805, #67133, #36904, #48864 ) ) ;
#62542=CARTESIAN_POINT ( 'NONE',  ( 24.46225921258299962, 8.785799836126999551, 8.709231069799999503 ) ) ;
#62554=AXIS2_PLACEMENT_3D ( 'NONE', #1435, #64701, #16812 ) ;
#62558=CARTESIAN_POINT ( 'NONE',  ( 11.49999672495000169, -3.632761979779000061, 11.06912554803999882 ) ) ;
#62561=CARTESIAN_POINT ( 'NONE',  ( 13.82798078375900275, -9.420238147574000465, -8.170996254510999535 ) ) ;
#62564=EDGE_CURVE ( 'NONE', #14826, #44907, #3960, .T. ) ;
#62570=ORIENTED_EDGE ( 'NONE', *, *, #31576, .T. ) ;
#62584=CARTESIAN_POINT ( 'NONE',  ( 18.50001572531400029, 2.908166856580999937, -12.18270046149000052 ) ) ;
#62585=CARTESIAN_POINT ( 'NONE',  ( 24.53429015151300163, -3.614318902553999902, -12.31267542782000035 ) ) ;
#62586=CARTESIAN_POINT ( 'NONE',  ( 24.63408906255500241, -3.094015452922999732, -11.81699230461000028 ) ) ;
#62591=CARTESIAN_POINT ( 'NONE',  ( 15.92727146503378499, -9.312591611299774641, -8.375703117199135406 ) ) ;
#62605=B_SPLINE_CURVE_WITH_KNOTS ( 'NONE', 3,
 ( #32419, #42222, #58286, #53395, #5145, #26481, #42557, #63866, #5494, #26829, #21565, #23642, #1288, #44980, #22258, #44301, #28915, #66285, #18409, #60360, #48837, #11764 ),
 .UNSPECIFIED., .F., .F.,
 ( 4, 2, 2, 1, 1, 2, 2, 2, 2, 2, 2, 4 ),
 ( 0.000000000000000000, 0.1249999999999863998, 0.1874999999999805433, 0.2187499999999784062, 0.2343749999999749367, 0.2421874999999744926, 0.2499999999999740208, 0.3749999999999827360, 0.4374999999999875655, 0.4687499999999886202, 0.4999999999999896749, 1.000000000000000000 ),
 .UNSPECIFIED. ) ;
#62608=FACE_OUTER_BOUND ( 'NONE', #29961, .T. ) ;
#62609=PLANE ( 'NONE',  #48183 ) ;
#62617=ORIENTED_EDGE ( 'NONE', *, *, #1617, .T. ) ;
#62620=CARTESIAN_POINT ( 'NONE',  ( 16.00806624337635142, 9.235483320791411543, 8.460674029563245213 ) ) ;
#62627=TOROIDAL_SURFACE ( 'NONE', #54807, 8.250000000000000000, 1.000000000000000000 ) ;
#62634=CARTESIAN_POINT ( 'NONE',  ( 11.30000285318000230, -11.76356368987999979, -1.428410073821000159 ) ) ;
#62635=ORIENTED_EDGE ( 'NONE', *, *, #51447, .F. ) ;
#62636=AXIS2_PLACEMENT_3D ( 'NONE', #39666, #66567, #50843 ) ;
#62648=CARTESIAN_POINT ( 'NONE',  ( 23.51706216425600360, 2.929165934761999601, -13.82547941210000175 ) ) ;
#62649=EDGE_LOOP ( 'NONE', ( #62273, #52881, #9595, #60054, #56529, #7314 ) ) ;
#62651=ADVANCED_FACE ( 'NONE', ( #3783 ), #63919, .F. ) ;
#62652=B_SPLINE_CURVE_WITH_KNOTS ( 'NONE', 3,
 ( #53926, #52903, #6026, #22109, #21418, #42416, #63722, #37165, #58485, #17918 ),
 .UNSPECIFIED., .F., .F.,
 ( 4, 2, 2, 2, 4 ),
 ( 0.5007402250167770630, 0.6255551687625827695, 0.7503701125083885870, 0.8751850562541942935, 1.000000000000000000 ),
 .UNSPECIFIED. ) ;
#62665=CARTESIAN_POINT ( 'NONE',  ( 13.55266668291200105, -9.123246021508000680, -7.477861434740999513 ) ) ;
#62680=CARTESIAN_POINT ( 'NONE',  ( 24.53428993882599940, 8.855929947951999281, -9.286429770520999938 ) ) ;
#62691=DIRECTION ( 'NONE',  ( 1.000000000000000000, 0.000000000000000000, 0.000000000000000000 ) ) ;
#62694=CARTESIAN_POINT ( 'NONE',  ( 24.50549018585800098, -12.34681877080999968, -3.084981659446000002 ) ) ;
#62695=CARTESIAN_POINT ( 'NONE',  ( 23.60000000000000142, 0.000000000000000000, 0.000000000000000000 ) ) ;
#62697=CARTESIAN_POINT ( 'NONE',  ( 24.45617574099272673, 3.500160185366723908, -12.27858218217408925 ) ) ;
#62702=CARTESIAN_POINT ( 'NONE',  ( 18.07439970769999960, 3.110573872314000177, 11.47478625844000177 ) ) ;
#62703=AXIS2_PLACEMENT_3D ( 'NONE', #3545, #3214, #30144 ) ;
#62708=CYLINDRICAL_SURFACE ( 'NONE', #22112, 0.5000000000000004441 ) ;
#62710=CARTESIAN_POINT ( 'NONE',  ( 25.36443153939400119, 8.489939778973999651, -7.945402963458000123 ) ) ;
#62711=CARTESIAN_POINT ( 'NONE',  ( 23.54917043075800009, 10.40012418511999925, -9.429198771629000220 ) ) ;
#62717=DIRECTION ( 'NONE',  ( 0.000000000000000000, 0.3352635608502960163, 0.9421243786071880066 ) ) ;
#62726=CARTESIAN_POINT ( 'NONE',  ( 15.83777337640989202, -9.021763928136902422, -8.400065602738662207 ) ) ;
#62727=CARTESIAN_POINT ( 'NONE',  ( 16.13125657744143737, -3.735736757528830054, -11.95504925864019441 ) ) ;
#62748=ORIENTED_EDGE ( 'NONE', *, *, #29004, .F. ) ;
#62750=VERTEX_POINT ( 'NONE', #30714 ) ;
#62754=CARTESIAN_POINT ( 'NONE',  ( 15.95192027319500205, 8.515023616297000331, 8.165096030563999463 ) ) ;
#62755=EDGE_LOOP ( 'NONE', ( #3029, #2717, #44422, #15649 ) ) ;
#62776=CARTESIAN_POINT ( 'NONE',  ( 18.39984528086700166, 2.531308496144999716E-14, 2.131628207279999844E-14 ) ) ;
#62779=B_SPLINE_CURVE_WITH_KNOTS ( 'NONE', 3,
 ( #29440, #44821, #45840, #2843 ),
 .UNSPECIFIED., .F., .F.,
 ( 4, 4 ),
 ( 0.000000000000000000, 1.000000000000000000 ),
 .UNSPECIFIED. ) ;
#62795=LINE ( 'NONE', #8639, #1608 ) ;
#62800=B_SPLINE_CURVE_WITH_KNOTS ( 'NONE', 3,
 ( #67236, #3273, #42059, #20384 ),
 .UNSPECIFIED., .F., .F.,
 ( 4, 4 ),
 ( 0.000000000000000000, 1.000000000000000000 ),
 .UNSPECIFIED. ) ;
#62801=B_SPLINE_CURVE_WITH_KNOTS ( 'NONE', 3,
 ( #12976, #56647, #46158, #67462 ),
 .UNSPECIFIED., .F., .F.,
 ( 4, 4 ),
 ( 0.000000000000000000, 1.000000000000000000 ),
 .UNSPECIFIED. ) ;
#62804=CARTESIAN_POINT ( 'NONE',  ( 24.45625628206627766, -8.883598553532051412, 9.170492330253466662 ) ) ;
#62805=CARTESIAN_POINT ( 'NONE',  ( 23.85182611390700202, 9.643708492127998966, 9.632179236076000350 ) ) ;
#62808=EDGE_CURVE ( 'NONE', #44937, #5174, #26626, .T. ) ;
#62811=DIRECTION ( 'NONE',  ( -0.000000000000000000, 0.9659258262890756397, 0.2588190451024934280 ) ) ;
#62813=CARTESIAN_POINT ( 'NONE',  ( 18.30830001818700126, 3.300182612895000478, 12.02694835946000040 ) ) ;
#62816=ORIENTED_EDGE ( 'NONE', *, *, #36972, .F. ) ;
#62818=CARTESIAN_POINT ( 'NONE',  ( 24.84557120767344429, -8.580242956840624657, 9.011385558522297501 ) ) ;
#62820=CARTESIAN_POINT ( 'NONE',  ( 13.99999999485600277, -9.471999751521998689, -8.194948195317001804 ) ) ;
#62823=CARTESIAN_POINT ( 'NONE',  ( 25.37955899411765159, -11.36924665038260329, -3.069077516866383082 ) ) ;
#62828=ORIENTED_EDGE ( 'NONE', *, *, #52081, .T. ) ;
#62832=ADVANCED_FACE ( 'NONE', ( #63192 ), #2922, .T. ) ;
#62842=DIRECTION ( 'NONE',  ( -0.000000000000000000, 0.9127899773906427150, 0.4084292560226189250 ) ) ;
#62844=CARTESIAN_POINT ( 'NONE',  ( 16.39999999379500295, -3.351248059343999941, -11.15756683833000018 ) ) ;
#62847=CARTESIAN_POINT ( 'NONE',  ( 11.79999999771000141, 3.595163221087000149, -11.99793848941000007 ) ) ;
#62853=CARTESIAN_POINT ( 'NONE',  ( 17.76900185986900027, -3.411877013825000304, -11.89794217324999970 ) ) ;
#62859=ORIENTED_EDGE ( 'NONE', *, *, #17890, .T. ) ;
#62860=ORIENTED_EDGE ( 'NONE', *, *, #26944, .T. ) ;
#62863=DIRECTION ( 'NONE',  ( -1.000000000000000000, 0.000000000000000000, 0.000000000000000000 ) ) ;
#62868=CARTESIAN_POINT ( 'NONE',  ( 18.12310803393399894, 3.320912951897000198, -11.92519506916999994 ) ) ;
#62872=ORIENTED_EDGE ( 'NONE', *, *, #31105, .F. ) ;
#62874=CARTESIAN_POINT ( 'NONE',  ( 23.56665676678100141, -10.37811504717999966, -9.381458738969000066 ) ) ;
#62879=CARTESIAN_POINT ( 'NONE',  ( 25.59994555223599733, 8.527741194213000142, 7.260611644044000279 ) ) ;
#62880=CARTESIAN_POINT ( 'NONE',  ( 24.56892835520400098, 8.742292411382999617, 8.862186445043999328 ) ) ;
#62883=CARTESIAN_POINT ( 'NONE',  ( 18.30003129332100187, -2.732683818840999646, -11.53064095373000164 ) ) ;
#62884=CARTESIAN_POINT ( 'NONE',  ( 11.48831242699000121, -3.364143239851999923, 11.30418287150000012 ) ) ;
#62891=CARTESIAN_POINT ( 'NONE',  ( 14.39999999734000191, 11.41071763148134544, -4.623975354790890613 ) ) ;
#62894=ORIENTED_EDGE ( 'NONE', *, *, #67081, .F. ) ;
#62895=EDGE_CURVE ( 'NONE', #13607, #63587, #12971, .T. ) ;
#62897=CARTESIAN_POINT ( 'NONE',  ( 11.29998636608000062, -3.695122995756999984, 11.25914041192000070 ) ) ;
#62899=CARTESIAN_POINT ( 'NONE',  ( 13.46395943152100116, -9.515552291263999152, -7.774702642439999423 ) ) ;
#62905=CARTESIAN_POINT ( 'NONE',  ( 24.94504657985486418, -11.54140607358216286, 3.218788503616806906 ) ) ;
#62913=CARTESIAN_POINT ( 'NONE',  ( 23.83637964422599964, 3.383983541727000333, 13.10295583586000134 ) ) ;
#62921=CARTESIAN_POINT ( 'NONE',  ( 23.72389859521504007, -3.247326028998003267, 13.28501015257995910 ) ) ;
#62928=EDGE_LOOP ( 'NONE', ( #23256, #19855, #2288, #35546 ) ) ;
#62946=ADVANCED_FACE ( 'NONE', ( #9368 ), #15321, .T. ) ;
#62973=AXIS2_PLACEMENT_3D ( 'NONE', #33067, #21530, #26445 ) ;
#62976=CARTESIAN_POINT ( 'NONE',  ( 24.14474077035201915, -9.246824227896013326, 9.586721910999997931 ) ) ;
#62977=DIRECTION ( 'NONE',  ( -1.000000000000000000, 0.000000000000000000, 0.000000000000000000 ) ) ;
#62990=CARTESIAN_POINT ( 'NONE',  ( 13.99999999439439335, -9.377150629848445718, -8.201012428486357919 ) ) ;
#62996=CARTESIAN_POINT ( 'NONE',  ( 29.60000000000000142, 0.000000000000000000, 8.250000000000000000 ) ) ;
#62998=CARTESIAN_POINT ( 'NONE',  ( 13.73862479881500143, -8.949604875896001843, -7.398842444207000213 ) ) ;
#63005=DIRECTION ( 'NONE',  ( 1.000000000000000000, 0.000000000000000000, 0.000000000000000000 ) ) ;
#63009=CARTESIAN_POINT ( 'NONE',  ( 17.89176949848240028, 3.347044352179603610, -11.15884716666442600 ) ) ;
#63010=DIRECTION ( 'NONE',  ( 1.000000000000000000, 0.000000000000000000, 0.000000000000000000 ) ) ;
#63013=DIRECTION ( 'NONE',  ( 0.000000000000000000, 1.000000000000000000, 0.000000000000000000 ) ) ;
#63017=ORIENTED_EDGE ( 'NONE', *, *, #68895, .T. ) ;
#63025=EDGE_CURVE ( 'NONE', #10995, #62306, #39767, .T. ) ;
#63026=CARTESIAN_POINT ( 'NONE',  ( 24.30000000000000071, 2.078227429405999693, 11.31065739696999906 ) ) ;
#63034=DIRECTION ( 'NONE',  ( 0.000000000000000000, -0.9516627692381158798, 0.3071448740351048756 ) ) ;
#63037=CARTESIAN_POINT ( 'NONE',  ( 17.99211270977099986, 3.227071166021000082, 11.34499727797000013 ) ) ;
#63044=CARTESIAN_POINT ( 'NONE',  ( 24.56658884197400283, 8.743998557975999120, -8.863912221221001531 ) ) ;
#63056=B_SPLINE_CURVE_WITH_KNOTS ( 'NONE', 3,
 ( #18031, #55774, #7877, #60666 ),
 .UNSPECIFIED., .F., .F.,
 ( 4, 4 ),
 ( 0.000000000000000000, 1.000000000000000000 ),
 .UNSPECIFIED. ) ;
#63059=CARTESIAN_POINT ( 'NONE',  ( 16.04514873068900016, -3.655338946640000142, -11.11851555082999887 ) ) ;
#63060=CARTESIAN_POINT ( 'NONE',  ( 13.46222979673600051, 9.132942286732999904, 7.608635239113000104 ) ) ;
#63082=CARTESIAN_POINT ( 'NONE',  ( 13.07616489729400122, 12.32806027643999869, 1.877794484342000025 ) ) ;
#63092=CARTESIAN_POINT ( 'NONE',  ( 16.39999999393278429, 3.428567374516922506, 11.90640519000895559 ) ) ;
#63093=CARTESIAN_POINT ( 'NONE',  ( 23.60000000000000142, 9.305479840184000651, 8.315530346521999405 ) ) ;
#63101=VERTEX_POINT ( 'NONE', #38714 ) ;
#63105=CARTESIAN_POINT ( 'NONE',  ( 11.79999999684100054, 12.15995044155999949, 2.000340912084999978 ) ) ;
#63106=CARTESIAN_POINT ( 'NONE',  ( 23.89491057039001731, 12.87866800254527888, -3.584029398659131616 ) ) ;
#63110=CARTESIAN_POINT ( 'NONE',  ( 25.46375345652300126, 2.879422156700999658, -11.30951020355999859 ) ) ;
#63113=EDGE_CURVE ( 'NONE', #49620, #49843, #10759, .T. ) ;
#63116=EDGE_CURVE ( 'NONE', #67674, #28175, #51622, .T. ) ;
#63117=EDGE_LOOP ( 'NONE', ( #35291, #37162, #40109, #11497 ) ) ;
#63124=CARTESIAN_POINT ( 'NONE',  ( 25.20345855277900071, 2.651890812380999662, 11.40160123550000115 ) ) ;
#63125=CARTESIAN_POINT ( 'NONE',  ( 15.90018573812399971, 8.493548356068000516, 8.263529029821000904 ) ) ;
#63128=ORIENTED_EDGE ( 'NONE', *, *, #20398, .T. ) ;
#63138=B_SPLINE_CURVE_WITH_KNOTS ( 'NONE', 3,
 ( #64441, #6763, #60603, #55362, #7457, #6414, #12714, #491, #11315, #44194 ),
 .UNSPECIFIED., .F., .F.,
 ( 4, 2, 2, 2, 4 ),
 ( 0.000000000000000000, 0.2500000000000000555, 0.5000000000000000000, 0.7499999999999998890, 1.000000000000000000 ),
 .UNSPECIFIED. ) ;
#63140=AXIS2_PLACEMENT_3D ( 'NONE', #6274, #27616, #6630 ) ;
#63149=DIRECTION ( 'NONE',  ( 1.000000000000000000, 0.000000000000000000, 0.000000000000000000 ) ) ;
#63150=ORIENTED_EDGE ( 'NONE', *, *, #31654, .F. ) ;
#63154=VERTEX_POINT ( 'NONE', #46369 ) ;
#63159=CARTESIAN_POINT ( 'NONE',  ( 24.67921139482200132, 8.727627377900999406, -9.158314240160001063 ) ) ;
#63162=CARTESIAN_POINT ( 'NONE',  ( 13.99999999347100044, 9.187456302440001110, 8.213201953411001455 ) ) ;
#63166=ORIENTED_EDGE ( 'NONE', *, *, #18959, .F. ) ;
#63170=FACE_OUTER_BOUND ( 'NONE', #59164, .T. ) ;
#63181=DIRECTION ( 'NONE',  ( 1.000000000000000000, 0.000000000000000000, 0.000000000000000000 ) ) ;
#63186=CARTESIAN_POINT ( 'NONE',  ( 15.90000000000000036, -8.729799320958107955, -8.474717466973274327 ) ) ;
#63190=DIRECTION ( 'NONE',  ( -1.000000000000000000, 0.000000000000000000, 0.000000000000000000 ) ) ;
#63191=FACE_OUTER_BOUND ( 'NONE', #54076, .T. ) ;
#63192=FACE_OUTER_BOUND ( 'NONE', #32691, .T. ) ;
#63202=DIRECTION ( 'NONE',  ( -1.000000000000000000, 0.000000000000000000, 0.000000000000000000 ) ) ;
#63207=CARTESIAN_POINT ( 'NONE',  ( 23.73691858855699977, -13.28034100689999875, 3.697799110653999577 ) ) ;
#63215=EDGE_CURVE ( 'NONE', #21757, #20699, #40675, .T. ) ;
#63219=AXIS2_PLACEMENT_3D ( 'NONE', #3182, #40246, #20288 ) ;
#63227=CARTESIAN_POINT ( 'NONE',  ( 11.35180279716000129, -3.678144743825999985, 11.20807767738999949 ) ) ;
#63231=CARTESIAN_POINT ( 'NONE',  ( 20.07256264693999981, 0.000000000000000000, 0.000000000000000000 ) ) ;
#63240=PRODUCT_DEFINITION_CONTEXT ( 'detailed design', #54308, 'design' ) ;
#63243=CARTESIAN_POINT ( 'NONE',  ( 24.67921569845699992, 12.29514839105000057, -2.979196030862000022 ) ) ;
#63252=B_SPLINE_CURVE_WITH_KNOTS ( 'NONE', 3,
 ( #43814, #23512, #34019, #28076 ),
 .UNSPECIFIED., .F., .F.,
 ( 4, 4 ),
 ( 0.000000000000000000, 0.4999999998439638160 ),
 .UNSPECIFIED. ) ;
#63253=CARTESIAN_POINT ( 'NONE',  ( 13.70003001321900449, 12.06139972930709270, 3.524828382075550604 ) ) ;
#63257=CARTESIAN_POINT ( 'NONE',  ( 24.25866820969800131, 3.167022761916999940, 12.13987262450000060 ) ) ;
#63268=CARTESIAN_POINT ( 'NONE',  ( 25.36444459794699924, -2.635932456649999978, -11.32519762123999918 ) ) ;
#63270=B_SPLINE_CURVE_WITH_KNOTS ( 'NONE', 3,
 ( #13954, #56596, #8703, #2087 ),
 .UNSPECIFIED., .F., .F.,
 ( 4, 4 ),
 ( 0.000000000000000000, 1.000000000000000000 ),
 .UNSPECIFIED. ) ;
#63275=CARTESIAN_POINT ( 'NONE',  ( 23.59999441188499958, 10.30760541648000128, -9.317696302454001156 ) ) ;
#63292=CARTESIAN_POINT ( 'NONE',  ( 24.34833292450100117, 8.895958855249167740, 8.895958855249167740 ) ) ;
#63296=CARTESIAN_POINT ( 'NONE',  ( 13.70005190196300227, 9.005348107749998832, 7.391036106496999381 ) ) ;
#63300=VERTEX_POINT ( 'NONE', #26773 ) ;
#63306=ADVANCED_FACE ( 'NONE', ( #48085 ), #5085, .F. ) ;
#63316=CARTESIAN_POINT ( 'NONE',  ( 17.77443075273995277, -11.85817042883088845, 3.314254474333838907 ) ) ;
#63322=CARTESIAN_POINT ( 'NONE',  ( 23.66004879239100234, -9.998911572074998588, 9.691526907171001071 ) ) ;
#63328=CARTESIAN_POINT ( 'NONE',  ( 23.55075434807899981, 2.914196937700999968, -13.72993838155000113 ) ) ;
#63329=B_SPLINE_CURVE_WITH_KNOTS ( 'NONE', 3,
 ( #66525, #49070, #18645, #44189 ),
 .UNSPECIFIED., .F., .F.,
 ( 4, 4 ),
 ( 0.000000000000000000, 1.000000000000000000 ),
 .UNSPECIFIED. ) ;
#63333=AXIS2_PLACEMENT_3D ( 'NONE', #53980, #31636, #52958 ) ;
#63347=CARTESIAN_POINT ( 'NONE',  ( 23.67309711513813397, 9.998428628671371499, -9.464667082479147453 ) ) ;
#63349=CARTESIAN_POINT ( 'NONE',  ( 23.73832405981900351, 13.27898672761999954, -3.695569413652000534 ) ) ;
#63366=CARTESIAN_POINT ( 'NONE',  ( 13.50567905817900183, 9.332645239999999731, 7.987984570204999635 ) ) ;
#63371=B_SPLINE_CURVE_WITH_KNOTS ( 'NONE', 3,
 ( #37050, #22679, #1708, #43330 ),
 .UNSPECIFIED., .F., .F.,
 ( 4, 4 ),
 ( 0.000000000000000000, 1.000000000000000000 ),
 .UNSPECIFIED. ) ;
#63374=ORIENTED_EDGE ( 'NONE', *, *, #19624, .T. ) ;
#63381=CARTESIAN_POINT ( 'NONE',  ( 24.39664322086668946, -3.224866850466631796, 12.03536693359005483 ) ) ;
#63382=B_SPLINE_CURVE_WITH_KNOTS ( 'NONE', 3,
 ( #42352, #21353, #53520, #47245 ),
 .UNSPECIFIED., .F., .F.,
 ( 4, 4 ),
 ( 0.000000000000000000, 1.000000000000000000 ),
 .UNSPECIFIED. ) ;
#63386=DIRECTION ( 'NONE',  ( 0.000000000000000000, -1.000000000000000000, 0.000000000000000000 ) ) ;
#63391=CARTESIAN_POINT ( 'NONE',  ( 12.79999999975700042, -11.86189249994999884, 3.298671769835999967 ) ) ;
#63397=CARTESIAN_POINT ( 'NONE',  ( 11.64459549376230285, 11.53034370889877813, 1.666360518327090201 ) ) ;
#63406=CARTESIAN_POINT ( 'NONE',  ( 24.30000000000000071, 11.49391741900999975, -4.090215442373000165 ) ) ;
#63413=CARTESIAN_POINT ( 'NONE',  ( 15.52628979459880298, -9.187490316955878811, -8.213190486479959418 ) ) ;
#63424=CARTESIAN_POINT ( 'NONE',  ( 24.30000000000000071, 3.224868684338999980, -12.03537377768999939 ) ) ;
#63428=ORIENTED_EDGE ( 'NONE', *, *, #42141, .F. ) ;
#63434=CARTESIAN_POINT ( 'NONE',  ( 13.46087891924500113, -11.63300053112000043, -2.447944685581000090 ) ) ;
#63435=CARTESIAN_POINT ( 'NONE',  ( 21.00000012402660232, -1.355091984497000173E-13, 1.088018564133000035E-14 ) ) ;
#63438=ORIENTED_EDGE ( 'NONE', *, *, #58166, .F. ) ;
#63446=DIRECTION ( 'NONE',  ( -1.000000000000000000, 0.000000000000000000, 0.000000000000000000 ) ) ;
#63448=CARTESIAN_POINT ( 'NONE',  ( 25.60000000000000142, -2.258942858049999725, 10.99402034467349232 ) ) ;
#63450=ORIENTED_EDGE ( 'NONE', *, *, #8547, .F. ) ;
#63453=CARTESIAN_POINT ( 'NONE',  ( 12.10004069261200677, 11.60802777289553411, -4.146429405016670344 ) ) ;
#63458=CARTESIAN_POINT ( 'NONE',  ( 24.13789454551274005, 12.48572713186856831, -3.365239671874099781 ) ) ;
#63462=CARTESIAN_POINT ( 'NONE',  ( 24.26287088544855308, 12.27454670750946697, 3.288953945731635464 ) ) ;
#63472=CARTESIAN_POINT ( 'NONE',  ( 12.80000000000000071, 11.23412379136000006, -3.084957477885999833 ) ) ;
#63475=VECTOR ( 'NONE', #59522, 1000.000000000000000 ) ;
#63477=VERTEX_POINT ( 'NONE', #4042 ) ;
#63479=AXIS2_PLACEMENT_3D ( 'NONE', #4599, #25935, #394 ) ;
#63480=CARTESIAN_POINT ( 'NONE',  ( 12.53679426224900162, -11.40784081139999984, 4.532785132108998916 ) ) ;
#63486=CARTESIAN_POINT ( 'NONE',  ( 13.63331750507211559, 9.617283495289667528, 7.919506078536236338 ) ) ;
#63492=B_SPLINE_SURFACE_WITH_KNOTS ( 'NONE', 3, 3, ( 
 ( #35482, #50521, #67611, #57133 ),
 ( #56803, #7874, #51544, #2621 ),
 ( #13811, #50867, #9230, #24293 ),
 ( #62380, #8217, #45630, #62039 ),
 ( #46657, #25319, #29906, #3640 ),
 ( #8900, #24977, #45962, #29210 ),
 ( #51211, #46310, #40372, #2964 ),
 ( #19738, #30239, #67962, #30569 ),
 ( #13475, #66934, #41060, #35142 ),
 ( #56106, #34795, #3307, #29565 ) ),
 .UNSPECIFIED., .F., .F., .F.,
 ( 4, 1, 1, 1, 1, 1, 1, 4 ),
 ( 4, 4 ),
 ( 0.04183311431307000505, 0.1428571428570999946, 0.2857142857143000203, 0.4285714285713999594, 0.5714285714286000406, 0.7142857142856999797, 0.8571428571429000609, 0.9292981235707000742 ),
 ( -0.1917799910644999994, 1.191756862851000021 ),
 .UNSPECIFIED. ) ;
#63494=CARTESIAN_POINT ( 'NONE',  ( 24.32785187986800324, 9.022984283431000563, 9.340288652106000455 ) ) ;
#63503=FACE_OUTER_BOUND ( 'NONE', #43350, .T. ) ;
#63507=ADVANCED_FACE ( 'NONE', ( #36217 ), #36410, .T. ) ;
#63516=EDGE_CURVE ( 'NONE', #62306, #30294, #20494, .T. ) ;
#63523=CARTESIAN_POINT ( 'NONE',  ( 16.39967273502900014, -3.641490841173999904, -12.02437761214999945 ) ) ;
#63524=B_SPLINE_CURVE_WITH_KNOTS ( 'NONE', 3,
 ( #1942, #23261, #12429, #29562, #28162, #39341, #60662, #33760 ),
 .UNSPECIFIED., .F., .F.,
 ( 4, 2, 2, 4 ),
 ( 0.000000000000000000, 0.2500000000000002220, 0.5000000000000004441, 1.000000000000000000 ),
 .UNSPECIFIED. ) ;
#63525=CARTESIAN_POINT ( 'NONE',  ( 11.48394322905000031, 11.59615457572999908, 1.579582225534999829 ) ) ;
#63526=ORIENTED_EDGE ( 'NONE', *, *, #56537, .F. ) ;
#63527=CARTESIAN_POINT ( 'NONE',  ( 16.09997386696500143, -7.697446472043792731, -8.794756076490951813 ) ) ;
#63528=PLANE ( 'NONE',  #66949 ) ;
#63530=B_SPLINE_CURVE_WITH_KNOTS ( 'NONE', 3,
 ( #19991, #68204, #20323, #51115, #57041, #41650, #45871, #15081, #67179, #62620, #57723, #14742, #9831, #19293 ),
 .UNSPECIFIED., .F., .F.,
 ( 4, 2, 2, 2, 2, 2, 4 ),
 ( 0.000000000000000000, 0.1249999999999997502, 0.2499999999999995004, 0.4999999999999976685, 0.6249999999999990008, 0.7500000000000002220, 1.000000000000000000 ),
 .UNSPECIFIED. ) ;
#63538=VERTEX_POINT ( 'NONE', #38276 ) ;
#63554=ORIENTED_EDGE ( 'NONE', *, *, #27708, .T. ) ;
#63560=CARTESIAN_POINT ( 'NONE',  ( 18.19991693152165979, 3.160411602603945269, -11.91446363486501703 ) ) ;
#63561=ADVANCED_FACE ( 'NONE', ( #48773 ), #42725, .F. ) ;
#63566=EDGE_CURVE ( 'NONE', #38268, #14826, #54043, .T. ) ;
#63575=CARTESIAN_POINT ( 'NONE',  ( 24.69899870589400237, 8.733950678133000523, 9.243023888125000198 ) ) ;
#63579=CARTESIAN_POINT ( 'NONE',  ( 11.44749694427000186, -3.679776032594999968, 11.11060924501999914 ) ) ;
#63587=VERTEX_POINT ( 'NONE', #2262 ) ;
#63589=FACE_OUTER_BOUND ( 'NONE', #52378, .T. ) ;
#63592=CARTESIAN_POINT ( 'NONE',  ( 15.89994436294300151, 8.847904542234999781, 8.580301953175000662 ) ) ;
#63597=CARTESIAN_POINT ( 'NONE',  ( 24.69611861387416951, -11.79505474561326039, 3.190916355391951509 ) ) ;
#63603=EDGE_CURVE ( 'NONE', #61665, #57654, #9468, .T. ) ;
#63605=DIRECTION ( 'NONE',  ( 0.000000000000000000, 0.000000000000000000, -1.000000000000000000 ) ) ;
#63610=EDGE_LOOP ( 'NONE', ( #3289, #5999, #36352, #56401 ) ) ;
#63616=B_SPLINE_CURVE_WITH_KNOTS ( 'NONE', 3,
 ( #27433, #27093, #21488, #22517 ),
 .UNSPECIFIED., .F., .F.,
 ( 4, 4 ),
 ( 0.000000000000000000, 1.000000000000000000 ),
 .UNSPECIFIED. ) ;
#63617=CARTESIAN_POINT ( 'NONE',  ( 24.13225220766125645, -3.329780019911785960, 12.50570657898502702 ) ) ;
#63618=CARTESIAN_POINT ( 'NONE',  ( 24.30001696810800027, 12.21047201856000086, 3.271805692349999628 ) ) ;
#63620=EDGE_CURVE ( 'NONE', #21235, #52300, #34868, .T. ) ;
#63621=CARTESIAN_POINT ( 'NONE',  ( 24.60115017431256490, -12.20856115934854635, -3.061105476207797160 ) ) ;
#63623=CARTESIAN_POINT ( 'NONE',  ( 25.34480285809352296, -8.474813500079264372, -7.997915891567656033 ) ) ;
#63624=ORIENTED_EDGE ( 'NONE', *, *, #28020, .T. ) ;
#63627=DIRECTION ( 'NONE',  ( 0.000000000000000000, 0.000000000000000000, -1.000000000000000000 ) ) ;
#63643=CARTESIAN_POINT ( 'NONE',  ( 11.43330331963142044, -3.865571928678541269, 11.84352938576710734 ) ) ;
#63645=EDGE_CURVE ( 'NONE', #58173, #26251, #67344, .T. ) ;
#63648=ORIENTED_EDGE ( 'NONE', *, *, #17757, .F. ) ;
#63649=CARTESIAN_POINT ( 'NONE',  ( 24.43232361759900328, 8.806075257782000065, 8.751960807121999864 ) ) ;
#63651=DIRECTION ( 'NONE',  ( 2.888199747633069555E-10, 0.5897878662160149776, 0.8075582163933199276 ) ) ;
#63657=CARTESIAN_POINT ( 'NONE',  ( 21.65000086032551252, 3.970157536060000036E-13, -13.94999929344982448 ) ) ;
#63662=CARTESIAN_POINT ( 'NONE',  ( 25.59997324745700098, 8.218963665694001719, 8.043524865688999270 ) ) ;
#63665=CARTESIAN_POINT ( 'NONE',  ( 15.35917414208899956, -8.811049802147000065, -7.563839685023999948 ) ) ;
#63669=DIRECTION ( 'NONE',  ( 0.000000000000000000, -0.7071067811864953923, -0.7071067811865995312 ) ) ;
#63670=CARTESIAN_POINT ( 'NONE',  ( 15.90000000000314451, 3.738168175168965046, 11.41174933108808176 ) ) ;
#63680=EDGE_CURVE ( 'NONE', #47157, #56428, #12666, .T. ) ;
#63686=AXIS2_PLACEMENT_3D ( 'NONE', #25865, #67816, #68720 ) ;
#63694=CARTESIAN_POINT ( 'NONE',  ( 13.00000000009400303, -11.69118001589999878, -1.923222888683999932 ) ) ;
#63704=CARTESIAN_POINT ( 'NONE',  ( 13.21911358530772773, 12.38522838340865562, 1.866030466704203583 ) ) ;
#63707=ADVANCED_FACE ( 'NONE', ( #36393 ), #63995, .F. ) ;
#63708=CARTESIAN_POINT ( 'NONE',  ( 12.79999999734009464, -10.99220013531737372, 4.481500379774075782 ) ) ;
#63710=CARTESIAN_POINT ( 'NONE',  ( 18.35192688406300121, -2.803631260452999818, 11.45923525916999886 ) ) ;
#63713=FACE_OUTER_BOUND ( 'NONE', #48959, .T. ) ;
#63714=CARTESIAN_POINT ( 'NONE',  ( 13.64382898362900143, 11.47858090575000034, 2.288513382665999796 ) ) ;
#63722=CARTESIAN_POINT ( 'NONE',  ( 17.94511861457986868, 11.84188429194256109, -3.380847647125635014 ) ) ;
#63728=CARTESIAN_POINT ( 'NONE',  ( 18.31073753479499899, 11.62544123506999938, -4.252388861798999997 ) ) ;
#63733=CARTESIAN_POINT ( 'NONE',  ( 17.79055474012400140, -3.643253463509999790, 12.02383756773999934 ) ) ;
#63742=CARTESIAN_POINT ( 'NONE',  ( 11.43320385462400424, 12.36501045767315077, 1.521867244384402129 ) ) ;
#63749=ORIENTED_EDGE ( 'NONE', *, *, #33393, .F. ) ;
#63762=ADVANCED_FACE ( 'NONE', ( #62608 ), #12754, .T. ) ;
#63774=( BOUNDED_SURFACE ( )  B_SPLINE_SURFACE ( 3, 3, ( 
 ( #60758, #66339, #56206, #12875 ),
 ( #34202, #7622, #38749, #12180 ),
 ( #54826, #13228, #1687, #65654 ),
 ( #23004, #17776, #18463, #39788 ) ),
 .UNSPECIFIED., .F., .F., .T. ) 
 B_SPLINE_SURFACE_WITH_KNOTS ( ( 4, 4 ),
 ( 4, 4 ),
 ( 0.000000000000000000, 1.000000000000000000 ),
 ( 0.000000000000000000, 1.000000000000000000 ),
 .UNSPECIFIED. ) 
 GEOMETRIC_REPRESENTATION_ITEM ( )  RATIONAL_B_SPLINE_SURFACE ( (
 ( 1.512182578520000042, 1.160176301760999840, 1.160176301760999840, 1.512182578520000042),
 ( 1.111288591041000196, 0.8526025270081000196, 0.8526025270081000196, 1.111288591041000196),
 ( 1.111288591041000196, 0.8526025270081000196, 0.8526025270081000196, 1.111288591041000196),
 ( 1.512182578520000042, 1.160176301760999840, 1.160176301760999840, 1.512182578520000042) ) ) 
 REPRESENTATION_ITEM ( '' )  SURFACE ( )  );
#63778=PLANE ( 'NONE',  #65201 ) ;
#63787=CARTESIAN_POINT ( 'NONE',  ( 15.86087891924500148, 8.502609378008999741, 8.308114605954999732 ) ) ;
#63789=VERTEX_POINT ( 'NONE', #47922 ) ;
#63790=CARTESIAN_POINT ( 'NONE',  ( 12.79999999914999975, -12.11987927271999865, 3.159802730921999814 ) ) ;
#63795=ORIENTED_EDGE ( 'NONE', *, *, #13587, .F. ) ;
#63797=CARTESIAN_POINT ( 'NONE',  ( 25.26979655960100146, 11.11692128343999997, -3.473710019957000128 ) ) ;
#63799=ORIENTED_EDGE ( 'NONE', *, *, #1823, .F. ) ;
#63800=CARTESIAN_POINT ( 'NONE',  ( 11.29998578400000042, -3.824193979571000046, 11.71675423233000046 ) ) ;
#63802=CARTESIAN_POINT ( 'NONE',  ( 11.79999999713069947, 12.23671679745269181, 1.944304699248228685 ) ) ;
#63804=CARTESIAN_POINT ( 'NONE',  ( 18.36662463489988184, 2.877217017167648550, -12.05304703251516152 ) ) ;
#63809=CARTESIAN_POINT ( 'NONE',  ( 24.14104127787211240, 12.48046602493499080, 3.363062335187216867 ) ) ;
#63817=CARTESIAN_POINT ( 'NONE',  ( 24.67921310950000091, -12.29514723793999842, -2.979192343402000009 ) ) ;
#63818=DIRECTION ( 'NONE',  ( 3.927529531862125126E-06, -0.2588384783032084413, -0.9659206189611307947 ) ) ;
#63824=CARTESIAN_POINT ( 'NONE',  ( 12.78082384918899983, -11.55157311154999888, 4.942237549596000257 ) ) ;
#63832=B_SPLINE_CURVE_WITH_KNOTS ( 'NONE', 3,
 ( #5131, #53721, #69108, #5818, #933, #37979, #6509, #59303 ),
 .UNSPECIFIED., .F., .F.,
 ( 4, 2, 2, 4 ),
 ( 0.000000000000000000, 0.2499999999999998890, 0.4999999999999997780, 1.000000000000000000 ),
 .UNSPECIFIED. ) ;
#63833=CARTESIAN_POINT ( 'NONE',  ( 25.19214535676100297, -11.35759380094999926, 3.218642521839000015 ) ) ;
#63837=CARTESIAN_POINT ( 'NONE',  ( 24.08694690297700092, 9.258999421897000204, 9.302244280904000462 ) ) ;
#63856=CARTESIAN_POINT ( 'NONE',  ( 25.46372779695100164, -11.23407511953000082, -3.161075425950000017 ) ) ;
#63863=VERTEX_POINT ( 'NONE', #20658 ) ;
#63865=CARTESIAN_POINT ( 'NONE',  ( 24.90040311280328567, 3.015665883976863526, -11.63994628420445032 ) ) ;
#63866=CARTESIAN_POINT ( 'NONE',  ( 24.70906580553056742, -8.654462107696843987, -8.608367302003138377 ) ) ;
#63882=ORIENTED_EDGE ( 'NONE', *, *, #48924, .T. ) ;
#63889=CARTESIAN_POINT ( 'NONE',  ( 18.32727125556129977, 3.363648366952159297, 12.06493410109839637 ) ) ;
#63893=ORIENTED_EDGE ( 'NONE', *, *, #47610, .T. ) ;
#63901=AXIS2_PLACEMENT_3D ( 'NONE', #6909, #50602, #44339 ) ;
#63902=CARTESIAN_POINT ( 'NONE',  ( 23.73417960609100064, -13.39756163216000040, 3.632377255137999583 ) ) ;
#63903=EDGE_CURVE ( 'NONE', #40828, #32947, #34002, .T. ) ;
#63913=CARTESIAN_POINT ( 'NONE',  ( 18.26087544840899923, 2.716371057353000218, -11.57326339378999869 ) ) ;
#63918=CARTESIAN_POINT ( 'NONE',  ( 24.67921580188599862, 3.567514645466999923, -12.13750897870000145 ) ) ;
#63919=B_SPLINE_SURFACE_WITH_KNOTS ( 'NONE', 3, 3, ( 
 ( #51685, #9036, #62177, #18515 ),
 ( #50669, #45428, #8705, #30377 ),
 ( #56940, #2769, #62517, #40511 ),
 ( #13956, #3109, #25121, #35283 ),
 ( #3443, #40183, #24095, #66392 ),
 ( #24780, #46453, #46107, #14636 ) ),
 .UNSPECIFIED., .F., .F., .F.,
 ( 4, 1, 1, 4 ),
 ( 4, 4 ),
 ( 0.1423941212541000034, 0.3333333333333000081, 0.6666666666667000474, 0.8219462477342999174 ),
 ( -0.1256563615234000120, 1.125656361508000192 ),
 .UNSPECIFIED. ) ;
#63925=CARTESIAN_POINT ( 'NONE',  ( 24.50549018585800098, 8.845081872695999436, -9.150167881723000107 ) ) ;
#63930=DIRECTION ( 'NONE',  ( 0.000000000000000000, 0.8075584957945176612, -0.5897874836499127360 ) ) ;
#63933=UNCERTAINTY_MEASURE_WITH_UNIT (LENGTH_MEASURE( 1.000000000000000082E-05 ), #8267, 'distance_accuracy_value', 'NONE');
#63935=VERTEX_POINT ( 'NONE', #22022 ) ;
#63948=CARTESIAN_POINT ( 'NONE',  ( 24.33654969819199820, 3.364569167692000207, 12.26690921096999887 ) ) ;
#63949=ORIENTED_EDGE ( 'NONE', *, *, #12968, .T. ) ;
#63954=ORIENTED_EDGE ( 'NONE', *, *, #67686, .T. ) ;
#63956=EDGE_CURVE ( 'NONE', #9331, #47642, #43142, .T. ) ;
#63959=CARTESIAN_POINT ( 'NONE',  ( 24.84742874851600192, -3.386177995241999916, -11.85235341148000110 ) ) ;
#63963=CARTESIAN_POINT ( 'NONE',  ( 23.77345882393642995, 9.774756027420808735, 9.437281717087342869 ) ) ;
#63964=ORIENTED_EDGE ( 'NONE', *, *, #44538, .F. ) ;
#63968=FACE_OUTER_BOUND ( 'NONE', #55827, .T. ) ;
#63976=CARTESIAN_POINT ( 'NONE',  ( 24.68353817070021705, -3.140007193288423704, 11.82111472263500218 ) ) ;
#63978=CARTESIAN_POINT ( 'NONE',  ( 24.92740991898443426, 8.563816619416252607, 8.404006304129723048 ) ) ;
#63987=VERTEX_POINT ( 'NONE', #34259 ) ;
#63995=CONICAL_SURFACE ( 'NONE', #56182, 1.150066570905000196, 0.7854484257638207900 ) ;
#64020=VECTOR ( 'NONE', #12158, 1000.000000000000000 ) ;
#64021=CARTESIAN_POINT ( 'NONE',  ( 18.28832092577789581, -2.855728055076846683, 11.50255606648410200 ) ) ;
#64022=CARTESIAN_POINT ( 'NONE',  ( 17.89176949849500886, -3.347044352179931792, 11.15884716666432475 ) ) ;
#64031=CARTESIAN_POINT ( 'NONE',  ( 23.78804094696696581, 9.744952014918238703, -9.430323830586468503 ) ) ;
#64042=AXIS2_PLACEMENT_3D ( 'NONE', #50063, #2171, #66473 ) ;
#64043=CARTESIAN_POINT ( 'NONE',  ( 24.13559297464179565, 3.329017028593327598, -12.49970664374816565 ) ) ;
#64044=CARTESIAN_POINT ( 'NONE',  ( 18.35481935287100086, -2.723593151845999927, 11.47751840123000022 ) ) ;
#64047=CARTESIAN_POINT ( 'NONE',  ( 11.53937265905000054, 3.642773248484000082, -11.02530338024999956 ) ) ;
#64048=CARTESIAN_POINT ( 'NONE',  ( 13.73573769406200107, 11.39043216638999922, 2.256426478477000064 ) ) ;
#64057=CARTESIAN_POINT ( 'NONE',  ( 24.89163395459006978, -8.575320083348136890, 8.440772679311232096 ) ) ;
#64059=B_SPLINE_SURFACE_WITH_KNOTS ( 'NONE', 3, 3, ( 
 ( #15349, #57996, #41570, #63575 ),
 ( #62542, #62880, #10096, #19907 ),
 ( #37956, #31431, #52747, #51715 ),
 ( #3807, #46477, #67785, #14663 ),
 ( #35979, #57297, #9399, #61190 ),
 ( #44434, #54906, #2120, #33936 ),
 ( #8048, #45796, #45116, #50701 ),
 ( #55255, #67109, #61531, #29045 ) ),
 .UNSPECIFIED., .F., .F., .F.,
 ( 4, 1, 1, 1, 1, 4 ),
 ( 4, 4 ),
 ( 0.008355517289528000338, 0.05882352941176000050, 0.1176470588234999892, 0.1764705882353000133, 0.2352941176471000095, 0.2534843112964000333 ),
 ( -0.1830816879725000179, 1.182949857028000151 ),
 .UNSPECIFIED. ) ;
#64066=CARTESIAN_POINT ( 'NONE',  ( 11.95023821374600104, 11.77429045505000005, -4.110796463462000006 ) ) ;
#64067=AXIS2_PLACEMENT_3D ( 'NONE', #14754, #36071, #3561 ) ;
#64068=CARTESIAN_POINT ( 'NONE',  ( 18.44976178625400109, 11.77429045505000005, -4.110796463462000006 ) ) ;
#64073=CARTESIAN_POINT ( 'NONE',  ( 18.23019412026599895, -3.031170125296999807, 11.90979123982999965 ) ) ;
#64078=CARTESIAN_POINT ( 'NONE',  ( 24.53429015151300163, -3.614318902553999902, -12.31267542782000035 ) ) ;
#64081=CARTESIAN_POINT ( 'NONE',  ( 18.30000000000000071, 0.000000000000000000, 0.000000000000000000 ) ) ;
#64089=ORIENTED_EDGE ( 'NONE', *, *, #29718, .T. ) ;
#64098=CARTESIAN_POINT ( 'NONE',  ( 16.31144947526900069, -3.254927130315000028, -11.33654363332999893 ) ) ;
#64100=CARTESIAN_POINT ( 'NONE',  ( 13.55168611684300117, -12.14221570691000096, -2.415203473206000151 ) ) ;
#64105=DIRECTION ( 'NONE',  ( 0.000000000000000000, -0.7071067811865475727, -0.7071067811865475727 ) ) ;
#64106=ORIENTED_EDGE ( 'NONE', *, *, #11784, .F. ) ;
#64116=CARTESIAN_POINT ( 'NONE',  ( 24.45617572375350690, -3.500160191032958945, 12.27858220308102766 ) ) ;
#64125=CARTESIAN_POINT ( 'NONE',  ( 23.66004879239100234, -3.393653467490999720, 13.50507469661999949 ) ) ;
#64134=VERTEX_POINT ( 'NONE', #17833 ) ;
#64136=CARTESIAN_POINT ( 'NONE',  ( 24.63779784258400340, 11.77742452909999926, -3.228730981588999960 ) ) ;
#64148=CARTESIAN_POINT ( 'NONE',  ( 16.04731601457200085, 3.899361801049999965, 11.84592592973999992 ) ) ;
#64150=CARTESIAN_POINT ( 'NONE',  ( 24.14062698496121939, 12.48115957962327904, 3.363346990936225911 ) ) ;
#64160=CARTESIAN_POINT ( 'NONE',  ( 13.00000000005200107, 12.15994572112000149, 2.000334444851999738 ) ) ;
#64169=CARTESIAN_POINT ( 'NONE',  ( 13.59982064663300072, 2.566835632933000434E-13, 1.354472090042999897E-14 ) ) ;
#64203=CARTESIAN_POINT ( 'NONE',  ( 11.53935620825160768, 11.69940330537452589, 1.870140110077450402 ) ) ;
#64204=CARTESIAN_POINT ( 'NONE',  ( 11.25913316395000052, 11.80170809442000035, 1.433206434934999995 ) ) ;
#64206=CARTESIAN_POINT ( 'NONE',  ( 24.44496487975900223, 3.224879802562000464, -12.03535984693000138 ) ) ;
#64207=DIRECTION ( 'NONE',  ( -1.000000000000000000, 0.000000000000000000, 0.000000000000000000 ) ) ;
#64214=CARTESIAN_POINT ( 'NONE',  ( 11.35399482404719329, 3.445326802703547742, -11.33548354870907637 ) ) ;
#64221=CARTESIAN_POINT ( 'NONE',  ( 16.00156003475500199, -9.132520755637999699, -8.493756974768999157 ) ) ;
#64228=CARTESIAN_POINT ( 'NONE',  ( 21.65000086032565108, -2.247091401841000284E-13, 4.272138198758000206E-13 ) ) ;
#64233=ORIENTED_EDGE ( 'NONE', *, *, #5726, .T. ) ;
#64238=CARTESIAN_POINT ( 'NONE',  ( 25.34478631770858925, 2.688917760716752703, -11.33837770301359527 ) ) ;
#64247=ORIENTED_EDGE ( 'NONE', *, *, #2748, .T. ) ;
#64248=CARTESIAN_POINT ( 'NONE',  ( 18.53573769406200356, 2.787008136214999876, 11.27235516822999983 ) ) ;
#64252=CARTESIAN_POINT ( 'NONE',  ( 24.30001682246400208, -8.938702682732001747, -8.938676171235998780 ) ) ;
#64254=CARTESIAN_POINT ( 'NONE',  ( 17.77441288034700051, 3.189751316310999840, -11.45074679932000095 ) ) ;
#64258=CARTESIAN_POINT ( 'NONE',  ( 24.51195315439300160, -8.843582221221000239, -9.168329703202999781 ) ) ;
#64265=CARTESIAN_POINT ( 'NONE',  ( 24.62773497368900166, 8.736972494143998347, -9.042113496790999960 ) ) ;
#64287=VERTEX_POINT ( 'NONE', #37683 ) ;
#64317=CARTESIAN_POINT ( 'NONE',  ( 11.56571517796000137, 12.12283255502000046, 1.989142034170999995 ) ) ;
#64323=ORIENTED_EDGE ( 'NONE', *, *, #66706, .T. ) ;
#64336=EDGE_CURVE ( 'NONE', #56866, #16567, #65547, .T. ) ;
#64341=CARTESIAN_POINT ( 'NONE',  ( 12.68562097720201898, 12.11848650044656672, -3.165127050490344374 ) ) ;
#64346=DIRECTION ( 'NONE',  ( 1.000000000000000000, 0.000000000000000000, 0.000000000000000000 ) ) ;
#64349=CARTESIAN_POINT ( 'NONE',  ( 23.85399087666008811, -9.637233594680219895, 9.713115531358498700 ) ) ;
#64350=CARTESIAN_POINT ( 'NONE',  ( 12.01556330254184601, -11.99897551495956272, 3.593484177663201606 ) ) ;
#64356=CARTESIAN_POINT ( 'NONE',  ( 23.60000000000000142, 0.000000000000000000, 0.000000000000000000 ) ) ;
#64357=CARTESIAN_POINT ( 'NONE',  ( 18.01246087681489172, -10.82907928505310124, 4.296547899025035200 ) ) ;
#64358=AXIS2_PLACEMENT_3D ( 'NONE', #30617, #52621, #4026 ) ;
#64360=DIRECTION ( 'NONE',  ( -1.000000000000000000, 0.000000000000000000, 0.000000000000000000 ) ) ;
#64364=ADVANCED_FACE ( 'NONE', ( #47147 ), #26029, .F. ) ;
#64365=FACE_OUTER_BOUND ( 'NONE', #53728, .T. ) ;
#64367=AXIS2_PLACEMENT_3D ( 'NONE', #40737, #4005, #67637 ) ;
#64370=CARTESIAN_POINT ( 'NONE',  ( 25.39990883465370430, 2.060145121004215873, 11.21224557561489910 ) ) ;
#64372=CARTESIAN_POINT ( 'NONE',  ( 24.70869262301700076, 12.32777590421999925, 2.948351121266000074 ) ) ;
#64377=VERTEX_POINT ( 'NONE', #32108 ) ;
#64379=CARTESIAN_POINT ( 'NONE',  ( 24.30000000000000071, 10.83443035398000021, -3.855530949778000149 ) ) ;
#64385=CARTESIAN_POINT ( 'NONE',  ( 18.07439970769999960, -3.110573872314000177, 11.47478625844000177 ) ) ;
#64390=CARTESIAN_POINT ( 'NONE',  ( 12.99518154839200257, 11.72294562696999876, 1.966205464704999795 ) ) ;
#64393=ORIENTED_EDGE ( 'NONE', *, *, #26837, .F. ) ;
#64396=ORIENTED_EDGE ( 'NONE', *, *, #57372, .T. ) ;
#64400=CARTESIAN_POINT ( 'NONE',  ( 13.49980696792483137, 10.14812545701388657, 7.065329385613729585 ) ) ;
#64406=CARTESIAN_POINT ( 'NONE',  ( 12.18555568849200021, 11.56145208044000050, -4.416819796118000241 ) ) ;
#64407=CARTESIAN_POINT ( 'NONE',  ( 18.26809521658400115, 11.96733320521999921, -3.503025077341000326 ) ) ;
#64413=CARTESIAN_POINT ( 'NONE',  ( 18.40156003475500057, -3.148349829928000165, 12.06792178657999948 ) ) ;
#64434=CIRCLE ( 'NONE', #4158, 11.79499999999999993 ) ;
#64437=CARTESIAN_POINT ( 'NONE',  ( 16.13869549901199818, -3.415897281711999689, -11.19349503352999875 ) ) ;
#64441=CARTESIAN_POINT ( 'NONE',  ( 11.50029455687000102, 11.65000000000000036, 0.000000000000000000 ) ) ;
#64456=FACE_OUTER_BOUND ( 'NONE', #44701, .T. ) ;
#64460=CIRCLE ( 'NONE', #52203, 1.300164684427999706 ) ;
#64465=CARTESIAN_POINT ( 'NONE',  ( 24.57714555854880345, 8.720582753219940031, -8.720580432860286280 ) ) ;
#64466=CARTESIAN_POINT ( 'NONE',  ( 15.39229341877100232, 8.812225371893999792, 7.562487140343000291 ) ) ;
#64468=DIRECTION ( 'NONE',  ( 1.000000000000000000, 0.000000000000000000, 0.000000000000000000 ) ) ;
#64472=ORIENTED_EDGE ( 'NONE', *, *, #63603, .F. ) ;
#64474=CARTESIAN_POINT ( 'NONE',  ( 24.59232787866800152, 12.25045818421999932, -3.053350602882999976 ) ) ;
#64478=CARTESIAN_POINT ( 'NONE',  ( 16.03350391962103316, 3.653603504000401792, 11.13263026093595975 ) ) ;
#64483=EDGE_CURVE ( 'NONE', #25042, #19870, #18884, .T. ) ;
#64486=CARTESIAN_POINT ( 'NONE',  ( 16.43986884071599874, 3.414349888938000177, 11.89720686373000191 ) ) ;
#64488=CARTESIAN_POINT ( 'NONE',  ( 24.08707324615214418, 12.57025408754081752, 3.402056317565807397 ) ) ;
#64511=CARTESIAN_POINT ( 'NONE',  ( 12.79999999202000005, -11.41069016990000051, 4.623987642516999230 ) ) ;
#64515=B_SPLINE_CURVE_WITH_KNOTS ( 'NONE', 3,
 ( #39320, #12753, #31165, #37764, #32192, #63976, #42669, #10504, #4566, #16094, #37420, #20657, #4912, #48252, #30807, #25561, #36392, #52120, #43011, #41638, #15418 ),
 .UNSPECIFIED., .F., .F.,
 ( 4, 2, 2, 1, 1, 2, 2, 2, 1, 2, 2, 4 ),
 ( 0.000000000000000000, 0.1250000000000165978, 0.1875000000000261180, 0.2187500000000308920, 0.2343750000000332512, 0.2421875000000328071, 0.2500000000000323075, 0.3750000000000177081, 0.4375000000000116573, 0.4687500000000097700, 0.5000000000000078826, 1.000000000000000000 ),
 .UNSPECIFIED. ) ;
#64516=CARTESIAN_POINT ( 'NONE',  ( 23.58838885791947249, 10.19767132316656522, -9.565245332708771642 ) ) ;
#64525=PLANE ( 'NONE',  #6590 ) ;
#64531=B_SPLINE_CURVE_WITH_KNOTS ( 'NONE', 3,
 ( #34039, #32989, #54305, #6408 ),
 .UNSPECIFIED., .F., .F.,
 ( 4, 4 ),
 ( 0.000000000000000000, 1.000000000000000000 ),
 .UNSPECIFIED. ) ;
#64544=EDGE_CURVE ( 'NONE', #28653, #16735, #59559, .T. ) ;
#64546=AXIS2_PLACEMENT_3D ( 'NONE', #20761, #42091, #5368 ) ;
#64549=CARTESIAN_POINT ( 'NONE',  ( 11.35179910620000143, 11.71014626380999957, 1.422059914427000082 ) ) ;
#64552=DIRECTION ( 'NONE',  ( 0.000000000000000000, -0.9421243786071880066, 0.3352635608502960163 ) ) ;
#64555=CARTESIAN_POINT ( 'NONE',  ( 13.50000000000303224, 9.278109357271722146, 7.623553959385361622 ) ) ;
#64557=CARTESIAN_POINT ( 'NONE',  ( 24.53429010005800137, -12.47024913742999885, 3.026245653581999928 ) ) ;
#64574=CARTESIAN_POINT ( 'NONE',  ( 24.23080321643887558, -3.300949962372413005, -12.33052574769844156 ) ) ;
#64580=VERTEX_POINT ( 'NONE', #15842 ) ;
#64583=CONICAL_SURFACE ( 'NONE', #37797, 12.42515511468000078, 0.7854106315584118425 ) ;
#64584=CARTESIAN_POINT ( 'NONE',  ( 17.10000442166958123, -12.52500000000000036, -4.938443340346877723E-11 ) ) ;
#64589=CARTESIAN_POINT ( 'NONE',  ( 23.74239655349000344, -13.04589975639999899, 3.828642821684999920 ) ) ;
#64591=FACE_OUTER_BOUND ( 'NONE', #492, .T. ) ;
#64597=CARTESIAN_POINT ( 'NONE',  ( 17.79514046837899954, 3.190852705101999920, -11.45040944101999969 ) ) ;
#64599=AXIS2_PLACEMENT_3D ( 'NONE', #40780, #62103, #28942 ) ;
#64604=CARTESIAN_POINT ( 'NONE',  ( 23.52037815668899867, -10.38720552913000006, -9.576763669727000661 ) ) ;
#64605=CARTESIAN_POINT ( 'NONE',  ( 24.08682485015900099, -9.259169203442999319, 9.302355310768000152 ) ) ;
#64618=DIRECTION ( 'NONE',  ( -1.000000000000000000, 0.000000000000000000, 0.000000000000000000 ) ) ;
#64622=VECTOR ( 'NONE', #69175, 999.9999999999998863 ) ;
#64628=CARTESIAN_POINT ( 'NONE',  ( 24.53003472522700434, 12.09081557278000041, -3.147842171699999803 ) ) ;
#64631=CARTESIAN_POINT ( 'NONE',  ( 12.83560584653800163, -12.04942283913000090, 3.198386977700000244 ) ) ;
#64637=CARTESIAN_POINT ( 'NONE',  ( 24.92845787801541491, -11.55909985197292222, -3.214028671284849370 ) ) ;
#64652=CARTESIAN_POINT ( 'NONE',  ( 23.80820421035304335, 9.703756284516773079, 9.420712133314477654 ) ) ;
#64653=ORIENTED_EDGE ( 'NONE', *, *, #9293, .T. ) ;
#64661=CARTESIAN_POINT ( 'NONE',  ( 14.04809435262700035, 9.134678144910999720, 8.215103563399999587 ) ) ;
#64677=VERTEX_POINT ( 'NONE', #2870 ) ;
#64694=LINE ( 'NONE', #33247, #40846 ) ;
#64699=CARTESIAN_POINT ( 'NONE',  ( 23.67741258883705768, -9.992411001872515186, -9.459257071873569345 ) ) ;
#64700=CARTESIAN_POINT ( 'NONE',  ( 12.33432433144335505, -11.58110100107811746, 4.770114854519521330 ) ) ;
#64701=DIRECTION ( 'NONE',  ( 0.000000000000000000, 0.9867381147929490393, 0.1623203401144079905 ) ) ;
#64709=CARTESIAN_POINT ( 'NONE',  ( 18.30003129334700063, -2.732683817159999862, 11.53064095410000078 ) ) ;
#64712=PLANE ( 'NONE',  #29747 ) ;
#64713=DIRECTION ( 'NONE',  ( 0.000000000000000000, -0.6664713972123997854, 0.7455306007789026523 ) ) ;
#64719=CARTESIAN_POINT ( 'NONE',  ( 23.80948321181408289, 9.702294094131053370, -9.418753252065425130 ) ) ;
#64727=VERTEX_POINT ( 'NONE', #44848 ) ;
#64731=CARTESIAN_POINT ( 'NONE',  ( 24.30001120144517301, -3.256147830695084178, 12.15210914111320939 ) ) ;
#64738=CARTESIAN_POINT ( 'NONE',  ( 13.46001156276200028, 11.65487838447000080, 2.352687191044000148 ) ) ;
#64741=ORIENTED_EDGE ( 'NONE', *, *, #52495, .F. ) ;
#64742=AXIS2_PLACEMENT_3D ( 'NONE', #52104, #20296, #63627 ) ;
#64744=ORIENTED_EDGE ( 'NONE', *, *, #36134, .F. ) ;
#64751=CARTESIAN_POINT ( 'NONE',  ( 23.89320776801300283, -8.928716006283003992, -8.952507060077003587 ) ) ;
#64759=CARTESIAN_POINT ( 'NONE',  ( 17.96055895400804303, 12.10036481531685837, -3.233715407583658052 ) ) ;
#64763=ORIENTED_EDGE ( 'NONE', *, *, #50188, .T. ) ;
#64777=ORIENTED_EDGE ( 'NONE', *, *, #67215, .F. ) ;
#64787=AXIS2_PLACEMENT_3D ( 'NONE', #51053, #18901, #29057 ) ;
#64790=B_SPLINE_SURFACE_WITH_KNOTS ( 'NONE', 3, 3, ( 
 ( #21320, #31145, #20983, #53140 ),
 ( #68514, #63268, #37402, #52447 ),
 ( #20636, #41962, #36025, #47903 ),
 ( #32171, #37065, #15399, #42320 ),
 ( #36725, #10146, #15737, #9443 ),
 ( #62586, #42648, #63959, #58377 ),
 ( #30787, #16069, #58723, #10827 ),
 ( #3854, #46524, #19952, #14708 ) ),
 .UNSPECIFIED., .F., .F., .F.,
 ( 4, 1, 1, 1, 1, 4 ),
 ( 4, 4 ),
 ( 0.7453059214372000918, 0.7647058823529000460, 0.8235294117646999590, 0.8823529411764999830, 0.9411764705882000870, 0.9905827220917999831 ),
 ( -0.1830915291640000109, 1.182948984815999971 ),
 .UNSPECIFIED. ) ;
#64792=CARTESIAN_POINT ( 'NONE',  ( 24.26682857475500299, -3.229948578041999863, 12.20213974738999951 ) ) ;
#64793=CARTESIAN_POINT ( 'NONE',  ( 13.50018479229300006, -11.60142623882999935, -2.415183939829000259 ) ) ;
#64795=DIRECTION ( 'NONE',  ( 0.000000000000000000, 0.5000000000000168754, -0.8660254037844288266 ) ) ;
#64796=CARTESIAN_POINT ( 'NONE',  ( 25.29574836898500223, -8.389549047707998142, 8.302753013563000550 ) ) ;
#64803=DIRECTION ( 'NONE',  ( 0.000000000000000000, 0.9999830366945593463, 0.005824630728861762523 ) ) ;
#64805=CARTESIAN_POINT ( 'NONE',  ( 13.32310803393400178, 12.20807901729000022, 2.049767542799999731 ) ) ;
#64806=ORIENTED_EDGE ( 'NONE', *, *, #11821, .T. ) ;
#64809=ORIENTED_EDGE ( 'NONE', *, *, #37952, .T. ) ;
#64810=CARTESIAN_POINT ( 'NONE',  ( 23.60000000000000142, 11.85420044612000012, -3.901016762742000488 ) ) ;
#64811=CARTESIAN_POINT ( 'NONE',  ( 25.29995734509200034, 8.533537492639000632, -7.925519463018001254 ) ) ;
#64815=CARTESIAN_POINT ( 'NONE',  ( 23.72390811943373023, -13.12880825172584309, 3.830220858725267519 ) ) ;
#64818=EDGE_CURVE ( 'NONE', #40442, #47396, #56396, .T. ) ;
#64823=CARTESIAN_POINT ( 'NONE',  ( 24.98632903739299849, 11.60054622243000111, -3.134150054602000246 ) ) ;
#64827=B_SPLINE_CURVE_WITH_KNOTS ( 'NONE', 3,
 ( #55094, #24572, #66868, #18981 ),
 .UNSPECIFIED., .F., .F.,
 ( 4, 4 ),
 ( 0.000000000000000000, 1.000000000000000000 ),
 .UNSPECIFIED. ) ;
#64828=ORIENTED_EDGE ( 'NONE', *, *, #1974, .F. ) ;
#64833=AXIS2_PLACEMENT_3D ( 'NONE', #60400, #12505, #43637 ) ;
#64835=CARTESIAN_POINT ( 'NONE',  ( 24.71800983586086886, 11.77345325639867113, -3.190795111280438690 ) ) ;
#64836=CARTESIAN_POINT ( 'NONE',  ( 25.29986734212600297, -2.596989636639000398, 11.35306351421000137 ) ) ;
#64841=CARTESIAN_POINT ( 'NONE',  ( 18.47744389612467941, -11.93152012402699391, 3.811457427748914384 ) ) ;
#64846=CARTESIAN_POINT ( 'NONE',  ( 24.78225916701600440, -3.612170063153999688, 12.07974787419999885 ) ) ;
#64867=FACE_OUTER_BOUND ( 'NONE', #43995, .T. ) ;
#64869=VECTOR ( 'NONE', #57477, 1000.000000000000000 ) ;
#64873=B_SPLINE_CURVE_WITH_KNOTS ( 'NONE', 3,
 ( #49355, #60547, #11953, #65433 ),
 .UNSPECIFIED., .F., .F.,
 ( 4, 4 ),
 ( 0.000000000000000000, 1.000000000000000000 ),
 .UNSPECIFIED. ) ;
#64877=ORIENTED_EDGE ( 'NONE', *, *, #67709, .F. ) ;
#64892=CARTESIAN_POINT ( 'NONE',  ( 11.80890711774500090, 11.72268911462999874, 1.968096114907999628 ) ) ;
#64895=CARTESIAN_POINT ( 'NONE',  ( 16.34806348789000197, 3.378436248652000096, 11.11006988061000023 ) ) ;
#64898=ORIENTED_EDGE ( 'NONE', *, *, #44678, .T. ) ;
#64901=EDGE_CURVE ( 'NONE', #41440, #28381, #9349, .T. ) ;
#64915=CARTESIAN_POINT ( 'NONE',  ( 24.30000000000000071, 0.000000000000000000, 0.000000000000000000 ) ) ;
#64928=CARTESIAN_POINT ( 'NONE',  ( 23.81896843540200237, 12.91808259626999877, 3.708628114615999838 ) ) ;
#64931=ORIENTED_EDGE ( 'NONE', *, *, #19735, .T. ) ;
#64933=EDGE_CURVE ( 'NONE', #56058, #6251, #56234, .T. ) ;
#64938=CARTESIAN_POINT ( 'NONE',  ( 17.88015371777900242, 3.314513509857999640, -11.22393657228000130 ) ) ;
#64941=AXIS2_PLACEMENT_3D ( 'NONE', #62695, #5004, #42071 ) ;
#64942=CARTESIAN_POINT ( 'NONE',  ( 23.64839641905800249, -10.02576512143000009, -9.635306756802998862 ) ) ;
#64944=CARTESIAN_POINT ( 'NONE',  ( 11.71289336965100070, -3.191014699919000108, 11.45041132747999946 ) ) ;
#64949=EDGE_CURVE ( 'NONE', #7451, #2756, #37264, .T. ) ;
#64953=B_SPLINE_CURVE_WITH_KNOTS ( 'NONE', 3,
 ( #40062, #13148, #19060, #23284 ),
 .UNSPECIFIED., .F., .F.,
 ( 4, 4 ),
 ( 0.000000000000000000, 1.000000000000000000 ),
 .UNSPECIFIED. ) ;
#64959=CARTESIAN_POINT ( 'NONE',  ( 24.63332956304826737, -10.83443035036254365, 3.855530959951017689 ) ) ;
#64960=ORIENTED_EDGE ( 'NONE', *, *, #33142, .F. ) ;
#64967=CARTESIAN_POINT ( 'NONE',  ( 24.54687940532799928, 12.52318695592999909, -3.000795290450999797 ) ) ;
#64968=CARTESIAN_POINT ( 'NONE',  ( 12.11132301796900101, -11.62873132690000055, 4.501748577889000735 ) ) ;
#64979=ORIENTED_EDGE ( 'NONE', *, *, #2457, .F. ) ;
#64987=CARTESIAN_POINT ( 'NONE',  ( 23.60205915885299888, 11.53346724329999873, 4.150849519424002487 ) ) ;
#64989=EDGE_LOOP ( 'NONE', ( #5508, #38933, #68627, #27097 ) ) ;
#64996=CARTESIAN_POINT ( 'NONE',  ( 17.60804966294600149, -11.49744311106999994, 4.819470927255000703 ) ) ;
#64998=CARTESIAN_POINT ( 'NONE',  ( 13.73899430609700190, 9.712898924749000074, 7.967785796560000300 ) ) ;
#65003=ORIENTED_EDGE ( 'NONE', *, *, #36236, .T. ) ;
#65004=CARTESIAN_POINT ( 'NONE',  ( 24.35365242081699932, -10.79182034089001796, 4.028979492054000744 ) ) ;
#65006=CARTESIAN_POINT ( 'NONE',  ( 11.44793382097000034, 12.36841772234000025, 1.594008128907999922 ) ) ;
#65018=CARTESIAN_POINT ( 'NONE',  ( 24.50549018585800098, -3.501736898117000063, -12.23514954116999931 ) ) ;
#65029=CARTESIAN_POINT ( 'NONE',  ( 18.48260618742725470, -3.086131726334561343, -12.13914505220688689 ) ) ;
#65034=CARTESIAN_POINT ( 'NONE',  ( 24.97036913652599210, 11.51451018643214042, 3.225694753612683652 ) ) ;
#65042=CARTESIAN_POINT ( 'NONE',  ( 12.35268573730777675, -12.09127048605781241, 3.267865047145097179 ) ) ;
#65043=CARTESIAN_POINT ( 'NONE',  ( 24.37816253747470441, -3.385900881186148847, -12.24459612271480502 ) ) ;
#65046=CARTESIAN_POINT ( 'NONE',  ( 23.83543860380300217, 3.383577400584000028, -13.10464564587000069 ) ) ;
#65052=CARTESIAN_POINT ( 'NONE',  ( 13.99999999347100044, -9.187456302440001110, -8.213201953411001455 ) ) ;
#65059=B_SPLINE_CURVE_WITH_KNOTS ( 'NONE', 3,
 ( #528, #31318, #32015, #4385, #42493, #21843, #53329, #10326, #36212, #68355, #52290, #47397, #52630, #57528, #9632, #47053, #26070, #20818 ),
 .UNSPECIFIED., .F., .F.,
 ( 4, 2, 1, 2, 2, 2, 1, 2, 2, 4 ),
 ( 0.000000000000000000, 0.2499999999999804601, 0.3749999999999698019, 0.4374999999999593658, 0.4999999999999489297, 0.6249999999999243938, 0.6874999999999182876, 0.7187499999999220623, 0.7499999999999258371, 1.000000000000000000 ),
 .UNSPECIFIED. ) ;
#65060=CARTESIAN_POINT ( 'NONE',  ( 18.50001572531400029, -0.9783175529277773341, -12.52499999999999503 ) ) ;
#65061=CARTESIAN_POINT ( 'NONE',  ( 21.60000000000000142, 0.000000000000000000, 0.000000000000000000 ) ) ;
#65066=VECTOR ( 'NONE', #24733, 999.9999999999998863 ) ;
#65073=EDGE_CURVE ( 'NONE', #60256, #40899, #24700, .T. ) ;
#65075=EDGE_CURVE ( 'NONE', #20439, #57654, #18304, .T. ) ;
#65107=VERTEX_POINT ( 'NONE', #47585 ) ;
#65111=CARTESIAN_POINT ( 'NONE',  ( 29.91622776632000225, -7.451149524158998971E-09, 6.772075922106999712 ) ) ;
#65113=CARTESIAN_POINT ( 'NONE',  ( 24.30001680106099826, 12.21047197645999915, -3.271805488357999891 ) ) ;
#65123=B_SPLINE_CURVE_WITH_KNOTS ( 'NONE', 3,
 ( #26717, #16555, #22486, #480, #43828, #48372 ),
 .UNSPECIFIED., .F., .F.,
 ( 4, 2, 4 ),
 ( 0.000000000000000000, 0.5000000000000000000, 1.000000000000000000 ),
 .UNSPECIFIED. ) ;
#65131=CARTESIAN_POINT ( 'NONE',  ( 11.83936489023500194, 3.414328975993000004, -11.89720897182000137 ) ) ;
#65139=B_SPLINE_CURVE_WITH_KNOTS ( 'NONE', 3,
 ( #47520, #51723, #30752, #14674 ),
 .UNSPECIFIED., .F., .F.,
 ( 4, 4 ),
 ( 0.000000000000000000, 1.000000000000000000 ),
 .UNSPECIFIED. ) ;
#65143=CARTESIAN_POINT ( 'NONE',  ( 24.84742924726900171, -8.571349809962997668, 8.858692393521000241 ) ) ;
#65145=EDGE_LOOP ( 'NONE', ( #63128, #2474, #55643, #15711 ) ) ;
#65146=FACE_OUTER_BOUND ( 'NONE', #11338, .T. ) ;
#65149=DIRECTION ( 'NONE',  ( 0.000000000000000000, -0.7180577844781753649, -0.6959834898546763959 ) ) ;
#65152=CARTESIAN_POINT ( 'NONE',  ( 13.43590051321700152, 12.19118104410000036, 2.154281854449000555 ) ) ;
#65154=CARTESIAN_POINT ( 'NONE',  ( 24.35365242081699932, 8.948887819794997256, 8.923422014253004519 ) ) ;
#65158=CARTESIAN_POINT ( 'NONE',  ( 24.76116842704180598, 8.629365340259456119, -8.563010230132558576 ) ) ;
#65161=CARTESIAN_POINT ( 'NONE',  ( 17.60000003185799855, -12.11983897296999935, 3.159727888982000188 ) ) ;
#65171=DIRECTION ( 'NONE',  ( 0.000000000000000000, 0.000000000000000000, -1.000000000000000000 ) ) ;
#65175=CARTESIAN_POINT ( 'NONE',  ( 11.30000000000000071, -3.738146657027650033, 11.41167835205686742 ) ) ;
#65182=CARTESIAN_POINT ( 'NONE',  ( 24.90037535684063741, 11.58835108095975563, -3.208324347671906995 ) ) ;
#65186=ORIENTED_EDGE ( 'NONE', *, *, #42149, .T. ) ;
#65190=CARTESIAN_POINT ( 'NONE',  ( 18.04298231209847359, -12.08956857263229168, 3.273859435796452999 ) ) ;
#65196=CARTESIAN_POINT ( 'NONE',  ( 25.41802129974299973, -2.807511311350999961, 11.31773419928000024 ) ) ;
#65201=AXIS2_PLACEMENT_3D ( 'NONE', #5739, #4362, #15889 ) ;
#65207=CARTESIAN_POINT ( 'NONE',  ( 25.27002764979846816, 8.359940994488436417, -8.486676288913415078 ) ) ;
#65209=DIRECTION ( 'NONE',  ( 0.000000000000000000, 0.9466492601157000530, -0.3222656952305000266 ) ) ;
#65210=DIRECTION ( 'NONE',  ( 0.000000000000000000, -0.9466492601157000530, 0.3222656952305000266 ) ) ;
#65211=CARTESIAN_POINT ( 'NONE',  ( 24.30857393632600250, -8.915481952665000875, -8.861377372684998477 ) ) ;
#65212=EDGE_CURVE ( 'NONE', #31626, #10089, #30581, .T. ) ;
#65215=B_SPLINE_SURFACE_WITH_KNOTS ( 'NONE', 3, 3, ( 
 ( #68146, #51396, #46154, #62899 ),
 ( #9764, #68837, #37037, #57660 ),
 ( #40904, #31115, #58352, #25852 ),
 ( #20609, #62225, #31449, #10454 ),
 ( #68486, #35666, #36695, #56981 ),
 ( #15019, #62561, #3491, #57317 ),
 ( #4861, #19925, #9417, #41934 ),
 ( #24827, #9084, #52419, #58016 ),
 ( #52768, #26204, #30423, #51733 ) ),
 .UNSPECIFIED., .F., .F., .F.,
 ( 4, 1, 1, 1, 1, 1, 4 ),
 ( 4, 4 ),
 ( 0.05214259105098999897, 0.1666666666667000196, 0.3333333333333000081, 0.5000000000000000000, 0.6666666666667000474, 0.8333333333333000637, 0.9777068595523999983 ),
 ( -0.1900882580235000174, 1.190231865545000156 ),
 .UNSPECIFIED. ) ;
#65221=DIRECTION ( 'NONE',  ( 0.000000000000000000, -1.000000000000000000, 0.000000000000000000 ) ) ;
#65224=CARTESIAN_POINT ( 'NONE',  ( 23.60205915885299888, 9.230633470682002795, -8.204162215359994903 ) ) ;
#65228=B_SPLINE_SURFACE_WITH_KNOTS ( 'NONE', 3, 3, ( 
 ( #33924, #55245, #17135, #39509 ),
 ( #22382, #65723, #28684, #65374 ),
 ( #49650, #17847, #44073, #6997 ),
 ( #49298, #11893, #65018, #1755 ),
 ( #33233, #38470, #50001, #22727 ),
 ( #5955, #59790, #54897, #33577 ) ),
 .UNSPECIFIED., .F., .F., .F.,
 ( 4, 1, 1, 4 ),
 ( 4, 4 ),
 ( 0.1423941366080999915, 0.3333333333333000081, 0.6666666666667000474, 0.8219462302419999755 ),
 ( -0.1256563615234000120, 1.125656361508000192 ),
 .UNSPECIFIED. ) ;
#65231=EDGE_LOOP ( 'NONE', ( #24236, #2865, #47999, #22796 ) ) ;
#65237=VERTEX_POINT ( 'NONE', #59781 ) ;
#65247=VERTEX_POINT ( 'NONE', #11885 ) ;
#65249=CARTESIAN_POINT ( 'NONE',  ( 16.39965637475000193, 3.313349101483999970, 11.22428178643999885 ) ) ;
#65251=ORIENTED_EDGE ( 'NONE', *, *, #19128, .F. ) ;
#65252=CARTESIAN_POINT ( 'NONE',  ( 15.58179592144909265, -8.803826609191874653, -7.629963841725977858 ) ) ;
#65259=VERTEX_POINT ( 'NONE', #54544 ) ;
#65263=AXIS2_PLACEMENT_3D ( 'NONE', #46097, #13945, #18156 ) ;
#65265=CARTESIAN_POINT ( 'NONE',  ( 15.39403162610500075, -9.133592062008998980, -8.216350050208999889 ) ) ;
#65277=ORIENTED_EDGE ( 'NONE', *, *, #51471, .F. ) ;
#65278=ADVANCED_FACE ( 'NONE', ( #39156 ), #48891, .F. ) ;
#65280=CARTESIAN_POINT ( 'NONE',  ( 11.80427293869800032, -12.43391773449000048, -1.801004847141999932 ) ) ;
#65286=CARTESIAN_POINT ( 'NONE',  ( 24.15333686126099977, 12.81676537908000135, 3.250112501260999931 ) ) ;
#65293=CARTESIAN_POINT ( 'NONE',  ( 18.18404792230800382, 3.205001206845999651, -11.25648540289999922 ) ) ;
#65295=B_SPLINE_CURVE_WITH_KNOTS ( 'NONE', 3,
 ( #56078, #2591, #23922, #18681 ),
 .UNSPECIFIED., .F., .F.,
 ( 4, 4 ),
 ( 0.000000000000000000, 1.000000000000000000 ),
 .UNSPECIFIED. ) ;
#65297=VECTOR ( 'NONE', #20055, 1000.000000000000000 ) ;
#65298=CARTESIAN_POINT ( 'NONE',  ( 24.13718290469899941, -9.106000876233000696, -8.983949862985999957 ) ) ;
#65299=CARTESIAN_POINT ( 'NONE',  ( 24.33639158961700133, -8.941349246732999134, 9.047440025103000494 ) ) ;
#65302=EDGE_LOOP ( 'NONE', ( #43377, #36895, #20258, #40821 ) ) ;
#65309=B_SPLINE_CURVE_WITH_KNOTS ( 'NONE', 3,
 ( #40406, #3001, #65596, #40084 ),
 .UNSPECIFIED., .F., .F.,
 ( 4, 4 ),
 ( 0.000000000000000000, 1.000000000000000000 ),
 .UNSPECIFIED. ) ;
#65310=CARTESIAN_POINT ( 'NONE',  ( 25.47132134066600173, 2.701728734476000149, -11.27934147707000179 ) ) ;
#65313=CARTESIAN_POINT ( 'NONE',  ( 25.50734665507583188, -11.18386470588408876, 3.138222106905402597 ) ) ;
#65314=ORIENTED_EDGE ( 'NONE', *, *, #2457, .T. ) ;
#65321=CARTESIAN_POINT ( 'NONE',  ( 11.30000000000000071, 0.000000000000000000, 0.000000000000000000 ) ) ;
#65323=CARTESIAN_POINT ( 'NONE',  ( 12.29459504890700039, -12.00990144118000025, 3.349639255392000248 ) ) ;
#65327=CARTESIAN_POINT ( 'NONE',  ( 23.64816362642000414, 3.331185260057999642, 13.50063194398999933 ) ) ;
#65329=ORIENTED_EDGE ( 'NONE', *, *, #59478, .T. ) ;
#65330=CARTESIAN_POINT ( 'NONE',  ( 24.23080253867526679, -9.028074447669709457, 9.023970195626347390 ) ) ;
#65345=CARTESIAN_POINT ( 'NONE',  ( 23.89320776801300283, 10.75689324692999804, 4.023240149044999825 ) ) ;
#65346=CARTESIAN_POINT ( 'NONE',  ( 23.56664318980499928, 10.37807351222000030, 9.381504534996999212 ) ) ;
#65347=ORIENTED_EDGE ( 'NONE', *, *, #64483, .F. ) ;
#65349=CIRCLE ( 'NONE', #47554, 1.000000000000000666 ) ;
#65355=CARTESIAN_POINT ( 'NONE',  ( 13.59022209853100094, 9.429754002912000388, 8.017367994085999428 ) ) ;
#65361=EDGE_CURVE ( 'NONE', #43628, #15277, #66489, .T. ) ;
#65364=CARTESIAN_POINT ( 'NONE',  ( 11.53681706333000179, 12.46890164658000089, 1.535189833763999978 ) ) ;
#65365=EDGE_CURVE ( 'NONE', #31118, #22245, #21628, .T. ) ;
#65367=CARTESIAN_POINT ( 'NONE',  ( 13.49980696793000057, -9.514462421839999351, -7.834836582454001608 ) ) ;
#65374=CARTESIAN_POINT ( 'NONE',  ( 24.70869262301700076, -3.610540981815000272, -12.15034266584999934 ) ) ;
#65376=B_SPLINE_SURFACE_WITH_KNOTS ( 'NONE', 3, 3, ( 
 ( #5383, #7027, #54581, #60514 ),
 ( #23103, #65750, #12281, #1440 ),
 ( #6676, #61210, #39539, #42790 ),
 ( #44104, #11922, #33263, #66096 ),
 ( #17162, #45132, #28712, #12978 ),
 ( #18563, #13327, #38495, #28362 ),
 ( #39890, #17522, #34651, #59818 ),
 ( #26722, #140, #64100, #50029 ),
 ( #65403, #60175, #49678, #33607 ),
 ( #1787, #60861, #17874, #39191 ) ),
 .UNSPECIFIED., .F., .F., .F.,
 ( 4, 1, 1, 1, 1, 1, 1, 4 ),
 ( 4, 4 ),
 ( 0.07203983506772999867, 0.1428571428570999946, 0.2857142857143000203, 0.4285714285713999594, 0.5714285714286000406, 0.7142857142856999797, 0.8571428571429000609, 0.9589780836993999635 ),
 ( -0.1900620218102000158, 1.190128522698000069 ),
 .UNSPECIFIED. ) ;
#65386=DIRECTION ( 'NONE',  ( 0.000000000000000000, -0.3380467785883188858, -0.9411293085894520960 ) ) ;
#65388=CARTESIAN_POINT ( 'NONE',  ( 25.26126930374652346, 11.18199973298772498, 3.383911755808009403 ) ) ;
#65390=CARTESIAN_POINT ( 'NONE',  ( 16.40000000000000213, -14.76315775485999993, -50.50083396221000243 ) ) ;
#65393=B_SPLINE_CURVE_WITH_KNOTS ( 'NONE', 3,
 ( #10677, #6114, #49116, #32025, #11362, #32366, #38984, #65536, #5440, #48089, #193, #5773, #21510, #42843 ),
 .UNSPECIFIED., .F., .F.,
 ( 4, 2, 2, 2, 2, 2, 4 ),
 ( 0.000000000000000000, 0.1249999999999986955, 0.2499999999999973910, 0.4999999999999992228, 0.6249999999999998890, 0.7500000000000005551, 1.000000000000000000 ),
 .UNSPECIFIED. ) ;
#65397=CARTESIAN_POINT ( 'NONE',  ( 12.74229120054538811, -12.11986439831272655, 3.159827838237132092 ) ) ;
#65403=CARTESIAN_POINT ( 'NONE',  ( 13.73936233968600185, -12.30487262812000004, -2.534071019599000163 ) ) ;
#65406=DIRECTION ( 'NONE',  ( 1.000000000000000000, 0.000000000000000000, 0.000000000000000000 ) ) ;
#65408=DIRECTION ( 'NONE',  ( 0.9999999999889699343, -2.769066800191914947E-06, -3.793722030192884931E-06 ) ) ;
#65411=CARTESIAN_POINT ( 'NONE',  ( 25.60000000000000142, -2.023988666086999899, -11.01546541709000060 ) ) ;
#65418=CARTESIAN_POINT ( 'NONE',  ( 24.35146665670700017, 12.30647607894000117, 3.205652257177999953 ) ) ;
#65422=ORIENTED_EDGE ( 'NONE', *, *, #24808, .T. ) ;
#65424=ORIENTED_EDGE ( 'NONE', *, *, #62427, .F. ) ;
#65430=CARTESIAN_POINT ( 'NONE',  ( 23.75089607250696133, 3.269771166517764449, -13.22954999995908487 ) ) ;
#65433=CARTESIAN_POINT ( 'NONE',  ( 24.30000000000000071, -8.810505093353000916, -8.810505093353000916 ) ) ;
#65434=CARTESIAN_POINT ( 'NONE',  ( 17.33333333119166753, -3.345268056437868953, -11.86064107241928234 ) ) ;
#65435=CARTESIAN_POINT ( 'NONE',  ( 11.64596081258699911, 3.342173145742999729, -11.21570452027999920 ) ) ;
#65437=CARTESIAN_POINT ( 'NONE',  ( 25.49994615399570819, -8.603880941064405263, -7.325437794649179324 ) ) ;
#65444=ORIENTED_EDGE ( 'NONE', *, *, #4916, .T. ) ;
#65447=ADVANCED_FACE ( 'NONE', ( #13969 ), #10905, .F. ) ;
#65454=ORIENTED_EDGE ( 'NONE', *, *, #39309, .F. ) ;
#65455=CARTESIAN_POINT ( 'NONE',  ( 12.82764013820600013, 11.38891548326999903, -4.574441164091999745 ) ) ;
#65457=CARTESIAN_POINT ( 'NONE',  ( 23.55651145941100211, -3.262678050158999810, -13.70323023102000093 ) ) ;
#65463=CARTESIAN_POINT ( 'NONE',  ( 23.73952225791441606, 3.508702178794984139, 13.37374633488916054 ) ) ;
#65464=DIRECTION ( 'NONE',  ( -4.468462273946190507E-09, 0.2714605545367115846, -0.9624495661231402543 ) ) ;
#65465=FACE_OUTER_BOUND ( 'NONE', #19392, .T. ) ;
#65471=DIRECTION ( 'NONE',  ( -0.7071101187282218259, 0.000000000000000000, -0.7071034436291199210 ) ) ;
#65473=EDGE_LOOP ( 'NONE', ( #18564, #67734, #33754, #60457, #47293 ) ) ;
#65478=EDGE_CURVE ( 'NONE', #66938, #27264, #50650, .T. ) ;
#65483=CARTESIAN_POINT ( 'NONE',  ( 11.83124374198900064, 3.528976724670999765, -11.96046730081999954 ) ) ;
#65490=CARTESIAN_POINT ( 'NONE',  ( 25.30000327618300204, 8.756202924575998026, 7.455126447192999883 ) ) ;
#65493=CARTESIAN_POINT ( 'NONE',  ( 13.99999999231800096, 8.833253877201999060, 7.896562762484000686 ) ) ;
#65494=CARTESIAN_POINT ( 'NONE',  ( 25.08240868301900406, -8.543484405703001272, 8.158957461736999761 ) ) ;
#65499=FACE_OUTER_BOUND ( 'NONE', #11943, .T. ) ;
#65501=CARTESIAN_POINT ( 'NONE',  ( 24.87966566241900068, -8.586230768662000301, -8.375222081007999364 ) ) ;
#65511=CARTESIAN_POINT ( 'NONE',  ( 17.92913687483822116, 3.216295279492294767, 11.40344415251901644 ) ) ;
#65512=CARTESIAN_POINT ( 'NONE',  ( 15.46873602477000276, 8.828190495471000432, 7.821444125541998638 ) ) ;
#65517=ORIENTED_EDGE ( 'NONE', *, *, #1760, .T. ) ;
#65531=DIRECTION ( 'NONE',  ( 0.000000000000000000, 0.9421243786071880066, -0.3352635608502960163 ) ) ;
#65532=CARTESIAN_POINT ( 'NONE',  ( 11.74267124137200113, -11.57041781403000158, -1.757356211607000063 ) ) ;
#65536=CARTESIAN_POINT ( 'NONE',  ( 13.52727141073796169, -12.35275327559112490, -2.070326479556442667 ) ) ;
#65547=B_SPLINE_CURVE_WITH_KNOTS ( 'NONE', 3,
 ( #31414, #26168, #37340, #25817 ),
 .UNSPECIFIED., .F., .F.,
 ( 4, 4 ),
 ( 0.000000000000000000, 1.000000000000000000 ),
 .UNSPECIFIED. ) ;
#65563=ADVANCED_FACE ( 'NONE', ( #11803 ), #61817, .F. ) ;
#65568=ORIENTED_EDGE ( 'NONE', *, *, #5998, .T. ) ;
#65582=CARTESIAN_POINT ( 'NONE',  ( 24.52301487334444730, -12.12194136125221888, 3.142914510258483229 ) ) ;
#65583=CARTESIAN_POINT ( 'NONE',  ( 23.60000333624175184, -13.25018707633487658, -4.190178083890355509 ) ) ;
#65589=CARTESIAN_POINT ( 'NONE',  ( 24.57937622088081042, -8.815984698211464021, 9.246564899790328695 ) ) ;
#65590=VECTOR ( 'NONE', #4615, 1000.000000000000000 ) ;
#65596=CARTESIAN_POINT ( 'NONE',  ( 15.96683822361880090, -3.674392175451292264, -11.19597380828251687 ) ) ;
#65597=CARTESIAN_POINT ( 'NONE',  ( 16.07059379716000080, 3.381060347337999872, 11.29912544500000138 ) ) ;
#65602=AXIS2_PLACEMENT_3D ( 'NONE', #18475, #13583, #50975 ) ;
#65606=ORIENTED_EDGE ( 'NONE', *, *, #23935, .T. ) ;
#65608=CARTESIAN_POINT ( 'NONE',  ( 24.42335427832999883, -12.73360904536999882, -3.018931263375000285 ) ) ;
#65609=CARTESIAN_POINT ( 'NONE',  ( 15.39046541331000029, -9.526477069417000010, -8.190982836632000996 ) ) ;
#65612=ADVANCED_FACE ( 'NONE', ( #39418 ), #16492, .F. ) ;
#65614=CARTESIAN_POINT ( 'NONE',  ( 24.67921580316900076, -12.29514843751999997, 2.979196179828000002 ) ) ;
#65616=CARTESIAN_POINT ( 'NONE',  ( 24.30000000000000071, 8.810505093353000916, 8.810505093353000916 ) ) ;
#65628=AXIS2_PLACEMENT_3D ( 'NONE', #51316, #52342, #62481 ) ;
#65630=CARTESIAN_POINT ( 'NONE',  ( 23.86797489265400074, 13.28660945761000001, 3.449435190502999848 ) ) ;
#65632=ORIENTED_EDGE ( 'NONE', *, *, #23148, .F. ) ;
#65637=CARTESIAN_POINT ( 'NONE',  ( 17.79999999998900151, -3.595165934733000057, 11.99793354950999991 ) ) ;
#65643=EDGE_CURVE ( 'NONE', #37994, #55008, #22281, .T. ) ;
#65645=CARTESIAN_POINT ( 'NONE',  ( 24.25865867642400175, -8.929940475172999825, 8.812671217186998973 ) ) ;
#65646=AXIS2_PLACEMENT_3D ( 'NONE', #56240, #55900, #39472 ) ;
#65654=CARTESIAN_POINT ( 'NONE',  ( 23.60205915885299888, -2.489696159912998752, 12.09604418629000122 ) ) ;
#65656=EDGE_LOOP ( 'NONE', ( #11431, #48263, #13318, #55538 ) ) ;
#65657=CARTESIAN_POINT ( 'NONE',  ( 24.95781717674400113, 3.530132479599000117, -11.86561275887000022 ) ) ;
#65669=CARTESIAN_POINT ( 'NONE',  ( 24.55996189763800075, 12.50738814877000138, -2.996555333880000394 ) ) ;
#65671=CARTESIAN_POINT ( 'NONE',  ( 12.52995381683800247, -11.92229088141000126, 3.300664210127000064 ) ) ;
#65678=CARTESIAN_POINT ( 'NONE',  ( 24.01967398689980371, -9.335314603828233970, 9.252502456888306526 ) ) ;
#65680=ORIENTED_EDGE ( 'NONE', *, *, #51382, .T. ) ;
#65681=DIRECTION ( 'NONE',  ( -1.000000000000000000, 0.000000000000000000, 0.000000000000000000 ) ) ;
#65682=ORIENTED_EDGE ( 'NONE', *, *, #48128, .T. ) ;
#65686=CARTESIAN_POINT ( 'NONE',  ( 24.08774000868300291, 12.68430291248000152, -3.366812948787999638 ) ) ;
#65691=CIRCLE ( 'NONE', #13266, 5.760713961201000544 ) ;
#65693=CARTESIAN_POINT ( 'NONE',  ( 23.56666365135700403, 11.61524011585000160, 3.333188920242000197 ) ) ;
#65701=CARTESIAN_POINT ( 'NONE',  ( 18.44490890441100106, -11.76218143194999755, 4.145213721498999249 ) ) ;
#65714=CARTESIAN_POINT ( 'NONE',  ( 24.38582837070600107, -3.342331292268000187, 12.19039702797000047 ) ) ;
#65718=DIRECTION ( 'NONE',  ( 2.887534672467944307E-10, -0.4812251768484908099, 0.8765970164032835799 ) ) ;
#65723=CARTESIAN_POINT ( 'NONE',  ( 24.51327040776200050, -3.324719603035999782, -12.06512239505999950 ) ) ;
#65734=EDGE_CURVE ( 'NONE', #7968, #56428, #24984, .T. ) ;
#65735=EDGE_CURVE ( 'NONE', #63935, #42844, #1350, .T. ) ;
#65736=DIRECTION ( 'NONE',  ( 1.000000000000000000, 0.000000000000000000, 0.000000000000000000 ) ) ;
#65737=CARTESIAN_POINT ( 'NONE',  ( 11.64444011870698148, -3.380850026685724430, 11.14878564716274667 ) ) ;
#65743=CARTESIAN_POINT ( 'NONE',  ( 18.29983863915590803, -0.9627071483039522093, 12.32514597438827941 ) ) ;
#65744=CARTESIAN_POINT ( 'NONE',  ( 16.40000000000000213, 14.76315775485999993, 50.50083396221000243 ) ) ;
#65750=CARTESIAN_POINT ( 'NONE',  ( 12.99165415090800124, -12.32813973498000060, -1.877091699536999947 ) ) ;
#65754=CARTESIAN_POINT ( 'NONE',  ( 12.38752622470988918, 11.20128320849600811, -3.203207420725545873 ) ) ;
#65760=FACE_OUTER_BOUND ( 'NONE', #27823, .T. ) ;
#65779=DIRECTION ( 'NONE',  ( -2.260144215113719931E-16, 0.3352635608502960163, -0.9421243786071880066 ) ) ;
#65780=CARTESIAN_POINT ( 'NONE',  ( 23.66004879239100234, 13.39256445865000167, -3.813547382634999483 ) ) ;
#65782=ADVANCED_FACE ( 'NONE', ( #22551 ), #38278, .F. ) ;
#65785=PLANE ( 'NONE',  #62359 ) ;
#65799=EDGE_LOOP ( 'NONE', ( #23680, #10891, #43443, #49349 ) ) ;
#65801=CARTESIAN_POINT ( 'NONE',  ( 17.60531108750599927, 11.81466229355000053, -3.323436300174000380 ) ) ;
#65802=CIRCLE ( 'NONE', #8915, 11.50000000000000178 ) ;
#65803=CARTESIAN_POINT ( 'NONE',  ( 24.38452244591600149, -3.342920588330999809, -12.19242501195000017 ) ) ;
#65839=CARTESIAN_POINT ( 'NONE',  ( 24.46580263708699832, -3.340075003801000086, 12.12245366788000034 ) ) ;
#65843=CARTESIAN_POINT ( 'NONE',  ( 25.18907852600200314, -8.466516726705998863, 8.230855237650001044 ) ) ;
#65845=EDGE_LOOP ( 'NONE', ( #10566, #32901, #19308, #11251 ) ) ;
#65848=CARTESIAN_POINT ( 'NONE',  ( 13.73849254682300192, -8.874722368053999944, -7.906926164786999500 ) ) ;
#65850=CIRCLE ( 'NONE', #35724, 9.250000000000000000 ) ;
#65855=CARTESIAN_POINT ( 'NONE',  ( 23.56666365135700403, 8.694246338441999455, 8.392498551189996547 ) ) ;
#65859=CARTESIAN_POINT ( 'NONE',  ( 24.77780384695583749, 8.621836997252826151, -8.548042839575236584 ) ) ;
#65861=CARTESIAN_POINT ( 'NONE',  ( 24.30001694391200218, -12.21047201246000036, 3.271805662802000025 ) ) ;
#65865=VERTEX_POINT ( 'NONE', #66240 ) ;
#65871=ORIENTED_EDGE ( 'NONE', *, *, #59699, .T. ) ;
#65877=CARTESIAN_POINT ( 'NONE',  ( 11.48831242699000121, -11.66400889920000061, -1.747256858593000173 ) ) ;
#65878=EDGE_CURVE ( 'NONE', #2543, #65237, #43083, .T. ) ;
#65887=CARTESIAN_POINT ( 'NONE',  ( 24.74074867997300231, 3.240101435799000118, 11.83468233123000068 ) ) ;
#65889=CARTESIAN_POINT ( 'NONE',  ( 25.52469074519600056, -2.886190667329999737, 11.27615698518999920 ) ) ;
#65890=ORIENTED_EDGE ( 'NONE', *, *, #39310, .T. ) ;
#65891=ORIENTED_EDGE ( 'NONE', *, *, #39541, .F. ) ;
#65901=CIRCLE ( 'NONE', #6756, 14.00000000000000355 ) ;
#65915=DIRECTION ( 'NONE',  ( 0.000000000000000000, 1.000000000000000000, 0.000000000000000000 ) ) ;
#65936=AXIS2_PLACEMENT_3D ( 'NONE', #2359, #30560, #24632 ) ;
#65941=CARTESIAN_POINT ( 'NONE',  ( 23.66004879239100234, -9.998910854163000295, -9.691527647852998584 ) ) ;
#65945=ORIENTED_EDGE ( 'NONE', *, *, #49708, .F. ) ;
#65947=CARTESIAN_POINT ( 'NONE',  ( 24.13681598081500113, -12.33402671357999836, -3.394326608267999923 ) ) ;
#65962=ORIENTED_EDGE ( 'NONE', *, *, #36133, .T. ) ;
#65971=CARTESIAN_POINT ( 'NONE',  ( 23.73948084457800078, 13.16333625243999883, 3.763513502666000043 ) ) ;
#65986=CARTESIAN_POINT ( 'NONE',  ( 24.13647503573200126, -9.107098899030999561, 8.984880450811999708 ) ) ;
#65987=CIRCLE ( 'NONE', #67094, 13.98989063587000281 ) ;
#65990=ORIENTED_EDGE ( 'NONE', *, *, #24217, .T. ) ;
#65994=CARTESIAN_POINT ( 'NONE',  ( 25.29987261391899978, -8.756202924575998026, 7.455126447192999883 ) ) ;
#65997=CARTESIAN_POINT ( 'NONE',  ( 25.58980614432099898, 2.739981116774000025, -11.22452184305999978 ) ) ;
#65999=EDGE_CURVE ( 'NONE', #2756, #45376, #8045, .T. ) ;
#66002=AXIS2_PLACEMENT_3D ( 'NONE', #17023, #60027, #43958 ) ;
#66011=CARTESIAN_POINT ( 'NONE',  ( 24.62769666374716238, 12.35739842157732937, 2.995926059509618877 ) ) ;
#66017=ORIENTED_EDGE ( 'NONE', *, *, #7422, .F. ) ;
#66018=CARTESIAN_POINT ( 'NONE',  ( 24.44496350777200178, -12.03536639536000052, -3.224849854974999985 ) ) ;
#66022=DIRECTION ( 'NONE',  ( 0.000000000000000000, 0.9617682669560660980, -0.2738645663029905530 ) ) ;
#66024=B_SPLINE_CURVE_WITH_KNOTS ( 'NONE', 3,
 ( #58605, #16982, #5470, #58956 ),
 .UNSPECIFIED., .F., .F.,
 ( 4, 4 ),
 ( 0.000000000000000000, 1.000000000000000000 ),
 .UNSPECIFIED. ) ;
#66027=CARTESIAN_POINT ( 'NONE',  ( 13.99999999231800096, 8.833253877201999060, 7.896562762484000686 ) ) ;
#66032=ORIENTED_EDGE ( 'NONE', *, *, #54312, .F. ) ;
#66036=CARTESIAN_POINT ( 'NONE',  ( 29.91622776632000225, 7.451147316196999408E-09, -6.772075922106999712 ) ) ;
#66040=CARTESIAN_POINT ( 'NONE',  ( 23.56666365135700403, 2.488348886664998538, -11.45224114467999499 ) ) ;
#66042=CARTESIAN_POINT ( 'NONE',  ( 18.26683600807099950, -11.61819309989999915, 4.528402979683000318 ) ) ;
#66046=EDGE_CURVE ( 'NONE', #47642, #63538, #29736, .T. ) ;
#66052=EDGE_CURVE ( 'NONE', #49024, #11162, #6233, .T. ) ;
#66056=CARTESIAN_POINT ( 'NONE',  ( 23.60205915885299888, -11.88166580723999921, 3.967996863072999147 ) ) ;
#66080=CARTESIAN_POINT ( 'NONE',  ( 24.53428993882599940, 8.855929947951999281, -9.286429770520999938 ) ) ;
#66089=DIRECTION ( 'NONE',  ( 0.000000000000000000, -0.9624505444715647506, 0.2714570858282915333 ) ) ;
#66091=CARTESIAN_POINT ( 'NONE',  ( 17.80000000001300009, 3.351264566333000072, 11.15757590352999884 ) ) ;
#66096=CARTESIAN_POINT ( 'NONE',  ( 13.15534550153200044, -12.11329499872000071, -2.052871598439000245 ) ) ;
#66101=AXIS2_PLACEMENT_3D ( 'NONE', #27296, #44425, #60487 ) ;
#66106=B_SPLINE_CURVE_WITH_KNOTS ( 'NONE', 3,
 ( #67683, #62449, #35886, #57201 ),
 .UNSPECIFIED., .F., .F.,
 ( 4, 4 ),
 ( 0.000000000000000000, 1.000000000000000000 ),
 .UNSPECIFIED. ) ;
#66107=CARTESIAN_POINT ( 'NONE',  ( 11.30000285318000230, -11.76356368987999979, -1.428410073821000159 ) ) ;
#66110=CARTESIAN_POINT ( 'NONE',  ( 18.49993212792200126, 2.908182645667999999, 12.18276646858999968 ) ) ;
#66113=CARTESIAN_POINT ( 'NONE',  ( 12.10000669845703847, -11.02846243759423039, 3.754394857303111621 ) ) ;
#66116=B_SPLINE_CURVE_WITH_KNOTS ( 'NONE', 3,
 ( #46663, #41411, #15527, #41066, #47002, #62385 ),
 .UNSPECIFIED., .F., .F.,
 ( 4, 2, 4 ),
 ( 0.000000000000000000, 0.5000000000000000000, 1.000000000000000000 ),
 .UNSPECIFIED. ) ;
#66128=CARTESIAN_POINT ( 'NONE',  ( 16.39999999347100257, -3.345256695718999751, -11.86066175541999890 ) ) ;
#66130=CARTESIAN_POINT ( 'NONE',  ( 11.75766493321900086, 3.377423597792000187, -11.11036430104999972 ) ) ;
#66140=B_SPLINE_CURVE_WITH_KNOTS ( 'NONE', 3,
 ( #47505, #36671, #3468, #14658, #15343, #57991, #19558, #62874 ),
 .UNSPECIFIED., .F., .F.,
 ( 4, 2, 2, 4 ),
 ( 0.000000000000000000, 0.2499999999999985567, 0.4999999999999971134, 1.000000000000000000 ),
 .UNSPECIFIED. ) ;
#66141=DIRECTION ( 'NONE',  ( -0.7071068187612229439, 0.000000000000000000, -0.7071067436118699812 ) ) ;
#66146=EDGE_LOOP ( 'NONE', ( #245, #44990, #68365, #60728, #52344 ) ) ;
#66152=ADVANCED_FACE ( 'NONE', ( #28523 ), #44610, .F. ) ;
#66153=CARTESIAN_POINT ( 'NONE',  ( 23.55066277914299988, -2.916948873479999982, -13.72949264782000078 ) ) ;
#66155=VECTOR ( 'NONE', #54093, 999.9999999999998863 ) ;
#66165=DIRECTION ( 'NONE',  ( 0.000000000000000000, 0.000000000000000000, -1.000000000000000000 ) ) ;
#66179=EDGE_LOOP ( 'NONE', ( #46315, #11510, #18121, #23606 ) ) ;
#66181=AXIS2_PLACEMENT_3D ( 'NONE', #14589, #31022, #3396 ) ;
#66194=CARTESIAN_POINT ( 'NONE',  ( 25.08544203593700317, -8.543220285963998961, -8.155323815290000056 ) ) ;
#66201=EDGE_LOOP ( 'NONE', ( #4848, #51408, #61138, #3437, #51809 ) ) ;
#66215=ORIENTED_EDGE ( 'NONE', *, *, #45095, .F. ) ;
#66223=CARTESIAN_POINT ( 'NONE',  ( 21.60000000000000142, 0.000000000000000000, 0.000000000000000000 ) ) ;
#66224=CARTESIAN_POINT ( 'NONE',  ( 11.84802180303800156, -11.72322844712000034, -1.964617572541000001 ) ) ;
#66225=B_SPLINE_CURVE_WITH_KNOTS ( 'NONE', 3,
 ( #30613, #30281, #36896, #51586, #10314, #41787, #9618, #36197, #47037, #3680, #36542, #5067, #46353, #46699, #68003, #52276, #9971, #52618, #4371, #40756, #25022, #4712 ),
 .UNSPECIFIED., .F., .F.,
 ( 4, 2, 2, 1, 2, 2, 2, 2, 1, 2, 2, 4 ),
 ( 0.000000000000000000, 0.2499999999999695799, 0.3749999999999543698, 0.4374999999999433231, 0.4687499999999412137, 0.4999999999999390488, 0.5624999999999437117, 0.6249999999999484857, 0.6874999999999531486, 0.7187499999999569233, 0.7499999999999606981, 1.000000000000000000 ),
 .UNSPECIFIED. ) ;
#66235=AXIS2_PLACEMENT_3D ( 'NONE', #50612, #66333, #2714 ) ;
#66240=CARTESIAN_POINT ( 'NONE',  ( 11.29998636608000062, 3.695122995756999984, -11.25914041192000070 ) ) ;
#66248=CARTESIAN_POINT ( 'NONE',  ( 24.53428988874600236, -8.855929874993998752, -9.286429786912000495 ) ) ;
#66252=ORIENTED_EDGE ( 'NONE', *, *, #68111, .F. ) ;
#66253=CARTESIAN_POINT ( 'NONE',  ( 25.44993529014200107, -2.258942858049999725, 11.14410496443800014 ) ) ;
#66269=EDGE_LOOP ( 'NONE', ( #62635, #52454, #13328, #43086 ) ) ;
#66273=CARTESIAN_POINT ( 'NONE',  ( 24.66122485234200212, 3.625879222137000202, -12.20767898207999913 ) ) ;
#66277=DIRECTION ( 'NONE',  ( 0.000000000000000000, -0.9659258262890756397, 0.2588190451024932059 ) ) ;
#66278=CARTESIAN_POINT ( 'NONE',  ( 24.67921321800200118, -8.727630028894999725, 9.158313644156001132 ) ) ;
#66285=CARTESIAN_POINT ( 'NONE',  ( 24.94502883495008305, -8.558261254986113897, -8.385775660771827233 ) ) ;
#66287=ORIENTED_EDGE ( 'NONE', *, *, #17260, .T. ) ;
#66297=CARTESIAN_POINT ( 'NONE',  ( 23.68315609214200279, -13.13569427494999964, -3.949142898887999742 ) ) ;
#66312=ORIENTED_EDGE ( 'NONE', *, *, #43168, .F. ) ;
#66326=DIRECTION ( 'NONE',  ( -1.055605809059559446E-16, 0.9835354258236025382, -0.1807154286440004198 ) ) ;
#66330=FACE_OUTER_BOUND ( 'NONE', #55196, .T. ) ;
#66333=DIRECTION ( 'NONE',  ( -1.000000000000000000, 0.000000000000000000, 0.000000000000000000 ) ) ;
#66339=CARTESIAN_POINT ( 'NONE',  ( 23.89320776801300283, -1.894218448783000941, 11.32736289219000270 ) ) ;
#66342=AXIS2_PLACEMENT_3D ( 'NONE', #36550, #51593, #62085 ) ;
#66343=CARTESIAN_POINT ( 'NONE',  ( 17.79284288850699980, 3.413161633892000335, 11.89755489758000095 ) ) ;
#66358=DIRECTION ( 'NONE',  ( 0.000000000000000000, -1.000000000000000000, 0.000000000000000000 ) ) ;
#66365=CARTESIAN_POINT ( 'NONE',  ( 19.89999890908300273, 0.000000000000000000, 0.000000000000000000 ) ) ;
#66368=DIRECTION ( 'NONE',  ( -3.667764737047155134E-10, 0.9466472399347399813, -0.3222716294121134584 ) ) ;
#66377=EDGE_CURVE ( 'NONE', #7211, #60567, #58509, .T. ) ;
#66379=FACE_OUTER_BOUND ( 'NONE', #36967, .T. ) ;
#66386=B_SPLINE_SURFACE_WITH_KNOTS ( 'NONE', 3, 3, ( 
 ( #38036, #21611, #6216, #64254 ),
 ( #32461, #60062, #54117, #64597 ),
 ( #37696, #64938, #33151, #5535 ),
 ( #17052, #47856, #27909, #38384 ),
 ( #59025, #65293, #17410, #11810 ),
 ( #54466, #58677, #11129, #32803 ),
 ( #1326, #22644, #53777, #38734 ),
 ( #69163, #16023, #12167, #5874 ),
 ( #10776, #33498, #54812, #26528 ),
 ( #27212, #21272, #53439, #63913 ) ),
 .UNSPECIFIED., .F., .F., .F.,
 ( 4, 1, 1, 1, 1, 1, 1, 4 ),
 ( 4, 4 ),
 ( 0.07063076901675000019, 0.1428571428570999946, 0.2857142857143000203, 0.4285714285713999594, 0.5714285714286000406, 0.7142857142856999797, 0.8571428571429000609, 0.9582423226859000387 ),
 ( -0.1917799910644999994, 1.191756862851000021 ),
 .UNSPECIFIED. ) ;
#66390=CARTESIAN_POINT ( 'NONE',  ( 13.00000000000000178, 50.50083396221999976, 7.800765400072998901 ) ) ;
#66391=CARTESIAN_POINT ( 'NONE',  ( 25.60000000000000142, 0.000000000000000000, 0.000000000000000000 ) ) ;
#66392=CARTESIAN_POINT ( 'NONE',  ( 24.56046482358600258, -8.848342285144999764, 9.332993723418001153 ) ) ;
#66398=ORIENTED_EDGE ( 'NONE', *, *, #24889, .T. ) ;
#66399=AXIS2_PLACEMENT_3D ( 'NONE', #6117, #52996, #196 ) ;
#66407=CARTESIAN_POINT ( 'NONE',  ( 18.23590051321700400, 3.219096189435000088, -11.95421454054999977 ) ) ;
#66419=B_SPLINE_CURVE_WITH_KNOTS ( 'NONE', 3,
 ( #909, #5108, #32385, #36937, #31690, #58942, #53698, #64511 ),
 .UNSPECIFIED., .F., .F.,
 ( 4, 2, 2, 4 ),
 ( 0.4992598756095557033, 0.7496299378047774908, 0.8748149689023887454, 1.000000000000000000 ),
 .UNSPECIFIED. ) ;
#66427=CARTESIAN_POINT ( 'NONE',  ( 25.12926878881309989, 11.33915774497326012, 3.290756510447234273 ) ) ;
#66434=CARTESIAN_POINT ( 'NONE',  ( 24.67921321864300310, 12.29514728640000065, 2.979192498689000157 ) ) ;
#66438=CARTESIAN_POINT ( 'NONE',  ( 24.62774583285700203, -12.19917312477000060, 3.045379866084000131 ) ) ;
#66442=CARTESIAN_POINT ( 'NONE',  ( 23.71897700387453511, 13.13847632678408495, 3.829971267513319511 ) ) ;
#66446=CARTESIAN_POINT ( 'NONE',  ( 23.56665676678100141, -2.935523947847999970, 13.67844066972000050 ) ) ;
#66459=CARTESIAN_POINT ( 'NONE',  ( 24.25375554908000097, 12.19812635653999955, 3.308082274583000526 ) ) ;
#66462=EDGE_LOOP ( 'NONE', ( #34971, #25455, #41365, #40992 ) ) ;
#66469=CARTESIAN_POINT ( 'NONE',  ( 20.75138802851920161, 0.000000000000000000, 0.000000000000000000 ) ) ;
#66473=DIRECTION ( 'NONE',  ( 0.000000000000000000, 1.000000000000000000, 0.000000000000000000 ) ) ;
#66474=CARTESIAN_POINT ( 'NONE',  ( 11.53971429488000133, 3.572666839320000065, -11.04878221693000029 ) ) ;
#66475=CARTESIAN_POINT ( 'NONE',  ( 23.57777266354770873, -13.28347985581029356, -4.287254563653999817 ) ) ;
#66489=B_SPLINE_CURVE_WITH_KNOTS ( 'NONE', 3,
 ( #3459, #51701, #46122, #24797 ),
 .UNSPECIFIED., .F., .F.,
 ( 4, 4 ),
 ( 0.000000000000000000, 1.000000000000000000 ),
 .UNSPECIFIED. ) ;
#66495=CARTESIAN_POINT ( 'NONE',  ( 24.32732080885899961, -3.577499572665000294, -12.48500538494000089 ) ) ;
#66497=AXIS2_PLACEMENT_3D ( 'NONE', #44618, #27842, #43568 ) ;
#66511=CARTESIAN_POINT ( 'NONE',  ( 23.61842251754734079, -13.40083422037635863, 3.925480009447839702 ) ) ;
#66517=EDGE_CURVE ( 'NONE', #60567, #64580, #2901, .T. ) ;
#66518=CARTESIAN_POINT ( 'NONE',  ( 23.89320776801300283, 10.87822567731000234, -3.284864823438000236 ) ) ;
#66525=CARTESIAN_POINT ( 'NONE',  ( 11.50029455687000102, -11.56505190006999939, -1.404305717648999918 ) ) ;
#66529=CARTESIAN_POINT ( 'NONE',  ( 24.53003472522700434, -3.319296498592000155, 12.04487452434999994 ) ) ;
#66533=CARTESIAN_POINT ( 'NONE',  ( 25.31010666462800174, 11.20360457085999961, 3.315062111770000097 ) ) ;
#66534=ORIENTED_EDGE ( 'NONE', *, *, #61621, .T. ) ;
#66537=DIRECTION ( 'NONE',  ( 1.000000000000000000, 0.000000000000000000, 0.000000000000000000 ) ) ;
#66548=CARTESIAN_POINT ( 'NONE',  ( 11.79999999771000141, 12.39026187696000036, 1.832249219479999969 ) ) ;
#66549=CARTESIAN_POINT ( 'NONE',  ( 44.24148000000000280, 9.517611874540000017, 8.103398312166000039 ) ) ;
#66552=CARTESIAN_POINT ( 'NONE',  ( 24.11585382079778839, -12.52247569921947701, 3.380851800467152390 ) ) ;
#66567=DIRECTION ( 'NONE',  ( -1.000000000000000000, 0.000000000000000000, 0.000000000000000000 ) ) ;
#66568=CARTESIAN_POINT ( 'NONE',  ( 24.95271118850850556, 11.53329584871545599, -3.220779843859221891 ) ) ;
#66569=CARTESIAN_POINT ( 'NONE',  ( 11.48394322905000031, -11.59615457572999908, -1.579582225534999829 ) ) ;
#66570=EDGE_CURVE ( 'NONE', #4716, #30294, #26321, .T. ) ;
#66573=EDGE_LOOP ( 'NONE', ( #4287, #19000, #5005, #56332 ) ) ;
#66584=VERTEX_POINT ( 'NONE', #14423 ) ;
#66587=DIRECTION ( 'NONE',  ( -1.000000000000000000, 0.000000000000000000, 0.000000000000000000 ) ) ;
#66590=CARTESIAN_POINT ( 'NONE',  ( 23.73801811364100089, 9.840518919942999432, -9.652166885300999866 ) ) ;
#66597=AXIS2_PLACEMENT_3D ( 'NONE', #46587, #34812, #61371 ) ;
#66599=CARTESIAN_POINT ( 'NONE',  ( 23.89320776801300283, -12.21745654481001075, -3.256241354617000816 ) ) ;
#66609=CYLINDRICAL_SURFACE ( 'NONE', #2553, 9.250000000000000000 ) ;
#66614=ORIENTED_EDGE ( 'NONE', *, *, #22725, .T. ) ;
#66617=CARTESIAN_POINT ( 'NONE',  ( 24.23036330766939983, -12.32981272787003135, -3.306814091776679287 ) ) ;
#66618=CARTESIAN_POINT ( 'NONE',  ( 24.60999195316300003, 3.467950226999999774, -12.10892777233999951 ) ) ;
#66623=EDGE_CURVE ( 'NONE', #28653, #58094, #43829, .T. ) ;
#66624=CARTESIAN_POINT ( 'NONE',  ( 23.60000000000000142, 0.000000000000000000, 0.000000000000000000 ) ) ;
#66628=ORIENTED_EDGE ( 'NONE', *, *, #22330, .T. ) ;
#66654=CARTESIAN_POINT ( 'NONE',  ( 24.08707381732377684, -3.338859752676834880, -12.58718648024971820 ) ) ;
#66661=EDGE_LOOP ( 'NONE', ( #34452, #29466, #34947, #31315, #3543 ) ) ;
#66662=CYLINDRICAL_SURFACE ( 'NONE', #37809, 0.6999999999999992895 ) ;
#66666=FACE_OUTER_BOUND ( 'NONE', #39307, .T. ) ;
#66676=VECTOR ( 'NONE', #67521, 1000.000000000000114 ) ;
#66680=CARTESIAN_POINT ( 'NONE',  ( 24.61098151538899970, 3.467630292425999627, 12.10773253045999986 ) ) ;
#66682=CARTESIAN_POINT ( 'NONE',  ( 17.60000000024299993, 11.86189249994999884, -3.298671769835999967 ) ) ;
#66686=EDGE_CURVE ( 'NONE', #60348, #5919, #41986, .T. ) ;
#66689=DIRECTION ( 'NONE',  ( 1.000000000000000000, -1.056835174927999956E-13, 0.000000000000000000 ) ) ;
#66696=ORIENTED_EDGE ( 'NONE', *, *, #62055, .T. ) ;
#66702=FACE_BOUND ( 'NONE', #68989, .T. ) ;
#66703=ORIENTED_EDGE ( 'NONE', *, *, #68293, .T. ) ;
#66706=EDGE_CURVE ( 'NONE', #49580, #50821, #19682, .T. ) ;
#66717=CARTESIAN_POINT ( 'NONE',  ( 18.43317799840268023, -2.892723637958458216, -12.11800683821374314 ) ) ;
#66735=CARTESIAN_POINT ( 'NONE',  ( 13.70005190196300227, -9.005348107749998832, -7.391036106496999381 ) ) ;
#66740=AXIS2_PLACEMENT_3D ( 'NONE', #58099, #52854, #4953 ) ;
#66744=B_SPLINE_CURVE_WITH_KNOTS ( 'NONE', 3,
 ( #32863, #33555, #54529, #1051 ),
 .UNSPECIFIED., .F., .F.,
 ( 4, 4 ),
 ( 0.000000000000000000, 1.000000000000000000 ),
 .UNSPECIFIED. ) ;
#66745=VERTEX_POINT ( 'NONE', #41328 ) ;
#66747=VECTOR ( 'NONE', #5308, 999.9999999999998863 ) ;
#66748=FACE_OUTER_BOUND ( 'NONE', #51390, .T. ) ;
#66750=CARTESIAN_POINT ( 'NONE',  ( 24.22093787138100041, -3.188036788074999794, 12.21311288046000065 ) ) ;
#66751=FACE_OUTER_BOUND ( 'NONE', #19857, .T. ) ;
#66753=ADVANCED_FACE ( 'NONE', ( #32224 ), #15180, .F. ) ;
#66758=ORIENTED_EDGE ( 'NONE', *, *, #38569, .T. ) ;
#66763=B_SPLINE_CURVE_WITH_KNOTS ( 'NONE', 3,
 ( #18252, #56001, #50067, #13014 ),
 .UNSPECIFIED., .F., .F.,
 ( 4, 4 ),
 ( 0.000000000000000000, 1.000000000000000000 ),
 .UNSPECIFIED. ) ;
#66774=ADVANCED_FACE ( 'NONE', ( #36422 ), #36771, .T. ) ;
#66785=CARTESIAN_POINT ( 'NONE',  ( 12.68583900966313038, -11.53041019655163879, 4.891346001956513589 ) ) ;
#66795=CARTESIAN_POINT ( 'NONE',  ( 13.40279821320924114, -11.66091458874562470, -2.117181037223689888 ) ) ;
#66801=CARTESIAN_POINT ( 'NONE',  ( 13.99999999231800096, -8.833253877201999060, -7.896562762484000686 ) ) ;
#66802=EDGE_CURVE ( 'NONE', #23870, #47396, #26631, .T. ) ;
#66806=AXIS2_PLACEMENT_3D ( 'NONE', #11414, #11079, #32414 ) ;
#66809=CARTESIAN_POINT ( 'NONE',  ( 11.79999999771000141, 3.595163221087000149, -11.99793848941000007 ) ) ;
#66818=CARTESIAN_POINT ( 'NONE',  ( 24.92848015187707844, -2.996103346371080001, -11.61747088698863806 ) ) ;
#66826=CARTESIAN_POINT ( 'NONE',  ( 25.55279310973962126, 11.13093580945219685, 3.116563969436135118 ) ) ;
#66838=VERTEX_POINT ( 'NONE', #68220 ) ;
#66844=CARTESIAN_POINT ( 'NONE',  ( 23.58457962933900376, -3.197576462624000193, -13.62102450554000121 ) ) ;
#66850=FACE_OUTER_BOUND ( 'NONE', #61756, .T. ) ;
#66856=CARTESIAN_POINT ( 'NONE',  ( 15.76715644869600119, -8.722854347492999594, -8.080426068599999567 ) ) ;
#66859=DIRECTION ( 'NONE',  ( 1.000000000000000000, 0.000000000000000000, 0.000000000000000000 ) ) ;
#66860=ORIENTED_EDGE ( 'NONE', *, *, #57372, .F. ) ;
#66866=CARTESIAN_POINT ( 'NONE',  ( 24.52301462737445803, 12.12194122193224821, -3.142914130639136605 ) ) ;
#66868=CARTESIAN_POINT ( 'NONE',  ( 23.57773640739606691, 2.928864175545800919, -13.64745269084981061 ) ) ;
#66879=CARTESIAN_POINT ( 'NONE',  ( 25.08240915828700324, 11.33760612088999942, 3.319396049943999838 ) ) ;
#66887=CARTESIAN_POINT ( 'NONE',  ( 15.95370777310256294, 3.574818104395620200, 11.79277689209176749 ) ) ;
#66893=CARTESIAN_POINT ( 'NONE',  ( 25.02476365129393088, 2.919224782832727794, 11.54271202783471750 ) ) ;
#66895=CARTESIAN_POINT ( 'NONE',  ( 23.84021428159876521, -12.96267928454988727, 3.649536305042122120 ) ) ;
#66896=B_SPLINE_CURVE_WITH_KNOTS ( 'NONE', 3,
 ( #62680, #57782, #9894, #67579, #20730, #9539 ),
 .UNSPECIFIED., .F., .F.,
 ( 4, 2, 4 ),
 ( 0.000000000000000000, 0.5000000000000000000, 1.000000000000000000 ),
 .UNSPECIFIED. ) ;
#66903=CARTESIAN_POINT ( 'NONE',  ( 25.59994555223700274, -10.55174472786000095, 3.754934689065000164 ) ) ;
#66909=CARTESIAN_POINT ( 'NONE',  ( 11.83156678923300120, -11.57054462408999917, -1.756438942007999993 ) ) ;
#66912=CARTESIAN_POINT ( 'NONE',  ( 24.70869262301700076, -12.32777590421999925, -2.948351121266000074 ) ) ;
#66913=EDGE_CURVE ( 'NONE', #45182, #47043, #23016, .T. ) ;
#66914=EDGE_CURVE ( 'NONE', #52478, #18634, #48285, .T. ) ;
#66921=B_SPLINE_CURVE_WITH_KNOTS ( 'NONE', 3,
 ( #10398, #3011, #50912, #55473, #33462, #50569 ),
 .UNSPECIFIED., .F., .F.,
 ( 4, 1, 1, 4 ),
 ( 0.000000000000000000, 0.2305484662882832936, 0.8346924768963898122, 1.000000000000000000 ),
 .UNSPECIFIED. ) ;
#66927=VERTEX_POINT ( 'NONE', #60164 ) ;
#66929=CARTESIAN_POINT ( 'NONE',  ( 23.56664675778400309, 10.37811020278999941, -9.381454169592000625 ) ) ;
#66931=CARTESIAN_POINT ( 'NONE',  ( 23.78804273620877652, 3.294425019659333653, 13.15453432728574867 ) ) ;
#66933=CARTESIAN_POINT ( 'NONE',  ( 23.81982430084200075, 9.669052596895998164, -9.332375605283999676 ) ) ;
#66934=CARTESIAN_POINT ( 'NONE',  ( 17.79325612864500172, -3.315492466914999881, -11.22361417850999921 ) ) ;
#66938=VERTEX_POINT ( 'NONE', #43042 ) ;
#66947=DIRECTION ( 'NONE',  ( -1.000000000000000000, 0.000000000000000000, 0.000000000000000000 ) ) ;
#66949=AXIS2_PLACEMENT_3D ( 'NONE', #36626, #41865, #69120 ) ;
#66952=B_SPLINE_SURFACE_WITH_KNOTS ( 'NONE', 3, 3, ( 
 ( #6534, #9445, #52099, #4204 ),
 ( #25542, #46867, #20291, #2333 ),
 ( #65947, #44312, #17732, #65608 ),
 ( #39054, #50230, #60372, #1993 ),
 ( #34846, #28925, #18075, #7232 ),
 ( #23653, #7926, #49530, #45335 ),
 ( #2674, #50572, #18420, #55128 ),
 ( #66297, #39745, #34157, #43955 ),
 ( #61065, #13527, #44657, #60025 ),
 ( #39396, #13183, #29263, #22959 ),
 ( #17375, #23315, #55476, #38703 ),
 ( #8265, #12480, #33812, #24002 ) ),
 .UNSPECIFIED., .F., .F., .F.,
 ( 4, 1, 1, 1, 1, 1, 1, 1, 1, 4 ),
 ( 4, 4 ),
 ( 0.01098209966893000031, 0.05000000000000000278, 0.1000000000000000056, 0.1499999999999999944, 0.2000000000000000111, 0.2500000000000000000, 0.2999999999999999889, 0.3499999999999999778, 0.4000000000000000222, 0.4470359006038999716 ),
 ( -0.2706693970313999720, 1.270788585263999959 ),
 .UNSPECIFIED. ) ;
#66960=CARTESIAN_POINT ( 'NONE',  ( 24.52306328729269680, -8.782889800526138657, 8.926437641650338151 ) ) ;
#66962=CARTESIAN_POINT ( 'NONE',  ( 18.28832092538753429, -2.855728056445002494, -11.50255606616314452 ) ) ;
#66969=ORIENTED_EDGE ( 'NONE', *, *, #6858, .F. ) ;
#66979=CARTESIAN_POINT ( 'NONE',  ( 25.59994555223599733, 2.024003533649000097, -11.01554633311000053 ) ) ;
#66986=B_SPLINE_CURVE_WITH_KNOTS ( 'NONE', 3,
 ( #36827, #58144, #32276, #22105, #38893, #43095 ),
 .UNSPECIFIED., .F., .F.,
 ( 4, 2, 4 ),
 ( 0.000000000000000000, 0.5000000000000000000, 1.000000000000000000 ),
 .UNSPECIFIED. ) ;
#66989=CARTESIAN_POINT ( 'NONE',  ( 23.61437394302592452, 13.25091963169895060, -4.104830024061406846 ) ) ;
#66997=EDGE_CURVE ( 'NONE', #49685, #15848, #59846, .T. ) ;
#67010=VERTEX_POINT ( 'NONE', #28351 ) ;
#67019=CARTESIAN_POINT ( 'NONE',  ( 23.50387503050299998, 0.000000000000000000, 0.000000000000000000 ) ) ;
#67023=CARTESIAN_POINT ( 'NONE',  ( 25.59994555223700274, -10.55174472786000095, 3.754934689065000164 ) ) ;
#67041=ADVANCED_FACE ( 'NONE', ( #5629 ), #28006, .T. ) ;
#67043=CARTESIAN_POINT ( 'NONE',  ( 23.50387503050299998, -14.00000000000000000, 0.000000000000000000 ) ) ;
#67045=CARTESIAN_POINT ( 'NONE',  ( 11.42397234076999979, -3.432581932914000156, 11.79497283202000091 ) ) ;
#67047=AXIS2_PLACEMENT_3D ( 'NONE', #7093, #58849, #54645 ) ;
#67052=ORIENTED_EDGE ( 'NONE', *, *, #40926, .F. ) ;
#67055=VERTEX_POINT ( 'NONE', #1428 ) ;
#67056=DIRECTION ( 'NONE',  ( -1.000000000000000000, -4.956352788505168356E-14, -1.734723475976808988E-14 ) ) ;
#67060=CARTESIAN_POINT ( 'NONE',  ( 19.89999890908300273, -12.52500000000000036, 0.000000000000000000 ) ) ;
#67064=FACE_OUTER_BOUND ( 'NONE', #12189, .T. ) ;
#67074=CARTESIAN_POINT ( 'NONE',  ( 17.75870478550200104, -3.641518898264000548, -12.02435208579999859 ) ) ;
#67077=DIRECTION ( 'NONE',  ( 1.000000000000000000, 0.000000000000000000, 0.000000000000000000 ) ) ;
#67081=EDGE_CURVE ( 'NONE', #34904, #6782, #17953, .T. ) ;
#67082=ORIENTED_EDGE ( 'NONE', *, *, #65643, .T. ) ;
#67088=CARTESIAN_POINT ( 'NONE',  ( 24.42400389426000373, -3.752283608186000041, 12.53632670480000044 ) ) ;
#67091=CARTESIAN_POINT ( 'NONE',  ( 18.04816728597000264, 3.610133590554000182, -12.03375048192000207 ) ) ;
#67094=AXIS2_PLACEMENT_3D ( 'NONE', #33154, #28248, #49568 ) ;
#67100=EDGE_CURVE ( 'NONE', #9579, #33910, #33806, .T. ) ;
#67109=CARTESIAN_POINT ( 'NONE',  ( 25.37646820717300145, 8.494765293177998444, 7.922169669001000614 ) ) ;
#67116=ORIENTED_EDGE ( 'NONE', *, *, #54400, .F. ) ;
#67119=DIRECTION ( 'NONE',  ( 2.186536431443105034E-10, -0.8764392776392420092, 0.4815124013057229813 ) ) ;
#67120=CARTESIAN_POINT ( 'NONE',  ( 11.48381255716000027, 3.703723199601000271, -11.90766076753999947 ) ) ;
#67122=CARTESIAN_POINT ( 'NONE',  ( 25.59997239626699894, -8.218962899087999929, 8.043524294852000267 ) ) ;
#67123=CARTESIAN_POINT ( 'NONE',  ( 15.58179592144799486, 8.803826609192167751, 7.629963841725643903 ) ) ;
#67124=DIRECTION ( 'NONE',  ( -1.000000000000000000, 0.000000000000000000, 0.000000000000000000 ) ) ;
#67133=ORIENTED_EDGE ( 'NONE', *, *, #56460, .T. ) ;
#67143=CARTESIAN_POINT ( 'NONE',  ( 11.49999672495000169, 3.632761979779000061, -11.06912554803999882 ) ) ;
#67146=ORIENTED_EDGE ( 'NONE', *, *, #1611, .F. ) ;
#67164=ADVANCED_FACE ( 'NONE', ( #10071 ), #68443, .F. ) ;
#67176=ORIENTED_EDGE ( 'NONE', *, *, #37310, .F. ) ;
#67179=CARTESIAN_POINT ( 'NONE',  ( 15.95676543642414025, 9.288185316739934194, 8.402783510542153778 ) ) ;
#67181=TOROIDAL_SURFACE ( 'NONE', #48270, 7.720759220056000238, 1.000000000000000000 ) ;
#67185=CARTESIAN_POINT ( 'NONE',  ( 17.60000001947600268, -11.86186880240999919, 3.298627760718999991 ) ) ;
#67195=CARTESIAN_POINT ( 'NONE',  ( 23.60440866767097745, -13.39487733609081843, 3.977422972493961595 ) ) ;
#67199=AXIS2_PLACEMENT_3D ( 'NONE', #48438, #58239, #52648 ) ;
#67202=DIRECTION ( 'NONE',  ( 1.000000000000000000, 0.000000000000000000, 0.000000000000000000 ) ) ;
#67209=DIRECTION ( 'NONE',  ( 1.000000000000000000, 0.000000000000000000, 0.000000000000000000 ) ) ;
#67215=EDGE_CURVE ( 'NONE', #15615, #50564, #30462, .T. ) ;
#67219=ORIENTED_EDGE ( 'NONE', *, *, #18095, .F. ) ;
#67222=CARTESIAN_POINT ( 'NONE',  ( 13.46018463513500052, -9.195629459350000090, -7.535158378801000367 ) ) ;
#67223=CARTESIAN_POINT ( 'NONE',  ( 17.80000000009400196, 3.216307036143000175, -11.40341376487999980 ) ) ;
#67236=CARTESIAN_POINT ( 'NONE',  ( 13.69992376746900042, -12.26631831379999937, -2.532779022035999805 ) ) ;
#67238=ORIENTED_EDGE ( 'NONE', *, *, #1524, .T. ) ;
#67247=ORIENTED_EDGE ( 'NONE', *, *, #24719, .T. ) ;
#67251=CARTESIAN_POINT ( 'NONE',  ( 11.26443347348000046, -11.78677031080999882, -1.538950076482000107 ) ) ;
#67262=CARTESIAN_POINT ( 'NONE',  ( 17.71321509766717739, 11.53250522934357036, -4.886416279629735016 ) ) ;
#67267=DIRECTION ( 'NONE',  ( 0.000000000000000000, -1.000000000000000000, 0.000000000000000000 ) ) ;
#67269=CARTESIAN_POINT ( 'NONE',  ( 24.03569479623928018, 3.344478585231344780, 12.68125857544483637 ) ) ;
#67271=CARTESIAN_POINT ( 'NONE',  ( 23.55064458304499908, 10.43113086418000002, -9.391476572615999885 ) ) ;
#67279=CARTESIAN_POINT ( 'NONE',  ( 24.35365242081699932, -10.79182034090998776, -4.028979491970003934 ) ) ;
#67283=CARTESIAN_POINT ( 'NONE',  ( 25.49994615388218477, -2.042074746146404607, 11.11389836488523741 ) ) ;
#67285=FACE_OUTER_BOUND ( 'NONE', #37646, .T. ) ;
#67286=CARTESIAN_POINT ( 'NONE',  ( 23.58333993777100090, 3.286260152889999888E-13, -3.641531520771000148E-13 ) ) ;
#67291=ORIENTED_EDGE ( 'NONE', *, *, #60750, .T. ) ;
#67296=CYLINDRICAL_SURFACE ( 'NONE', #64367, 0.5000000000000028866 ) ;
#67297=CARTESIAN_POINT ( 'NONE',  ( 24.46580263708699832, 3.340075003801000086, -12.12245366788000034 ) ) ;
#67298=DIRECTION ( 'NONE',  ( 0.000000000000000000, -0.7614089499631907509, 0.6482718649732928107 ) ) ;
#67299=ORIENTED_EDGE ( 'NONE', *, *, #14802, .F. ) ;
#67304=CARTESIAN_POINT ( 'NONE',  ( 13.16012107570600342, -11.71981102724999957, -1.988987020038000209 ) ) ;
#67314=CARTESIAN_POINT ( 'NONE',  ( 23.56665676678700194, 0.000000000000000000, -3.819167204710999951E-13 ) ) ;
#67324=CIRCLE ( 'NONE', #66181, 0.6999999999999992895 ) ;
#67328=CARTESIAN_POINT ( 'NONE',  ( 24.12728270886359994, 12.50344094810666284, -3.372677501753305052 ) ) ;
#67329=CARTESIAN_POINT ( 'NONE',  ( 21.72233714749290101, 0.000000000000000000, 0.000000000000000000 ) ) ;
#67343=CARTESIAN_POINT ( 'NONE',  ( 15.39999999998900293, 9.471998555523999386, 8.194929586088999685 ) ) ;
#67344=CIRCLE ( 'NONE', #53965, 0.6999999999999992895 ) ;
#67345=CARTESIAN_POINT ( 'NONE',  ( 23.61807751515700105, 13.16786766521000196, 4.269890910948000773 ) ) ;
#67350=CARTESIAN_POINT ( 'NONE',  ( 15.98069952315600162, 9.346107076637000688, 8.395568570714997847 ) ) ;
#67355=CARTESIAN_POINT ( 'NONE',  ( 25.50764038565079161, -2.874079281045797796, -11.25426173516229511 ) ) ;
#67358=CARTESIAN_POINT ( 'NONE',  ( 24.35146665670700017, 3.377061749054000028, 12.26054704401999906 ) ) ;
#67361=ORIENTED_EDGE ( 'NONE', *, *, #17313, .T. ) ;
#67373=ORIENTED_EDGE ( 'NONE', *, *, #65073, .F. ) ;
#67381=CARTESIAN_POINT ( 'NONE',  ( 11.82312259374200103, -3.643624473348999970, 12.02372562982000126 ) ) ;
#67392=CARTESIAN_POINT ( 'NONE',  ( 16.09997386696500143, -4.522001505202896787, -10.77728718286270215 ) ) ;
#67402=EDGE_CURVE ( 'NONE', #12705, #58173, #47628, .T. ) ;
#67406=CARTESIAN_POINT ( 'NONE',  ( 25.46373029971899982, -8.354610197568000274, -8.148451206582999262 ) ) ;
#67411=DIRECTION ( 'NONE',  ( 1.000000000000000000, 0.000000000000000000, 0.000000000000000000 ) ) ;
#67412=CARTESIAN_POINT ( 'NONE',  ( 18.06944243593800081, -3.222040310929999762, -11.85748006108999952 ) ) ;
#67416=B_SPLINE_CURVE_WITH_KNOTS ( 'NONE', 3,
 ( #5653, #58456, #32584, #37821, #42041, #53895, #53214, #21732, #31553, #26994, #764, #16494, #47974, #27689, #52875, #15473, #5316, #26657, #27336, #22080, #43425, #72, #21393, #64719, #36799, #64031, #68591, #63347, #42727, #16151, #48311 ),
 .UNSPECIFIED., .F., .F.,
 ( 4, 2, 2, 1, 1, 2, 2, 2, 1, 2, 2, 2, 2, 2, 2, 2, 4 ),
 ( 0.000000000000000000, 0.06250000000001226796, 0.09375000000001840195, 0.1093750000000199701, 0.1171875000000205391, 0.1210937500000210665, 0.1250000000000215661, 0.1875000000000251188, 0.2187500000000255629, 0.2343750000000240641, 0.2500000000000225930, 0.3750000000000187628, 0.4375000000000192069, 0.4687500000000189848, 0.5000000000000187628, 0.7500000000000094369, 1.000000000000000000 ),
 .UNSPECIFIED. ) ;
#67419=EDGE_LOOP ( 'NONE', ( #54275, #10534, #1045, #56012 ) ) ;
#67423=FACE_OUTER_BOUND ( 'NONE', #66179, .T. ) ;
#67428=CARTESIAN_POINT ( 'NONE',  ( 23.61702328491799818, -13.18027949750999994, 4.241847907418000219 ) ) ;
#67432=ORIENTED_EDGE ( 'NONE', *, *, #12968, .F. ) ;
#67449=DIRECTION ( 'NONE',  ( 1.000000000000000000, 0.000000000000000000, 0.000000000000000000 ) ) ;
#67458=CARTESIAN_POINT ( 'NONE',  ( 11.44731512799000228, 3.899625435828999898, -11.84583327264999930 ) ) ;
#67460=CARTESIAN_POINT ( 'NONE',  ( 14.39999999806400055, -11.53037610505381494, 4.891426364203002919 ) ) ;
#67462=CARTESIAN_POINT ( 'NONE',  ( 24.30000000000000071, -3.224868684338999980, -12.03537377768999939 ) ) ;
#67468=B_SPLINE_CURVE_WITH_KNOTS ( 'NONE', 3,
 ( #59031, #53097, #15004, #62883 ),
 .UNSPECIFIED., .F., .F.,
 ( 4, 4 ),
 ( 0.000000000000000000, 1.000000000000000000 ),
 .UNSPECIFIED. ) ;
#67472=DIRECTION ( 'NONE',  ( 4.468469752125040125E-09, 0.9867386997955089889, 0.1623167838699015042 ) ) ;
#67484=CARTESIAN_POINT ( 'NONE',  ( 23.89491049328219319, -3.335473474314862852, 12.94526851323479910 ) ) ;
#67494=ORIENTED_EDGE ( 'NONE', *, *, #37396, .F. ) ;
#67496=EDGE_CURVE ( 'NONE', #21757, #16879, #51254, .T. ) ;
#67497=CARTESIAN_POINT ( 'NONE',  ( 25.21376650222272531, -2.724979797188207264, -11.40630329634163331 ) ) ;
#67511=CARTESIAN_POINT ( 'NONE',  ( 18.50001572531400029, 1.956586052127241571, -12.40985500457068547 ) ) ;
#67517=EDGE_LOOP ( 'NONE', ( #15921, #40422, #42568, #64393 ) ) ;
#67519=CARTESIAN_POINT ( 'NONE',  ( 25.37957628771734875, 8.342521315683184113, 8.311489950699764151 ) ) ;
#67521=DIRECTION ( 'NONE',  ( 2.887756364189944304E-10, 0.4812251768484908099, 0.8765970164032835799 ) ) ;
#67525=B_SPLINE_SURFACE_WITH_KNOTS ( 'NONE', 3, 3, ( 
 ( #105, #52558, #5006, #36833 ),
 ( #47668, #20749, #4654, #43104 ),
 ( #21769, #48345, #9910, #25994 ),
 ( #31936, #47325, #52213, #15839 ),
 ( #25649, #58150, #32287, #10253 ),
 ( #68980, #21422, #31249, #53594 ),
 ( #46978, #37171, #57450, #42759 ),
 ( #36478, #58490, #42073, #68282 ),
 ( #68628, #64066, #20402, #52909 ),
 ( #41726, #31588, #26342, #10594 ),
 ( #5690, #5352, #64406, #16184 ),
 ( #451, #37510, #15507, #27032 ),
 ( #15158, #57802, #9560, #16530 ),
 ( #21094, #42420, #28067, #28417 ),
 ( #39243, #33660, #44157, #43461 ),
 ( #11622, #6034, #28769, #65455 ) ),
 .UNSPECIFIED., .F., .F., .F.,
 ( 4, 1, 1, 1, 1, 1, 1, 1, 1, 1, 1, 1, 1, 4 ),
 ( 4, 4 ),
 ( 0.02931725585745999924, 0.07692307692307999434, 0.1538461538461999845, 0.2307692307692000011, 0.3076923076922999933, 0.3846153846154000133, 0.4615384615385000333, 0.5384615384614999112, 0.6153846153845999867, 0.6923076923076999512, 0.7692307692308000266, 0.8461538461537999600, 0.9230769230769000355, 0.9830414450855999853 ),
 ( -0.1835260008787999997, 1.183623993927000129 ),
 .UNSPECIFIED. ) ;
#67536=CARTESIAN_POINT ( 'NONE',  ( 15.86242637978999959, -8.523064092628001021, -8.288181269780999116 ) ) ;
#67538=CARTESIAN_POINT ( 'NONE',  ( 23.63687345803960227, -13.40365592222601521, 3.866661307165411454 ) ) ;
#67541=AXIS2_PLACEMENT_3D ( 'NONE', #11227, #6317, #12274 ) ;
#67548=ORIENTED_EDGE ( 'NONE', *, *, #6858, .T. ) ;
#67559=CARTESIAN_POINT ( 'NONE',  ( 25.37703561905400207, 11.10734551254999936, 3.396345752903999760 ) ) ;
#67564=CARTESIAN_POINT ( 'NONE',  ( 44.24148000000000280, -9.517611874540000017, 8.103398312166998352 ) ) ;
#67565=LINE ( 'NONE', #35094, #8059 ) ;
#67566=CARTESIAN_POINT ( 'NONE',  ( 17.91921746558519146, -11.21561494459223773, 3.152940210883220296 ) ) ;
#67574=CARTESIAN_POINT ( 'NONE',  ( 25.09888356831554290, 2.850926811815151840, 11.48730284164415494 ) ) ;
#67579=CARTESIAN_POINT ( 'NONE',  ( 23.85395508732198167, 9.637287106755159982, -9.713125223865638702 ) ) ;
#67580=CARTESIAN_POINT ( 'NONE',  ( 11.29997394663803867, -12.21464834820976897, -1.635338273580426494 ) ) ;
#67581=ORIENTED_EDGE ( 'NONE', *, *, #16948, .F. ) ;
#67587=( LENGTH_UNIT ( ) NAMED_UNIT ( * ) SI_UNIT ( .MILLI., .METRE. ) );
#67591=CARTESIAN_POINT ( 'NONE',  ( 11.35619132127000164, -11.69822877698999974, -1.509327410273999970 ) ) ;
#67592=CARTESIAN_POINT ( 'NONE',  ( 24.53002386606100060, -12.09082868768999930, -3.147845687315999896 ) ) ;
#67593=CARTESIAN_POINT ( 'NONE',  ( 13.50003721581400029, -9.159934378815998812, -7.517910889891000537 ) ) ;
#67600=CARTESIAN_POINT ( 'NONE',  ( 18.38722619340700248, 3.117741388420999904, 11.18549237633000004 ) ) ;
#67603=EDGE_CURVE ( 'NONE', #29053, #12282, #4558, .T. ) ;
#67609=CARTESIAN_POINT ( 'NONE',  ( 24.00507476546492569, 3.345682322440594714, 12.73790407563989469 ) ) ;
#67611=CARTESIAN_POINT ( 'NONE',  ( 18.35296092448800209, -2.690559717027000364, -11.48481263514000084 ) ) ;
#67615=VECTOR ( 'NONE', #20998, 1000.000000000000114 ) ;
#67624=CARTESIAN_POINT ( 'NONE',  ( 24.34832118766533071, 12.03536993114527398, 3.224867653659703404 ) ) ;
#67627=CARTESIAN_POINT ( 'NONE',  ( 13.94806348789000161, 8.812672976752997656, 7.562028778248000016 ) ) ;
#67628=CARTESIAN_POINT ( 'NONE',  ( 16.32020863168424185, -3.595521563589213265, -11.99782687963371153 ) ) ;
#67634=ORIENTED_EDGE ( 'NONE', *, *, #6309, .F. ) ;
#67637=DIRECTION ( 'NONE',  ( 0.000000000000000000, 0.6664713972123997854, -0.7455306007789026523 ) ) ;
#67640=VERTEX_POINT ( 'NONE', #32250 ) ;
#67643=CARTESIAN_POINT ( 'NONE',  ( 13.64720874474600087, -11.45913667646999912, -2.381478076492999918 ) ) ;
#67662=CARTESIAN_POINT ( 'NONE',  ( 12.79999999202000005, 11.41069016990000051, -4.623987642516999230 ) ) ;
#67667=CARTESIAN_POINT ( 'NONE',  ( 24.07540745826431916, 12.58941621619760021, -3.411518517344679147 ) ) ;
#67668=TOROIDAL_SURFACE ( 'NONE', #2952, 12.20000000000000107, 0.6999999999999999556 ) ;
#67674=VERTEX_POINT ( 'NONE', #16150 ) ;
#67678=B_SPLINE_CURVE_WITH_KNOTS ( 'NONE', 3,
 ( #54422, #60703, #33801, #22601 ),
 .UNSPECIFIED., .F., .F.,
 ( 4, 4 ),
 ( 0.000000000000000000, 1.000000000000000000 ),
 .UNSPECIFIED. ) ;
#67683=CARTESIAN_POINT ( 'NONE',  ( 17.80000000009400196, -3.216307036143000175, -11.40341376487999980 ) ) ;
#67686=EDGE_CURVE ( 'NONE', #60256, #6863, #10374, .T. ) ;
#67687=EDGE_CURVE ( 'NONE', #25573, #9331, #48775, .T. ) ;
#67692=CARTESIAN_POINT ( 'NONE',  ( 16.13682146000800088, 8.990085112443999549, 8.775549782916998609 ) ) ;
#67695=CARTESIAN_POINT ( 'NONE',  ( 23.60205915885299888, -2.171992490544001786, -12.06370038613001228 ) ) ;
#67697=CARTESIAN_POINT ( 'NONE',  ( 24.74447986542299915, -11.86527187233999925, 3.111026911665999872 ) ) ;
#67700=CARTESIAN_POINT ( 'NONE',  ( 25.39994675526091683, -10.74016667838613515, 3.821986401712638592 ) ) ;
#67702=CARTESIAN_POINT ( 'NONE',  ( 23.54908358533199930, 10.40234127004999998, 9.426912626873999557 ) ) ;
#67709=EDGE_CURVE ( 'NONE', #56039, #27101, #352, .T. ) ;
#67710=CARTESIAN_POINT ( 'NONE',  ( 18.01722669115800102, 3.499390932422000056, 11.96939125376999868 ) ) ;
#67711=( GEOMETRIC_REPRESENTATION_CONTEXT ( 3 ) GLOBAL_UNCERTAINTY_ASSIGNED_CONTEXT ( ( #57658 ) ) GLOBAL_UNIT_ASSIGNED_CONTEXT ( ( #62354, #36825, #67935 ) ) REPRESENTATION_CONTEXT ( 'NONE', 'WORKASPACE' ) );
#67714=ORIENTED_EDGE ( 'NONE', *, *, #67402, .T. ) ;
#67722=CARTESIAN_POINT ( 'NONE',  ( 11.25950692870000047, -3.811441498709999820, 11.68087307222999982 ) ) ;
#67724=CARTESIAN_POINT ( 'NONE',  ( 15.90018573812399971, 8.493548356068000516, 8.263529029821000904 ) ) ;
#67728=EDGE_LOOP ( 'NONE', ( #43021, #31024, #65962, #18485, #28403 ) ) ;
#67733=CARTESIAN_POINT ( 'NONE',  ( 11.50029455687000102, -11.65000000000000036, 0.000000000000000000 ) ) ;
#67734=ORIENTED_EDGE ( 'NONE', *, *, #13213, .F. ) ;
#67746=ORIENTED_EDGE ( 'NONE', *, *, #39146, .F. ) ;
#67751=CARTESIAN_POINT ( 'NONE',  ( 17.86459523290600160, -11.80388957783000059, 3.369424016599000371 ) ) ;
#67759=ORIENTED_EDGE ( 'NONE', *, *, #41039, .F. ) ;
#67762=PLANE ( 'NONE',  #110 ) ;
#67768=DIRECTION ( 'NONE',  ( -0.000000000000000000, 0.008867170401640299751, 0.9999606858717338120 ) ) ;
#67776=ORIENTED_EDGE ( 'NONE', *, *, #25273, .F. ) ;
#67782=AXIS2_PLACEMENT_3D ( 'NONE', #13489, #66947, #50881 ) ;
#67785=CARTESIAN_POINT ( 'NONE',  ( 25.09299597186400277, 8.442821527965000072, 8.583356320261000150 ) ) ;
#67790=CARTESIAN_POINT ( 'NONE',  ( 11.53713315544000118, -3.620704573398000115, 11.03277391605000091 ) ) ;
#67805=CARTESIAN_POINT ( 'NONE',  ( 13.50003721581400029, 9.159934378815998812, 7.517910889891000537 ) ) ;
#67808=CARTESIAN_POINT ( 'NONE',  ( 24.76779883137896476, -11.72407962198572839, 3.191093704755281202 ) ) ;
#67816=DIRECTION ( 'NONE',  ( 0.000000000000000000, 0.7071067811865475727, -0.7071067811865475727 ) ) ;
#67819=DIRECTION ( 'NONE',  ( 0.000000000000000000, 0.9516627710998093459, 0.3071448682668031505 ) ) ;
#67827=DIRECTION ( 'NONE',  ( -1.000000000000000000, 0.000000000000000000, 0.000000000000000000 ) ) ;
#67831=CARTESIAN_POINT ( 'NONE',  ( 23.85399112845500369, -3.593188128842942586, -13.20264652469179545 ) ) ;
#67841=CARTESIAN_POINT ( 'NONE',  ( 15.90018573812399971, 8.493548356068000516, 8.263529029821000904 ) ) ;
#67848=CARTESIAN_POINT ( 'NONE',  ( 23.58888758076617265, -13.25332336394347621, -4.277527736586637097 ) ) ;
#67851=ORIENTED_EDGE ( 'NONE', *, *, #53523, .F. ) ;
#67856=CYLINDRICAL_SURFACE ( 'NONE', #18291, 11.79499999999999993 ) ;
#67862=EDGE_CURVE ( 'NONE', #32077, #23499, #3763, .T. ) ;
#67870=B_SPLINE_CURVE_WITH_KNOTS ( 'NONE', 3,
 ( #23683, #54810, #40121, #1673 ),
 .UNSPECIFIED., .F., .F.,
 ( 4, 4 ),
 ( 0.4999999997918080918, 1.000000000000000000 ),
 .UNSPECIFIED. ) ;
#67888=DIRECTION ( 'NONE',  ( 0.000000000000000000, -0.3222656952305000266, -0.9466492601157001641 ) ) ;
#67891=CARTESIAN_POINT ( 'NONE',  ( 23.54905757042499914, -2.963884539164999943, 13.72195237095000131 ) ) ;
#67892=CONICAL_SURFACE ( 'NONE', #53378, 13.94234658587000197, 1.233427434088239627 ) ;
#67893=CARTESIAN_POINT ( 'NONE',  ( 24.60109515015806281, 12.20853554534348007, -3.061026489875391388 ) ) ;
#67894=DIRECTION ( 'NONE',  ( 1.000000000000000000, 0.000000000000000000, 0.000000000000000000 ) ) ;
#67896=CARTESIAN_POINT ( 'NONE',  ( 23.64710177088100096, 3.329564310917000114, -13.50251062865999963 ) ) ;
#67913=FACE_OUTER_BOUND ( 'NONE', #68434, .T. ) ;
#67920=VERTEX_POINT ( 'NONE', #14954 ) ;
#67922=CARTESIAN_POINT ( 'NONE',  ( 12.79999999202000005, -11.41069016990000051, 4.623987642516999230 ) ) ;
#67924=CARTESIAN_POINT ( 'NONE',  ( 13.99999999347100044, 9.187456302440001110, 8.213201953411001455 ) ) ;
#67935=( NAMED_UNIT ( * ) SI_UNIT ( $, .STERADIAN. ) SOLID_ANGLE_UNIT ( ) );
#67939=CARTESIAN_POINT ( 'NONE',  ( 11.40156680346000151, -11.68030187645999973, -1.636056047313999784 ) ) ;
#67942=EDGE_CURVE ( 'NONE', #24760, #63789, #61287, .T. ) ;
#67943=CARTESIAN_POINT ( 'NONE',  ( 24.44496483130000186, -3.224879855413000040, 12.03535978074999946 ) ) ;
#67949=CARTESIAN_POINT ( 'NONE',  ( 25.46371819568200223, 2.879482785682999868, 11.30954024936000124 ) ) ;
#67952=CARTESIAN_POINT ( 'NONE',  ( 17.76427412810700091, 3.313981393620000215, 11.22406656470000108 ) ) ;
#67959=CARTESIAN_POINT ( 'NONE',  ( 23.80948464333900816, 3.305733230510045750, 13.11180694039508943 ) ) ;
#67962=CARTESIAN_POINT ( 'NONE',  ( 17.86873602477000134, -3.252323392204000019, -11.33729809900999896 ) ) ;
#67964=CARTESIAN_POINT ( 'NONE',  ( 25.46375152665800101, -2.879425814940999917, -11.30951176145000048 ) ) ;
#67975=CARTESIAN_POINT ( 'NONE',  ( 24.39664237533066427, 12.03536608459189772, 3.224866623003459498 ) ) ;
#67976=CARTESIAN_POINT ( 'NONE',  ( 25.49994615402906106, 10.64595569529905816, -3.788460566544836094 ) ) ;
#67990=B_SPLINE_CURVE_WITH_KNOTS ( 'NONE', 3,
 ( #12022, #38590, #43846, #48051 ),
 .UNSPECIFIED., .F., .F.,
 ( 4, 4 ),
 ( 0.000000000000000000, 1.000000000000000000 ),
 .UNSPECIFIED. ) ;
#67995=VERTEX_POINT ( 'NONE', #60017 ) ;
#68000=FACE_OUTER_BOUND ( 'NONE', #21280, .T. ) ;
#68002=ORIENTED_EDGE ( 'NONE', *, *, #7796, .F. ) ;
#68003=CARTESIAN_POINT ( 'NONE',  ( 23.60091554815658554, 10.15345215840743087, 9.602364516840143693 ) ) ;
#68011=CARTESIAN_POINT ( 'NONE',  ( 23.59999172348799945, -10.30759808834999980, 9.317726582648999667 ) ) ;
#68021=B_SPLINE_CURVE_WITH_KNOTS ( 'NONE', 3,
 ( #24939, #52537, #63009, #14798, #36813, #26320, #58131, #35779, #47647, #46272, #57094, #9193, #41368, #30534 ),
 .UNSPECIFIED., .F., .F.,
 ( 4, 2, 2, 2, 2, 2, 4 ),
 ( 0.000000000000000000, 0.1250000000000022204, 0.2500000000000044409, 0.5000000000000093259, 0.6250000000000076605, 0.7500000000000059952, 1.000000000000000000 ),
 .UNSPECIFIED. ) ;
#68027=EDGE_CURVE ( 'NONE', #59240, #44124, #17057, .T. ) ;
#68037=ORIENTED_EDGE ( 'NONE', *, *, #2057, .F. ) ;
#68040=CARTESIAN_POINT ( 'NONE',  ( 15.48701341325400094, 9.525963125313998248, 8.191611664426000416 ) ) ;
#68041=CARTESIAN_POINT ( 'NONE',  ( 23.73953457051037930, 9.827638729800828088, 9.725490280229180939 ) ) ;
#68052=CARTESIAN_POINT ( 'NONE',  ( 23.55340455206400208, 10.33190633022999982, 9.496206588478999677 ) ) ;
#68053=ORIENTED_EDGE ( 'NONE', *, *, #63516, .F. ) ;
#68058=CARTESIAN_POINT ( 'NONE',  ( 18.38069952315600020, 3.381269036354999979, 12.09968217836000015 ) ) ;
#68062=LINE ( 'NONE', #57232, #41748 ) ;
#68067=VERTEX_POINT ( 'NONE', #18756 ) ;
#68079=EDGE_CURVE ( 'NONE', #8953, #60567, #19679, .T. ) ;
#68087=VERTEX_POINT ( 'NONE', #14875 ) ;
#68111=EDGE_CURVE ( 'NONE', #26364, #49024, #66225, .T. ) ;
#68115=CARTESIAN_POINT ( 'NONE',  ( 23.61278986222799858, -13.29111433880999904, 4.056100357100000942 ) ) ;
#68125=CARTESIAN_POINT ( 'NONE',  ( 25.59994555223600088, 9.407310119913397273, 6.227539428019859713 ) ) ;
#68127=EDGE_CURVE ( 'NONE', #55894, #34052, #12867, .T. ) ;
#68128=AXIS2_PLACEMENT_3D ( 'NONE', #30773, #26218, #36711 ) ;
#68130=CARTESIAN_POINT ( 'NONE',  ( 18.29983863916000075, -2.861762957209999847, 11.98830831200999825 ) ) ;
#68132=CARTESIAN_POINT ( 'NONE',  ( 11.56631965465000178, -3.502676170607000206, 11.07146920481999963 ) ) ;
#68137=CARTESIAN_POINT ( 'NONE',  ( 12.79999999202000005, 11.41069016990000051, -4.623987642516999230 ) ) ;
#68141=ORIENTED_EDGE ( 'NONE', *, *, #38569, .F. ) ;
#68146=CARTESIAN_POINT ( 'NONE',  ( 13.73899430609700190, -9.712898924749000074, -7.967785796560000300 ) ) ;
#68147=CARTESIAN_POINT ( 'NONE',  ( 15.89979320884932967, 8.154023814690251726, 9.295983641917246132 ) ) ;
#68151=CARTESIAN_POINT ( 'NONE',  ( 24.51106630233162065, -11.97393966168535862, 3.208408158990909698 ) ) ;
#68168=CARTESIAN_POINT ( 'NONE',  ( 23.80818223285949742, -3.306687018882327855, 13.11409922197318956 ) ) ;
#68171=FACE_OUTER_BOUND ( 'NONE', #32509, .T. ) ;
#68177=CARTESIAN_POINT ( 'NONE',  ( 16.09992084546400193, -8.991497430826001391, -8.719551690569000257 ) ) ;
#68193=CARTESIAN_POINT ( 'NONE',  ( 25.44995096658100309, 2.258942858049999725, -12.29419282279000036 ) ) ;
#68198=CARTESIAN_POINT ( 'NONE',  ( 24.30000000000000071, 0.000000000000000000, 0.000000000000000000 ) ) ;
#68202=LINE ( 'NONE', #36757, #38200 ) ;
#68204=CARTESIAN_POINT ( 'NONE',  ( 15.44552286930765383, 9.471974105402711785, 8.194957690431849073 ) ) ;
#68209=DIRECTION ( 'NONE',  ( 0.000000000000000000, -0.6482718649732923666, 0.7614089499631913061 ) ) ;
#68218=DIRECTION ( 'NONE',  ( 4.468466013035040012E-09, -0.9867386997955089889, -0.1623167838699015042 ) ) ;
#68220=CARTESIAN_POINT ( 'NONE',  ( 11.29998636608000062, -3.695122995756999984, 11.25914041192000070 ) ) ;
#68229=CARTESIAN_POINT ( 'NONE',  ( 23.58134502776777097, -3.140546043133733978, -13.62725458207014917 ) ) ;
#68231=CARTESIAN_POINT ( 'NONE',  ( 13.00000000001300116, -11.52577654661000039, -1.696746661728000038 ) ) ;
#68241=ADVANCED_FACE ( 'NONE', ( #16244 ), #67668, .F. ) ;
#68261=CARTESIAN_POINT ( 'NONE',  ( 18.06247470497382324, 3.164801830445714614, -11.41978211466257243 ) ) ;
#68269=VERTEX_POINT ( 'NONE', #63790 ) ;
#68270=EDGE_CURVE ( 'NONE', #37115, #17632, #63616, .T. ) ;
#68276=CARTESIAN_POINT ( 'NONE',  ( 16.32020863168370894, 3.595521563589540559, 11.99782687963361205 ) ) ;
#68278=CIRCLE ( 'NONE', #1168, 0.5000000000000004441 ) ;
#68281=VERTEX_POINT ( 'NONE', #65161 ) ;
#68282=CARTESIAN_POINT ( 'NONE',  ( 12.13642952379600004, 11.66478987891999886, -3.865847705614000152 ) ) ;
#68287=CARTESIAN_POINT ( 'NONE',  ( 18.16715644869600155, 3.024463723863999753, 11.49930835314999911 ) ) ;
#68293=EDGE_CURVE ( 'NONE', #49843, #64580, #23627, .T. ) ;
#68296=CARTESIAN_POINT ( 'NONE',  ( 24.14324463483463390, 3.327227329398946942, 12.48606449362839754 ) ) ;
#68303=B_SPLINE_CURVE_WITH_KNOTS ( 'NONE', 3,
 ( #33945, #5975, #44786, #59463, #64699, #17515, #11914, #17867, #22053, #33254, #38136, #11226, #32562, #16810, #11560, #54917, #32904, #1089, #33599, #22403, #7361, #6316, #49318, #39182, #7020, #2129, #28355, #23449, #22747, #49671, #50021, #1779 ),
 .UNSPECIFIED., .F., .F.,
 ( 4, 2, 2, 2, 2, 2, 2, 2, 1, 2, 2, 2, 1, 1, 1, 2, 2, 4 ),
 ( 0.000000000000000000, 0.2500000000000237033, 0.3750000000000346945, 0.4375000000000415779, 0.4687500000000449085, 0.5000000000000481837, 0.6250000000000585088, 0.6875000000000665024, 0.7187500000000688338, 0.7343750000000688338, 0.7500000000000688338, 0.8125000000000668354, 0.8437500000000682787, 0.8593750000000691669, 0.8671875000000695000, 0.8710937500000708322, 0.8750000000000721645, 1.000000000000000000 ),
 .UNSPECIFIED. ) ;
#68305=CARTESIAN_POINT ( 'NONE',  ( 18.90826270587400160, 0.000000000000000000, 0.000000000000000000 ) ) ;
#68311=CARTESIAN_POINT ( 'NONE',  ( 14.02348875342600110, 8.812421938351000961, 7.562304860556999131 ) ) ;
#68330=CARTESIAN_POINT ( 'NONE',  ( 13.55296092448800138, -11.54193659611999934, -2.433871908353000268 ) ) ;
#68339=CARTESIAN_POINT ( 'NONE',  ( 16.13573769406199787, 8.400696156758000299, 8.016340154447000543 ) ) ;
#68340=ORIENTED_EDGE ( 'NONE', *, *, #11422, .T. ) ;
#68341=CARTESIAN_POINT ( 'NONE',  ( 16.39999999485600313, 3.595156957901000094, 11.99794989424000136 ) ) ;
#68342=DIRECTION ( 'NONE',  ( 0.000000000000000000, 0.6460229165592984435, -0.7633180145130977756 ) ) ;
#68352=CARTESIAN_POINT ( 'NONE',  ( 29.91622776601699840, 0.000000000000000000, 0.000000000000000000 ) ) ;
#68355=CARTESIAN_POINT ( 'NONE',  ( 23.59536289310526413, -10.17255618909020498, 9.586547987916594238 ) ) ;
#68357=EDGE_CURVE ( 'NONE', #67055, #60176, #1094, .T. ) ;
#68358=CARTESIAN_POINT ( 'NONE',  ( 11.30000000000000071, -6.616929226765999876E-14, -1.143529715363999905E-14 ) ) ;
#68365=ORIENTED_EDGE ( 'NONE', *, *, #18959, .T. ) ;
#68372=CARTESIAN_POINT ( 'NONE',  ( 25.59994555223600088, -9.407310119913413260, -6.227539428019629675 ) ) ;
#68379=DIRECTION ( 'NONE',  ( 0.000000000000000000, 0.4739929102870218958, -0.8805286599524397850 ) ) ;
#68407=EDGE_CURVE ( 'NONE', #31626, #37115, #46175, .T. ) ;
#68412=VERTEX_POINT ( 'NONE', #50828 ) ;
#68414=CARTESIAN_POINT ( 'NONE',  ( 16.00261247405899923, -3.453035413593999792, -11.78892418867000025 ) ) ;
#68420=AXIS2_PLACEMENT_3D ( 'NONE', #18628, #44171, #66165 ) ;
#68433=CARTESIAN_POINT ( 'NONE',  ( 11.79999999684100054, 3.345264396959000130, -11.86064773189999855 ) ) ;
#68434=EDGE_LOOP ( 'NONE', ( #21500, #46872, #14424, #13099, #3163 ) ) ;
#68438=CARTESIAN_POINT ( 'NONE',  ( 18.36457177586446221, 3.090900475971610550, 11.23268385208956488 ) ) ;
#68439=CARTESIAN_POINT ( 'NONE',  ( 24.35365242081700288, -8.326148686863003689, 7.789520173261992753 ) ) ;
#68443=PLANE ( 'NONE',  #59893 ) ;
#68447=CARTESIAN_POINT ( 'NONE',  ( 11.30000000000000071, 0.000000000000000000, 0.000000000000000000 ) ) ;
#68452=CARTESIAN_POINT ( 'NONE',  ( 23.95125525613000050, -12.88154415998999980, 3.488952313995000054 ) ) ;
#68459=AXIS2_PLACEMENT_3D ( 'NONE', #14030, #3187, #61572 ) ;
#68462=CARTESIAN_POINT ( 'NONE',  ( 11.66889198508051884, -11.69116221025809921, -1.923144176179720555 ) ) ;
#68468=EDGE_CURVE ( 'NONE', #7379, #43730, #41083, .T. ) ;
#68486=CARTESIAN_POINT ( 'NONE',  ( 13.80650642310300036, -9.578547012936001082, -8.130125899688998459 ) ) ;
#68514=CARTESIAN_POINT ( 'NONE',  ( 25.25777475496700220, -2.569644838348999816, -11.37092172327999862 ) ) ;
#68517=CARTESIAN_POINT ( 'NONE',  ( 11.30000285318000230, 11.76356368987999979, 1.428410073821000159 ) ) ;
#68518=VERTEX_POINT ( 'NONE', #24602 ) ;
#68521=ORIENTED_EDGE ( 'NONE', *, *, #50106, .T. ) ;
#68523=ADVANCED_FACE ( 'NONE', ( #68607 ), #15487, .F. ) ;
#68543=AXIS2_PLACEMENT_3D ( 'NONE', #51154, #45223, #30181 ) ;
#68546=CARTESIAN_POINT ( 'NONE',  ( 24.53003472522700434, 8.771519074185000875, 8.897032352648000852 ) ) ;
#68548=CARTESIAN_POINT ( 'NONE',  ( 13.70005190196300227, -9.005348107749998832, -7.391036106496999381 ) ) ;
#68565=DIRECTION ( 'NONE',  ( -1.000000000000000000, 0.000000000000000000, 0.000000000000000000 ) ) ;
#68572=CARTESIAN_POINT ( 'NONE',  ( 29.91622776601699840, -7.448824697892998696E-09, 6.772075922005999615 ) ) ;
#68575=DIRECTION ( 'NONE',  ( 0.000000000000000000, 0.2588190451024932059, -0.9659258262890756397 ) ) ;
#68588=CARTESIAN_POINT ( 'NONE',  ( 24.44496487975900223, 3.224879802562000464, -12.03535984693000138 ) ) ;
#68591=CARTESIAN_POINT ( 'NONE',  ( 23.71888924647654306, 9.886276567970025297, -9.463295795964285162 ) ) ;
#68594=CARTESIAN_POINT ( 'NONE',  ( 24.63808311177700361, 12.49523003131000110, -2.948547624863999683 ) ) ;
#68601=DIRECTION ( 'NONE',  ( 0.000000000000000000, 0.000000000000000000, -1.000000000000000000 ) ) ;
#68605=EDGE_CURVE ( 'NONE', #13517, #12282, #6904, .T. ) ;
#68607=FACE_OUTER_BOUND ( 'NONE', #29783, .T. ) ;
#68614=CARTESIAN_POINT ( 'NONE',  ( 13.80650642310300036, 9.578547012936001082, 8.130125899688998459 ) ) ;
#68627=ORIENTED_EDGE ( 'NONE', *, *, #53652, .F. ) ;
#68628=CARTESIAN_POINT ( 'NONE',  ( 11.85864217039400259, 11.85700164854999983, -4.150661879143999755 ) ) ;
#68629=CARTESIAN_POINT ( 'NONE',  ( 17.71037843287399838, 11.39032026920000007, -4.571464210656999150 ) ) ;
#68633=CARTESIAN_POINT ( 'NONE',  ( 18.23043922992600230, -3.518658233831999826, 12.06062508533999988 ) ) ;
#68637=ORIENTED_EDGE ( 'NONE', *, *, #64336, .F. ) ;
#68640=EDGE_CURVE ( 'NONE', #24760, #45907, #41958, .T. ) ;
#68659=CARTESIAN_POINT ( 'NONE',  ( 13.55266668291200105, 9.123246021508000680, 7.477861434740999513 ) ) ;
#68671=CARTESIAN_POINT ( 'NONE',  ( 24.52301487032427829, 3.339126876001507593, -12.06936641334276672 ) ) ;
#68674=CARTESIAN_POINT ( 'NONE',  ( 18.30008632280270930, 2.887848135250621385E-14, -11.85014035451981762 ) ) ;
#68679=CARTESIAN_POINT ( 'NONE',  ( 11.49999672495000347, -8.721203281753666658, 7.819494091976963546 ) ) ;
#68693=ADVANCED_FACE ( 'NONE', ( #59500 ), #39848, .F. ) ;
#68702=ORIENTED_EDGE ( 'NONE', *, *, #52731, .F. ) ;
#68703=CARTESIAN_POINT ( 'NONE',  ( 11.79999999742035044, 12.31348763297674331, 1.888274624276562896 ) ) ;
#68710=AXIS2_PLACEMENT_3D ( 'NONE', #54017, #28150, #21515 ) ;
#68712=EDGE_LOOP ( 'NONE', ( #6153, #38958, #59608, #48503 ) ) ;
#68720=DIRECTION ( 'NONE',  ( -1.000000000000000000, 0.000000000000000000, 0.000000000000000000 ) ) ;
#68724=ADVANCED_FACE ( 'NONE', ( #10233 ), #58337, .F. ) ;
#68728=CARTESIAN_POINT ( 'NONE',  ( 15.83590051321700010, 9.131200976137998637, 8.359844154751998602 ) ) ;
#68731=CARTESIAN_POINT ( 'NONE',  ( 23.60205915885299888, -2.489696159930001595, -12.09604418630999945 ) ) ;
#68734=B_SPLINE_CURVE_WITH_KNOTS ( 'NONE', 3,
 ( #51527, #15505, #56785, #36831, #3623, #67593 ),
 .UNSPECIFIED., .F., .F.,
 ( 4, 2, 4 ),
 ( 0.000000000000000000, 0.5000000000000000000, 1.000000000000000000 ),
 .UNSPECIFIED. ) ;
#68739=CARTESIAN_POINT ( 'NONE',  ( 18.10505187282240058, -3.528432543146287070, 12.01774066417138087 ) ) ;
#68740=VERTEX_POINT ( 'NONE', #49707 ) ;
#68745=CARTESIAN_POINT ( 'NONE',  ( 25.50731686952359212, -11.18389986068883601, -3.138234620650206086 ) ) ;
#68750=EDGE_LOOP ( 'NONE', ( #45173, #47155, #15459, #52349 ) ) ;
#68756=ORIENTED_EDGE ( 'NONE', *, *, #31576, .F. ) ;
#68757=DIRECTION ( 'NONE',  ( 0.000000000000000000, 1.000000000000000000, 0.000000000000000000 ) ) ;
#68762=CARTESIAN_POINT ( 'NONE',  ( 11.35400411985998304, 11.72677417300536362, 1.687001524046905399 ) ) ;
#68766=CARTESIAN_POINT ( 'NONE',  ( 18.43329252113700534, -2.892698357136523235, 12.11790064375147047 ) ) ;
#68768=ORIENTED_EDGE ( 'NONE', *, *, #38391, .T. ) ;
#68785=ORIENTED_EDGE ( 'NONE', *, *, #18191, .T. ) ;
#68787=CARTESIAN_POINT ( 'NONE',  ( 18.15262501848119925, 3.263149105983724763, 11.18369374219401635 ) ) ;
#68788=CARTESIAN_POINT ( 'NONE',  ( 23.60000000000000497, -1.954456612737695442, 13.79170061782608414 ) ) ;
#68804=ORIENTED_EDGE ( 'NONE', *, *, #13110, .F. ) ;
#68815=CONICAL_SURFACE ( 'NONE', #38688, 13.94234652582999878, 1.233427434088239627 ) ;
#68821=CARTESIAN_POINT ( 'NONE',  ( 11.53937265905000054, -3.642773248484000082, 11.02530338024999956 ) ) ;
#68825=CARTESIAN_POINT ( 'NONE',  ( 11.50001496185000249, 12.52500000000000036, 0.000000000000000000 ) ) ;
#68833=EDGE_CURVE ( 'NONE', #42930, #4322, #61053, .T. ) ;
#68837=CARTESIAN_POINT ( 'NONE',  ( 13.64506009312500190, -9.630614656729999723, -7.923290881757000470 ) ) ;
#68847=CARTESIAN_POINT ( 'NONE',  ( 13.70003001321900449, 10.31266399190333516, 7.179884396236115407 ) ) ;
#68852=ORIENTED_EDGE ( 'NONE', *, *, #5864, .F. ) ;
#68862=CARTESIAN_POINT ( 'NONE',  ( 24.67921310950000091, -12.29514723793999842, -2.979192343402000009 ) ) ;
#68863=AXIS2_PLACEMENT_3D ( 'NONE', #50453, #34390, #7113 ) ;
#68868=B_SPLINE_CURVE_WITH_KNOTS ( 'NONE', 3,
 ( #48419, #27443, #59940, #69056, #16936, #53326 ),
 .UNSPECIFIED., .F., .F.,
 ( 4, 2, 4 ),
 ( 0.000000000000000000, 0.5000000000000000000, 1.000000000000000000 ),
 .UNSPECIFIED. ) ;
#68869=FACE_OUTER_BOUND ( 'NONE', #40586, .T. ) ;
#68873=MECHANICAL_DESIGN_GEOMETRIC_PRESENTATION_REPRESENTATION('',(#10781),#67711);
#68875=EDGE_CURVE ( 'NONE', #55008, #10995, #38610, .T. ) ;
#68895=EDGE_CURVE ( 'NONE', #11014, #43802, #1863, .T. ) ;
#68896=ORIENTED_EDGE ( 'NONE', *, *, #35553, .F. ) ;
#68897=CARTESIAN_POINT ( 'NONE',  ( 24.62774583285499830, 8.736962890587999908, 9.042103898172999976 ) ) ;
#68910=CARTESIAN_POINT ( 'NONE',  ( 11.90028836426310122, 11.81686663804764770, -4.153560932554616336 ) ) ;
#68933=AXIS2_PLACEMENT_3D ( 'NONE', #30180, #56045, #13411 ) ;
#68937=DIRECTION ( 'NONE',  ( -3.751129491691894952E-06, -0.2588385419140925015, 0.9659206019159729539 ) ) ;
#68942=CARTESIAN_POINT ( 'NONE',  ( 24.78000005981499854, 12.27029765734999955, 2.912405417372000205 ) ) ;
#68944=B_SPLINE_SURFACE_WITH_KNOTS ( 'NONE', 3, 3, ( 
 ( #39322, #66909, #55400, #66224 ),
 ( #49456, #28851, #23579, #49810 ),
 ( #18347, #65532, #60989, #7496 ),
 ( #7157, #28493, #44584, #13104 ),
 ( #29187, #23928, #65877, #50498 ),
 ( #45264, #66569, #67939, #35458 ),
 ( #41722, #45939, #67591, #67251 ),
 ( #61673, #19024, #36474, #46288 ),
 ( #56432, #52208, #9207, #56782 ) ),
 .UNSPECIFIED., .F., .F., .F.,
 ( 4, 1, 1, 1, 1, 1, 4 ),
 ( 4, 4 ),
 ( 0.05136528901823000232, 0.1666666666667000196, 0.3333333333333000081, 0.5000000000000000000, 0.6666666666667000474, 0.8333333333333000637, 0.9784615765758000183 ),
 ( -0.1917159053268999991, 1.191863452461999984 ),
 .UNSPECIFIED. ) ;
#68953=CARTESIAN_POINT ( 'NONE',  ( 13.09019624054850617, 12.38961571551778640, 1.836606440307306354 ) ) ;
#68959=CARTESIAN_POINT ( 'NONE',  ( 17.85726930274100255, -3.190143309604999811, 11.45065656613999927 ) ) ;
#68960=ADVANCED_FACE ( 'NONE', ( #29354 ), #39708, .F. ) ;
#68972=ORIENTED_EDGE ( 'NONE', *, *, #52834, .T. ) ;
#68979=ORIENTED_EDGE ( 'NONE', *, *, #1062, .T. ) ;
#68980=CARTESIAN_POINT ( 'NONE',  ( 12.05989062672900047, 12.07342271643000053, -3.473919584753000223 ) ) ;
#68981=CARTESIAN_POINT ( 'NONE',  ( 18.01587601577499953, 11.44428158143999852, -4.450268217599000486 ) ) ;
#68982=DIRECTION ( 'NONE',  ( -1.000000000000000000, 0.000000000000000000, 0.000000000000000000 ) ) ;
#68987=CARTESIAN_POINT ( 'NONE',  ( 16.00000001290300133, -11.86188960208913912, 3.298666395463871304 ) ) ;
#68989=EDGE_LOOP ( 'NONE', ( #31451, #14108 ) ) ;
#69009=CARTESIAN_POINT ( 'NONE',  ( 16.04750315638899849, -3.679714098878999806, -11.11063745184000062 ) ) ;
#69010=CARTESIAN_POINT ( 'NONE',  ( 13.75961700471900073, 8.905065757320999253, 7.452879173751000508 ) ) ;
#69022=AXIS2_PLACEMENT_3D ( 'NONE', #15518, #31946, #53261 ) ;
#69029=CARTESIAN_POINT ( 'NONE',  ( 24.48564577462000003, -8.805068883974998428, -8.922048782936000677 ) ) ;
#69033=CARTESIAN_POINT ( 'NONE',  ( 12.99165415090800124, 12.32813973498000060, 1.877091699536999947 ) ) ;
#69040=CARTESIAN_POINT ( 'NONE',  ( 18.39984528086700166, -1.003641614260999896E-13, 7.549516567450998842E-14 ) ) ;
#69041=AXIS2_PLACEMENT_3D ( 'NONE', #8106, #2853, #44830 ) ;
#69042=EDGE_CURVE ( 'NONE', #63477, #52918, #1836, .T. ) ;
#69045=EDGE_CURVE ( 'NONE', #54862, #15717, #28136, .T. ) ;
#69050=ORIENTED_EDGE ( 'NONE', *, *, #16478, .T. ) ;
#69056=CARTESIAN_POINT ( 'NONE',  ( 11.53935385204243147, -3.267863779230331112, 11.38835623221634386 ) ) ;
#69057=B_SPLINE_CURVE_WITH_KNOTS ( 'NONE', 3,
 ( #25846, #9077, #26197, #25504, #46833, #15361 ),
 .UNSPECIFIED., .F., .F.,
 ( 4, 1, 1, 4 ),
 ( 0.000000000000000000, 0.1550125193756538011, 0.7488612380692285520, 1.000000000000000000 ),
 .UNSPECIFIED. ) ;
#69064=CARTESIAN_POINT ( 'NONE',  ( 24.00507812729757973, 12.70419977581086712, 3.471507264481290989 ) ) ;
#69077=AXIS2_PLACEMENT_3D ( 'NONE', #24825, #46151, #8061 ) ;
#69081=CARTESIAN_POINT ( 'NONE',  ( 21.72233714749290101, 0.000000000000000000, 0.000000000000000000 ) ) ;
#69083=CARTESIAN_POINT ( 'NONE',  ( 13.99999999393279104, 9.282302710986076733, 8.207095416277889299 ) ) ;
#69084=CARTESIAN_POINT ( 'NONE',  ( 13.63328756540911790, 11.47070279790940717, 2.387969831734693127 ) ) ;
#69093=CARTESIAN_POINT ( 'NONE',  ( 23.91178178635799867, 9.488588060152000736, 9.248841913497999556 ) ) ;
#69098=DIRECTION ( 'NONE',  ( 0.000000000000000000, 0.2714570858282905341, -0.9624505444715651947 ) ) ;
#69099=ORIENTED_EDGE ( 'NONE', *, *, #44683, .F. ) ;
#69108=CARTESIAN_POINT ( 'NONE',  ( 15.88832047282410720, -8.582214862760457308, -8.173711952084849131 ) ) ;
#69109=DIRECTION ( 'NONE',  ( 0.000000000000000000, -0.9421243786071877846, -0.3352635608502960718 ) ) ;
#69116=CARTESIAN_POINT ( 'NONE',  ( 16.13837349797499954, -3.856691945087999951, -11.95672051617999898 ) ) ;
#69117=CARTESIAN_POINT ( 'NONE',  ( 11.83979429613600232, 11.64688653560999931, 1.860528257274000064 ) ) ;
#69118=ORIENTED_EDGE ( 'NONE', *, *, #2057, .T. ) ;
#69119=CARTESIAN_POINT ( 'NONE',  ( 24.71803605778425705, 3.123403878897051289, -11.79148459578962971 ) ) ;
#69120=DIRECTION ( 'NONE',  ( 0.000000000000000000, 0.2588190451024934280, -0.9659258262890756397 ) ) ;
#69146=ORIENTED_EDGE ( 'NONE', *, *, #29201, .T. ) ;
#69163=CARTESIAN_POINT ( 'NONE',  ( 18.53574650668400281, 2.786976374009999535, -11.27236326136999978 ) ) ;
#69168=CARTESIAN_POINT ( 'NONE',  ( 11.26374551471000274, -3.753781600817000186, 11.28122097457000095 ) ) ;
#69169=EDGE_CURVE ( 'NONE', #36015, #45376, #65295, .T. ) ;
#69175=DIRECTION ( 'NONE',  ( 2.186552006505938554E-10, 0.8077514394224775129, -0.5895232074404836986 ) ) ;
#69183=EDGE_LOOP ( 'NONE', ( #20655, #9909, #50135, #23235 ) ) ;
#69192=FACE_OUTER_BOUND ( 'NONE', #58713, .T. ) ;
ENDSEC;
END-ISO-10303-21;
